ISO-10303-21;
HEADER;
FILE_DESCRIPTION (('STEP AP214'),
    '1' );
FILE_NAME ('stud.step',
    '2026-10-26T19:46:16',
    ( '' ),
    ( '' ),
    'SwSTEP 2.0',
    'SolidWorks 2025',
    '' );
FILE_SCHEMA (( 'AUTOMOTIVE_DESIGN' ));
ENDSEC;

DATA;
#22=CARTESIAN_POINT ( 'NONE',  ( 7.188101187500001821, 14.06249999795161365, -2.977408999572650483 ) ) ;
#23=CARTESIAN_POINT ( 'NONE',  ( 5.656854249492381470, 104.7500000040967905, 5.656854249492379694 ) ) ;
#31=LINE ( 'NONE', #63370, #20979 ) ;
#32=CARTESIAN_POINT ( 'NONE',  ( -4.401442555609581635E-16, 107.2812500020483810, -7.188101187500000044 ) ) ;
#39=CARTESIAN_POINT ( 'NONE',  ( 9.797174393178825657E-16, 125.0000000000000000, -8.000000000000000000 ) ) ;
#41=ORIENTED_EDGE ( 'NONE', *, *, #6114, .F. ) ;
#51=CARTESIAN_POINT ( 'NONE',  ( -5.656854249492380582, 97.81250000000000000, -5.656854249492380582 ) ) ;
#57=CARTESIAN_POINT ( 'NONE',  ( 7.188101187500000044, 0.8437499979516100979, 0.000000000000000000 ) ) ;
#59=CARTESIAN_POINT ( 'NONE',  ( -5.082755093536325930, 121.3437500020483952, -5.082755093536325930 ) ) ;
#83=CARTESIAN_POINT ( 'NONE',  ( 5.656854249492378806, 7.124999995903221084, 5.656854249492381470 ) ) ;
#84=CARTESIAN_POINT ( 'NONE',  ( 2.977408999572654480, 112.6250000020483810, 7.188101187499999156 ) ) ;
#89=CARTESIAN_POINT ( 'NONE',  ( -7.188101187500000044, 114.0312500020483952, 0.000000000000000000 ) ) ;
#111=VERTEX_POINT ( 'NONE', #39096 ) ;
#113=CARTESIAN_POINT ( 'NONE',  ( -5.656854249492381470, 0.9375000000000001110, 5.656854249492379694 ) ) ;
#116=CARTESIAN_POINT ( 'NONE',  ( -1.320432766682874540E-15, 25.96874999795161543, 7.188101187500000044 ) ) ;
#124=EDGE_CURVE ( 'NONE', #54105, #45186, #50774, .T. ) ;
#142=CARTESIAN_POINT ( 'NONE',  ( 8.000000000000000000, 121.2500000000000000, -9.797174393178825657E-16 ) ) ;
#151=CARTESIAN_POINT ( 'NONE',  ( 8.000000000000000000, 5.812499995903220196, 0.000000000000000000 ) ) ;
#173=CARTESIAN_POINT ( 'NONE',  ( -7.188101187500000044, 98.65625000204838102, 0.000000000000000000 ) ) ;
#197=CARTESIAN_POINT ( 'NONE',  ( 5.082755093536324154, 26.15624999795161543, 5.082755093536326818 ) ) ;
#206=CARTESIAN_POINT ( 'NONE',  ( 5.082755093536324154, 9.281249997951610098, 5.082755093536326818 ) ) ;
#209=CARTESIAN_POINT ( 'NONE',  ( 5.082755093536325930, 5.531249997951610098, -5.082755093536325930 ) ) ;
#216=ORIENTED_EDGE ( 'NONE', *, *, #37600, .T. ) ;
#217=ADVANCED_FACE ( 'NONE', ( #26642 ), #49664, .T. ) ;
#224=CARTESIAN_POINT ( 'NONE',  ( -2.977408999572654480, 16.49999999795161543, 7.188101187499999156 ) ) ;
#228=CARTESIAN_POINT ( 'NONE',  ( 1.320432766682874540E-15, 108.4062500020483810, 7.188101187500000044 ) ) ;
#241=CARTESIAN_POINT ( 'NONE',  ( 0.000000000000000000, 125.0000000000000000, 0.000000000000000000 ) ) ;
#247=CARTESIAN_POINT ( 'NONE',  ( -8.000000000000000000, 5.156250000000000888, -3.313708498984762496 ) ) ;
#257=CARTESIAN_POINT ( 'NONE',  ( -2.977408999572651815, 119.9375000020483952, 7.188101187500000933 ) ) ;
#266=CARTESIAN_POINT ( 'NONE',  ( -5.082755093536326818, 23.90624999795161543, 5.082755093536325042 ) ) ;
#272=CARTESIAN_POINT ( 'NONE',  ( 3.313708498984802020, 25.78125000000000355, -7.999999999999958256 ) ) ;
#281=CARTESIAN_POINT ( 'NONE',  ( -5.656854249492381470, 27.74999999590322020, 5.656854249492379694 ) ) ;
#284=CARTESIAN_POINT ( 'NONE',  ( 3.313708498984652362, 115.5312500000000000, -8.000000000000108358 ) ) ;
#289=CARTESIAN_POINT ( 'NONE',  ( -2.977408999572650039, 5.812499997951610986, -7.188101187500000933 ) ) ;
#290=( BOUNDED_CURVE ( )  B_SPLINE_CURVE ( 2, ( #68375, #16672, #62703, #11041, #5381, #30972, #35180, #7969, #58556 ),
 .UNSPECIFIED., .F., .F. ) 
 B_SPLINE_CURVE_WITH_KNOTS ( ( 3, 2, 2, 2, 3 ),
 ( 0.4895833333333333148, 0.4947916666666666852, 0.5000000000000000000, 0.5052083333333333703, 0.5104166666666666297 ),
 .UNSPECIFIED. ) 
 CURVE ( )  GEOMETRIC_REPRESENTATION_ITEM ( )  RATIONAL_B_SPLINE_CURVE ( ( 1.000000000000000000, 0.9238795325112867385, 1.000000000000000000, 0.9238795325112867385, 1.000000000000000000, 0.9238795325112867385, 1.000000000000000000, 0.9238795325112867385, 1.000000000000000000 ) ) 
 REPRESENTATION_ITEM ( '' )  );
#306=CARTESIAN_POINT ( 'NONE',  ( -3.313708498984760720, 18.46875000000000000, -8.000000000000000000 ) ) ;
#308=ADVANCED_FACE ( 'NONE', ( #40955 ), #58321, .T. ) ;
#309=CARTESIAN_POINT ( 'NONE',  ( 1.320432766682874540E-15, 121.5312500020483810, 7.188101187500000044 ) ) ;
#345=CARTESIAN_POINT ( 'NONE',  ( -7.188101187500000044, 22.59374999795161187, -8.802885111219163269E-16 ) ) ;
#348=CARTESIAN_POINT ( 'NONE',  ( -2.977408999572652260, 96.31250000204838102, 7.188101187500000044 ) ) ;
#364=CARTESIAN_POINT ( 'NONE',  ( 1.320432766682874540E-15, 91.53125000204836681, 7.188101187500000044 ) ) ;
#370=CARTESIAN_POINT ( 'NONE',  ( 5.082755093536326818, 95.09375000204838102, 5.082755093536325042 ) ) ;
#393=CARTESIAN_POINT ( 'NONE',  ( 5.082755093536324154, 12.28124999795161187, 5.082755093536326818 ) ) ;
#394=CARTESIAN_POINT ( 'NONE',  ( -5.656854249492378806, 104.3750000040967763, 5.656854249492381470 ) ) ;
#404=ORIENTED_EDGE ( 'NONE', *, *, #58829, .T. ) ;
#406=CARTESIAN_POINT ( 'NONE',  ( -7.188101187500000044, 103.1562500020483810, 0.000000000000000000 ) ) ;
#408=CARTESIAN_POINT ( 'NONE',  ( -8.000000000000001776, 15.65624999590322197, 3.313708498984759387 ) ) ;
#423=CARTESIAN_POINT ( 'NONE',  ( 5.656854249492379694, 100.4375000000000000, -5.656854249492380582 ) ) ;
#426=CARTESIAN_POINT ( 'NONE',  ( 8.000000000000000000, 1.593750000000000222, -3.313708498984761164 ) ) ;
#428=CARTESIAN_POINT ( 'NONE',  ( -7.188101187500002709, 6.187499997951610986, 2.977408999572649151 ) ) ;
#431=CARTESIAN_POINT ( 'NONE',  ( -2.977408999572652260, 114.3125000020483668, 7.188101187500000044 ) ) ;
#435=CARTESIAN_POINT ( 'NONE',  ( -8.000000000000000000, 3.656250000000000444, -3.313708498984762496 ) ) ;
#452=CARTESIAN_POINT ( 'NONE',  ( -7.188101187499999156, 109.2500000020483952, 2.977408999572654924 ) ) ;
#457=CARTESIAN_POINT ( 'NONE',  ( 7.188101187500001821, 116.3750000020483810, -2.977408999572651371 ) ) ;
#483=CARTESIAN_POINT ( 'NONE',  ( -8.000000000000000000, 3.750000000000000888, -9.797174393178825657E-16 ) ) ;
#484=LINE ( 'NONE', #23464, #58928 ) ;
#486=CARTESIAN_POINT ( 'NONE',  ( 5.082755093536325930, 26.53124999795161543, -5.082755093536325930 ) ) ;
#487=CARTESIAN_POINT ( 'NONE',  ( -7.999999999999998224, 120.7812500040967905, 3.313708498984766493 ) ) ;
#493=VERTEX_POINT ( 'NONE', #52645 ) ;
#509=CARTESIAN_POINT ( 'NONE',  ( -5.656854249492380582, 117.3125000000000000, -5.656854249492380582 ) ) ;
#539=CARTESIAN_POINT ( 'NONE',  ( -4.401442555609581635E-16, 96.78125000204838102, -7.188101187500000044 ) ) ;
#551=CARTESIAN_POINT ( 'NONE',  ( -8.000000000000000000, 6.468749995903221084, -3.313708498984762496 ) ) ;
#555=DIRECTION ( 'NONE',  ( 0.000000000000000000, 0.000000000000000000, 1.000000000000000000 ) ) ;
#558=CARTESIAN_POINT ( 'NONE',  ( -1.469576158976823947E-15, 17.43749999590322375, 8.000000000000000000 ) ) ;
#562=CARTESIAN_POINT ( 'NONE',  ( -1.320432766682874540E-15, 24.46874999795161543, 7.188101187500000044 ) ) ;
#572=CARTESIAN_POINT ( 'NONE',  ( -2.977408999572650039, 17.43749999795161187, -7.188101187500001821 ) ) ;
#575=CARTESIAN_POINT ( 'NONE',  ( -2.977408999572654480, 4.874999997951610098, 7.188101187499999156 ) ) ;
#581=UNCERTAINTY_MEASURE_WITH_UNIT (LENGTH_MEASURE( 1.000000000000000082E-05 ), #26051, 'distance_accuracy_value', 'NONE');
#588=CARTESIAN_POINT ( 'NONE',  ( -5.082755093536325930, 116.4687500020483810, -5.082755093536325930 ) ) ;
#591=CARTESIAN_POINT ( 'NONE',  ( 4.401442555609581635E-16, 15.84374999795161365, -7.188101187500000044 ) ) ;
#596=CARTESIAN_POINT ( 'NONE',  ( 2.977408999572650039, 98.56250000204838102, -7.188101187500001821 ) ) ;
#620=CARTESIAN_POINT ( 'NONE',  ( 1.469576158976823947E-15, 110.3750000000000000, 8.000000000000000000 ) ) ;
#623=CARTESIAN_POINT ( 'NONE',  ( 5.656854249492378806, 10.31250000000000178, 5.656854249492381470 ) ) ;
#629=CARTESIAN_POINT ( 'NONE',  ( -7.188101187500001821, 118.0625000020483952, -2.977408999572650483 ) ) ;
#659=CARTESIAN_POINT ( 'NONE',  ( 5.082755093536325930, 8.531249997951611874, -5.082755093536325930 ) ) ;
#663=VERTEX_POINT ( 'NONE', #70001 ) ;
#677=CARTESIAN_POINT ( 'NONE',  ( -3.313708498984765161, 16.03125000000000355, 7.999999999999998224 ) ) ;
#679=CARTESIAN_POINT ( 'NONE',  ( -2.977408999572651815, 121.4375000020483668, 7.188101187500000933 ) ) ;
#687=CARTESIAN_POINT ( 'NONE',  ( -1.320432766682874540E-15, 1.593749997951610098, 7.188101187500000044 ) ) ;
#691=CARTESIAN_POINT ( 'NONE',  ( 2.977408999572650039, 124.0625000020483810, -7.188101187500001821 ) ) ;
#692=CARTESIAN_POINT ( 'NONE',  ( 1.469576158976823947E-15, 101.5625000040967763, 8.000000000000000000 ) ) ;
#700=EDGE_LOOP ( 'NONE', ( #13343, #47684, #31600, #1250 ) ) ;
#708=ORIENTED_EDGE ( 'NONE', *, *, #37558, .F. ) ;
#715=CARTESIAN_POINT ( 'NONE',  ( -7.188101187500002709, 21.18749999795161187, 2.977408999572649151 ) ) ;
#717=CARTESIAN_POINT ( 'NONE',  ( 7.188101187500002709, 99.68750000204838102, 2.977408999572649151 ) ) ;
#725=( BOUNDED_CURVE ( )  B_SPLINE_CURVE ( 2, ( #40249, #284, #10464, #63251, #46275, #74203, #63623, #11953, #68176 ),
 .UNSPECIFIED., .F., .F. ) 
 B_SPLINE_CURVE_WITH_KNOTS ( ( 3, 2, 2, 2, 3 ),
 ( 0.2604166666666664631, 0.2656249999999997780, 0.2708333333333330928, 0.2760416666666664631, 0.2812499999999997780 ),
 .UNSPECIFIED. ) 
 CURVE ( )  GEOMETRIC_REPRESENTATION_ITEM ( )  RATIONAL_B_SPLINE_CURVE ( ( 1.000000000000003331, 0.9238795325112835188, 1.000000000000000000, 0.9238795325112867385, 1.000000000000000000, 0.9238795325112867385, 1.000000000000000000, 0.9238795325112899581, 0.9999999999999967804 ) ) 
 REPRESENTATION_ITEM ( '' )  );
#734=CARTESIAN_POINT ( 'NONE',  ( 4.898587196589412829E-16, 25.68749999590322375, -8.000000000000000000 ) ) ;
#735=CARTESIAN_POINT ( 'NONE',  ( -5.082755093536324154, 89.84375000204839523, 5.082755093536326818 ) ) ;
#740=CARTESIAN_POINT ( 'NONE',  ( -7.188101187500001821, 98.93750000204838102, -2.977408999572650483 ) ) ;
#752=CARTESIAN_POINT ( 'NONE',  ( -5.656854249492381470, 11.24999999590322197, 5.656854249492379694 ) ) ;
#762=VECTOR ( 'NONE', #41647, 1000.000000000000000 ) ;
#763=CARTESIAN_POINT ( 'NONE',  ( -5.656854249492378806, 105.8750000040967763, 5.656854249492381470 ) ) ;
#765=EDGE_CURVE ( 'NONE', #10294, #72478, #11549, .T. ) ;
#772=DIRECTION ( 'NONE',  ( 0.000000000000000000, 0.000000000000000000, 1.000000000000000000 ) ) ;
#773=CARTESIAN_POINT ( 'NONE',  ( 5.082755093536325042, 107.0937500020483810, -5.082755093536325930 ) ) ;
#777=ORIENTED_EDGE ( 'NONE', *, *, #6709, .F. ) ;
#785=CARTESIAN_POINT ( 'NONE',  ( -1.469576158976823947E-15, 2.625000000000000444, 8.000000000000000000 ) ) ;
#792=CARTESIAN_POINT ( 'NONE',  ( 8.000000000000001776, 98.65625000000001421, 3.313708498984759387 ) ) ;
#797=CARTESIAN_POINT ( 'NONE',  ( 4.401442555609581635E-16, 4.218749997951610098, -7.188101187500000044 ) ) ;
#800=CARTESIAN_POINT ( 'NONE',  ( 7.188101187500000933, 113.3750000020483810, -2.977408999572651371 ) ) ;
#820=CARTESIAN_POINT ( 'NONE',  ( 5.082755093536326818, 114.2187500020483810, 5.082755093536325042 ) ) ;
#823=EDGE_CURVE ( 'NONE', #12576, #61133, #52080, .T. ) ;
#826=CARTESIAN_POINT ( 'NONE',  ( 7.188101187500000044, 116.2812500020483810, -8.802885111219163269E-16 ) ) ;
#832=VERTEX_POINT ( 'NONE', #13014 ) ;
#853=CARTESIAN_POINT ( 'NONE',  ( -3.313708498984760720, 7.968750000000000888, -8.000000000000000000 ) ) ;
#855=CARTESIAN_POINT ( 'NONE',  ( -1.320432766682874540E-15, 21.46874999795161543, 7.188101187500000044 ) ) ;
#856=CARTESIAN_POINT ( 'NONE',  ( 8.000000000000001776, 121.3437500040967763, 3.313708498984759387 ) ) ;
#858=CARTESIAN_POINT ( 'NONE',  ( -3.313708498984765161, 7.031250000000000888, 7.999999999999998224 ) ) ;
#878=CARTESIAN_POINT ( 'NONE',  ( -3.313708498984762496, 116.2812500000000000, 7.999999999999998224 ) ) ;
#882=EDGE_CURVE ( 'NONE', #48510, #70312, #66666, .T. ) ;
#885=CARTESIAN_POINT ( 'NONE',  ( 5.656854249492380582, 14.99999999590322020, -5.656854249492380582 ) ) ;
#888=CARTESIAN_POINT ( 'NONE',  ( -1.469576158976823947E-15, 12.93749999590322197, 8.000000000000000000 ) ) ;
#909=CARTESIAN_POINT ( 'NONE',  ( 1.320432766682874540E-15, 96.03125000204838102, 7.188101187500000044 ) ) ;
#929=CARTESIAN_POINT ( 'NONE',  ( 3.313708498984802020, 18.09374999590322020, -7.999999999999958256 ) ) ;
#930=CLOSED_SHELL ( 'NONE', ( #53514, #18000, #60311, #31115, #43787, #19093, #37149, #47317, #49746, #67519, #37721, #31449, #51316, #39633, #44816, #10281, #12434, #56331, #30520, #59091, #14525, #47783, #43704, #55496, #6376, #308, #70391, #29353, #51728, #23744, #10579, #38890, #50434, #64293, #60151, #36189, #64670, #63661, #60820, #61884, #46953, #47094, #2677, #62513, #3095, #53816, #65760, #63914, #61256, #62071, #47220, #43361, #60220, #5353, #10859, #45491, #46407, #69702, #64376, #15469, #30860, #59977, #40736, #18077, #65645, #26081, #54283, #59683, #24802, #16598, #50305, #48307, #217, #18722, #66993, #74304, #49636, #64399, #31436, #28895, #4640, #3079, #36392, #47949, #42933, #9569, #67487, #58394, #12651, #51210, #44023, #62069, #53673, #53231, #36000, #63563, #3965, #2864, #5983, #15096, #64347, #18944, #31178, #18920, #74500 ) ) ;
#939=CYLINDRICAL_SURFACE ( 'NONE', #47674, 8.000000000000000000 ) ;
#942=CARTESIAN_POINT ( 'NONE',  ( -5.082755093536325042, 16.03124999795161543, -5.082755093536325930 ) ) ;
#945=CARTESIAN_POINT ( 'NONE',  ( 7.188101187500001821, 5.437499997951610098, -2.977408999572650483 ) ) ;
#958=CARTESIAN_POINT ( 'NONE',  ( -5.082755093536324154, 113.8437500020483810, 5.082755093536326818 ) ) ;
#962=CARTESIAN_POINT ( 'NONE',  ( -5.082755093536326818, 14.90624999795161187, 5.082755093536325042 ) ) ;
#967=CARTESIAN_POINT ( 'NONE',  ( 7.188101187500001821, 102.8750000020483810, -2.977408999572651371 ) ) ;
#979=DIRECTION ( 'NONE',  ( -0.000000000000000000, 1.000000000000000000, -0.000000000000000000 ) ) ;
#982=CARTESIAN_POINT ( 'NONE',  ( -7.999999999999998224, 119.0937500000000000, 3.313708498984766049 ) ) ;
#984=DIRECTION ( 'NONE',  ( -0.000000000000000000, 1.000000000000000000, -0.000000000000000000 ) ) ;
#986=CARTESIAN_POINT ( 'NONE',  ( 5.656854249492381470, 110.5625000000000000, 5.656854249492379694 ) ) ;
#991=CARTESIAN_POINT ( 'NONE',  ( -4.898587196589412829E-16, 111.3125000040967905, -8.000000000000000000 ) ) ;
#993=CARTESIAN_POINT ( 'NONE',  ( 0.000000000000000000, 125.0000000000000000, 0.000000000000000000 ) ) ;
#997=CARTESIAN_POINT ( 'NONE',  ( 5.082755093536326818, 115.7187500020483810, 5.082755093536325042 ) ) ;
#1006=CARTESIAN_POINT ( 'NONE',  ( 3.313708498984733186, 109.5312500000000000, -8.000000000000026645 ) ) ;
#1027=CARTESIAN_POINT ( 'NONE',  ( -5.082755093536326818, 6.281249997951610098, 5.082755093536325042 ) ) ;
#1036=CARTESIAN_POINT ( 'NONE',  ( -5.656854249492380582, 93.50000000409677625, -5.656854249492380582 ) ) ;
#1044=CARTESIAN_POINT ( 'NONE',  ( 5.656854249492380582, 18.18750000000000355, -5.656854249492380582 ) ) ;
#1047=CARTESIAN_POINT ( 'NONE',  ( 2.977408999572650039, 122.1875000020483668, -7.188101187500001821 ) ) ;
#1058=CARTESIAN_POINT ( 'NONE',  ( 7.188101187500001821, 119.3750000020483810, -2.977408999572651371 ) ) ;
#1085=CARTESIAN_POINT ( 'NONE',  ( 5.082755093536325930, 23.53124999795161543, -5.082755093536325930 ) ) ;
#1087=CARTESIAN_POINT ( 'NONE',  ( 5.082755093536326818, 99.59375000204838102, 5.082755093536325042 ) ) ;
#1093=CARTESIAN_POINT ( 'NONE',  ( 9.491012693391981871E-16, 0.000000000000000000, -7.499999999999992895 ) ) ;
#1096=DIRECTION ( 'NONE',  ( -0.000000000000000000, 1.000000000000000000, -0.000000000000000000 ) ) ;
#1099=AXIS2_PLACEMENT_3D ( 'NONE', #65004, #59365, #21871 ) ;
#1107=AXIS2_PLACEMENT_3D ( 'NONE', #26560, #67318, #10346 ) ;
#1109=CARTESIAN_POINT ( 'NONE',  ( 7.188101187500001821, 95.37500000204839523, -2.977408999572651371 ) ) ;
#1120=CARTESIAN_POINT ( 'NONE',  ( 4.898587196589412829E-16, 10.68749999590322020, -8.000000000000000000 ) ) ;
#1130=CARTESIAN_POINT ( 'NONE',  ( -8.000000000000000000, 102.6875000040967763, 0.000000000000000000 ) ) ;
#1132=LINE ( 'NONE', #24110, #55314 ) ;
#1139=CARTESIAN_POINT ( 'NONE',  ( 2.977408999572654480, 97.62500000204836681, 7.188101187499999156 ) ) ;
#1141=CARTESIAN_POINT ( 'NONE',  ( 3.313708498984731410, 119.6562500040967905, 8.000000000000031974 ) ) ;
#1147=( BOUNDED_CURVE ( )  B_SPLINE_CURVE ( 2, ( #9682, #37979, #32702, #55711, #4025, #20605, #60603, #8927, #49277 ),
 .UNSPECIFIED., .F., .F. ) 
 B_SPLINE_CURVE_WITH_KNOTS ( ( 3, 2, 2, 2, 3 ),
 ( 0.6527777777777777901, 0.6597222222222222099, 0.6666666666666665186, 0.6736111111111110494, 0.6805555555555554692 ),
 .UNSPECIFIED. ) 
 CURVE ( )  GEOMETRIC_REPRESENTATION_ITEM ( )  RATIONAL_B_SPLINE_CURVE ( ( 1.000000000000000000, 0.9238795325112867385, 1.000000000000000000, 0.9238795325112867385, 1.000000000000000000, 0.9238795325112867385, 1.000000000000000000, 0.9238795325112879597, 0.9999999999999987788 ) ) 
 REPRESENTATION_ITEM ( '' )  );
#1148=ORIENTED_EDGE ( 'NONE', *, *, #4407, .T. ) ;
#1157=CARTESIAN_POINT ( 'NONE',  ( -3.313708498984762496, 98.28125000000000000, 7.999999999999998224 ) ) ;
#1163=CARTESIAN_POINT ( 'NONE',  ( -2.977408999572654480, 6.374999997951610098, 7.188101187499999156 ) ) ;
#1165=CARTESIAN_POINT ( 'NONE',  ( -2.977408999572650927, 116.7500000020483810, -7.188101187500000933 ) ) ;
#1183=CYLINDRICAL_SURFACE ( 'NONE', #3487, 8.000000000000000000 ) ;
#1185=CARTESIAN_POINT ( 'NONE',  ( -4.401442555609581635E-16, 107.2812500020483810, -7.188101187500000044 ) ) ;
#1191=CARTESIAN_POINT ( 'NONE',  ( 2.977408999572654480, 117.5000000020483810, 7.188101187499999156 ) ) ;
#1194=ORIENTED_EDGE ( 'NONE', *, *, #15500, .T. ) ;
#1200=CARTESIAN_POINT ( 'NONE',  ( -5.656854249492378806, 108.6874999999999858, 5.656854249492381470 ) ) ;
#1217=VERTEX_POINT ( 'NONE', #71703 ) ;
#1218=CARTESIAN_POINT ( 'NONE',  ( 7.999999999999998224, 4.406250000000000000, 3.313708498984766493 ) ) ;
#1220=CARTESIAN_POINT ( 'NONE',  ( 7.188101187500001821, 3.562499997951610542, -2.977408999572650483 ) ) ;
#1221=CARTESIAN_POINT ( 'NONE',  ( 1.469576158976823947E-15, 119.5625000040967763, 8.000000000000000000 ) ) ;
#1227=ORIENTED_EDGE ( 'NONE', *, *, #62624, .F. ) ;
#1228=EDGE_CURVE ( 'NONE', #23857, #38745, #61384, .T. ) ;
#1247=CARTESIAN_POINT ( 'NONE',  ( 5.656854249492379694, 116.9375000000000000, -5.656854249492380582 ) ) ;
#1250=ORIENTED_EDGE ( 'NONE', *, *, #4932, .T. ) ;
#1252=CARTESIAN_POINT ( 'NONE',  ( -8.000000000000001776, 14.15624999590322730, 3.313708498984759387 ) ) ;
#1273=CARTESIAN_POINT ( 'NONE',  ( 1.320432766682874540E-15, 121.5312500020483810, 7.188101187500000044 ) ) ;
#1280=CARTESIAN_POINT ( 'NONE',  ( 5.082755093536325042, 98.09375000204838102, -5.082755093536325930 ) ) ;
#1285=ORIENTED_EDGE ( 'NONE', *, *, #28712, .F. ) ;
#1307=CARTESIAN_POINT ( 'NONE',  ( 2.977408999572651815, 18.18749999795161187, 7.188101187500000933 ) ) ;
#1311=CARTESIAN_POINT ( 'NONE',  ( 4.401442555609581635E-16, 11.71874999795161010, -7.188101187500000044 ) ) ;
#1324=CARTESIAN_POINT ( 'NONE',  ( 5.082755093536325042, 116.0937500020483810, -5.082755093536325930 ) ) ;
#1330=CARTESIAN_POINT ( 'NONE',  ( -2.977408999572654480, 20.99999999795161898, 7.188101187499999156 ) ) ;
#1333=CARTESIAN_POINT ( 'NONE',  ( 8.000000000000000000, 13.50000000000000178, 0.000000000000000000 ) ) ;
#1336=CARTESIAN_POINT ( 'NONE',  ( 5.082755093536326818, 99.59375000204838102, 5.082755093536325042 ) ) ;
#1349=CARTESIAN_POINT ( 'NONE',  ( 3.313708498984869077, 91.53125000000000000, -7.999999999999892530 ) ) ;
#1354=CARTESIAN_POINT ( 'NONE',  ( 3.313708498984706985, 111.0312500000000284, -8.000000000000055067 ) ) ;
#1364=CARTESIAN_POINT ( 'NONE',  ( -7.188101187500000044, 116.6562500020483810, 0.000000000000000000 ) ) ;
#1375=CARTESIAN_POINT ( 'NONE',  ( 8.000000000000000000, 109.2500000000000000, -9.797174393178825657E-16 ) ) ;
#1384=CARTESIAN_POINT ( 'NONE',  ( 0.000000000000000000, 125.0000000000000000, 0.000000000000000000 ) ) ;
#1388=CARTESIAN_POINT ( 'NONE',  ( -1.469576158976823947E-15, 26.43749999590322375, 8.000000000000000000 ) ) ;
#1389=VERTEX_POINT ( 'NONE', #37725 ) ;
#1395=CARTESIAN_POINT ( 'NONE',  ( 7.188101187499999156, 9.749999997951610098, 2.977408999572654924 ) ) ;
#1400=DIRECTION ( 'NONE',  ( -0.000000000000000000, 1.000000000000000000, -0.000000000000000000 ) ) ;
#1401=CARTESIAN_POINT ( 'NONE',  ( 8.000000000000000000, 98.93750000409677625, -9.797174393178825657E-16 ) ) ;
#1414=CARTESIAN_POINT ( 'NONE',  ( 5.656854249492380582, 24.18750000000000355, -5.656854249492380582 ) ) ;
#1420=AXIS2_PLACEMENT_3D ( 'NONE', #39706, #32957, #55962 ) ;
#1424=CARTESIAN_POINT ( 'NONE',  ( 2.977408999572652260, 6.187499997951610986, 7.188101187500000044 ) ) ;
#1428=CARTESIAN_POINT ( 'NONE',  ( -2.977408999572651815, 120.3125000020483668, 7.188101187500000933 ) ) ;
#1441=CARTESIAN_POINT ( 'NONE',  ( 3.313708498984765161, 104.6562500040968047, 7.999999999999998224 ) ) ;
#1447=CARTESIAN_POINT ( 'NONE',  ( -3.313708498984760276, 1.968750000000000444, -8.000000000000000000 ) ) ;
#1455=CARTESIAN_POINT ( 'NONE',  ( -5.082755093536325042, 20.90624999795161543, -5.082755093536325930 ) ) ;
#1457=CARTESIAN_POINT ( 'NONE',  ( -7.188101187500000044, 100.5312500020483810, 0.000000000000000000 ) ) ;
#1472=CYLINDRICAL_SURFACE ( 'NONE', #62506, 8.000000000000000000 ) ;
#1473=CARTESIAN_POINT ( 'NONE',  ( 7.188101187500000044, 90.40625000204838102, -8.802885111219163269E-16 ) ) ;
#1478=CARTESIAN_POINT ( 'NONE',  ( -7.188101187500000044, 93.03125000204836681, 0.000000000000000000 ) ) ;
#1504=CARTESIAN_POINT ( 'NONE',  ( 8.000000000000000000, 102.0312500040967905, -3.313708498984762496 ) ) ;
#1508=DIRECTION ( 'NONE',  ( -0.000000000000000000, 1.000000000000000000, -0.000000000000000000 ) ) ;
#1514=CARTESIAN_POINT ( 'NONE',  ( 7.188101187500001821, 101.0000000020483810, -2.977408999572651371 ) ) ;
#1535=CARTESIAN_POINT ( 'NONE',  ( -7.188101187500000044, 7.593749997951610986, -8.802885111219163269E-16 ) ) ;
#1538=CARTESIAN_POINT ( 'NONE',  ( -7.188101187499999156, 118.6250000020483810, 2.977408999572654924 ) ) ;
#1542=CARTESIAN_POINT ( 'NONE',  ( -1.469576158976823947E-15, 4.125000000000000888, 8.000000000000000000 ) ) ;
#1557=CARTESIAN_POINT ( 'NONE',  ( 9.797174393178825657E-16, 125.0000000000000000, -8.000000000000000000 ) ) ;
#1558=CARTESIAN_POINT ( 'NONE',  ( -2.977408999572650927, 105.8750000020483668, -7.188101187500000933 ) ) ;
#1563=CARTESIAN_POINT ( 'NONE',  ( -4.401442555609581635E-16, 113.6562500020483952, -7.188101187500000044 ) ) ;
#1568=ORIENTED_EDGE ( 'NONE', *, *, #7512, .T. ) ;
#1584=CARTESIAN_POINT ( 'NONE',  ( -5.656854249492381470, 6.937500000000000888, 5.656854249492379694 ) ) ;
#1585=CARTESIAN_POINT ( 'NONE',  ( -1.469576158976823947E-15, 11.62500000000000178, 8.000000000000000000 ) ) ;
#1587=CARTESIAN_POINT ( 'NONE',  ( -7.188101187500000044, 27.09374999795161898, -8.802885111219163269E-16 ) ) ;
#1596=EDGE_CURVE ( 'NONE', #38779, #65598, #30095, .T. ) ;
#1598=CARTESIAN_POINT ( 'NONE',  ( -5.656854249492381470, 15.93750000000000355, 5.656854249492379694 ) ) ;
#1599=EDGE_CURVE ( 'NONE', #73206, #64471, #35405, .T. ) ;
#1609=CARTESIAN_POINT ( 'NONE',  ( 8.000000000000000000, 104.7500000000000000, -9.797174393178825657E-16 ) ) ;
#1612=CARTESIAN_POINT ( 'NONE',  ( 3.313708498984765161, 120.9687500000000284, 7.999999999999998224 ) ) ;
#1617=CARTESIAN_POINT ( 'NONE',  ( -3.313708498984760720, 12.28124999590322375, -8.000000000000000000 ) ) ;
#1639=CARTESIAN_POINT ( 'NONE',  ( 5.082755093536325042, 123.5937500020483952, -5.082755093536325930 ) ) ;
#1643=CARTESIAN_POINT ( 'NONE',  ( -2.977408999572651815, 97.43750000204839523, 7.188101187500000933 ) ) ;
#1660=CARTESIAN_POINT ( 'NONE',  ( 8.000000000000000000, 17.90624999590322375, -3.313708498984761164 ) ) ;
#1664=CARTESIAN_POINT ( 'NONE',  ( 7.188101187499999156, 27.74999999795161543, 2.977408999572654924 ) ) ;
#1672=CARTESIAN_POINT ( 'NONE',  ( -7.188101187500001821, 13.12499999795161187, -2.977408999572651371 ) ) ;
#1674=CARTESIAN_POINT ( 'NONE',  ( 0.6939194017716557861, 124.5665190883579783, -7.910544316330307524 ) ) ;
#1675=CARTESIAN_POINT ( 'NONE',  ( -5.082755093536326818, 9.281249997951610098, 5.082755093536325042 ) ) ;
#1679=AXIS2_PLACEMENT_3D ( 'NONE', #15570, #31445, #66895 ) ;
#1682=ORIENTED_EDGE ( 'NONE', *, *, #21963, .T. ) ;
#1689=CARTESIAN_POINT ( 'NONE',  ( -7.188101187499999156, 116.7500000020483810, 2.977408999572654924 ) ) ;
#1690=DIRECTION ( 'NONE',  ( -0.000000000000000000, 1.000000000000000000, -0.000000000000000000 ) ) ;
#1693=CARTESIAN_POINT ( 'NONE',  ( 4.401442555609581635E-16, 20.34374999795161543, -7.188101187500000044 ) ) ;
#1700=CARTESIAN_POINT ( 'NONE',  ( -5.082755093536324154, 99.21875000204838102, 5.082755093536326818 ) ) ;
#1720=CARTESIAN_POINT ( 'NONE',  ( 5.656854249492379694, 110.9375000000000000, -5.656854249492380582 ) ) ;
#1721=FACE_OUTER_BOUND ( 'NONE', #24090, .T. ) ;
#1724=DIRECTION ( 'NONE',  ( -0.000000000000000000, 1.000000000000000000, -0.000000000000000000 ) ) ;
#1729=CARTESIAN_POINT ( 'NONE',  ( -2.977408999572650927, 117.8750000020483810, -7.188101187500001821 ) ) ;
#1736=CARTESIAN_POINT ( 'NONE',  ( 1.469576158976823947E-15, 92.56250000409677625, 8.000000000000000000 ) ) ;
#1737=CARTESIAN_POINT ( 'NONE',  ( 1.469576158976823947E-15, 108.8750000000000000, 8.000000000000000000 ) ) ;
#1751=ORIENTED_EDGE ( 'NONE', *, *, #12564, .F. ) ;
#1757=CARTESIAN_POINT ( 'NONE',  ( -5.082755093536326818, 15.28124999795161187, 5.082755093536325042 ) ) ;
#1765=CARTESIAN_POINT ( 'NONE',  ( -8.000000000000000000, 98.18750000409677625, 0.000000000000000000 ) ) ;
#1772=CARTESIAN_POINT ( 'NONE',  ( -1.469576158976823947E-15, 26.62500000000000355, 8.000000000000000000 ) ) ;
#1781=CARTESIAN_POINT ( 'NONE',  ( 5.082755093536324154, 3.281249997951610098, 5.082755093536326818 ) ) ;
#1783=CARTESIAN_POINT ( 'NONE',  ( -2.977408999572651815, 118.8125000020484094, 7.188101187500000933 ) ) ;
#1794=CARTESIAN_POINT ( 'NONE',  ( 8.000000000000001776, 104.8437500040967763, 3.313708498984759387 ) ) ;
#1807=CARTESIAN_POINT ( 'NONE',  ( 2.977408999572650927, 22.12499999795161543, -7.188101187500001821 ) ) ;
#1809=CARTESIAN_POINT ( 'NONE',  ( 7.188101187500000933, 93.87500000204838102, -2.977408999572651371 ) ) ;
#1818=CYLINDRICAL_SURFACE ( 'NONE', #45959, 8.000000000000000000 ) ;
#1833=CARTESIAN_POINT ( 'NONE',  ( 5.082755093536326818, 92.09375000204838102, 5.082755093536325042 ) ) ;
#1853=CARTESIAN_POINT ( 'NONE',  ( 8.000000000000001776, 100.3437500040967905, 3.313708498984759387 ) ) ;
#1856=LINE ( 'NONE', #47860, #69782 ) ;
#1862=CARTESIAN_POINT ( 'NONE',  ( -5.082755093536325930, 99.96875000204838102, -5.082755093536325930 ) ) ;
#1863=VECTOR ( 'NONE', #60276, 1000.000000000000000 ) ;
#1868=CARTESIAN_POINT ( 'NONE',  ( -5.656854249492378806, 101.3750000040967905, 5.656854249492381470 ) ) ;
#1872=VERTEX_POINT ( 'NONE', #7481 ) ;
#1883=CARTESIAN_POINT ( 'NONE',  ( -1.469576158976823947E-15, 3.937499995903220640, 8.000000000000000000 ) ) ;
#1885=CARTESIAN_POINT ( 'NONE',  ( 2.977408999572650927, 7.124999997951610098, -7.188101187500001821 ) ) ;
#1888=CARTESIAN_POINT ( 'NONE',  ( 2.977408999572650039, 116.5625000020483810, -7.188101187500000933 ) ) ;
#1897=CARTESIAN_POINT ( 'NONE',  ( 3.313708498984846429, 111.9687500000000000, 7.999999999999918288 ) ) ;
#1908=CARTESIAN_POINT ( 'NONE',  ( -2.977408999572652260, 104.9375000020483810, 7.188101187500000044 ) ) ;
#1914=CARTESIAN_POINT ( 'NONE',  ( -2.977408999572651815, 108.3125000020483810, 7.188101187500000933 ) ) ;
#1932=CARTESIAN_POINT ( 'NONE',  ( -8.000000000000000000, 122.0937500040967905, -3.313708498984761164 ) ) ;
#1937=VERTEX_POINT ( 'NONE', #59531 ) ;
#1938=CARTESIAN_POINT ( 'NONE',  ( -3.313708498984760720, 3.468750000000000444, -8.000000000000000000 ) ) ;
#1940=CARTESIAN_POINT ( 'NONE',  ( -1.320432766682874540E-15, 4.593749997951610986, 7.188101187500000044 ) ) ;
#1941=CARTESIAN_POINT ( 'NONE',  ( -5.656854249492380582, 120.5000000040967905, -5.656854249492380582 ) ) ;
#1944=DIRECTION ( 'NONE',  ( 0.000000000000000000, 0.000000000000000000, 1.000000000000000000 ) ) ;
#1958=ORIENTED_EDGE ( 'NONE', *, *, #28415, .T. ) ;
#1963=CARTESIAN_POINT ( 'NONE',  ( -4.898587196589412829E-16, 105.1250000000000000, -8.000000000000000000 ) ) ;
#1966=CARTESIAN_POINT ( 'NONE',  ( 5.656854249492379694, 119.9375000000000000, -5.656854249492380582 ) ) ;
#1969=ORIENTED_EDGE ( 'NONE', *, *, #25390, .F. ) ;
#1971=CARTESIAN_POINT ( 'NONE',  ( -8.000000000000001776, 12.65624999590322375, 3.313708498984759387 ) ) ;
#1985=ORIENTED_EDGE ( 'NONE', *, *, #25955, .F. ) ;
#1999=CARTESIAN_POINT ( 'NONE',  ( -2.977408999572651815, 92.93750000204839523, 7.188101187500000933 ) ) ;
#2028=CARTESIAN_POINT ( 'NONE',  ( 7.188101187499999156, 15.37499999795161187, 2.977408999572654924 ) ) ;
#2031=CARTESIAN_POINT ( 'NONE',  ( 7.188101187500001821, 12.93749999795161365, -2.977408999572650483 ) ) ;
#2043=CARTESIAN_POINT ( 'NONE',  ( 2.977408999572650039, 116.1875000020483952, -7.188101187500001821 ) ) ;
#2047=CARTESIAN_POINT ( 'NONE',  ( -5.082755093536326818, 22.40624999795161187, 5.082755093536325042 ) ) ;
#2053=CARTESIAN_POINT ( 'NONE',  ( -7.188101187499999156, 97.62500000204836681, 2.977408999572654924 ) ) ;
#2056=LINE ( 'NONE', #71072, #6048 ) ;
#2082=CARTESIAN_POINT ( 'NONE',  ( -5.082755093536325930, 113.4687500020483810, -5.082755093536325930 ) ) ;
#2103=ORIENTED_EDGE ( 'NONE', *, *, #23555, .F. ) ;
#2110=CARTESIAN_POINT ( 'NONE',  ( -1.320432766682874540E-15, 9.468749997951610098, 7.188101187500000044 ) ) ;
#2124=EDGE_CURVE ( 'NONE', #48333, #2977, #20922, .T. ) ;
#2127=CARTESIAN_POINT ( 'NONE',  ( -5.656854249492379694, 24.56250000000000355, -5.656854249492380582 ) ) ;
#2139=CARTESIAN_POINT ( 'NONE',  ( -2.977408999572650039, 2.437499997951610542, -7.188101187500000933 ) ) ;
#2140=EDGE_CURVE ( 'NONE', #59499, #25519, #30674, .T. ) ;
#2141=CARTESIAN_POINT ( 'NONE',  ( 7.188101187500002709, 117.6875000020484094, 2.977408999572649151 ) ) ;
#2152=CARTESIAN_POINT ( 'NONE',  ( 5.656854249492378806, 2.812500000000000444, 5.656854249492381470 ) ) ;
#2163=ORIENTED_EDGE ( 'NONE', *, *, #45223, .T. ) ;
#2168=CARTESIAN_POINT ( 'NONE',  ( -7.188101187500001821, 26.99999999795161543, -2.977408999572651371 ) ) ;
#2170=CARTESIAN_POINT ( 'NONE',  ( 7.188101187500002709, 92.18750000204838102, 2.977408999572649151 ) ) ;
#2188=CARTESIAN_POINT ( 'NONE',  ( -5.082755093536325930, 89.46875000204838102, -5.082755093536325930 ) ) ;
#2194=CARTESIAN_POINT ( 'NONE',  ( -5.082755093536324154, 93.21875000204838102, 5.082755093536326818 ) ) ;
#2214=CARTESIAN_POINT ( 'NONE',  ( -3.313708498984770934, 3.843749995903220196, 7.999999999999992895 ) ) ;
#2216=CARTESIAN_POINT ( 'NONE',  ( -4.898587196589412829E-16, 100.8125000040967763, -8.000000000000000000 ) ) ;
#2223=ORIENTED_EDGE ( 'NONE', *, *, #31265, .T. ) ;
#2225=CARTESIAN_POINT ( 'NONE',  ( 1.320432766682874540E-15, 97.53125000204838102, 7.188101187500000044 ) ) ;
#2231=CARTESIAN_POINT ( 'NONE',  ( -3.313708498984762496, 101.4687500040967763, 7.999999999999998224 ) ) ;
#2235=( BOUNDED_SURFACE ( )  B_SPLINE_SURFACE ( 1, 2, ( 
 ( #13912, #65240, #3369, #59957, #19959, #8653, #8275, #65616, #43725, #66361, #53567, #53935, #71265, #25977, #55060, #49002, #31668, #26356, #19584, #36951, #37706, #25614, #59235, #20326, #65986, #2625, #43342, #60707, #1883, #9027, #7908, #14291, #32040, #24869, #47888, #49377, #72396, #25242, #70908, #31285, #19222, #20708, #54314, #42227, #13544, #36584, #59595, #2249, #48258, #48628, #71636, #22195, #4493, #50499, #10146, #67492, #44108, #33551, #27485, #38825, #72779, #32800, #27865, #3742, #21820, #15044, #44852, #21085, #73148, #56555, #33927, #56180, #21455, #15790, #33184, #74259, #9403, #50875, #28242, #32422, #51250, #10519, #67118, #15412, #4127, #61455, #27118, #38453, #67858, #44478, #73891, #66739, #9781, #4870, #16527, #55809, #56926, #26742, #38079, #50132, #16150, #49762, #61827, #73513, #39190, #45220, #62193, #68232, #39566, #62562, #22568, #61077, #10893, #5241, #55433, #54028, #69527, #1617, #58958, #36677, #46880, #1971, #12905, #41228, #7265, #2338, #70270, #46508, #31003, #18583, #19308, #29905, #24963, #58230, #17839, #41595, #35213, #1252, #7997, #52546, #23870, #41952, #52919, #64235, #7634, #24230, #885, #12545, #69903, #53293, #40855, #6529, #58587, #24599, #63862, #47978, #29535, #70991, #12175, #30640, #70629, #18215, #47244, #35573, #6893, #64609, #42318, #35939, #30274, #47605, #18948, #64960, #13269, #36308, #59325, #65336, #53659, #13638, #59689, #49473, #9118, #60419, #15508, #72492, #32898, #31379, #54405, #3087, #55902, #54776, #26072, #31755, #21173, #43819, #66451, #66075, #8746, #61549, #20801, #60042, #3840, #14758, #14385, #48720, #9870, #25332, #49093, #48347, #71354, #32517, #72106, #32135, #3459, #2712, #15136, #20418, #19677, #66834, #38169, #49850, #55153, #9502, #26448, #38548, #42689, #65701, #61172, #37797, #14005, #25699, #55530, #60793, #20041, #26836, #37042, #43435, #8363, #71727, #72869, #44198, #43059, #67211, #37419, #11353, #50220, #11721, #5327, #34388, #33638, #57389, #22283, #57015, #10612, #4959, #17372, #34018, #56645, #63028, #4214, #4584, #16999, #28696, #33267, #69068, #15881, #27203, #44944, #28330, #61914, #27579, #27961, #10240, #5697, #39653, #10984, #68690, #50588, #63395, #34761, #74346, #73606, #38913, #73241, #51338, #62651, #21546, #22656, #51710, #45675 ),
 ( #57, #40397, #40026, #23038, #46049, #44572, #67585, #56266, #21913, #50966, #67951, #45306, #16244, #73979, #68320, #39282, #62284, #16618, #29817, #30555, #41140, #13182, #69437, #65242, #6804, #46423, #12456, #19224, #63770, #35124, #53201, #64146, #52459, #18861, #35485, #12087, #797, #58140, #64519, #57763, #17748, #69809, #12817, #42230, #59238, #40763, #7547, #6069, #41867, #7178, #52096, #58498, #23783, #23407, #29449, #53569, #52830, #428, #6447, #1163, #29076, #24141, #46787, #13548, #36220, #18125, #64880, #1885, #30184, #41502, #47152, #47890, #1535, #70185, #18494, #35852, #58867, #24515, #47519, #70545, #24871, #70910, #55062, #2998, #2627, #71639, #44112, #60327, #25244, #65988, #72782, #42603, #13914, #32042, #42967, #31287, #72399, #14293, #65618, #54317, #36953, #43345, #36586, #48261, #48630, #66363, #21088, #38082, #71267, #61079, #59597, #20710, #60709, #30916, #37330, #25616, #2251, #8277, #9407, #8655, #53937, #19587, #31670, #7910, #54689, #59959, #67121, #15046, #19961, #43727, #66741, #9029, #20329, #25979, #26746, #3371, #49004, #72014, #14668, #37708, #26358, #49380, #32425, #55436, #3746, #49765, #56558, #56184, #50502, #51628, #62566, #50136, #68606, #4873, #4496, #38828, #74643, #22958, #73516, #15416, #45967, #22572, #62197, #22198, #68237, #67495, #5245, #21823, #61458, #10896, #33930, #39938, #73894, #74264, #16530, #5615, #38456, #9784, #45224, #27868, #28615, #15793, #45592, #50878, #10150, #39570, #32804, #39194, #55813, #4130, #16915, #62944, #27121, #56929, #11268, #34300, #73151, #21459, #28245, #57303, #44855, #44481, #33554, #51253, #67861, #16154, #61831, #33187, #27489, #10522, #41791, #52379, #24436, #5987, #1455, #12376, #47071, #715, #69728, #7468, #68981, #53490, #41058, #64799, #23699, #47444, #28989, #1807, #18043, #57679, #46704, #30473, #345, #46337, #64440, #64068, #63684, #30105, #35412, #23325, #12011, #69353, #1085, #17290, #52007, #6367, #24061, #24793, #70468, #17664, #18785, #40309, #53122, #18414, #63311, #58422, #35044, #34674, #40682, #13102, #6728, #11638, #58056, #29734, #29373, #52749, #70108, #41428, #36138, #12740, #59159, #35771, #58787, #7097, #8196, #37996, #20243, #55353, #53856, #2168, #25533, #3658, #2541, #48546, #54233, #43641, #66278, #14209, #13829 ) ),
 .UNSPECIFIED., .F., .F., .F. ) 
 B_SPLINE_SURFACE_WITH_KNOTS ( ( 2, 2 ),
 ( 3, 2, 2, 2, 2, 2, 2, 2, 2, 2, 2, 2, 2, 2, 2, 2, 2, 2, 2, 2, 2, 2, 2, 2, 2, 2, 2, 2, 2, 2, 2, 2, 2, 2, 2, 2, 2, 2, 2, 2, 2, 2, 2, 2, 2, 2, 2, 2, 2, 2, 2, 2, 2, 2, 2, 2, 2, 2, 2, 2, 2, 2, 2, 2, 2, 2, 2, 2, 2, 2, 2, 2, 2, 2, 2, 2, 2, 2, 2, 2, 2, 2, 2, 2, 2, 2, 2, 2, 2, 2, 2, 2, 2, 2, 2, 2, 2, 2, 2, 2, 2, 2, 2, 2, 2, 2, 2, 2, 2, 2, 2, 2, 2, 2, 2, 2, 2, 2, 2, 2, 2, 2, 2, 2, 2, 2, 2, 2, 2, 2, 2, 2, 2, 2, 2, 2, 2, 2, 2, 2, 2, 2, 2, 2, 3 ),
 ( 0.000000000000000000, 1.000000000000000000 ),
 ( 0.000000000000000000, 0.006944444444444444059, 0.01388888888888888812, 0.02083333333333333218, 0.02777777777777777624, 0.03472222222222222376, 0.04166666666666666435, 0.04861111111111111188, 0.05555555555555555247, 0.06250000000000000000, 0.06944444444444444753, 0.07638888888888889506, 0.08333333333333332871, 0.09027777777777777624, 0.09722222222222222376, 0.1041666666666666713, 0.1111111111111111049, 0.1180555555555555525, 0.1250000000000000000, 0.1319444444444444475, 0.1388888888888888951, 0.1458333333333333426, 0.1527777777777777901, 0.1597222222222222099, 0.1666666666666666574, 0.1736111111111111049, 0.1805555555555555525, 0.1875000000000000000, 0.1944444444444444475, 0.2013888888888888951, 0.2083333333333333426, 0.2152777777777777901, 0.2222222222222222099, 0.2291666666666666574, 0.2361111111111111049, 0.2430555555555555525, 0.2500000000000000000, 0.2569444444444444198, 0.2638888888888888951, 0.2708333333333333148, 0.2777777777777777901, 0.2847222222222222099, 0.2916666666666666852, 0.2986111111111111049, 0.3055555555555555802, 0.3125000000000000000, 0.3194444444444444198, 0.3263888888888888951, 0.3333333333333333148, 0.3402777777777777901, 0.3472222222222222099, 0.3541666666666666852, 0.3611111111111111049, 0.3680555555555555802, 0.3750000000000000000, 0.3819444444444444198, 0.3888888888888888951, 0.3958333333333333148, 0.4027777777777777901, 0.4097222222222222099, 0.4166666666666666852, 0.4236111111111111049, 0.4305555555555555802, 0.4375000000000000000, 0.4444444444444444198, 0.4513888888888888951, 0.4583333333333333148, 0.4652777777777777901, 0.4722222222222222099, 0.4791666666666666852, 0.4861111111111111049, 0.4930555555555555802, 0.5000000000000000000, 0.5069444444444444198, 0.5138888888888888395, 0.5208333333333333703, 0.5277777777777777901, 0.5347222222222222099, 0.5416666666666666297, 0.5486111111111111605, 0.5555555555555555802, 0.5625000000000000000, 0.5694444444444444198, 0.5763888888888888395, 0.5833333333333333703, 0.5902777777777777901, 0.5972222222222222099, 0.6041666666666666297, 0.6111111111111111605, 0.6180555555555555802, 0.6250000000000000000, 0.6319444444444444198, 0.6388888888888888395, 0.6458333333333333703, 0.6527777777777777901, 0.6597222222222222099, 0.6666666666666666297, 0.6736111111111111605, 0.6805555555555555802, 0.6875000000000000000, 0.6944444444444444198, 0.7013888888888888395, 0.7083333333333333703, 0.7152777777777777901, 0.7222222222222222099, 0.7291666666666666297, 0.7361111111111111605, 0.7430555555555555802, 0.7500000000000000000, 0.7569444444444444198, 0.7638888888888888395, 0.7708333333333333703, 0.7777777777777777901, 0.7847222222222222099, 0.7916666666666666297, 0.7986111111111111605, 0.8055555555555555802, 0.8125000000000000000, 0.8194444444444444198, 0.8263888888888888395, 0.8333333333333333703, 0.8402777777777777901, 0.8472222222222222099, 0.8541666666666666297, 0.8611111111111111605, 0.8680555555555555802, 0.8750000000000000000, 0.8819444444444444198, 0.8888888888888888395, 0.8958333333333333703, 0.9027777777777777901, 0.9097222222222222099, 0.9166666666666666297, 0.9236111111111111605, 0.9305555555555555802, 0.9375000000000000000, 0.9444444444444444198, 0.9513888888888888395, 0.9583333333333333703, 0.9652777777777777901, 0.9722222222222222099, 0.9791666666666666297, 0.9861111111111111605, 0.9930555555555555802, 1.000000000000000000 ),
 .UNSPECIFIED. ) 
 GEOMETRIC_REPRESENTATION_ITEM ( )  RATIONAL_B_SPLINE_SURFACE ( (
 ( 1.000000000000000000, 0.9238795325112867385, 1.000000000000000000, 0.9238795325112867385, 1.000000000000000000, 0.9238795325112867385, 1.000000000000000000, 0.9238795325112867385, 1.000000000000000000, 0.9238795325112867385, 1.000000000000000000, 0.9238795325112867385, 1.000000000000000000, 0.9238795325112867385, 1.000000000000000000, 0.9238795325112867385, 1.000000000000000000, 0.9238795325112867385, 1.000000000000000000, 0.9238795325112867385, 1.000000000000000000, 0.9238795325112867385, 1.000000000000000000, 0.9238795325112867385, 1.000000000000000000, 0.9238795325112867385, 1.000000000000000000, 0.9238795325112867385, 1.000000000000000000, 0.9238795325112867385, 1.000000000000000000, 0.9238795325112867385, 1.000000000000000000, 0.9238795325112867385, 1.000000000000000000, 0.9238795325112867385, 1.000000000000000000, 0.9238795325112867385, 1.000000000000000000, 0.9238795325112867385, 1.000000000000000000, 0.9238795325112867385, 1.000000000000000000, 0.9238795325112867385, 1.000000000000000000, 0.9238795325112867385, 1.000000000000000000, 0.9238795325112867385, 1.000000000000000000, 0.9238795325112867385, 1.000000000000000000, 0.9238795325112867385, 1.000000000000000000, 0.9238795325112867385, 1.000000000000000000, 0.9238795325112867385, 1.000000000000000000, 0.9238795325112867385, 1.000000000000000000, 0.9238795325112867385, 1.000000000000000000, 0.9238795325112867385, 1.000000000000000000, 0.9238795325112867385, 1.000000000000000000, 0.9238795325112867385, 1.000000000000000000, 0.9238795325112867385, 1.000000000000000000, 0.9238795325112867385, 1.000000000000000000, 0.9238795325112867385, 1.000000000000000000, 0.9238795325112867385, 1.000000000000000000, 0.9238795325112867385, 1.000000000000000000, 0.9238795325112867385, 1.000000000000000000, 0.9238795325112867385, 1.000000000000000000, 0.9238795325112867385, 1.000000000000000000, 0.9238795325112867385, 1.000000000000000000, 0.9238795325112867385, 1.000000000000000000, 0.9238795325112867385, 1.000000000000000000, 0.9238795325112867385, 1.000000000000000000, 0.9238795325112867385, 1.000000000000000000, 0.9238795325112867385, 1.000000000000000000, 0.9238795325112867385, 1.000000000000000000, 0.9238795325112867385, 1.000000000000000000, 0.9238795325112867385, 1.000000000000000000, 0.9238795325112867385, 1.000000000000000000, 0.9238795325112867385, 1.000000000000000000, 0.9238795325112867385, 1.000000000000000000, 0.9238795325112867385, 1.000000000000000000, 0.9238795325112867385, 1.000000000000000000, 0.9238795325112867385, 1.000000000000000000, 0.9238795325112867385, 1.000000000000000000, 0.9238795325112867385, 1.000000000000000000, 0.9238795325112867385, 1.000000000000000000, 0.9238795325112867385, 1.000000000000000000, 0.9238795325112867385, 1.000000000000000000, 0.9238795325112867385, 1.000000000000000000, 0.9238795325112867385, 1.000000000000000000, 0.9238795325112867385, 1.000000000000000000, 0.9238795325112867385, 1.000000000000000000, 0.9238795325112867385, 1.000000000000000000, 0.9238795325112867385, 1.000000000000000000, 0.9238795325112867385, 1.000000000000000000, 0.9238795325112867385, 1.000000000000000000, 0.9238795325112867385, 1.000000000000000000, 0.9238795325112867385, 1.000000000000000000, 0.9238795325112867385, 1.000000000000000000, 0.9238795325112867385, 1.000000000000000000, 0.9238795325112867385, 1.000000000000000000, 0.9238795325112867385, 1.000000000000000000, 0.9238795325112867385, 1.000000000000000000, 0.9238795325112867385, 1.000000000000000000, 0.9238795325112867385, 1.000000000000000000, 0.9238795325112867385, 1.000000000000000000, 0.9238795325112867385, 1.000000000000000000, 0.9238795325112867385, 1.000000000000000000, 0.9238795325112867385, 1.000000000000000000, 0.9238795325112867385, 1.000000000000000000, 0.9238795325112867385, 1.000000000000000000, 0.9238795325112867385, 1.000000000000000000, 0.9238795325112867385, 1.000000000000000000, 0.9238795325112867385, 1.000000000000000000, 0.9238795325112867385, 1.000000000000000000, 0.9238795325112867385, 1.000000000000000000, 0.9238795325112867385, 1.000000000000000000, 0.9238795325112867385, 1.000000000000000000, 0.9238795325112867385, 1.000000000000000000, 0.9238795325112867385, 1.000000000000000000, 0.9238795325112867385, 1.000000000000000000, 0.9238795325112867385, 1.000000000000000000, 0.9238795325112867385, 1.000000000000000000, 0.9238795325112867385, 1.000000000000000000, 0.9238795325112867385, 1.000000000000000000, 0.9238795325112867385, 1.000000000000000000, 0.9238795325112867385, 1.000000000000000000, 0.9238795325112867385, 1.000000000000000000, 0.9238795325112867385, 1.000000000000000000, 0.9238795325112867385, 1.000000000000000000, 0.9238795325112867385, 1.000000000000000000, 0.9238795325112867385, 1.000000000000000000, 0.9238795325112867385, 1.000000000000000000, 0.9238795325112867385, 1.000000000000000000, 0.9238795325112867385, 1.000000000000000000, 0.9238795325112867385, 1.000000000000000000, 0.9238795325112867385, 1.000000000000000000, 0.9238795325112867385, 1.000000000000000000, 0.9238795325112867385, 1.000000000000000000, 0.9238795325112867385, 1.000000000000000000, 0.9238795325112867385, 1.000000000000000000, 0.9238795325112867385, 1.000000000000000000, 0.9238795325112867385, 1.000000000000000000, 0.9238795325112867385, 1.000000000000000000, 0.9238795325112867385, 1.000000000000000000, 0.9238795325112867385, 1.000000000000000000, 0.9238795325112867385, 1.000000000000000000, 0.9238795325112867385, 1.000000000000000000, 0.9238795325112867385, 1.000000000000000000, 0.9238795325112867385, 1.000000000000000000, 0.9238795325112867385, 1.000000000000000000, 0.9238795325112867385, 1.000000000000000000, 0.9238795325112867385, 1.000000000000000000, 0.9238795325112867385, 1.000000000000000000, 0.9238795325112867385, 1.000000000000000000, 0.9238795325112867385, 1.000000000000000000, 0.9238795325112867385, 1.000000000000000000, 0.9238795325112867385, 1.000000000000000000, 0.9238795325112867385, 1.000000000000000000, 0.9238795325112867385, 1.000000000000000000, 0.9238795325112867385, 1.000000000000000000, 0.9238795325112867385, 1.000000000000000000, 0.9238795325112867385, 1.000000000000000000, 0.9238795325112867385, 1.000000000000000000, 0.9238795325112867385, 1.000000000000000000, 0.9238795325112867385, 1.000000000000000000, 0.9238795325112867385, 1.000000000000000000, 0.9238795325112867385, 1.000000000000000000, 0.9238795325112867385, 1.000000000000000000, 0.9238795325112867385, 1.000000000000000000, 0.9238795325112867385, 1.000000000000000000),
 ( 1.000000000000000000, 0.9238795325112867385, 1.000000000000000000, 0.9238795325112867385, 1.000000000000000000, 0.9238795325112867385, 1.000000000000000000, 0.9238795325112867385, 1.000000000000000000, 0.9238795325112867385, 1.000000000000000000, 0.9238795325112867385, 1.000000000000000000, 0.9238795325112867385, 1.000000000000000000, 0.9238795325112867385, 1.000000000000000000, 0.9238795325112867385, 1.000000000000000000, 0.9238795325112867385, 1.000000000000000000, 0.9238795325112867385, 1.000000000000000000, 0.9238795325112867385, 1.000000000000000000, 0.9238795325112867385, 1.000000000000000000, 0.9238795325112867385, 1.000000000000000000, 0.9238795325112867385, 1.000000000000000000, 0.9238795325112867385, 1.000000000000000000, 0.9238795325112867385, 1.000000000000000000, 0.9238795325112867385, 1.000000000000000000, 0.9238795325112867385, 1.000000000000000000, 0.9238795325112867385, 1.000000000000000000, 0.9238795325112867385, 1.000000000000000000, 0.9238795325112867385, 1.000000000000000000, 0.9238795325112867385, 1.000000000000000000, 0.9238795325112867385, 1.000000000000000000, 0.9238795325112867385, 1.000000000000000000, 0.9238795325112867385, 1.000000000000000000, 0.9238795325112867385, 1.000000000000000000, 0.9238795325112867385, 1.000000000000000000, 0.9238795325112867385, 1.000000000000000000, 0.9238795325112867385, 1.000000000000000000, 0.9238795325112867385, 1.000000000000000000, 0.9238795325112867385, 1.000000000000000000, 0.9238795325112867385, 1.000000000000000000, 0.9238795325112867385, 1.000000000000000000, 0.9238795325112867385, 1.000000000000000000, 0.9238795325112867385, 1.000000000000000000, 0.9238795325112867385, 1.000000000000000000, 0.9238795325112867385, 1.000000000000000000, 0.9238795325112867385, 1.000000000000000000, 0.9238795325112867385, 1.000000000000000000, 0.9238795325112867385, 1.000000000000000000, 0.9238795325112867385, 1.000000000000000000, 0.9238795325112867385, 1.000000000000000000, 0.9238795325112867385, 1.000000000000000000, 0.9238795325112867385, 1.000000000000000000, 0.9238795325112867385, 1.000000000000000000, 0.9238795325112867385, 1.000000000000000000, 0.9238795325112867385, 1.000000000000000000, 0.9238795325112867385, 1.000000000000000000, 0.9238795325112867385, 1.000000000000000000, 0.9238795325112867385, 1.000000000000000000, 0.9238795325112867385, 1.000000000000000000, 0.9238795325112867385, 1.000000000000000000, 0.9238795325112867385, 1.000000000000000000, 0.9238795325112867385, 1.000000000000000000, 0.9238795325112867385, 1.000000000000000000, 0.9238795325112867385, 1.000000000000000000, 0.9238795325112867385, 1.000000000000000000, 0.9238795325112867385, 1.000000000000000000, 0.9238795325112867385, 1.000000000000000000, 0.9238795325112867385, 1.000000000000000000, 0.9238795325112867385, 1.000000000000000000, 0.9238795325112867385, 1.000000000000000000, 0.9238795325112867385, 1.000000000000000000, 0.9238795325112867385, 1.000000000000000000, 0.9238795325112867385, 1.000000000000000000, 0.9238795325112867385, 1.000000000000000000, 0.9238795325112867385, 1.000000000000000000, 0.9238795325112867385, 1.000000000000000000, 0.9238795325112867385, 1.000000000000000000, 0.9238795325112867385, 1.000000000000000000, 0.9238795325112867385, 1.000000000000000000, 0.9238795325112867385, 1.000000000000000000, 0.9238795325112867385, 1.000000000000000000, 0.9238795325112867385, 1.000000000000000000, 0.9238795325112867385, 1.000000000000000000, 0.9238795325112867385, 1.000000000000000000, 0.9238795325112867385, 1.000000000000000000, 0.9238795325112867385, 1.000000000000000000, 0.9238795325112867385, 1.000000000000000000, 0.9238795325112867385, 1.000000000000000000, 0.9238795325112867385, 1.000000000000000000, 0.9238795325112867385, 1.000000000000000000, 0.9238795325112867385, 1.000000000000000000, 0.9238795325112867385, 1.000000000000000000, 0.9238795325112867385, 1.000000000000000000, 0.9238795325112867385, 1.000000000000000000, 0.9238795325112867385, 1.000000000000000000, 0.9238795325112867385, 1.000000000000000000, 0.9238795325112867385, 1.000000000000000000, 0.9238795325112867385, 1.000000000000000000, 0.9238795325112867385, 1.000000000000000000, 0.9238795325112867385, 1.000000000000000000, 0.9238795325112867385, 1.000000000000000000, 0.9238795325112867385, 1.000000000000000000, 0.9238795325112867385, 1.000000000000000000, 0.9238795325112867385, 1.000000000000000000, 0.9238795325112867385, 1.000000000000000000, 0.9238795325112867385, 1.000000000000000000, 0.9238795325112867385, 1.000000000000000000, 0.9238795325112867385, 1.000000000000000000, 0.9238795325112867385, 1.000000000000000000, 0.9238795325112867385, 1.000000000000000000, 0.9238795325112867385, 1.000000000000000000, 0.9238795325112867385, 1.000000000000000000, 0.9238795325112867385, 1.000000000000000000, 0.9238795325112867385, 1.000000000000000000, 0.9238795325112867385, 1.000000000000000000, 0.9238795325112867385, 1.000000000000000000, 0.9238795325112867385, 1.000000000000000000, 0.9238795325112867385, 1.000000000000000000, 0.9238795325112867385, 1.000000000000000000, 0.9238795325112867385, 1.000000000000000000, 0.9238795325112867385, 1.000000000000000000, 0.9238795325112867385, 1.000000000000000000, 0.9238795325112867385, 1.000000000000000000, 0.9238795325112867385, 1.000000000000000000, 0.9238795325112867385, 1.000000000000000000, 0.9238795325112867385, 1.000000000000000000, 0.9238795325112867385, 1.000000000000000000, 0.9238795325112867385, 1.000000000000000000, 0.9238795325112867385, 1.000000000000000000, 0.9238795325112867385, 1.000000000000000000, 0.9238795325112867385, 1.000000000000000000, 0.9238795325112867385, 1.000000000000000000, 0.9238795325112867385, 1.000000000000000000, 0.9238795325112867385, 1.000000000000000000, 0.9238795325112867385, 1.000000000000000000, 0.9238795325112867385, 1.000000000000000000, 0.9238795325112867385, 1.000000000000000000, 0.9238795325112867385, 1.000000000000000000, 0.9238795325112867385, 1.000000000000000000, 0.9238795325112867385, 1.000000000000000000, 0.9238795325112867385, 1.000000000000000000, 0.9238795325112867385, 1.000000000000000000, 0.9238795325112867385, 1.000000000000000000, 0.9238795325112867385, 1.000000000000000000, 0.9238795325112867385, 1.000000000000000000, 0.9238795325112867385, 1.000000000000000000, 0.9238795325112867385, 1.000000000000000000, 0.9238795325112867385, 1.000000000000000000, 0.9238795325112867385, 1.000000000000000000, 0.9238795325112867385, 1.000000000000000000, 0.9238795325112867385, 1.000000000000000000) ) ) 
 REPRESENTATION_ITEM ( '' )  SURFACE ( )  );
#2249=CARTESIAN_POINT ( 'NONE',  ( 7.999999999999998224, 5.718749995903220196, 3.313708498984766493 ) ) ;
#2251=CARTESIAN_POINT ( 'NONE',  ( 4.401442555609581635E-16, 11.71874999795161010, -7.188101187500000044 ) ) ;
#2254=CARTESIAN_POINT ( 'NONE',  ( 7.188101187500000933, 111.8750000020483810, -2.977408999572651371 ) ) ;
#2259=CYLINDRICAL_SURFACE ( 'NONE', #29929, 8.000000000000000000 ) ;
#2273=CARTESIAN_POINT ( 'NONE',  ( -7.188101187499999156, 106.2500000020484094, 2.977408999572654924 ) ) ;
#2278=CARTESIAN_POINT ( 'NONE',  ( 1.320432766682874540E-15, 106.9062500020483810, 7.188101187500000044 ) ) ;
#2300=CARTESIAN_POINT ( 'NONE',  ( 4.898587196589412829E-16, 13.87500000000000178, -8.000000000000000000 ) ) ;
#2302=VECTOR ( 'NONE', #71596, 1000.000000000000000 ) ;
#2303=CARTESIAN_POINT ( 'NONE',  ( -7.188101187500001821, 2.624999997951610542, -2.977408999572651371 ) ) ;
#2304=CARTESIAN_POINT ( 'NONE',  ( -5.656854249492378806, 117.8750000040967905, 5.656854249492381470 ) ) ;
#2312=VERTEX_POINT ( 'NONE', #23159 ) ;
#2329=CARTESIAN_POINT ( 'NONE',  ( 8.000000000000001776, 104.6562499999999858, 3.313708498984759387 ) ) ;
#2331=CARTESIAN_POINT ( 'NONE',  ( 5.656854249492379694, 109.4375000000000000, -5.656854249492380582 ) ) ;
#2338=CARTESIAN_POINT ( 'NONE',  ( 3.313708498984762496, 13.03124999590322197, 7.999999999999998224 ) ) ;
#2341=CARTESIAN_POINT ( 'NONE',  ( 8.000000000000000000, 114.0312500040967763, -3.313708498984762496 ) ) ;
#2351=CARTESIAN_POINT ( 'NONE',  ( -7.999999999999998224, 107.2812500040967763, 3.313708498984766049 ) ) ;
#2361=CARTESIAN_POINT ( 'NONE',  ( -7.188101187500000933, 124.0625000020483810, -2.977408999572650483 ) ) ;
#2366=CARTESIAN_POINT ( 'NONE',  ( 1.320432766682874540E-15, 93.03125000204836681, 7.188101187500000044 ) ) ;
#2394=CARTESIAN_POINT ( 'NONE',  ( -7.188101187500002709, 20.81249999795161543, 2.977408999572649151 ) ) ;
#2396=CARTESIAN_POINT ( 'NONE',  ( 2.381929342089941226, 124.5336769686386589, -7.609644401984009932 ) ) ;
#2397=CARTESIAN_POINT ( 'NONE',  ( 7.188101187499999156, 12.74999999795161187, 2.977408999572654924 ) ) ;
#2400=AXIS2_PLACEMENT_3D ( 'NONE', #62351, #7161, #11427 ) ;
#2410=EDGE_CURVE ( 'NONE', #28168, #3547, #54517, .T. ) ;
#2412=CARTESIAN_POINT ( 'NONE',  ( 7.188101187500001821, 111.5000000020483810, -2.977408999572651371 ) ) ;
#2416=CARTESIAN_POINT ( 'NONE',  ( -2.977408999572650039, 20.43749999795161543, -7.188101187500000933 ) ) ;
#2422=CARTESIAN_POINT ( 'NONE',  ( -5.082755093536324154, 94.71875000204838102, 5.082755093536326818 ) ) ;
#2451=CARTESIAN_POINT ( 'NONE',  ( -0.5119134307784274363, 124.5885204352452718, -7.911479564754728244 ) ) ;
#2454=CARTESIAN_POINT ( 'NONE',  ( 2.977408999572650039, 107.1875000020483810, -7.188101187500001821 ) ) ;
#2459=CARTESIAN_POINT ( 'NONE',  ( -3.313708498984765161, 24.84374999590322375, 7.999999999999998224 ) ) ;
#2482=CARTESIAN_POINT ( 'NONE',  ( -7.188101187500000933, 13.49999999795161187, -2.977408999572651371 ) ) ;
#2491=LINE ( 'NONE', #25484, #22998 ) ;
#2499=CARTESIAN_POINT ( 'NONE',  ( -8.000000000000001776, 23.34375000000000355, 3.313708498984759387 ) ) ;
#2510=CARTESIAN_POINT ( 'NONE',  ( -7.188101187500000044, 4.218749997951610986, -8.802885111219163269E-16 ) ) ;
#2513=CARTESIAN_POINT ( 'NONE',  ( -7.188101187500001821, 119.9375000020483952, -2.977408999572650483 ) ) ;
#2527=EDGE_LOOP ( 'NONE', ( #71396, #50876, #73650, #74434 ) ) ;
#2529=CARTESIAN_POINT ( 'NONE',  ( -4.898587196589412829E-16, 102.1250000000000000, -8.000000000000000000 ) ) ;
#2541=CARTESIAN_POINT ( 'NONE',  ( -5.082755093536326818, 27.28124999795161543, 5.082755093536325042 ) ) ;
#2544=CARTESIAN_POINT ( 'NONE',  ( 7.188101187500000044, 92.28125000204836681, -8.802885111219163269E-16 ) ) ;
#2554=CARTESIAN_POINT ( 'NONE',  ( 4.898587196589412829E-16, 9.187499995903221972, -8.000000000000000000 ) ) ;
#2559=VERTEX_POINT ( 'NONE', #45622 ) ;
#2562=CARTESIAN_POINT ( 'NONE',  ( -3.313708498984707429, 102.2187500000000284, -8.000000000000055067 ) ) ;
#2568=( BOUNDED_CURVE ( )  B_SPLINE_CURVE ( 2, ( #7082, #53477, #47056, #70093, #18399, #1794, #30088, #1441, #18771 ),
 .UNSPECIFIED., .F., .F. ) 
 B_SPLINE_CURVE_WITH_KNOTS ( ( 3, 2, 2, 2, 3 ),
 ( 0.5104166666666666297, 0.5156250000000000000, 0.5208333333333333703, 0.5260416666666666297, 0.5312500000000000000 ),
 .UNSPECIFIED. ) 
 CURVE ( )  GEOMETRIC_REPRESENTATION_ITEM ( )  RATIONAL_B_SPLINE_CURVE ( ( 1.000000000000000000, 0.9238795325112867385, 1.000000000000000000, 0.9238795325112867385, 1.000000000000000000, 0.9238795325112867385, 1.000000000000000000, 0.9238795325112867385, 1.000000000000000000 ) ) 
 REPRESENTATION_ITEM ( '' )  );
#2570=CARTESIAN_POINT ( 'NONE',  ( -7.999999999999998224, 113.2812500040967763, 3.313708498984766049 ) ) ;
#2577=LINE ( 'NONE', #25566, #1863 ) ;
#2592=AXIS2_PLACEMENT_3D ( 'NONE', #46437, #48925, #54240 ) ;
#2594=CARTESIAN_POINT ( 'NONE',  ( 8.000000000000000000, 98.93750000409677625, -9.797174393178825657E-16 ) ) ;
#2604=CARTESIAN_POINT ( 'NONE',  ( -4.401442555609581635E-16, 98.28125000204838102, -7.188101187500000044 ) ) ;
#2605=CARTESIAN_POINT ( 'NONE',  ( 5.656854249492380582, 16.49999999590322375, -5.656854249492380582 ) ) ;
#2625=CARTESIAN_POINT ( 'NONE',  ( -8.000000000000001776, 3.656249995903220196, 3.313708498984759387 ) ) ;
#2627=CARTESIAN_POINT ( 'NONE',  ( 4.401442555609581635E-16, 8.718749997951611874, -7.188101187500000044 ) ) ;
#2628=CIRCLE ( 'NONE', #18303, 11.00000000000000000 ) ;
#2631=CARTESIAN_POINT ( 'NONE',  ( -2.977408999572652260, 111.3125000020483810, 7.188101187500000044 ) ) ;
#2648=CARTESIAN_POINT ( 'NONE',  ( 0.000000000000000000, 125.0000000000000000, 0.000000000000000000 ) ) ;
#2649=CARTESIAN_POINT ( 'NONE',  ( 2.977408999572650039, 107.1875000020483810, -7.188101187500000933 ) ) ;
#2654=CARTESIAN_POINT ( 'NONE',  ( -7.188101187500001821, 110.9375000020483810, -2.977408999572650483 ) ) ;
#2663=CARTESIAN_POINT ( 'NONE',  ( 5.082755093536325930, 1.031249997951610098, -5.082755093536325930 ) ) ;
#2669=ORIENTED_EDGE ( 'NONE', *, *, #67432, .T. ) ;
#2677=ADVANCED_FACE ( 'NONE', ( #26883 ), #33315, .T. ) ;
#2682=CARTESIAN_POINT ( 'NONE',  ( -7.188101187500000044, 1.218749997951610098, -8.802885111219163269E-16 ) ) ;
#2683=CARTESIAN_POINT ( 'NONE',  ( -7.999999999999998224, 113.2812500040967763, 3.313708498984766493 ) ) ;
#2686=DIRECTION ( 'NONE',  ( 0.000000000000000000, 0.000000000000000000, 1.000000000000000000 ) ) ;
#2694=CARTESIAN_POINT ( 'NONE',  ( -1.469576158976823947E-15, 16.12500000000000355, 8.000000000000000000 ) ) ;
#2707=CARTESIAN_POINT ( 'NONE',  ( -5.656854249492380582, 111.3125000000000000, -5.656854249492380582 ) ) ;
#2712=CARTESIAN_POINT ( 'NONE',  ( -3.313708498984760720, 21.28124999590322375, -8.000000000000000000 ) ) ;
#2735=CYLINDRICAL_SURFACE ( 'NONE', #51068, 8.000000000000000000 ) ;
#2738=EDGE_CURVE ( 'NONE', #50120, #12576, #63694, .T. ) ;
#2741=CARTESIAN_POINT ( 'NONE',  ( 5.082755093536326818, 90.21875000204838102, 5.082755093536325042 ) ) ;
#2756=ORIENTED_EDGE ( 'NONE', *, *, #65112, .F. ) ;
#2766=FACE_OUTER_BOUND ( 'NONE', #23101, .T. ) ;
#2771=CARTESIAN_POINT ( 'NONE',  ( -7.188101187500001821, 19.12499999795161187, -2.977408999572651371 ) ) ;
#2773=CARTESIAN_POINT ( 'NONE',  ( -8.000000000000000000, 117.6875000040967763, 0.000000000000000000 ) ) ;
#2774=CARTESIAN_POINT ( 'NONE',  ( 5.082755093536324154, 14.15624999795161187, 5.082755093536326818 ) ) ;
#2778=FACE_OUTER_BOUND ( 'NONE', #69494, .T. ) ;
#2783=( BOUNDED_CURVE ( )  B_SPLINE_CURVE ( 2, ( #30964, #53983, #48308, #71316, #69859, #18172, #9826, #26795, #61503 ),
 .UNSPECIFIED., .F., .F. ) 
 B_SPLINE_CURVE_WITH_KNOTS ( ( 3, 2, 2, 2, 3 ),
 ( 0.7083333333333332593, 0.7152777777777776791, 0.7222222222222220989, 0.7291666666666665186, 0.7361111111111110494 ),
 .UNSPECIFIED. ) 
 CURVE ( )  GEOMETRIC_REPRESENTATION_ITEM ( )  RATIONAL_B_SPLINE_CURVE ( ( 1.000000000000001110, 0.9238795325112855172, 1.000000000000000000, 0.9238795325112867385, 1.000000000000000000, 0.9238795325112867385, 1.000000000000000000, 0.9238795325112879597, 0.9999999999999987788 ) ) 
 REPRESENTATION_ITEM ( '' )  );
#2785=CARTESIAN_POINT ( 'NONE',  ( 2.977408999572654480, 112.6250000020483668, 7.188101187499999156 ) ) ;
#2789=CARTESIAN_POINT ( 'NONE',  ( 5.082755093536325930, 24.65624999795161543, -5.082755093536325930 ) ) ;
#2796=CARTESIAN_POINT ( 'NONE',  ( 5.082755093536326818, 93.59375000204838102, 5.082755093536325042 ) ) ;
#2808=CARTESIAN_POINT ( 'NONE',  ( 3.313708498984819339, 107.6562500040967905, 7.999999999999943157 ) ) ;
#2825=CARTESIAN_POINT ( 'NONE',  ( 5.082755093536326818, 106.7187500020483952, 5.082755093536325042 ) ) ;
#2831=CARTESIAN_POINT ( 'NONE',  ( -1.469576158976823947E-15, 27.93749999590322375, 8.000000000000000000 ) ) ;
#2853=CARTESIAN_POINT ( 'NONE',  ( 2.977408999572652260, 20.06249999795161543, 7.188101187500000044 ) ) ;
#2859=FACE_OUTER_BOUND ( 'NONE', #37853, .T. ) ;
#2862=CARTESIAN_POINT ( 'NONE',  ( 2.977408999572651815, 6.187499997951610986, 7.188101187500000933 ) ) ;
#2864=ADVANCED_FACE ( 'NONE', ( #42965 ), #2235, .T. ) ;
#2878=( BOUNDED_CURVE ( )  B_SPLINE_CURVE ( 2, ( #13138, #59193, #37288, #55019, #43304, #25941, #59921, #8607, #48958 ),
 .UNSPECIFIED., .F., .F. ) 
 B_SPLINE_CURVE_WITH_KNOTS ( ( 3, 2, 2, 2, 3 ),
 ( 0.04166666666666666435, 0.04861111111111111188, 0.05555555555555555247, 0.06250000000000000000, 0.06944444444444444753 ),
 .UNSPECIFIED. ) 
 CURVE ( )  GEOMETRIC_REPRESENTATION_ITEM ( )  RATIONAL_B_SPLINE_CURVE ( ( 1.000000000000000000, 0.9238795325112867385, 1.000000000000000000, 0.9238795325112867385, 1.000000000000000000, 0.9238795325112867385, 1.000000000000000000, 0.9238795325112867385, 1.000000000000000000 ) ) 
 REPRESENTATION_ITEM ( '' )  );
#2880=CARTESIAN_POINT ( 'NONE',  ( 5.082755093536325930, 5.156249997951610986, -5.082755093536325930 ) ) ;
#2884=CARTESIAN_POINT ( 'NONE',  ( -5.082755093536325930, 109.3437500020483810, -5.082755093536325930 ) ) ;
#2885=FACE_OUTER_BOUND ( 'NONE', #17803, .T. ) ;
#2889=ORIENTED_EDGE ( 'NONE', *, *, #15186, .F. ) ;
#2894=CARTESIAN_POINT ( 'NONE',  ( 8.000000000000000000, 106.3437500000000000, -3.313708498984762496 ) ) ;
#2899=CARTESIAN_POINT ( 'NONE',  ( 5.656854249492380582, 24.18750000000000355, -5.656854249492380582 ) ) ;
#2900=CARTESIAN_POINT ( 'NONE',  ( 3.313708498984765161, 96.96875000000000000, 7.999999999999998224 ) ) ;
#2907=ORIENTED_EDGE ( 'NONE', *, *, #54094, .F. ) ;
#2908=EDGE_CURVE ( 'NONE', #12358, #36743, #31208, .T. ) ;
#2915=CARTESIAN_POINT ( 'NONE',  ( -7.188101187500000933, 94.43750000204838102, -2.977408999572650483 ) ) ;
#2922=ORIENTED_EDGE ( 'NONE', *, *, #18195, .F. ) ;
#2924=CARTESIAN_POINT ( 'NONE',  ( -4.898587196589412829E-16, 93.12499999999998579, -8.000000000000000000 ) ) ;
#2935=CARTESIAN_POINT ( 'NONE',  ( 8.000000000000000000, 121.5312500040968047, -3.313708498984762496 ) ) ;
#2940=CARTESIAN_POINT ( 'NONE',  ( -8.000000000000000000, 113.0937500040968047, -3.313708498984761164 ) ) ;
#2955=ORIENTED_EDGE ( 'NONE', *, *, #38427, .F. ) ;
#2958=VECTOR ( 'NONE', #57365, 1000.000000000000000 ) ;
#2962=EDGE_CURVE ( 'NONE', #21298, #21405, #43263, .T. ) ;
#2963=CARTESIAN_POINT ( 'NONE',  ( 1.469576158976823947E-15, 95.56250000409677625, 8.000000000000000000 ) ) ;
#2969=AXIS2_PLACEMENT_3D ( 'NONE', #241, #979, #63579 ) ;
#2971=VERTEX_POINT ( 'NONE', #35803 ) ;
#2973=CARTESIAN_POINT ( 'NONE',  ( -7.188101187499999156, 89.75000000204839523, 2.977408999572654924 ) ) ;
#2977=VERTEX_POINT ( 'NONE', #64831 ) ;
#2998=CARTESIAN_POINT ( 'NONE',  ( 2.977408999572650927, 8.624999997951611874, -7.188101187500001821 ) ) ;
#3001=CARTESIAN_POINT ( 'NONE',  ( 2.977408999572654480, 110.0000000020483810, 7.188101187499999156 ) ) ;
#3007=CARTESIAN_POINT ( 'NONE',  ( 8.000000000000000000, 0.6562499979516100979, 0.000000000000000000 ) ) ;
#3018=CARTESIAN_POINT ( 'NONE',  ( 2.977408999572650039, 101.1875000020483810, -7.188101187500000933 ) ) ;
#3023=( BOUNDED_CURVE ( )  B_SPLINE_CURVE ( 2, ( #41955, #64612, #54408, #2341, #60045, #25335, #58961, #8749, #73244 ),
 .UNSPECIFIED., .F., .F. ) 
 B_SPLINE_CURVE_WITH_KNOTS ( ( 3, 2, 2, 2, 3 ),
 ( 0.2604166666666664631, 0.2656249999999997780, 0.2708333333333330928, 0.2760416666666664631, 0.2812499999999997780 ),
 .UNSPECIFIED. ) 
 CURVE ( )  GEOMETRIC_REPRESENTATION_ITEM ( )  RATIONAL_B_SPLINE_CURVE ( ( 1.000000000000003331, 0.9238795325112835188, 1.000000000000000000, 0.9238795325112867385, 1.000000000000000000, 0.9238795325112867385, 1.000000000000000000, 0.9238795325112899581, 0.9999999999999967804 ) ) 
 REPRESENTATION_ITEM ( '' )  );
#3024=EDGE_CURVE ( 'NONE', #48333, #48764, #48363, .T. ) ;
#3026=CARTESIAN_POINT ( 'NONE',  ( -2.977408999572651815, 109.8125000020483952, 7.188101187500000933 ) ) ;
#3031=VERTEX_POINT ( 'NONE', #7129 ) ;
#3038=CARTESIAN_POINT ( 'NONE',  ( 7.188101187500000933, 2.437499997951610542, -2.977408999572650483 ) ) ;
#3046=CARTESIAN_POINT ( 'NONE',  ( -3.313708498984744732, 121.9062500040967905, -8.000000000000019540 ) ) ;
#3051=ORIENTED_EDGE ( 'NONE', *, *, #35420, .F. ) ;
#3054=CARTESIAN_POINT ( 'NONE',  ( 2.977408999572651815, 10.68749999795161187, 7.188101187500000933 ) ) ;
#3056=CARTESIAN_POINT ( 'NONE',  ( -3.313708498984762052, 118.9062500040967905, -8.000000000000000000 ) ) ;
#3059=MECHANICAL_DESIGN_GEOMETRIC_PRESENTATION_REPRESENTATION('',(#35598),#45225);
#3079=ADVANCED_FACE ( 'NONE', ( #59551 ), #7866, .T. ) ;
#3081=CARTESIAN_POINT ( 'NONE',  ( 8.000000000000001776, 110.6562500000000000, 3.313708498984759387 ) ) ;
#3087=CARTESIAN_POINT ( 'NONE',  ( -3.313708498984765161, 18.84374999590322020, 7.999999999999998224 ) ) ;
#3095=ADVANCED_FACE ( 'NONE', ( #41089 ), #35442, .T. ) ;
#3111=CARTESIAN_POINT ( 'NONE',  ( -5.082755093536325930, 119.4687500020483810, -5.082755093536325930 ) ) ;
#3112=CARTESIAN_POINT ( 'NONE',  ( 1.347111479062088405E-15, 125.0000000000000000, -11.00000000000000000 ) ) ;
#3117=CARTESIAN_POINT ( 'NONE',  ( 5.082755093536326818, 93.21875000204838102, 5.082755093536325042 ) ) ;
#3123=( BOUNDED_CURVE ( )  B_SPLINE_CURVE ( 2, ( #47744, #70767, #36812, #58726, #65097, #59096, #48487, #64006, #64377 ),
 .UNSPECIFIED., .F., .F. ) 
 B_SPLINE_CURVE_WITH_KNOTS ( ( 3, 2, 2, 2, 3 ),
 ( 0.3020833333333331483, 0.3072916666666665186, 0.3124999999999998335, 0.3177083333333331483, 0.3229166666666665186 ),
 .UNSPECIFIED. ) 
 CURVE ( )  GEOMETRIC_REPRESENTATION_ITEM ( )  RATIONAL_B_SPLINE_CURVE ( ( 1.000000000000002442, 0.9238795325112842960, 1.000000000000000000, 0.9238795325112867385, 1.000000000000000000, 0.9238795325112867385, 1.000000000000000000, 0.9238795325112891810, 0.9999999999999975575 ) ) 
 REPRESENTATION_ITEM ( '' )  );
#3146=CARTESIAN_POINT ( 'NONE',  ( -7.188101187500001821, 22.12499999795161187, -2.977408999572651371 ) ) ;
#3148=CARTESIAN_POINT ( 'NONE',  ( -5.082755093536325042, 17.90624999795161187, -5.082755093536325930 ) ) ;
#3158=CARTESIAN_POINT ( 'NONE',  ( 2.977408999572654480, 108.1250000020483810, 7.188101187499999156 ) ) ;
#3166=CARTESIAN_POINT ( 'NONE',  ( 1.469576158976823947E-15, 116.3750000000000000, 8.000000000000000000 ) ) ;
#3170=CARTESIAN_POINT ( 'NONE',  ( 7.188101187500001821, 93.87500000204836681, -2.977408999572651371 ) ) ;
#3176=VECTOR ( 'NONE', #33098, 1000.000000000000000 ) ;
#3202=CARTESIAN_POINT ( 'NONE',  ( -7.188101187499999156, 106.2500000020484094, 2.977408999572654924 ) ) ;
#3224=CARTESIAN_POINT ( 'NONE',  ( -3.313708498984708317, 110.2812500000000000, 8.000000000000053291 ) ) ;
#3228=CARTESIAN_POINT ( 'NONE',  ( 5.082755093536324154, 18.65624999795161187, 5.082755093536326818 ) ) ;
#3237=CARTESIAN_POINT ( 'NONE',  ( 2.977408999572650927, 5.249999997951610986, -7.188101187500001821 ) ) ;
#3242=( BOUNDED_CURVE ( )  B_SPLINE_CURVE ( 2, ( #43863, #43104, #55571, #61957, #37844, #67257, #20090, #3886, #25746 ),
 .UNSPECIFIED., .F., .F. ) 
 B_SPLINE_CURVE_WITH_KNOTS ( ( 3, 2, 2, 2, 3 ),
 ( 0.7638888888888888395, 0.7708333333333333703, 0.7777777777777779011, 0.7847222222222223209, 0.7916666666666667407 ),
 .UNSPECIFIED. ) 
 CURVE ( )  GEOMETRIC_REPRESENTATION_ITEM ( )  RATIONAL_B_SPLINE_CURVE ( ( 1.000000000000000000, 0.9238795325112867385, 1.000000000000000000, 0.9238795325112867385, 1.000000000000000000, 0.9238795325112867385, 1.000000000000000000, 0.9238795325112855172, 1.000000000000001110 ) ) 
 REPRESENTATION_ITEM ( '' )  );
#3256=CARTESIAN_POINT ( 'NONE',  ( -5.082755093536326818, 13.40624999795161187, 5.082755093536325042 ) ) ;
#3261=CARTESIAN_POINT ( 'NONE',  ( 5.082755093536325042, 113.4687500020483810, -5.082755093536325930 ) ) ;
#3269=CARTESIAN_POINT ( 'NONE',  ( 9.797174393178825657E-16, 125.0000000000000000, -8.000000000000000000 ) ) ;
#3275=CARTESIAN_POINT ( 'NONE',  ( -8.000000000000000000, 93.50000000000000000, 0.000000000000000000 ) ) ;
#3288=CARTESIAN_POINT ( 'NONE',  ( 9.797174393178825657E-16, 125.0000000000000000, -8.000000000000000000 ) ) ;
#3290=CARTESIAN_POINT ( 'NONE',  ( -2.977408999572650927, 91.25000000204838102, -7.188101187500000933 ) ) ;
#3300=CARTESIAN_POINT ( 'NONE',  ( -1.320432766682874540E-15, 19.59374999795161543, 7.188101187500000044 ) ) ;
#3333=( BOUNDED_CURVE ( )  B_SPLINE_CURVE ( 2, ( #70420, #48130, #7417, #19459, #1765, #8893, #31906, #13780, #30424 ),
 .UNSPECIFIED., .F., .F. ) 
 B_SPLINE_CURVE_WITH_KNOTS ( ( 3, 2, 2, 2, 3 ),
 ( 0.6979166666666667407, 0.7031250000000001110, 0.7083333333333334814, 0.7135416666666667407, 0.7187500000000001110 ),
 .UNSPECIFIED. ) 
 CURVE ( )  GEOMETRIC_REPRESENTATION_ITEM ( )  RATIONAL_B_SPLINE_CURVE ( ( 0.9999999999999983347, 0.9238795325112884038, 1.000000000000000000, 0.9238795325112867385, 1.000000000000000000, 0.9238795325112867385, 1.000000000000000000, 0.9238795325112850731, 1.000000000000001554 ) ) 
 REPRESENTATION_ITEM ( '' )  );
#3336=CARTESIAN_POINT ( 'NONE',  ( 8.000000000000001776, 98.84375000409677625, 3.313708498984759387 ) ) ;
#3343=EDGE_CURVE ( 'NONE', #34934, #9708, #10102, .T. ) ;
#3345=CARTESIAN_POINT ( 'NONE',  ( -5.082755093536324154, 91.34375000204838102, 5.082755093536326818 ) ) ;
#3358=CARTESIAN_POINT ( 'NONE',  ( -7.999999999999998224, 105.7812500040967905, 3.313708498984766049 ) ) ;
#3363=DIRECTION ( 'NONE',  ( 0.000000000000000000, 0.000000000000000000, 1.000000000000000000 ) ) ;
#3369=CARTESIAN_POINT ( 'NONE',  ( 5.656854249492380582, 1.499999995903219974, -5.656854249492380582 ) ) ;
#3371=CARTESIAN_POINT ( 'NONE',  ( -7.188101187500001821, 13.49999999795161187, -2.977408999572651371 ) ) ;
#3374=CARTESIAN_POINT ( 'NONE',  ( 2.977408999572654480, 108.5000000020483810, 7.188101187499999156 ) ) ;
#3394=CARTESIAN_POINT ( 'NONE',  ( -7.188101187500000044, 101.6562500020483810, 0.000000000000000000 ) ) ;
#3400=CARTESIAN_POINT ( 'NONE',  ( -5.082755093536324154, 108.2187500020483810, 5.082755093536326818 ) ) ;
#3424=CARTESIAN_POINT ( 'NONE',  ( 2.977408999572650927, 8.249999997951611874, -7.188101187500001821 ) ) ;
#3425=CARTESIAN_POINT ( 'NONE',  ( 5.656854249492379694, 118.6250000040967905, -5.656854249492380582 ) ) ;
#3446=CARTESIAN_POINT ( 'NONE',  ( 4.898587196589412829E-16, 27.18749999590322375, -8.000000000000000000 ) ) ;
#3450=CARTESIAN_POINT ( 'NONE',  ( -4.898587196589412829E-16, 111.1250000000000000, -8.000000000000000000 ) ) ;
#3452=CARTESIAN_POINT ( 'NONE',  ( 3.313708498984760720, 112.5312500000000284, -8.000000000000000000 ) ) ;
#3457=( BOUNDED_CURVE ( )  B_SPLINE_CURVE ( 2, ( #64499, #52806, #59579, #18841, #54294, #30897, #53914, #1141, #24119 ),
 .UNSPECIFIED., .F., .F. ) 
 B_SPLINE_CURVE_WITH_KNOTS ( ( 3, 2, 2, 2, 3 ),
 ( 0.09375000000000006939, 0.09895833333333339810, 0.1041666666666667407, 0.1093750000000000694, 0.1145833333333333981 ),
 .UNSPECIFIED. ) 
 CURVE ( )  GEOMETRIC_REPRESENTATION_ITEM ( )  RATIONAL_B_SPLINE_CURVE ( ( 0.9999999999999990008, 0.9238795325112877377, 1.000000000000000000, 0.9238795325112867385, 1.000000000000000000, 0.9238795325112867385, 1.000000000000000000, 0.9238795325112857393, 1.000000000000001110 ) ) 
 REPRESENTATION_ITEM ( '' )  );
#3459=CARTESIAN_POINT ( 'NONE',  ( 4.898587196589412829E-16, 21.18749999590322375, -8.000000000000000000 ) ) ;
#3483=CARTESIAN_POINT ( 'NONE',  ( 2.977408999572650039, 116.1875000020483952, -7.188101187500000933 ) ) ;
#3484=CARTESIAN_POINT ( 'NONE',  ( 8.000000000000000000, 119.8437499999999858, -3.313708498984762496 ) ) ;
#3487=AXIS2_PLACEMENT_3D ( 'NONE', #41889, #11744, #24164 ) ;
#3489=EDGE_CURVE ( 'NONE', #31186, #34923, #56110, .T. ) ;
#3490=CARTESIAN_POINT ( 'NONE',  ( 7.188101187500001821, 123.8750000020483810, -2.977408999572651371 ) ) ;
#3515=EDGE_CURVE ( 'NONE', #67659, #32201, #60943, .T. ) ;
#3516=CARTESIAN_POINT ( 'NONE',  ( -5.082755093536326818, 23.90624999795161543, 5.082755093536325042 ) ) ;
#3519=CARTESIAN_POINT ( 'NONE',  ( -7.188101187500001821, 16.49999999795161543, -2.977408999572651371 ) ) ;
#3521=EDGE_CURVE ( 'NONE', #60057, #64023, #33564, .T. ) ;
#3524=FACE_OUTER_BOUND ( 'NONE', #54933, .T. ) ;
#3531=AXIS2_PLACEMENT_3D ( 'NONE', #34559, #22085, #27749 ) ;
#3543=CARTESIAN_POINT ( 'NONE',  ( -2.977408999572651815, 91.81250000204839523, 7.188101187500000933 ) ) ;
#3547=VERTEX_POINT ( 'NONE', #50308 ) ;
#3548=CARTESIAN_POINT ( 'NONE',  ( 3.313708498984782924, 8.531249995903223748, 7.999999999999979572 ) ) ;
#3567=VERTEX_POINT ( 'NONE', #8835 ) ;
#3575=CARTESIAN_POINT ( 'NONE',  ( -7.188101187500000044, 110.6562500020483810, 0.000000000000000000 ) ) ;
#3580=ORIENTED_EDGE ( 'NONE', *, *, #67238, .F. ) ;
#3589=CARTESIAN_POINT ( 'NONE',  ( -7.999999999999998224, 93.59375000000000000, 3.313708498984766049 ) ) ;
#3591=CARTESIAN_POINT ( 'NONE',  ( 0.000000000000000000, 125.0000000000000000, 8.000000000000000000 ) ) ;
#3596=CARTESIAN_POINT ( 'NONE',  ( 3.999982273345623174, 89.99927424231840689, -6.928213464733948612 ) ) ;
#3600=CARTESIAN_POINT ( 'NONE',  ( 5.082755093536325930, 17.53124999795161543, -5.082755093536325930 ) ) ;
#3609=CARTESIAN_POINT ( 'NONE',  ( -7.188101187500001821, 2.624999997951610542, -2.977408999572651371 ) ) ;
#3627=CARTESIAN_POINT ( 'NONE',  ( 2.977408999572652260, 9.187499997951610098, 7.188101187500000044 ) ) ;
#3631=CARTESIAN_POINT ( 'NONE',  ( 7.188101187500001821, 113.3750000020483810, -2.977408999572651371 ) ) ;
#3644=CARTESIAN_POINT ( 'NONE',  ( -5.656854249492378806, 93.68750000000000000, 5.656854249492381470 ) ) ;
#3658=CARTESIAN_POINT ( 'NONE',  ( -7.188101187500002709, 27.18749999795162609, 2.977408999572649151 ) ) ;
#3671=CARTESIAN_POINT ( 'NONE',  ( 5.082755093536325930, 20.15624999795161543, -5.082755093536325930 ) ) ;
#3680=CARTESIAN_POINT ( 'NONE',  ( 5.656854249492381470, 118.0625000000000000, 5.656854249492379694 ) ) ;
#3710=CARTESIAN_POINT ( 'NONE',  ( -3.313708498984765161, 10.03125000000000355, 7.999999999999998224 ) ) ;
#3713=CARTESIAN_POINT ( 'NONE',  ( 8.000000000000000000, 90.03125000409677625, -3.313708498984762496 ) ) ;
#3722=CARTESIAN_POINT ( 'NONE',  ( 2.977408999572654480, 93.12500000204836681, 7.188101187499999156 ) ) ;
#3734=CARTESIAN_POINT ( 'NONE',  ( -3.313708498984761608, 105.4062500040967905, -8.000000000000000000 ) ) ;
#3742=CARTESIAN_POINT ( 'NONE',  ( 7.999999999999998224, 7.218749995903221084, 3.313708498984766493 ) ) ;
#3746=CARTESIAN_POINT ( 'NONE',  ( 7.188101187500000044, 14.34374999795161187, 0.000000000000000000 ) ) ;
#3749=CARTESIAN_POINT ( 'NONE',  ( 2.977408999572654480, 105.5000000020483810, 7.188101187499999156 ) ) ;
#3766=CARTESIAN_POINT ( 'NONE',  ( 7.594050593750000466, 27.23437499897580949, 0.000000000000000000 ) ) ;
#3769=CARTESIAN_POINT ( 'NONE',  ( -5.082755093536324154, 97.34375000204838102, 5.082755093536326818 ) ) ;
#3774=CARTESIAN_POINT ( 'NONE',  ( 7.188101187500002709, 101.1875000020483810, 2.977408999572649151 ) ) ;
#3799=( BOUNDED_CURVE ( )  B_SPLINE_CURVE ( 2, ( #37901, #56002, #72970, #55631, #60899, #26556, #21646, #49199, #38650 ),
 .UNSPECIFIED., .F., .F. ) 
 B_SPLINE_CURVE_WITH_KNOTS ( ( 3, 2, 2, 2, 3 ),
 ( 0.6249999999999998890, 0.6319444444444443088, 0.6388888888888888395, 0.6458333333333333703, 0.6527777777777777901 ),
 .UNSPECIFIED. ) 
 CURVE ( )  GEOMETRIC_REPRESENTATION_ITEM ( )  RATIONAL_B_SPLINE_CURVE ( ( 1.000000000000001110, 0.9238795325112855172, 1.000000000000000000, 0.9238795325112867385, 1.000000000000000000, 0.9238795325112867385, 1.000000000000000000, 0.9238795325112867385, 1.000000000000000000 ) ) 
 REPRESENTATION_ITEM ( '' )  );
#3802=VERTEX_POINT ( 'NONE', #67246 ) ;
#3805=CARTESIAN_POINT ( 'NONE',  ( 4.401442555609581635E-16, 11.34374999795161010, -7.188101187500000044 ) ) ;
#3807=CARTESIAN_POINT ( 'NONE',  ( -5.656854249492378806, 111.8750000040967763, 5.656854249492381470 ) ) ;
#3821=CARTESIAN_POINT ( 'NONE',  ( 0.000000000000000000, 75.00000000000000000, 0.000000000000000000 ) ) ;
#3831=CARTESIAN_POINT ( 'NONE',  ( -3.313708498984681672, 111.7812500000000142, 8.000000000000078160 ) ) ;
#3834=CARTESIAN_POINT ( 'NONE',  ( 8.000000000000000000, 109.2500000000000000, -9.797174393178825657E-16 ) ) ;
#3840=CARTESIAN_POINT ( 'NONE',  ( -8.000000000000000000, 20.06249999590322375, -9.797174393178825657E-16 ) ) ;
#3865=CARTESIAN_POINT ( 'NONE',  ( 1.320432766682874540E-15, 118.5312500020483810, 7.188101187500000044 ) ) ;
#3870=CARTESIAN_POINT ( 'NONE',  ( -7.188101187500001821, 118.4375000020483810, -2.977408999572650483 ) ) ;
#3886=CARTESIAN_POINT ( 'NONE',  ( 3.313708498984720308, 22.59374999590322020, -8.000000000000040856 ) ) ;
#3896=CARTESIAN_POINT ( 'NONE',  ( -2.977408999572654480, 20.99999999795161898, 7.188101187499999156 ) ) ;
#3899=CARTESIAN_POINT ( 'NONE',  ( -5.082755093536325042, 19.40624999795161543, -5.082755093536325930 ) ) ;
#3917=EDGE_CURVE ( 'NONE', #38634, #663, #66807, .T. ) ;
#3928=CARTESIAN_POINT ( 'NONE',  ( 5.082755093536326818, 95.09375000204838102, 5.082755093536325042 ) ) ;
#3932=CARTESIAN_POINT ( 'NONE',  ( 3.313708498984869077, 94.53125000000001421, -7.999999999999892530 ) ) ;
#3957=CARTESIAN_POINT ( 'NONE',  ( -7.188101187500001821, 109.0625000020483810, -2.977408999572650483 ) ) ;
#3965=ADVANCED_FACE ( 'NONE', ( #60950 ), #56241, .T. ) ;
#3966=CARTESIAN_POINT ( 'NONE',  ( 8.000000000000000000, 28.31249999590322375, 0.000000000000000000 ) ) ;
#3972=VERTEX_POINT ( 'NONE', #23620 ) ;
#3975=DIRECTION ( 'NONE',  ( 0.000000000000000000, 0.000000000000000000, -1.000000000000000000 ) ) ;
#3980=VERTEX_POINT ( 'NONE', #17587 ) ;
#3986=CARTESIAN_POINT ( 'NONE',  ( 2.977408999572650927, 20.62499999795161543, -7.188101187500000933 ) ) ;
#3990=CARTESIAN_POINT ( 'NONE',  ( -3.313708498984707429, 96.40625000409680467, -8.000000000000055067 ) ) ;
#3994=CARTESIAN_POINT ( 'NONE',  ( 2.977408999572650927, 2.249999997951610098, -7.188101187500001821 ) ) ;
#3997=CARTESIAN_POINT ( 'NONE',  ( 4.898587196589412829E-16, 16.68749999590322375, -8.000000000000000000 ) ) ;
#3998=ORIENTED_EDGE ( 'NONE', *, *, #33498, .T. ) ;
#4012=CARTESIAN_POINT ( 'NONE',  ( 5.082755093536324154, 10.78124999795161187, 5.082755093536326818 ) ) ;
#4017=CARTESIAN_POINT ( 'NONE',  ( 2.977408999572650039, 110.5625000020483810, -7.188101187500001821 ) ) ;
#4025=CARTESIAN_POINT ( 'NONE',  ( 8.000000000000000000, 19.31249999590322020, 0.000000000000000000 ) ) ;
#4031=CARTESIAN_POINT ( 'NONE',  ( -3.313708498984762052, 93.21874999999998579, -8.000000000000000000 ) ) ;
#4046=AXIS2_PLACEMENT_3D ( 'NONE', #53789, #41723, #13034 ) ;
#4056=CARTESIAN_POINT ( 'NONE',  ( -2.977408999572650039, 18.93749999795161187, -7.188101187500001821 ) ) ;
#4090=CARTESIAN_POINT ( 'NONE',  ( -8.000000000000000000, 9.656250000000001776, -3.313708498984762496 ) ) ;
#4092=CARTESIAN_POINT ( 'NONE',  ( 3.313708498984760720, 93.21875000409680467, -8.000000000000000000 ) ) ;
#4103=CARTESIAN_POINT ( 'NONE',  ( 7.188101187500001821, 90.50000000204840944, -2.977408999572651371 ) ) ;
#4108=VERTEX_POINT ( 'NONE', #66109 ) ;
#4127=CARTESIAN_POINT ( 'NONE',  ( 4.898587196589412829E-16, 9.187499995903221972, -8.000000000000000000 ) ) ;
#4128=ORIENTED_EDGE ( 'NONE', *, *, #124, .T. ) ;
#4130=CARTESIAN_POINT ( 'NONE',  ( 2.977408999572651815, 18.56249999795161187, 7.188101187500000933 ) ) ;
#4133=CARTESIAN_POINT ( 'NONE',  ( -7.188101187500000933, 101.9375000020483810, -2.977408999572650483 ) ) ;
#4141=CARTESIAN_POINT ( 'NONE',  ( 5.656854249492380582, 21.18750000000000355, -5.656854249492380582 ) ) ;
#4152=CARTESIAN_POINT ( 'NONE',  ( -4.401442555609581635E-16, 98.28125000204838102, -7.188101187500000044 ) ) ;
#4159=CARTESIAN_POINT ( 'NONE',  ( -2.977408999572650927, 101.7500000020483810, -7.188101187500001821 ) ) ;
#4184=CARTESIAN_POINT ( 'NONE',  ( -7.188101187500002709, 7.312499997951610986, 2.977408999572649151 ) ) ;
#4185=CARTESIAN_POINT ( 'NONE',  ( 8.000000000000000000, 109.5312500040968047, -3.313708498984762496 ) ) ;
#4192=VERTEX_POINT ( 'NONE', #49743 ) ;
#4197=CARTESIAN_POINT ( 'NONE',  ( 0.000000000000000000, 125.0000000000000000, 0.000000000000000000 ) ) ;
#4200=VERTEX_POINT ( 'NONE', #56533 ) ;
#4208=CARTESIAN_POINT ( 'NONE',  ( -5.656854249492380582, 108.3124999999999858, -5.656854249492380582 ) ) ;
#4212=CARTESIAN_POINT ( 'NONE',  ( -7.999999999999998224, 102.7812500040967763, 3.313708498984766049 ) ) ;
#4214=CARTESIAN_POINT ( 'NONE',  ( 5.656854249492380582, 25.49999999590322375, -5.656854249492380582 ) ) ;
#4216=CARTESIAN_POINT ( 'NONE',  ( 1.320432766682874540E-15, 121.9062500020483810, 7.188101187500000044 ) ) ;
#4239=CARTESIAN_POINT ( 'NONE',  ( -7.188101187499999156, 116.7500000020483810, 2.977408999572654924 ) ) ;
#4244=CARTESIAN_POINT ( 'NONE',  ( -2.977408999572651815, 118.8125000020484094, 7.188101187500000933 ) ) ;
#4256=EDGE_LOOP ( 'NONE', ( #29127, #59898, #40141, #63474 ) ) ;
#4268=CARTESIAN_POINT ( 'NONE',  ( 8.000000000000000000, 1.593750000000000000, -3.313708498984761608 ) ) ;
#4271=CARTESIAN_POINT ( 'NONE',  ( 5.082755093536324154, 18.65624999795161187, 5.082755093536326818 ) ) ;
#4294=CARTESIAN_POINT ( 'NONE',  ( -7.188101187500000044, 90.03125000204838102, 0.000000000000000000 ) ) ;
#4309=DIRECTION ( 'NONE',  ( -0.000000000000000000, 1.000000000000000000, -0.000000000000000000 ) ) ;
#4325=CARTESIAN_POINT ( 'NONE',  ( -5.082755093536324154, 100.3437500020483810, 5.082755093536326818 ) ) ;
#4331=CARTESIAN_POINT ( 'NONE',  ( 5.656854249492378806, 28.12499999590322375, 5.656854249492381470 ) ) ;
#4341=CARTESIAN_POINT ( 'NONE',  ( -8.000000000000000000, 18.46874999590322020, -3.313708498984762496 ) ) ;
#4350=CARTESIAN_POINT ( 'NONE',  ( -2.977408999572654480, 15.37499999795161187, 7.188101187499999156 ) ) ;
#4353=VERTEX_POINT ( 'NONE', #44459 ) ;
#4354=CARTESIAN_POINT ( 'NONE',  ( 3.313708498984819339, 89.65625000409679046, 7.999999999999943157 ) ) ;
#4358=CARTESIAN_POINT ( 'NONE',  ( 4.401442555609581635E-16, 5.343749997951610986, -7.188101187500000044 ) ) ;
#4361=CARTESIAN_POINT ( 'NONE',  ( -1.320432766682874540E-15, 1.968749997951609876, 7.188101187500000044 ) ) ;
#4373=CARTESIAN_POINT ( 'NONE',  ( 1.469576158976823947E-15, 104.3750000000000000, 8.000000000000000000 ) ) ;
#4375=CARTESIAN_POINT ( 'NONE',  ( -2.977408999572650039, 12.93749999795161187, -7.188101187500000933 ) ) ;
#4379=CARTESIAN_POINT ( 'NONE',  ( 7.188101187500000044, 114.7812500020483952, -8.802885111219163269E-16 ) ) ;
#4396=CARTESIAN_POINT ( 'NONE',  ( 8.000000000000000000, 94.34374999999998579, -3.313708498984762496 ) ) ;
#4402=DIRECTION ( 'NONE',  ( 0.000000000000000000, 0.000000000000000000, 1.000000000000000000 ) ) ;
#4407=EDGE_CURVE ( 'NONE', #38634, #30969, #56908, .T. ) ;
#4409=CARTESIAN_POINT ( 'NONE',  ( -7.188101187500000044, 119.6562500020483810, 0.000000000000000000 ) ) ;
#4418=CARTESIAN_POINT ( 'NONE',  ( -7.188101187500002709, 19.31249999795161543, 2.977408999572649151 ) ) ;
#4419=CARTESIAN_POINT ( 'NONE',  ( -4.898587196589412829E-16, 108.3125000040967905, -8.000000000000000000 ) ) ;
#4446=CARTESIAN_POINT ( 'NONE',  ( -5.656854249492378806, 120.6875000000000000, 5.656854249492381470 ) ) ;
#4453=( BOUNDED_CURVE ( )  B_SPLINE_CURVE ( 2, ( #36629, #19999, #2663, #13591, #49044, #49420, #59635, #53977, #48671, #61119, #25655, #71678, #14335, #60367, #54731, #72442, #14710, #3038, #26021, #20368, #66402, #37748, #20751, #43767, #66781, #15085, #32466, #58004, #58368, #39515, #28559, #17984, #28185, #45532, #22897, #51197, #74208, #6309, #69298, #10838, #5189, #17232, #28934, #51952, #68181, #46279, #22511, #23645, #45909, #12325, #64010, #6673, #56873, #289, #29314, #40627, #68550, #51565, #1027, #40253, #16853, #62512, #11580, #52323, #34242, #33873, #41003, #45170, #23270, #39879, #34615, #16477, #17609, #62881, #11214, #57244, #63627, #29677, #63255, #57621, #11957, #68922, #659, #34988, #5933, #46652, #69670, #35356, #52693, #5556, #74581, #48491, #2110, #41736, #58730, #1395, #35715, #65101, #30415, #30780, #42089, #13772, #7408, #25104, #64381, #19450, #59825, #36816, #65479, #71127, #7776, #13412, #24738, #24381, #47388, #53062, #37186, #19819, #19086, #54546, #36450, #47748, #64746, #70772, #8141, #42462, #31144, #71495, #54176, #59463, #41372, #30049, #70411, #36082, #48121, #2482, #25474, #42825, #12681, #65843, #53436, #14151, #60185, #18727, #8508, #31524, #7041, #70048, #13044, #24007, #53800, #47016, #18357, #59100, #1757, #4350, #43201, #73005, #21314, #55294, #10009, #49619, #32660, #56041, #61688, #67722, #66593, #20563, #27340, #55669, #43577, #37562, #54919, #14523, #43960, #9257, #9640, #20939, #3600, #66218, #49989, #60561, #44336, #38686, #15645, #67347, #33041, #61315, #66969, #26597, #3228, #26215, #31898, #16020, #73376, #72635, #33404, #15273, #50357, #8885, #21681, #44707, #39050, #62053, #10378, #2853, #38309, #20184, #49235, #72249, #14898, #3986, #25841, #48861, #71870, #37935, #60935, #32280, #26975, #50729, #34527, #69203, #46557, #73744, #27718, #11126, #68455, #69578, #40161, #17514, #17889, #22050, #39781, #29217, #39420, #56778, #34149, #62419, #10744, #40530, #5840, #22418, #5465, #28466, #63167, #11492, #4723, #57532, #33778, #34896, #57149, #23545, #562, #40904, #68092, #28834, #63536, #51853, #5099, #62784, #12224, #57903, #28090, #45078, #22794, #11861, #45440, #16381, #52230, #56404, #197, #51105, #16755, #51474, #74487, #23173, #46185, #74117, #6210, #45814, #63912, #68825, #17137, #36355, #64286, #54076, #59370, #1664, #30320 ),
 .UNSPECIFIED., .F., .F. ) 
 B_SPLINE_CURVE_WITH_KNOTS ( ( 3, 2, 2, 2, 2, 2, 2, 2, 2, 2, 2, 2, 2, 2, 2, 2, 2, 2, 2, 2, 2, 2, 2, 2, 2, 2, 2, 2, 2, 2, 2, 2, 2, 2, 2, 2, 2, 2, 2, 2, 2, 2, 2, 2, 2, 2, 2, 2, 2, 2, 2, 2, 2, 2, 2, 2, 2, 2, 2, 2, 2, 2, 2, 2, 2, 2, 2, 2, 2, 2, 2, 2, 2, 2, 2, 2, 2, 2, 2, 2, 2, 2, 2, 2, 2, 2, 2, 2, 2, 2, 2, 2, 2, 2, 2, 2, 2, 2, 2, 2, 2, 2, 2, 2, 2, 2, 2, 2, 2, 2, 2, 2, 2, 2, 2, 2, 2, 2, 2, 2, 2, 2, 2, 2, 2, 2, 2, 2, 2, 2, 2, 2, 2, 2, 2, 2, 2, 2, 2, 2, 2, 2, 2, 2, 3 ),
 ( 0.000000000000000000, 0.006944444444444444059, 0.01388888888888888812, 0.02083333333333333218, 0.02777777777777777624, 0.03472222222222222376, 0.04166666666666666435, 0.04861111111111111188, 0.05555555555555555247, 0.06250000000000000000, 0.06944444444444444753, 0.07638888888888889506, 0.08333333333333332871, 0.09027777777777777624, 0.09722222222222222376, 0.1041666666666666713, 0.1111111111111111049, 0.1180555555555555525, 0.1250000000000000000, 0.1319444444444444475, 0.1388888888888888951, 0.1458333333333333426, 0.1527777777777777901, 0.1597222222222222099, 0.1666666666666666574, 0.1736111111111111049, 0.1805555555555555525, 0.1875000000000000000, 0.1944444444444444475, 0.2013888888888888951, 0.2083333333333333426, 0.2152777777777777901, 0.2222222222222222099, 0.2291666666666666574, 0.2361111111111111049, 0.2430555555555555525, 0.2500000000000000000, 0.2569444444444444198, 0.2638888888888888951, 0.2708333333333333148, 0.2777777777777777901, 0.2847222222222222099, 0.2916666666666666852, 0.2986111111111111049, 0.3055555555555555802, 0.3125000000000000000, 0.3194444444444444198, 0.3263888888888888951, 0.3333333333333333148, 0.3402777777777777901, 0.3472222222222222099, 0.3541666666666666852, 0.3611111111111111049, 0.3680555555555555802, 0.3750000000000000000, 0.3819444444444444198, 0.3888888888888888951, 0.3958333333333333148, 0.4027777777777777901, 0.4097222222222222099, 0.4166666666666666852, 0.4236111111111111049, 0.4305555555555555802, 0.4375000000000000000, 0.4444444444444444198, 0.4513888888888888951, 0.4583333333333333148, 0.4652777777777777901, 0.4722222222222222099, 0.4791666666666666852, 0.4861111111111111049, 0.4930555555555555802, 0.5000000000000000000, 0.5069444444444444198, 0.5138888888888888395, 0.5208333333333333703, 0.5277777777777777901, 0.5347222222222222099, 0.5416666666666666297, 0.5486111111111111605, 0.5555555555555555802, 0.5625000000000000000, 0.5694444444444444198, 0.5763888888888888395, 0.5833333333333333703, 0.5902777777777777901, 0.5972222222222222099, 0.6041666666666666297, 0.6111111111111111605, 0.6180555555555555802, 0.6250000000000000000, 0.6319444444444444198, 0.6388888888888888395, 0.6458333333333333703, 0.6527777777777777901, 0.6597222222222222099, 0.6666666666666666297, 0.6736111111111111605, 0.6805555555555555802, 0.6875000000000000000, 0.6944444444444444198, 0.7013888888888888395, 0.7083333333333333703, 0.7152777777777777901, 0.7222222222222222099, 0.7291666666666666297, 0.7361111111111111605, 0.7430555555555555802, 0.7500000000000000000, 0.7569444444444444198, 0.7638888888888888395, 0.7708333333333333703, 0.7777777777777777901, 0.7847222222222222099, 0.7916666666666666297, 0.7986111111111111605, 0.8055555555555555802, 0.8125000000000000000, 0.8194444444444444198, 0.8263888888888888395, 0.8333333333333333703, 0.8402777777777777901, 0.8472222222222222099, 0.8541666666666666297, 0.8611111111111111605, 0.8680555555555555802, 0.8750000000000000000, 0.8819444444444444198, 0.8888888888888888395, 0.8958333333333333703, 0.9027777777777777901, 0.9097222222222222099, 0.9166666666666666297, 0.9236111111111111605, 0.9305555555555555802, 0.9375000000000000000, 0.9444444444444444198, 0.9513888888888888395, 0.9583333333333333703, 0.9652777777777777901, 0.9722222222222222099, 0.9791666666666666297, 0.9861111111111111605, 0.9930555555555555802, 1.000000000000000000 ),
 .UNSPECIFIED. ) 
 CURVE ( )  GEOMETRIC_REPRESENTATION_ITEM ( )  RATIONAL_B_SPLINE_CURVE ( ( 1.000000000000000000, 0.9238795325112867385, 1.000000000000000000, 0.9238795325112867385, 1.000000000000000000, 0.9238795325112867385, 1.000000000000000000, 0.9238795325112867385, 1.000000000000000000, 0.9238795325112867385, 1.000000000000000000, 0.9238795325112867385, 1.000000000000000000, 0.9238795325112867385, 1.000000000000000000, 0.9238795325112867385, 1.000000000000000000, 0.9238795325112867385, 1.000000000000000000, 0.9238795325112867385, 1.000000000000000000, 0.9238795325112867385, 1.000000000000000000, 0.9238795325112867385, 1.000000000000000000, 0.9238795325112867385, 1.000000000000000000, 0.9238795325112867385, 1.000000000000000000, 0.9238795325112867385, 1.000000000000000000, 0.9238795325112867385, 1.000000000000000000, 0.9238795325112867385, 1.000000000000000000, 0.9238795325112867385, 1.000000000000000000, 0.9238795325112867385, 1.000000000000000000, 0.9238795325112867385, 1.000000000000000000, 0.9238795325112867385, 1.000000000000000000, 0.9238795325112867385, 1.000000000000000000, 0.9238795325112867385, 1.000000000000000000, 0.9238795325112867385, 1.000000000000000000, 0.9238795325112867385, 1.000000000000000000, 0.9238795325112867385, 1.000000000000000000, 0.9238795325112867385, 1.000000000000000000, 0.9238795325112867385, 1.000000000000000000, 0.9238795325112867385, 1.000000000000000000, 0.9238795325112867385, 1.000000000000000000, 0.9238795325112867385, 1.000000000000000000, 0.9238795325112867385, 1.000000000000000000, 0.9238795325112867385, 1.000000000000000000, 0.9238795325112867385, 1.000000000000000000, 0.9238795325112867385, 1.000000000000000000, 0.9238795325112867385, 1.000000000000000000, 0.9238795325112867385, 1.000000000000000000, 0.9238795325112867385, 1.000000000000000000, 0.9238795325112867385, 1.000000000000000000, 0.9238795325112867385, 1.000000000000000000, 0.9238795325112867385, 1.000000000000000000, 0.9238795325112867385, 1.000000000000000000, 0.9238795325112867385, 1.000000000000000000, 0.9238795325112867385, 1.000000000000000000, 0.9238795325112867385, 1.000000000000000000, 0.9238795325112867385, 1.000000000000000000, 0.9238795325112867385, 1.000000000000000000, 0.9238795325112867385, 1.000000000000000000, 0.9238795325112867385, 1.000000000000000000, 0.9238795325112867385, 1.000000000000000000, 0.9238795325112867385, 1.000000000000000000, 0.9238795325112867385, 1.000000000000000000, 0.9238795325112867385, 1.000000000000000000, 0.9238795325112867385, 1.000000000000000000, 0.9238795325112867385, 1.000000000000000000, 0.9238795325112867385, 1.000000000000000000, 0.9238795325112867385, 1.000000000000000000, 0.9238795325112867385, 1.000000000000000000, 0.9238795325112867385, 1.000000000000000000, 0.9238795325112867385, 1.000000000000000000, 0.9238795325112867385, 1.000000000000000000, 0.9238795325112867385, 1.000000000000000000, 0.9238795325112867385, 1.000000000000000000, 0.9238795325112867385, 1.000000000000000000, 0.9238795325112867385, 1.000000000000000000, 0.9238795325112867385, 1.000000000000000000, 0.9238795325112867385, 1.000000000000000000, 0.9238795325112867385, 1.000000000000000000, 0.9238795325112867385, 1.000000000000000000, 0.9238795325112867385, 1.000000000000000000, 0.9238795325112867385, 1.000000000000000000, 0.9238795325112867385, 1.000000000000000000, 0.9238795325112867385, 1.000000000000000000, 0.9238795325112867385, 1.000000000000000000, 0.9238795325112867385, 1.000000000000000000, 0.9238795325112867385, 1.000000000000000000, 0.9238795325112867385, 1.000000000000000000, 0.9238795325112867385, 1.000000000000000000, 0.9238795325112867385, 1.000000000000000000, 0.9238795325112867385, 1.000000000000000000, 0.9238795325112867385, 1.000000000000000000, 0.9238795325112867385, 1.000000000000000000, 0.9238795325112867385, 1.000000000000000000, 0.9238795325112867385, 1.000000000000000000, 0.9238795325112867385, 1.000000000000000000, 0.9238795325112867385, 1.000000000000000000, 0.9238795325112867385, 1.000000000000000000, 0.9238795325112867385, 1.000000000000000000, 0.9238795325112867385, 1.000000000000000000, 0.9238795325112867385, 1.000000000000000000, 0.9238795325112867385, 1.000000000000000000, 0.9238795325112867385, 1.000000000000000000, 0.9238795325112867385, 1.000000000000000000, 0.9238795325112867385, 1.000000000000000000, 0.9238795325112867385, 1.000000000000000000, 0.9238795325112867385, 1.000000000000000000, 0.9238795325112867385, 1.000000000000000000, 0.9238795325112867385, 1.000000000000000000, 0.9238795325112867385, 1.000000000000000000, 0.9238795325112867385, 1.000000000000000000, 0.9238795325112867385, 1.000000000000000000, 0.9238795325112867385, 1.000000000000000000, 0.9238795325112867385, 1.000000000000000000, 0.9238795325112867385, 1.000000000000000000, 0.9238795325112867385, 1.000000000000000000, 0.9238795325112867385, 1.000000000000000000, 0.9238795325112867385, 1.000000000000000000, 0.9238795325112867385, 1.000000000000000000, 0.9238795325112867385, 1.000000000000000000, 0.9238795325112867385, 1.000000000000000000, 0.9238795325112867385, 1.000000000000000000, 0.9238795325112867385, 1.000000000000000000, 0.9238795325112867385, 1.000000000000000000, 0.9238795325112867385, 1.000000000000000000, 0.9238795325112867385, 1.000000000000000000, 0.9238795325112867385, 1.000000000000000000, 0.9238795325112867385, 1.000000000000000000, 0.9238795325112867385, 1.000000000000000000, 0.9238795325112867385, 1.000000000000000000, 0.9238795325112867385, 1.000000000000000000, 0.9238795325112867385, 1.000000000000000000, 0.9238795325112867385, 1.000000000000000000, 0.9238795325112867385, 1.000000000000000000, 0.9238795325112867385, 1.000000000000000000, 0.9238795325112867385, 1.000000000000000000, 0.9238795325112867385, 1.000000000000000000, 0.9238795325112867385, 1.000000000000000000, 0.9238795325112867385, 1.000000000000000000, 0.9238795325112867385, 1.000000000000000000, 0.9238795325112867385, 1.000000000000000000, 0.9238795325112867385, 1.000000000000000000, 0.9238795325112867385, 1.000000000000000000, 0.9238795325112867385, 1.000000000000000000, 0.9238795325112867385, 1.000000000000000000, 0.9238795325112867385, 1.000000000000000000, 0.9238795325112867385, 1.000000000000000000, 0.9238795325112867385, 1.000000000000000000, 0.9238795325112867385, 1.000000000000000000, 0.9238795325112867385, 1.000000000000000000, 0.9238795325112867385, 1.000000000000000000, 0.9238795325112867385, 1.000000000000000000, 0.9238795325112867385, 1.000000000000000000, 0.9238795325112867385, 1.000000000000000000, 0.9238795325112867385, 1.000000000000000000 ) ) 
 REPRESENTATION_ITEM ( '' )  );
#4456=CARTESIAN_POINT ( 'NONE',  ( -5.656854249492379694, 9.562500000000001776, -5.656854249492380582 ) ) ;
#4460=CARTESIAN_POINT ( 'NONE',  ( -5.082755093536325930, 95.84375000204838102, -5.082755093536325930 ) ) ;
#4461=CARTESIAN_POINT ( 'NONE',  ( -5.656854249492378806, 89.37500000409679046, 5.656854249492381470 ) ) ;
#4462=EDGE_CURVE ( 'NONE', #72985, #60077, #58203, .T. ) ;
#4472=CARTESIAN_POINT ( 'NONE',  ( -7.188101187500001821, 89.56250000204838102, -2.977408999572650483 ) ) ;
#4473=DIRECTION ( 'NONE',  ( -0.000000000000000000, 1.000000000000000000, -0.000000000000000000 ) ) ;
#4477=ORIENTED_EDGE ( 'NONE', *, *, #67248, .F. ) ;
#4493=CARTESIAN_POINT ( 'NONE',  ( 4.898587196589412829E-16, 6.187499995903221084, -8.000000000000000000 ) ) ;
#4496=CARTESIAN_POINT ( 'NONE',  ( -5.082755093536326818, 15.28124999795161187, 5.082755093536325042 ) ) ;
#4499=CARTESIAN_POINT ( 'NONE',  ( -5.082755093536324154, 102.2187500020483810, 5.082755093536326818 ) ) ;
#4500=FACE_OUTER_BOUND ( 'NONE', #32423, .T. ) ;
#4517=CARTESIAN_POINT ( 'NONE',  ( -2.977408999572652260, 97.43750000204839523, 7.188101187500000044 ) ) ;
#4524=CARTESIAN_POINT ( 'NONE',  ( -5.082755093536325930, 100.3437500020483810, -5.082755093536325930 ) ) ;
#4549=CARTESIAN_POINT ( 'NONE',  ( -5.082755093536325042, 8.531249997951611874, -5.082755093536325930 ) ) ;
#4550=CARTESIAN_POINT ( 'NONE',  ( 5.656854249492379694, 111.1250000040967763, -5.656854249492380582 ) ) ;
#4560=CARTESIAN_POINT ( 'NONE',  ( -7.188101187500000044, 112.1562500020483952, 0.000000000000000000 ) ) ;
#4561=VECTOR ( 'NONE', #70931, 1000.000000000000000 ) ;
#4576=CARTESIAN_POINT ( 'NONE',  ( 8.000000000000000000, 104.8437500000000000, -3.313708498984762496 ) ) ;
#4584=CARTESIAN_POINT ( 'NONE',  ( 3.313708498984762052, 25.59374999590322375, -8.000000000000000000 ) ) ;
#4594=CARTESIAN_POINT ( 'NONE',  ( 8.000000000000000000, 100.4375000040967763, -9.797174393178825657E-16 ) ) ;
#4598=CARTESIAN_POINT ( 'NONE',  ( 0.000000000000000000, 125.0000000000000000, 8.000000000000000000 ) ) ;
#4606=CARTESIAN_POINT ( 'NONE',  ( -5.082755093536325930, 114.9687500020483810, -5.082755093536325930 ) ) ;
#4611=CARTESIAN_POINT ( 'NONE',  ( 1.320432766682874540E-15, 121.9062500020483810, 7.188101187500000044 ) ) ;
#4632=CARTESIAN_POINT ( 'NONE',  ( -7.683012701892240059, 124.8169872981077901, 0.000000000000000000 ) ) ;
#4637=ORIENTED_EDGE ( 'NONE', *, *, #62476, .T. ) ;
#4639=CARTESIAN_POINT ( 'NONE',  ( 8.000000000000000000, 0.09374999999999990286, -3.313708498984761608 ) ) ;
#4640=ADVANCED_FACE ( 'NONE', ( #13080 ), #47785, .T. ) ;
#4644=CARTESIAN_POINT ( 'NONE',  ( -5.082755093536325042, 20.90624999795161543, -5.082755093536325930 ) ) ;
#4648=CARTESIAN_POINT ( 'NONE',  ( -1.469576158976823947E-15, 20.43749999590322375, 8.000000000000000000 ) ) ;
#4660=CARTESIAN_POINT ( 'NONE',  ( -1.320432766682874540E-15, 27.09374999795161543, 7.188101187500000044 ) ) ;
#4663=DIRECTION ( 'NONE',  ( -0.000000000000000000, 1.000000000000000000, -0.000000000000000000 ) ) ;
#4667=CARTESIAN_POINT ( 'NONE',  ( -4.401442555609581635E-16, 91.15625000204838102, -7.188101187500000044 ) ) ;
#4685=CARTESIAN_POINT ( 'NONE',  ( 1.469576158976823947E-15, 90.87500000000000000, 8.000000000000000000 ) ) ;
#4698=CARTESIAN_POINT ( 'NONE',  ( 7.188101187500000044, 102.4062500020483810, -8.802885111219163269E-16 ) ) ;
#4702=ORIENTED_EDGE ( 'NONE', *, *, #62535, .F. ) ;
#4713=CARTESIAN_POINT ( 'NONE',  ( -3.313708498984599515, 93.21875000000000000, -8.000000000000163425 ) ) ;
#4723=CARTESIAN_POINT ( 'NONE',  ( -5.082755093536325042, 23.90624999795161543, -5.082755093536325930 ) ) ;
#4729=LINE ( 'NONE', #50735, #30604 ) ;
#4733=CARTESIAN_POINT ( 'NONE',  ( 2.977408999572650927, 9.749999997951611874, -7.188101187500001821 ) ) ;
#4736=CARTESIAN_POINT ( 'NONE',  ( 7.188101187500001821, 2.437499997951610542, -2.977408999572650483 ) ) ;
#4751=ORIENTED_EDGE ( 'NONE', *, *, #823, .T. ) ;
#4752=CARTESIAN_POINT ( 'NONE',  ( -5.082755093536325042, 8.531249997951611874, -5.082755093536325930 ) ) ;
#4756=CARTESIAN_POINT ( 'NONE',  ( 7.188101187500002709, 107.1875000020483810, 2.977408999572649151 ) ) ;
#4759=CARTESIAN_POINT ( 'NONE',  ( 0.000000000000000000, 125.0000000000000000, 0.000000000000000000 ) ) ;
#4772=CARTESIAN_POINT ( 'NONE',  ( 3.313708498984765161, 90.96875000000000000, 7.999999999999998224 ) ) ;
#4782=( BOUNDED_CURVE ( )  B_SPLINE_CURVE ( 2, ( #35155, #68352, #16647, #23068, #34049, #46077, #69096, #67979, #17403 ),
 .UNSPECIFIED., .F., .F. ) 
 B_SPLINE_CURVE_WITH_KNOTS ( ( 3, 2, 2, 2, 3 ),
 ( 0.07291666666666671293, 0.07812500000000005551, 0.08333333333333338422, 0.08854166666666674068, 0.09375000000000006939 ),
 .UNSPECIFIED. ) 
 CURVE ( )  GEOMETRIC_REPRESENTATION_ITEM ( )  RATIONAL_B_SPLINE_CURVE ( ( 0.9999999999999994449, 0.9238795325112872936, 1.000000000000000000, 0.9238795325112867385, 1.000000000000000000, 0.9238795325112867385, 1.000000000000000000, 0.9238795325112857393, 1.000000000000001110 ) ) 
 REPRESENTATION_ITEM ( '' )  );
#4786=CARTESIAN_POINT ( 'NONE',  ( -7.188101187500001821, 124.0625000020483810, -2.977408999572650483 ) ) ;
#4794=CARTESIAN_POINT ( 'NONE',  ( 3.313708498984657247, 92.46874999999998579, 8.000000000000106581 ) ) ;
#4795=CARTESIAN_POINT ( 'NONE',  ( 2.977408999572651815, 16.68749999795161543, 7.188101187500000933 ) ) ;
#4814=FACE_OUTER_BOUND ( 'NONE', #29957, .T. ) ;
#4820=ORIENTED_EDGE ( 'NONE', *, *, #15359, .T. ) ;
#4822=CARTESIAN_POINT ( 'NONE',  ( 9.184850993605175555E-16, 125.0000000000000000, 7.500000000000020428 ) ) ;
#4833=CARTESIAN_POINT ( 'NONE',  ( 5.656854249492380582, 13.68750000000000178, -5.656854249492380582 ) ) ;
#4835=CARTESIAN_POINT ( 'NONE',  ( -8.000000000000000000, 92.09375000409679046, -3.313708498984761608 ) ) ;
#4846=VERTEX_POINT ( 'NONE', #10042 ) ;
#4848=CARTESIAN_POINT ( 'NONE',  ( 1.926037949307475294, 89.22060463630471361, -7.188101187500001821 ) ) ;
#4870=CARTESIAN_POINT ( 'NONE',  ( 3.313708498984762496, 10.03124999590321842, 7.999999999999998224 ) ) ;
#4873=CARTESIAN_POINT ( 'NONE',  ( -7.188101187500002709, 15.18749999795161365, 2.977408999572649151 ) ) ;
#4875=CARTESIAN_POINT ( 'NONE',  ( -5.656854249492380582, 105.3125000000000000, -5.656854249492380582 ) ) ;
#4876=CARTESIAN_POINT ( 'NONE',  ( -2.977408999572652260, 105.3125000020483810, 7.188101187500000044 ) ) ;
#4878=DIRECTION ( 'NONE',  ( -0.000000000000000000, 1.000000000000000000, -0.000000000000000000 ) ) ;
#4891=CARTESIAN_POINT ( 'NONE',  ( -5.082755093536325930, 90.96875000204838102, -5.082755093536325930 ) ) ;
#4899=CARTESIAN_POINT ( 'NONE',  ( -5.082755093536324154, 100.7187500020483810, 5.082755093536326818 ) ) ;
#4908=( BOUNDED_CURVE ( )  B_SPLINE_CURVE ( 2, ( #8375, #18594, #48733, #12916, #71739, #20054, #43071, #35951, #66087 ),
 .UNSPECIFIED., .F., .F. ) 
 B_SPLINE_CURVE_WITH_KNOTS ( ( 3, 2, 2, 2, 3 ),
 ( 0.6562500000000000000, 0.6614583333333333703, 0.6666666666666667407, 0.6718750000000001110, 0.6770833333333334814 ),
 .UNSPECIFIED. ) 
 CURVE ( )  GEOMETRIC_REPRESENTATION_ITEM ( )  RATIONAL_B_SPLINE_CURVE ( ( 1.000000000000000000, 0.9238795325112867385, 1.000000000000000000, 0.9238795325112867385, 1.000000000000000000, 0.9238795325112867385, 1.000000000000000000, 0.9238795325112850731, 1.000000000000001554 ) ) 
 REPRESENTATION_ITEM ( '' )  );
#4928=CARTESIAN_POINT ( 'NONE',  ( -1.320432766682874540E-15, 12.09374999795161187, 7.188101187500000044 ) ) ;
#4929=CARTESIAN_POINT ( 'NONE',  ( -3.313708498984762052, 111.4062500040967763, -8.000000000000000000 ) ) ;
#4932=EDGE_CURVE ( 'NONE', #56053, #34167, #30234, .T. ) ;
#4939=CARTESIAN_POINT ( 'NONE',  ( -7.188101187499999156, 112.2500000020483952, 2.977408999572654924 ) ) ;
#4954=CARTESIAN_POINT ( 'NONE',  ( -5.656854249492380582, 106.8125000000000000, -5.656854249492380582 ) ) ;
#4957=CARTESIAN_POINT ( 'NONE',  ( -3.313708498984816231, 98.28125000000000000, 7.999999999999943157 ) ) ;
#4959=CARTESIAN_POINT ( 'NONE',  ( 3.313708498984762496, 25.03124999590322020, 7.999999999999998224 ) ) ;
#4962=CARTESIAN_POINT ( 'NONE',  ( -2.977408999572652260, 121.8125000020483810, 7.188101187500000044 ) ) ;
#4983=CARTESIAN_POINT ( 'NONE',  ( 5.082755093536325042, 114.5937500020483810, -5.082755093536325930 ) ) ;
#4989=CARTESIAN_POINT ( 'NONE',  ( -7.188101187500000044, 120.0312500020483810, 0.000000000000000000 ) ) ;
#4996=CARTESIAN_POINT ( 'NONE',  ( -4.898587196589412829E-16, 108.1250000000000000, -8.000000000000000000 ) ) ;
#5004=ORIENTED_EDGE ( 'NONE', *, *, #67751, .F. ) ;
#5014=CARTESIAN_POINT ( 'NONE',  ( 2.977408999572650927, 24.74999999795161543, -7.188101187500001821 ) ) ;
#5015=CARTESIAN_POINT ( 'NONE',  ( -8.000000000000000000, 110.0937500040967905, -3.313708498984761164 ) ) ;
#5018=CARTESIAN_POINT ( 'NONE',  ( 7.188101187500000044, 23.34374999795161543, 0.000000000000000000 ) ) ;
#5035=CARTESIAN_POINT ( 'NONE',  ( -4.898587196589412829E-16, 103.8125000040967763, -8.000000000000000000 ) ) ;
#5042=AXIS2_PLACEMENT_3D ( 'NONE', #39118, #27412, #67792 ) ;
#5043=CARTESIAN_POINT ( 'NONE',  ( -2.977408999572651815, 90.31250000204838102, 7.188101187500000933 ) ) ;
#5073=CARTESIAN_POINT ( 'NONE',  ( 1.320432766682874540E-15, 100.5312500020483810, 7.188101187500000044 ) ) ;
#5075=CYLINDRICAL_SURFACE ( 'NONE', #6086, 8.000000000000000000 ) ;
#5090=CARTESIAN_POINT ( 'NONE',  ( 1.469576158976823947E-15, 104.5625000040967763, 8.000000000000000000 ) ) ;
#5099=CARTESIAN_POINT ( 'NONE',  ( 5.082755093536325930, 25.03124999795161543, -5.082755093536325930 ) ) ;
#5102=ORIENTED_EDGE ( 'NONE', *, *, #57275, .F. ) ;
#5108=CARTESIAN_POINT ( 'NONE',  ( -5.082755093536325042, 11.53124999795161010, -5.082755093536325930 ) ) ;
#5126=CARTESIAN_POINT ( 'NONE',  ( 7.188101187500000044, 18.46874999795161187, 0.000000000000000000 ) ) ;
#5130=CARTESIAN_POINT ( 'NONE',  ( 7.188101187500000044, 107.2812500020483810, -8.802885111219163269E-16 ) ) ;
#5156=CARTESIAN_POINT ( 'NONE',  ( -3.313708498984765161, 20.53125000000000711, 7.999999999999998224 ) ) ;
#5157=DIRECTION ( 'NONE',  ( -0.000000000000000000, 1.000000000000000000, -0.000000000000000000 ) ) ;
#5161=CARTESIAN_POINT ( 'NONE',  ( 7.188101187500001821, 123.5000000020483952, -2.977408999572651371 ) ) ;
#5168=CARTESIAN_POINT ( 'NONE',  ( 5.082755093536324154, 27.28124999795161543, 5.082755093536326818 ) ) ;
#5173=LINE ( 'NONE', #28169, #6685 ) ;
#5189=CARTESIAN_POINT ( 'NONE',  ( -7.188101187500000044, 4.593749997951610098, -8.802885111219163269E-16 ) ) ;
#5195=CARTESIAN_POINT ( 'NONE',  ( -8.000000000000000000, 120.5000000000000000, 0.000000000000000000 ) ) ;
#5204=CARTESIAN_POINT ( 'NONE',  ( 5.656854249492378806, 19.31250000000000355, 5.656854249492381470 ) ) ;
#5207=CARTESIAN_POINT ( 'NONE',  ( 3.313708498984760720, 91.71875000409679046, -8.000000000000000000 ) ) ;
#5216=CARTESIAN_POINT ( 'NONE',  ( -4.401442555609581635E-16, 124.1562500020483810, -7.188101187500000044 ) ) ;
#5223=ORIENTED_EDGE ( 'NONE', *, *, #67248, .T. ) ;
#5241=CARTESIAN_POINT ( 'NONE',  ( 8.000000000000000000, 11.90624999590322197, -3.313708498984761608 ) ) ;
#5242=EDGE_CURVE ( 'NONE', #7343, #2312, #2056, .T. ) ;
#5245=CARTESIAN_POINT ( 'NONE',  ( -5.082755093536325042, 16.40624999795161543, -5.082755093536325930 ) ) ;
#5248=CARTESIAN_POINT ( 'NONE',  ( 7.188101187500000044, 101.2812500020483810, -8.802885111219163269E-16 ) ) ;
#5264=CARTESIAN_POINT ( 'NONE',  ( 2.977408999572650039, 92.18750000204838102, -7.188101187500000933 ) ) ;
#5271=CARTESIAN_POINT ( 'NONE',  ( 5.082755093536325042, 102.9687500020483810, -5.082755093536325930 ) ) ;
#5295=CARTESIAN_POINT ( 'NONE',  ( 2.977408999572651815, 15.18749999795161365, 7.188101187500000933 ) ) ;
#5296=CARTESIAN_POINT ( 'NONE',  ( -4.898587196589412829E-16, 109.8125000040967905, -8.000000000000000000 ) ) ;
#5303=EDGE_LOOP ( 'NONE', ( #19051, #14722, #55313, #64595 ) ) ;
#5304=CARTESIAN_POINT ( 'NONE',  ( 5.656854249492379694, 116.9375000000000000, -5.656854249492380582 ) ) ;
#5305=CARTESIAN_POINT ( 'NONE',  ( 2.977408999572654480, 103.6250000020483810, 7.188101187499999156 ) ) ;
#5321=CARTESIAN_POINT ( 'NONE',  ( -7.999999999999998224, 105.5937500000000000, 3.313708498984766493 ) ) ;
#5324=CARTESIAN_POINT ( 'NONE',  ( 5.656854249492380582, 1.687500000000000222, -5.656854249492380582 ) ) ;
#5327=CARTESIAN_POINT ( 'NONE',  ( -5.656854249492379694, 24.37499999590322375, -5.656854249492380582 ) ) ;
#5330=CARTESIAN_POINT ( 'NONE',  ( -7.188101187500000933, 122.9375000020483810, -2.977408999572650483 ) ) ;
#5349=CARTESIAN_POINT ( 'NONE',  ( 5.082755093536326818, 111.2187500020483810, 5.082755093536325042 ) ) ;
#5353=ADVANCED_FACE ( 'NONE', ( #26162 ), #22276, .T. ) ;
#5355=CARTESIAN_POINT ( 'NONE',  ( 2.977408999572650039, 119.5625000020483810, -7.188101187500001821 ) ) ;
#5359=VERTEX_POINT ( 'NONE', #32222 ) ;
#5368=CARTESIAN_POINT ( 'NONE',  ( -1.469576158976823947E-15, 19.12500000000000355, 8.000000000000000000 ) ) ;
#5380=CARTESIAN_POINT ( 'NONE',  ( -7.188101187500001821, 26.62499999795161543, -2.977408999572651371 ) ) ;
#5381=CARTESIAN_POINT ( 'NONE',  ( -8.000000000000000000, 107.0000000000000000, 0.000000000000000000 ) ) ;
#5383=CARTESIAN_POINT ( 'NONE',  ( 7.188101187500001821, 23.43749999795161898, -2.977408999572650483 ) ) ;
#5390=FACE_OUTER_BOUND ( 'NONE', #7700, .T. ) ;
#5391=ORIENTED_EDGE ( 'NONE', *, *, #45373, .T. ) ;
#5408=CARTESIAN_POINT ( 'NONE',  ( -5.082755093536324154, 90.21875000204838102, 5.082755093536326818 ) ) ;
#5425=EDGE_LOOP ( 'NONE', ( #58485, #50639, #6699, #59584 ) ) ;
#5439=CARTESIAN_POINT ( 'NONE',  ( 5.082755093536325042, 105.5937500020483810, -5.082755093536325930 ) ) ;
#5454=CARTESIAN_POINT ( 'NONE',  ( 3.313708498984762496, 4.218750000000000000, 7.999999999999998224 ) ) ;
#5459=ORIENTED_EDGE ( 'NONE', *, *, #38709, .T. ) ;
#5465=CARTESIAN_POINT ( 'NONE',  ( 5.082755093536325930, 23.53124999795161543, -5.082755093536325930 ) ) ;
#5473=CARTESIAN_POINT ( 'NONE',  ( -7.188101187500000044, 8.718749997951611874, -8.802885111219163269E-16 ) ) ;
#5476=CARTESIAN_POINT ( 'NONE',  ( 2.977408999572651815, 8.062499997951611874, 7.188101187500000933 ) ) ;
#5481=CYLINDRICAL_SURFACE ( 'NONE', #41411, 8.000000000000000000 ) ;
#5494=CARTESIAN_POINT ( 'NONE',  ( 5.082755093536324154, 19.78124999795161543, 5.082755093536326818 ) ) ;
#5498=CARTESIAN_POINT ( 'NONE',  ( 2.977408999572654480, 105.5000000020483810, 7.188101187499999156 ) ) ;
#5512=CARTESIAN_POINT ( 'NONE',  ( -5.656854249492380582, 118.8125000000000000, -5.656854249492380582 ) ) ;
#5526=CARTESIAN_POINT ( 'NONE',  ( 7.188101187500002709, 121.8125000020483810, 2.977408999572649151 ) ) ;
#5533=ORIENTED_EDGE ( 'NONE', *, *, #66685, .T. ) ;
#5535=CARTESIAN_POINT ( 'NONE',  ( -2.977408999572650039, 26.43749999795162253, -7.188101187500001821 ) ) ;
#5548=CARTESIAN_POINT ( 'NONE',  ( 1.469576158976823947E-15, 92.37499999999998579, 8.000000000000000000 ) ) ;
#5551=CARTESIAN_POINT ( 'NONE',  ( 0.000000000000000000, 75.00000000000000000, 0.000000000000000000 ) ) ;
#5556=CARTESIAN_POINT ( 'NONE',  ( -7.188101187500002709, 9.187499997951611874, 2.977408999572649151 ) ) ;
#5562=CARTESIAN_POINT ( 'NONE',  ( 3.313708498984887285, 115.1562500040967763, 7.999999999999878320 ) ) ;
#5576=CARTESIAN_POINT ( 'NONE',  ( 5.656854249492380582, 19.68750000000000355, -5.656854249492380582 ) ) ;
#5578=EDGE_CURVE ( 'NONE', #42278, #24630, #66348, .T. ) ;
#5580=CARTESIAN_POINT ( 'NONE',  ( -2.977408999572651815, 119.9375000020483952, 7.188101187500000933 ) ) ;
#5597=SHAPE_DEFINITION_REPRESENTATION ( #24083, #66259 ) ;
#5611=CARTESIAN_POINT ( 'NONE',  ( 8.000000000000001776, 101.6562500000000142, 3.313708498984759387 ) ) ;
#5615=CARTESIAN_POINT ( 'NONE',  ( 7.188101187499999156, 17.24999999795162253, 2.977408999572654924 ) ) ;
#5618=CARTESIAN_POINT ( 'NONE',  ( -4.401442555609581635E-16, 95.65625000204838102, -7.188101187500000044 ) ) ;
#5634=CARTESIAN_POINT ( 'NONE',  ( -7.188101187499999156, 95.75000000204838102, 2.977408999572654924 ) ) ;
#5640=CARTESIAN_POINT ( 'NONE',  ( 7.188101187500000044, 98.28125000204838102, -8.802885111219163269E-16 ) ) ;
#5664=CARTESIAN_POINT ( 'NONE',  ( 7.188101187500000044, 12.46874999795161187, 0.000000000000000000 ) ) ;
#5665=CARTESIAN_POINT ( 'NONE',  ( 3.313708498984765161, 103.1562500040967763, 7.999999999999998224 ) ) ;
#5675=CARTESIAN_POINT ( 'NONE',  ( 7.188101187500001821, 107.0000000020483810, -2.977408999572651371 ) ) ;
#5692=CARTESIAN_POINT ( 'NONE',  ( -4.898587196589412829E-16, 103.6250000000000000, -8.000000000000000000 ) ) ;
#5697=CARTESIAN_POINT ( 'NONE',  ( 8.000000000000000000, 26.81249999590322375, 0.000000000000000000 ) ) ;
#5699=CARTESIAN_POINT ( 'NONE',  ( 7.188101187500000044, 123.7812500020483810, -8.802885111219163269E-16 ) ) ;
#5706=CARTESIAN_POINT ( 'NONE',  ( 1.469576158976823947E-15, 122.3750000000000000, 8.000000000000000000 ) ) ;
#5719=CARTESIAN_POINT ( 'NONE',  ( -4.401442555609581635E-16, 110.2812500020483810, -7.188101187500000044 ) ) ;
#5723=VECTOR ( 'NONE', #11527, 1000.000000000000000 ) ;
#5725=CARTESIAN_POINT ( 'NONE',  ( -4.401442555609581635E-16, 115.1562500020483810, -7.188101187500000044 ) ) ;
#5726=CARTESIAN_POINT ( 'NONE',  ( -5.656854249492379694, 13.87499999590322375, -5.656854249492380582 ) ) ;
#5732=CARTESIAN_POINT ( 'NONE',  ( 5.656854249492381470, 107.5625000000000000, 5.656854249492379694 ) ) ;
#5740=ORIENTED_EDGE ( 'NONE', *, *, #15182, .T. ) ;
#5751=CARTESIAN_POINT ( 'NONE',  ( 4.898587196589412829E-16, 0.3749999999999999445, -8.000000000000000000 ) ) ;
#5754=CARTESIAN_POINT ( 'NONE',  ( -7.188101187500000044, 25.59374999795161543, -8.802885111219163269E-16 ) ) ;
#5755=DIRECTION ( 'NONE',  ( -0.000000000000000000, 1.000000000000000000, -0.000000000000000000 ) ) ;
#5771=ORIENTED_EDGE ( 'NONE', *, *, #7856, .T. ) ;
#5782=CARTESIAN_POINT ( 'NONE',  ( 12.79996984384835912, 89.17133544502674170, -0.9100696820822021804 ) ) ;
#5791=CARTESIAN_POINT ( 'NONE',  ( -8.000000000000000000, 23.15625000000000355, -3.313708498984762496 ) ) ;
#5814=CARTESIAN_POINT ( 'NONE',  ( -2.977408999572651815, 100.4375000020483668, 7.188101187500000933 ) ) ;
#5826=CARTESIAN_POINT ( 'NONE',  ( -3.313708498984760276, 6.281249995903221084, -8.000000000000000000 ) ) ;
#5828=DIRECTION ( 'NONE',  ( -0.000000000000000000, 1.000000000000000000, -0.000000000000000000 ) ) ;
#5831=CARTESIAN_POINT ( 'NONE',  ( 3.999985685286083115, 88.68677412680156635, -6.928211494859723985 ) ) ;
#5832=EDGE_CURVE ( 'NONE', #64356, #3031, #14792, .T. ) ;
#5840=CARTESIAN_POINT ( 'NONE',  ( 7.188101187500000044, 23.34374999795161543, 0.000000000000000000 ) ) ;
#5844=VERTEX_POINT ( 'NONE', #9693 ) ;
#5849=CARTESIAN_POINT ( 'NONE',  ( 2.977408999572650927, 8.249999997951611874, -7.188101187500001821 ) ) ;
#5852=CARTESIAN_POINT ( 'NONE',  ( 4.401442555609581635E-16, 4.218749997951610098, -7.188101187500000044 ) ) ;
#5867=CARTESIAN_POINT ( 'NONE',  ( -7.188101187500002709, 16.31249999795161543, 2.977408999572649151 ) ) ;
#5872=CARTESIAN_POINT ( 'NONE',  ( -7.188101187500001821, 107.9375000020483810, -2.977408999572650483 ) ) ;
#5875=CARTESIAN_POINT ( 'NONE',  ( -5.656854249492378806, 111.8750000040967763, 5.656854249492381470 ) ) ;
#5876=CARTESIAN_POINT ( 'NONE',  ( -4.898587196589412829E-16, 94.81250000409677625, -8.000000000000000000 ) ) ;
#5882=CARTESIAN_POINT ( 'NONE',  ( 8.000000000000000000, 27.65624999795161187, 0.000000000000000000 ) ) ;
#5890=CARTESIAN_POINT ( 'NONE',  ( -3.313708498984760276, 4.968750000000000888, -8.000000000000000000 ) ) ;
#5895=CARTESIAN_POINT ( 'NONE',  ( 8.000000000000000000, 10.50000000000000178, 0.000000000000000000 ) ) ;
#5896=LINE ( 'NONE', #45133, #55474 ) ;
#5897=CYLINDRICAL_SURFACE ( 'NONE', #6234, 8.000000000000000000 ) ;
#5899=CARTESIAN_POINT ( 'NONE',  ( 9.797174393178825657E-16, 125.0000000000000000, -8.000000000000000000 ) ) ;
#5901=CARTESIAN_POINT ( 'NONE',  ( 2.977408999572650039, 122.1875000020483668, -7.188101187500001821 ) ) ;
#5906=LINE ( 'NONE', #46253, #60663 ) ;
#5908=ORIENTED_EDGE ( 'NONE', *, *, #28712, .T. ) ;
#5910=CARTESIAN_POINT ( 'NONE',  ( 7.188101187500000044, 27.46874999795161543, 0.000000000000000000 ) ) ;
#5915=CARTESIAN_POINT ( 'NONE',  ( 7.999999999999998224, 25.40625000000000355, 3.313708498984766049 ) ) ;
#5926=ORIENTED_EDGE ( 'NONE', *, *, #44001, .T. ) ;
#5933=CARTESIAN_POINT ( 'NONE',  ( 4.401442555609581635E-16, 8.718749997951611874, -7.188101187500000044 ) ) ;
#5950=CARTESIAN_POINT ( 'NONE',  ( -5.656854249492381470, 17.43750000000000000, 5.656854249492379694 ) ) ;
#5952=CARTESIAN_POINT ( 'NONE',  ( 7.188101187500001821, 122.0000000020483668, -2.977408999572651371 ) ) ;
#5954=CARTESIAN_POINT ( 'NONE',  ( -1.469576158976823947E-15, 8.625000000000000000, 8.000000000000000000 ) ) ;
#5983=ADVANCED_FACE ( 'NONE', ( #15701 ), #8521, .T. ) ;
#5987=CARTESIAN_POINT ( 'NONE',  ( -2.977408999572650039, 20.81249999795161543, -7.188101187500001821 ) ) ;
#5989=CARTESIAN_POINT ( 'NONE',  ( -1.469576158976823947E-15, 8.437499995903221972, 8.000000000000000000 ) ) ;
#5990=CARTESIAN_POINT ( 'NONE',  ( -7.188101187499999156, 97.62500000204836681, 2.977408999572654924 ) ) ;
#6006=FACE_OUTER_BOUND ( 'NONE', #64268, .T. ) ;
#6007=CARTESIAN_POINT ( 'NONE',  ( -7.188101187500000044, 91.15625000204838102, 0.000000000000000000 ) ) ;
#6012=CARTESIAN_POINT ( 'NONE',  ( 5.082755093536325042, 96.96875000204838102, -5.082755093536325930 ) ) ;
#6023=DIRECTION ( 'NONE',  ( 0.000000000000000000, 0.7071067811865426878, 0.7071067811865524577 ) ) ;
#6035=CARTESIAN_POINT ( 'NONE',  ( -5.082755093536325042, 13.03124999795161187, -5.082755093536325930 ) ) ;
#6036=CARTESIAN_POINT ( 'NONE',  ( -3.313708498984762496, 104.4687500040967763, 7.999999999999998224 ) ) ;
#6045=CARTESIAN_POINT ( 'NONE',  ( 7.188101187500002709, 105.3125000020483668, 2.977408999572649151 ) ) ;
#6047=CARTESIAN_POINT ( 'NONE',  ( 1.469576158976823947E-15, 123.8750000000000000, 8.000000000000000000 ) ) ;
#6048=VECTOR ( 'NONE', #6979, 1000.000000000000000 ) ;
#6063=CARTESIAN_POINT ( 'NONE',  ( -8.000000000000000000, 100.9062500000000000, -3.313708498984761608 ) ) ;
#6066=CARTESIAN_POINT ( 'NONE',  ( -4.898587196589412829E-16, 97.62499999999998579, -8.000000000000000000 ) ) ;
#6067=VECTOR ( 'NONE', #50580, 1000.000000000000000 ) ;
#6069=CARTESIAN_POINT ( 'NONE',  ( 7.188101187499999156, 5.249999997951610098, 2.977408999572654924 ) ) ;
#6072=CARTESIAN_POINT ( 'NONE',  ( 2.977408999572654480, 114.5000000020483810, 7.188101187499999156 ) ) ;
#6073=DIRECTION ( 'NONE',  ( -0.000000000000000000, 1.000000000000000000, -0.000000000000000000 ) ) ;
#6075=CARTESIAN_POINT ( 'NONE',  ( -4.898587196589412829E-16, 96.31250000409677625, -8.000000000000000000 ) ) ;
#6086=AXIS2_PLACEMENT_3D ( 'NONE', #34505, #46537, #45793 ) ;
#6095=CARTESIAN_POINT ( 'NONE',  ( -4.401442555609581635E-16, 108.7812500020483810, -7.188101187500000044 ) ) ;
#6101=CARTESIAN_POINT ( 'NONE',  ( -7.188101187500000044, 115.5312500020483952, 0.000000000000000000 ) ) ;
#6114=EDGE_CURVE ( 'NONE', #1217, #51619, #23231, .T. ) ;
#6127=CARTESIAN_POINT ( 'NONE',  ( 5.656854249492378806, 4.312500000000000000, 5.656854249492381470 ) ) ;
#6129=CARTESIAN_POINT ( 'NONE',  ( 2.977408999572650927, 25.12499999795161187, -7.188101187500001821 ) ) ;
#6130=CARTESIAN_POINT ( 'NONE',  ( 3.313708498984760720, 121.7187500040967763, -8.000000000000000000 ) ) ;
#6147=CARTESIAN_POINT ( 'NONE',  ( 3.313708498984815343, 96.21875000409679046, -7.999999999999944933 ) ) ;
#6154=CARTESIAN_POINT ( 'NONE',  ( 8.000000000000000000, 118.3437499999999858, -3.313708498984762496 ) ) ;
#6170=DIRECTION ( 'NONE',  ( -0.000000000000000000, 1.000000000000000000, -0.000000000000000000 ) ) ;
#6185=CARTESIAN_POINT ( 'NONE',  ( -5.082755093536324154, 95.84375000204838102, 5.082755093536326818 ) ) ;
#6210=CARTESIAN_POINT ( 'NONE',  ( -5.082755093536325042, 26.90624999795161898, -5.082755093536325930 ) ) ;
#6219=CIRCLE ( 'NONE', #2592, 7.500000000000020428 ) ;
#6222=CARTESIAN_POINT ( 'NONE',  ( -5.082755093536326818, 7.406249997951610986, 5.082755093536325042 ) ) ;
#6225=CARTESIAN_POINT ( 'NONE',  ( -1.320432766682874540E-15, 7.968749997951610986, 7.188101187500000044 ) ) ;
#6234=AXIS2_PLACEMENT_3D ( 'NONE', #993, #68514, #40218 ) ;
#6238=CARTESIAN_POINT ( 'NONE',  ( 2.977408999572650039, 114.6875000020484094, -7.188101187500001821 ) ) ;
#6242=CARTESIAN_POINT ( 'NONE',  ( 2.977408999572652260, 15.18749999795161365, 7.188101187500000044 ) ) ;
#6247=CARTESIAN_POINT ( 'NONE',  ( 7.188101187500001821, 108.8750000020483810, -2.977408999572651371 ) ) ;
#6251=CARTESIAN_POINT ( 'NONE',  ( -8.000000000000000000, 95.09375000409679046, -3.313708498984761164 ) ) ;
#6265=CARTESIAN_POINT ( 'NONE',  ( 0.000000000000000000, 125.0000000000000000, 0.000000000000000000 ) ) ;
#6266=CARTESIAN_POINT ( 'NONE',  ( -3.313708498984775375, 5.531249999999999112, 7.999999999999988454 ) ) ;
#6277=CARTESIAN_POINT ( 'NONE',  ( -4.401442555609581635E-16, 116.2812500020483810, -7.188101187500000044 ) ) ;
#6290=VERTEX_POINT ( 'NONE', #23971 ) ;
#6309=CARTESIAN_POINT ( 'NONE',  ( -2.977408999572650039, 4.312499997951610098, -7.188101187500000933 ) ) ;
#6328=CARTESIAN_POINT ( 'NONE',  ( -5.656854249492379694, 15.56250000000000355, -5.656854249492380582 ) ) ;
#6330=CARTESIAN_POINT ( 'NONE',  ( -7.188101187500000044, 124.1562500020483810, 0.000000000000000000 ) ) ;
#6337=CARTESIAN_POINT ( 'NONE',  ( -5.082755093536325042, 1.031249997951609876, -5.082755093536325930 ) ) ;
#6341=CARTESIAN_POINT ( 'NONE',  ( -5.082755093536324154, 123.2187500020483952, 5.082755093536326818 ) ) ;
#6346=CARTESIAN_POINT ( 'NONE',  ( -7.188101187500000044, 124.1562500020483810, 0.000000000000000000 ) ) ;
#6354=ORIENTED_EDGE ( 'NONE', *, *, #1228, .T. ) ;
#6367=CARTESIAN_POINT ( 'NONE',  ( -2.977408999572650039, 23.81249999795161543, -7.188101187500001821 ) ) ;
#6369=CARTESIAN_POINT ( 'NONE',  ( 5.082755093536326818, 95.09375000204838102, 5.082755093536325042 ) ) ;
#6371=CARTESIAN_POINT ( 'NONE',  ( 0.000000000000000000, 124.5000000000000284, 8.000000000000000000 ) ) ;
#6376=ADVANCED_FACE ( 'NONE', ( #1721 ), #71091, .T. ) ;
#6380=DIRECTION ( 'NONE',  ( 0.000000000000000000, 0.000000000000000000, -1.000000000000000000 ) ) ;
#6386=CARTESIAN_POINT ( 'NONE',  ( -2.977408999572650927, 95.37500000204839523, -7.188101187500000933 ) ) ;
#6391=CARTESIAN_POINT ( 'NONE',  ( 7.188101187500000044, 93.78125000204836681, -8.802885111219163269E-16 ) ) ;
#6398=DIRECTION ( 'NONE',  ( 0.000000000000000000, 0.000000000000000000, 1.000000000000000000 ) ) ;
#6403=CARTESIAN_POINT ( 'NONE',  ( 0.000000000000000000, 0.5000000000000004441, 8.000000000000000000 ) ) ;
#6412=CARTESIAN_POINT ( 'NONE',  ( -3.313708498984762496, 102.9687500040967763, 7.999999999999998224 ) ) ;
#6421=CARTESIAN_POINT ( 'NONE',  ( 7.188101187500000044, 105.4062500020483810, -8.802885111219163269E-16 ) ) ;
#6442=CARTESIAN_POINT ( 'NONE',  ( 8.000000000000000000, 100.2499999999999858, -9.797174393178825657E-16 ) ) ;
#6447=CARTESIAN_POINT ( 'NONE',  ( -5.082755093536326818, 6.281249997951610098, 5.082755093536325042 ) ) ;
#6450=CARTESIAN_POINT ( 'NONE',  ( 7.188101187500002709, 116.1875000020483952, 2.977408999572649151 ) ) ;
#6470=CARTESIAN_POINT ( 'NONE',  ( 2.977408999572650039, 111.6875000020483810, -7.188101187500000933 ) ) ;
#6475=CARTESIAN_POINT ( 'NONE',  ( -2.977408999572650927, 112.2500000020483952, -7.188101187500001821 ) ) ;
#6499=CARTESIAN_POINT ( 'NONE',  ( -8.000000000000000000, 8.250000000000001776, -9.797174393178825657E-16 ) ) ;
#6500=CARTESIAN_POINT ( 'NONE',  ( -3.313708498984786033, 11.53125000000000533, 7.999999999999979572 ) ) ;
#6501=CARTESIAN_POINT ( 'NONE',  ( -2.977408999572650039, 26.81249999795161543, -7.188101187500001821 ) ) ;
#6518=CARTESIAN_POINT ( 'NONE',  ( 5.656854249492381470, 95.75000000409677625, 5.656854249492379694 ) ) ;
#6523=CARTESIAN_POINT ( 'NONE',  ( -5.656854249492380582, 118.8125000000000000, -5.656854249492380582 ) ) ;
#6526=EDGE_CURVE ( 'NONE', #53341, #4192, #45207, .T. ) ;
#6529=CARTESIAN_POINT ( 'NONE',  ( -8.000000000000000000, 15.46874999590322197, -3.313708498984762496 ) ) ;
#6550=CARTESIAN_POINT ( 'NONE',  ( -5.656854249492380582, 116.0000000040967905, -5.656854249492380582 ) ) ;
#6555=CARTESIAN_POINT ( 'NONE',  ( 7.188101187500001821, 98.00000000204838102, -2.977408999572651371 ) ) ;
#6570=DIRECTION ( 'NONE',  ( -0.000000000000000000, 1.000000000000000000, -0.000000000000000000 ) ) ;
#6586=CARTESIAN_POINT ( 'NONE',  ( 2.977408999572650927, 12.74999999795161187, -7.188101187500001821 ) ) ;
#6589=CARTESIAN_POINT ( 'NONE',  ( 7.188101187500000044, 6.843749997951610986, 0.000000000000000000 ) ) ;
#6593=CARTESIAN_POINT ( 'NONE',  ( 1.469576158976823947E-15, 98.56250000409677625, 8.000000000000000000 ) ) ;
#6603=CARTESIAN_POINT ( 'NONE',  ( -7.188101187500001821, 116.5625000020483810, -2.977408999572650483 ) ) ;
#6606=ORIENTED_EDGE ( 'NONE', *, *, #21051, .T. ) ;
#6607=CARTESIAN_POINT ( 'NONE',  ( -7.188101187500002709, 19.31249999795161543, 2.977408999572649151 ) ) ;
#6612=CARTESIAN_POINT ( 'NONE',  ( -7.188101187499999156, 99.12500000204838102, 2.977408999572654924 ) ) ;
#6643=CARTESIAN_POINT ( 'NONE',  ( -4.401442555609581635E-16, 113.2812500020483952, -7.188101187500000044 ) ) ;
#6652=CARTESIAN_POINT ( 'NONE',  ( -5.082755093536325042, 25.03124999795161543, -5.082755093536325930 ) ) ;
#6673=CARTESIAN_POINT ( 'NONE',  ( 2.977408999572650927, 5.624999997951610986, -7.188101187500000933 ) ) ;
#6685=VECTOR ( 'NONE', #45516, 1000.000000000000000 ) ;
#6691=CARTESIAN_POINT ( 'NONE',  ( -1.469576158976823947E-15, 16.12500000000000355, 8.000000000000000000 ) ) ;
#6692=ORIENTED_EDGE ( 'NONE', *, *, #11345, .F. ) ;
#6693=CARTESIAN_POINT ( 'NONE',  ( -7.188101187500001821, 119.5625000020483810, -2.977408999572650483 ) ) ;
#6699=ORIENTED_EDGE ( 'NONE', *, *, #42267, .T. ) ;
#6700=CARTESIAN_POINT ( 'NONE',  ( 7.188101187500000044, 0.4687499979516099868, 0.000000000000000000 ) ) ;
#6701=CARTESIAN_POINT ( 'NONE',  ( 9.797174393178825657E-16, 125.0000000000000000, -8.000000000000000000 ) ) ;
#6703=CARTESIAN_POINT ( 'NONE',  ( 7.188101187500001821, 116.3750000020483810, -2.977408999572651371 ) ) ;
#6708=ORIENTED_EDGE ( 'NONE', *, *, #1228, .F. ) ;
#6709=EDGE_CURVE ( 'NONE', #30969, #38665, #3799, .T. ) ;
#6728=CARTESIAN_POINT ( 'NONE',  ( 4.401442555609581635E-16, 25.21874999795161543, -7.188101187500000044 ) ) ;
#6732=CARTESIAN_POINT ( 'NONE',  ( 2.977408999572650039, 100.0625000020483810, -7.188101187500000933 ) ) ;
#6748=CARTESIAN_POINT ( 'NONE',  ( -4.898587196589412829E-16, 123.3125000040967905, -8.000000000000000000 ) ) ;
#6753=CARTESIAN_POINT ( 'NONE',  ( -7.188101187500000044, 94.53125000204836681, 0.000000000000000000 ) ) ;
#6760=DIRECTION ( 'NONE',  ( 0.000000000000000000, 0.000000000000000000, 1.000000000000000000 ) ) ;
#6777=CARTESIAN_POINT ( 'NONE',  ( -3.313708498984762052, 103.9062500040967905, -8.000000000000000000 ) ) ;
#6784=CARTESIAN_POINT ( 'NONE',  ( 7.188101187500001821, 96.50000000204838102, -2.977408999572651371 ) ) ;
#6800=CARTESIAN_POINT ( 'NONE',  ( 3.313708498984760720, 97.53125000000001421, -8.000000000000000000 ) ) ;
#6804=CARTESIAN_POINT ( 'NONE',  ( -7.188101187500000044, 3.093749997951610542, -8.802885111219163269E-16 ) ) ;
#6807=CARTESIAN_POINT ( 'NONE',  ( 1.320432766682874540E-15, 115.9062500020483810, 7.188101187500000044 ) ) ;
#6811=CARTESIAN_POINT ( 'NONE',  ( -3.313708498984760276, 3.468750000000000444, -8.000000000000000000 ) ) ;
#6820=CARTESIAN_POINT ( 'NONE',  ( -5.656854249492378806, 96.68750000000000000, 5.656854249492381470 ) ) ;
#6829=CARTESIAN_POINT ( 'NONE',  ( 2.977408999572650039, 102.6875000020483810, -7.188101187500000933 ) ) ;
#6834=CARTESIAN_POINT ( 'NONE',  ( -7.188101187500001821, 113.9375000020483952, -2.977408999572650483 ) ) ;
#6860=CARTESIAN_POINT ( 'NONE',  ( 7.999999999999998224, 2.906250000000000888, 3.313708498984766493 ) ) ;
#6862=CARTESIAN_POINT ( 'NONE',  ( 7.188101187500000044, 0.4687499979516099868, 0.000000000000000000 ) ) ;
#6863=CARTESIAN_POINT ( 'NONE',  ( 3.313708498984765161, 121.1562500040967763, 7.999999999999998224 ) ) ;
#6888=CARTESIAN_POINT ( 'NONE',  ( -8.000000000000000000, 120.4062500000000142, -3.313708498984761608 ) ) ;
#6893=CARTESIAN_POINT ( 'NONE',  ( 4.898587196589412829E-16, 16.68749999590322375, -8.000000000000000000 ) ) ;
#6920=CARTESIAN_POINT ( 'NONE',  ( -2.977408999572650927, 96.87500000204836681, -7.188101187500001821 ) ) ;
#6938=CARTESIAN_POINT ( 'NONE',  ( -8.000000000000000000, 112.9062500000000000, -3.313708498984761164 ) ) ;
#6939=CYLINDRICAL_SURFACE ( 'NONE', #14751, 8.000000000000000000 ) ;
#6945=ORIENTED_EDGE ( 'NONE', *, *, #44508, .T. ) ;
#6949=CARTESIAN_POINT ( 'NONE',  ( 2.977408999572650927, 15.74999999795161543, -7.188101187500001821 ) ) ;
#6953=CARTESIAN_POINT ( 'NONE',  ( 5.082755093536325930, 10.03124999795161187, -5.082755093536325930 ) ) ;
#6966=CARTESIAN_POINT ( 'NONE',  ( 5.082755093536326818, 117.2187500020483810, 5.082755093536325042 ) ) ;
#6970=CARTESIAN_POINT ( 'NONE',  ( 5.082755093536324154, 25.78124999795161543, 5.082755093536326818 ) ) ;
#6973=CARTESIAN_POINT ( 'NONE',  ( 5.656854249492378806, 13.31250000000000178, 5.656854249492381470 ) ) ;
#6975=CARTESIAN_POINT ( 'NONE',  ( -2.977408999572651815, 97.81250000204840944, 7.188101187500000933 ) ) ;
#6979=DIRECTION ( 'NONE',  ( -0.000000000000000000, 1.000000000000000000, -0.000000000000000000 ) ) ;
#6993=CARTESIAN_POINT ( 'NONE',  ( -8.000000000000000000, 119.0000000000000000, 0.000000000000000000 ) ) ;
#7002=EDGE_CURVE ( 'NONE', #31653, #1389, #68357, .T. ) ;
#7007=CARTESIAN_POINT ( 'NONE',  ( -5.841315287305287818, 124.7066856464806364, -5.183856896381568546 ) ) ;
#7010=CARTESIAN_POINT ( 'NONE',  ( -5.082755093536324154, 112.3437500020483810, 5.082755093536326818 ) ) ;
#7029=CYLINDRICAL_SURFACE ( 'NONE', #62924, 8.000000000000000000 ) ;
#7041=CARTESIAN_POINT ( 'NONE',  ( 5.082755093536325930, 14.53124999795161187, -5.082755093536325930 ) ) ;
#7045=LINE ( 'NONE', #45913, #69349 ) ;
#7058=CARTESIAN_POINT ( 'NONE',  ( 8.000000000000000000, 24.00000000000000355, 0.000000000000000000 ) ) ;
#7059=ORIENTED_EDGE ( 'NONE', *, *, #6526, .T. ) ;
#7067=ORIENTED_EDGE ( 'NONE', *, *, #55138, .T. ) ;
#7068=CARTESIAN_POINT ( 'NONE',  ( -1.320432766682874540E-15, 4.593749997951610986, 7.188101187500000044 ) ) ;
#7071=CARTESIAN_POINT ( 'NONE',  ( -5.082755093536325930, 116.8437500020483810, -5.082755093536325930 ) ) ;
#7076=ORIENTED_EDGE ( 'NONE', *, *, #10320, .T. ) ;
#7082=CARTESIAN_POINT ( 'NONE',  ( -4.898587196589412829E-16, 105.3125000040967763, -8.000000000000000000 ) ) ;
#7097=CARTESIAN_POINT ( 'NONE',  ( 7.188101187500001821, 26.43749999795162253, -2.977408999572650483 ) ) ;
#7099=CARTESIAN_POINT ( 'NONE',  ( -7.188101187500000933, 95.93750000204839523, -2.977408999572650483 ) ) ;
#7108=DIRECTION ( 'NONE',  ( -0.000000000000000000, 1.000000000000000000, -0.000000000000000000 ) ) ;
#7117=CARTESIAN_POINT ( 'NONE',  ( -7.188101187499999156, 89.75000000204838102, 2.977408999572654924 ) ) ;
#7122=CARTESIAN_POINT ( 'NONE',  ( 5.082755093536326818, 99.59375000204838102, 5.082755093536325042 ) ) ;
#7129=CARTESIAN_POINT ( 'NONE',  ( 1.469576158976823947E-15, 118.0625000040967763, 8.000000000000000000 ) ) ;
#7144=CARTESIAN_POINT ( 'NONE',  ( -4.898587196589412829E-16, 102.3125000040967763, -8.000000000000000000 ) ) ;
#7155=CARTESIAN_POINT ( 'NONE',  ( -2.977408999572650927, 99.87500000204838102, -7.188101187500001821 ) ) ;
#7158=VERTEX_POINT ( 'NONE', #37056 ) ;
#7161=DIRECTION ( 'NONE',  ( -0.000000000000000000, 1.000000000000000000, -0.000000000000000000 ) ) ;
#7178=CARTESIAN_POINT ( 'NONE',  ( 7.188101187500001821, 5.437499997951610098, -2.977408999572650483 ) ) ;
#7181=CARTESIAN_POINT ( 'NONE',  ( -7.188101187499999156, 117.1250000020483810, 2.977408999572654924 ) ) ;
#7185=CARTESIAN_POINT ( 'NONE',  ( 4.898587196589412829E-16, 3.375000000000000444, -8.000000000000000000 ) ) ;
#7192=CARTESIAN_POINT ( 'NONE',  ( -4.898587196589412829E-16, 112.6250000000000000, -8.000000000000000000 ) ) ;
#7202=CARTESIAN_POINT ( 'NONE',  ( 5.082755093536325042, 104.0937500020483810, -5.082755093536325930 ) ) ;
#7210=CARTESIAN_POINT ( 'NONE',  ( 7.188101187500000044, 111.7812500020483810, -8.802885111219163269E-16 ) ) ;
#7216=EDGE_CURVE ( 'NONE', #43418, #30852, #43449, .T. ) ;
#7217=CARTESIAN_POINT ( 'NONE',  ( 0.000000000000000000, 125.0000000000000000, 8.000000000000000000 ) ) ;
#7234=CARTESIAN_POINT ( 'NONE',  ( -8.000000000000001776, 6.843750000000000888, 3.313708498984759387 ) ) ;
#7235=CARTESIAN_POINT ( 'NONE',  ( -8.000000000000000000, 11.25000000000000178, -9.797174393178825657E-16 ) ) ;
#7236=CARTESIAN_POINT ( 'NONE',  ( 2.977408999572650927, 3.749999997951610542, -7.188101187500001821 ) ) ;
#7237=CARTESIAN_POINT ( 'NONE',  ( -5.656854249492380582, 119.0000000040967905, -5.656854249492380582 ) ) ;
#7242=CARTESIAN_POINT ( 'NONE',  ( 3.313708498984815343, 96.03124999999998579, -7.999999999999944933 ) ) ;
#7245=CARTESIAN_POINT ( 'NONE',  ( -3.313708498984760276, 15.46875000000000711, -8.000000000000000000 ) ) ;
#7253=CARTESIAN_POINT ( 'NONE',  ( -4.898587196589412829E-16, 123.1250000000000000, -8.000000000000000000 ) ) ;
#7259=AXIS2_PLACEMENT_3D ( 'NONE', #55935, #72897, #67243 ) ;
#7260=CARTESIAN_POINT ( 'NONE',  ( -3.313708498984762496, 120.7812500000000142, 7.999999999999998224 ) ) ;
#7263=EDGE_LOOP ( 'NONE', ( #69109, #10312, #63484, #11699 ) ) ;
#7265=CARTESIAN_POINT ( 'NONE',  ( -1.469576158976823947E-15, 12.93749999590322197, 8.000000000000000000 ) ) ;
#7292=CARTESIAN_POINT ( 'NONE',  ( -5.082755093536325930, 95.46875000204838102, -5.082755093536325930 ) ) ;
#7323=CARTESIAN_POINT ( 'NONE',  ( 5.082755093536324154, 13.78124999795161010, 5.082755093536326818 ) ) ;
#7327=CARTESIAN_POINT ( 'NONE',  ( 7.188101187500001821, 14.43749999795161365, -2.977408999572650483 ) ) ;
#7332=ORIENTED_EDGE ( 'NONE', *, *, #21387, .F. ) ;
#7338=CARTESIAN_POINT ( 'NONE',  ( -7.188101187500000044, 118.1562500020483810, 0.000000000000000000 ) ) ;
#7342=CARTESIAN_POINT ( 'NONE',  ( 2.977408999572650927, 21.74999999795161898, -7.188101187500000933 ) ) ;
#7343=VERTEX_POINT ( 'NONE', #38927 ) ;
#7348=CARTESIAN_POINT ( 'NONE',  ( -7.188101187500001821, 101.9375000020483810, -2.977408999572650483 ) ) ;
#7369=DIRECTION ( 'NONE',  ( -0.000000000000000000, 1.000000000000000000, -0.000000000000000000 ) ) ;
#7370=DIRECTION ( 'NONE',  ( -0.000000000000000000, 1.000000000000000000, -0.000000000000000000 ) ) ;
#7380=CARTESIAN_POINT ( 'NONE',  ( -7.188101187500000044, 113.6562500020483810, 0.000000000000000000 ) ) ;
#7386=VERTEX_POINT ( 'NONE', #25714 ) ;
#7389=CARTESIAN_POINT ( 'NONE',  ( -4.898587196589412829E-16, 109.6250000000000000, -8.000000000000000000 ) ) ;
#7408=CARTESIAN_POINT ( 'NONE',  ( -5.082755093536325042, 10.40624999795161187, -5.082755093536325930 ) ) ;
#7417=CARTESIAN_POINT ( 'NONE',  ( -5.656854249492378806, 98.37500000409677625, 5.656854249492381470 ) ) ;
#7426=CARTESIAN_POINT ( 'NONE',  ( 8.000000000000000000, 24.09375000000000355, -3.313708498984761608 ) ) ;
#7438=CARTESIAN_POINT ( 'NONE',  ( 5.082755093536325930, 6.656249997951611874, -5.082755093536325930 ) ) ;
#7441=CARTESIAN_POINT ( 'NONE',  ( -7.188101187500001821, 118.4375000020483810, -2.977408999572650483 ) ) ;
#7447=ORIENTED_EDGE ( 'NONE', *, *, #1599, .T. ) ;
#7460=ORIENTED_EDGE ( 'NONE', *, *, #65683, .F. ) ;
#7468=CARTESIAN_POINT ( 'NONE',  ( -2.977408999572654480, 21.37499999795161543, 7.188101187499999156 ) ) ;
#7470=CARTESIAN_POINT ( 'NONE',  ( 1.320432766682874540E-15, 90.40625000204838102, 7.188101187500000044 ) ) ;
#7481=CARTESIAN_POINT ( 'NONE',  ( -4.898587196589412829E-16, 94.62499999999998579, -8.000000000000000000 ) ) ;
#7487=CARTESIAN_POINT ( 'NONE',  ( 7.188101187500000933, 90.50000000204839523, -2.977408999572651371 ) ) ;
#7492=CARTESIAN_POINT ( 'NONE',  ( -2.977408999572651815, 91.81250000204839523, 7.188101187500000933 ) ) ;
#7512=EDGE_CURVE ( 'NONE', #44316, #52808, #50938, .T. ) ;
#7513=CARTESIAN_POINT ( 'NONE',  ( -5.656854249492380582, 95.00000000409677625, -5.656854249492380582 ) ) ;
#7524=CARTESIAN_POINT ( 'NONE',  ( -7.188101187500000044, 97.15625000204839523, 0.000000000000000000 ) ) ;
#7525=CARTESIAN_POINT ( 'NONE',  ( 8.000000000000000000, 16.40624999590322375, -3.313708498984761164 ) ) ;
#7547=CARTESIAN_POINT ( 'NONE',  ( 5.082755093536324154, 5.156249997951610098, 5.082755093536326818 ) ) ;
#7550=CARTESIAN_POINT ( 'NONE',  ( -5.082755093536325930, 113.8437500020483810, -5.082755093536325930 ) ) ;
#7560=CARTESIAN_POINT ( 'NONE',  ( 8.000000000000001776, 112.1562500000000000, 3.313708498984759387 ) ) ;
#7571=CARTESIAN_POINT ( 'NONE',  ( -2.977408999572652260, 103.4375000020483810, 7.188101187500000044 ) ) ;
#7577=CARTESIAN_POINT ( 'NONE',  ( 2.977408999572654480, 107.0000000020483810, 7.188101187499999156 ) ) ;
#7582=ORIENTED_EDGE ( 'NONE', *, *, #38427, .T. ) ;
#7598=CARTESIAN_POINT ( 'NONE',  ( -1.469576158976823947E-15, 7.125000000000000888, 8.000000000000000000 ) ) ;
#7600=CARTESIAN_POINT ( 'NONE',  ( -7.188101187500000044, 4.218749997951610986, -8.802885111219163269E-16 ) ) ;
#7601=CARTESIAN_POINT ( 'NONE',  ( 8.000000000000000000, 123.0312500040967763, -3.313708498984762496 ) ) ;
#7613=CARTESIAN_POINT ( 'NONE',  ( 1.469576158976823947E-15, 95.37499999999998579, 8.000000000000000000 ) ) ;
#7626=CARTESIAN_POINT ( 'NONE',  ( -4.898587196589412829E-16, 120.1250000000000000, -8.000000000000000000 ) ) ;
#7630=( BOUNDED_CURVE ( )  B_SPLINE_CURVE ( 2, ( #49091, #32513, #9499, #9867, #15878, #27577, #72491, #67581, #20800 ),
 .UNSPECIFIED., .F., .F. ) 
 B_SPLINE_CURVE_WITH_KNOTS ( ( 3, 2, 2, 2, 3 ),
 ( 0.7083333333333332593, 0.7152777777777776791, 0.7222222222222220989, 0.7291666666666665186, 0.7361111111111110494 ),
 .UNSPECIFIED. ) 
 CURVE ( )  GEOMETRIC_REPRESENTATION_ITEM ( )  RATIONAL_B_SPLINE_CURVE ( ( 1.000000000000001110, 0.9238795325112855172, 1.000000000000000000, 0.9238795325112867385, 1.000000000000000000, 0.9238795325112867385, 1.000000000000000000, 0.9238795325112879597, 0.9999999999999987788 ) ) 
 REPRESENTATION_ITEM ( '' )  );
#7634=CARTESIAN_POINT ( 'NONE',  ( 8.000000000000000000, 14.81249999590322020, 0.000000000000000000 ) ) ;
#7657=CARTESIAN_POINT ( 'NONE',  ( -4.401442555609581635E-16, 120.7812500020483810, -7.188101187500000044 ) ) ;
#7662=CARTESIAN_POINT ( 'NONE',  ( 5.082755093536325042, 96.59375000204838102, -5.082755093536325930 ) ) ;
#7668=EDGE_CURVE ( 'NONE', #7386, #3972, #34776, .T. ) ;
#7670=DIRECTION ( 'NONE',  ( -0.000000000000000000, 1.000000000000000000, -0.000000000000000000 ) ) ;
#7688=EDGE_CURVE ( 'NONE', #34934, #39259, #6219, .T. ) ;
#7689=CARTESIAN_POINT ( 'NONE',  ( -2.977408999572654480, 13.49999999795161187, 7.188101187499999156 ) ) ;
#7691=CARTESIAN_POINT ( 'NONE',  ( 3.674341569226420301, 124.5066941839809544, -7.107250865053953426 ) ) ;
#7692=CARTESIAN_POINT ( 'NONE',  ( -5.082755093536325042, 11.90624999795161010, -5.082755093536325930 ) ) ;
#7700=EDGE_LOOP ( 'NONE', ( #49144, #55321, #2669, #13454 ) ) ;
#7705=CARTESIAN_POINT ( 'NONE',  ( 2.977408999572650039, 117.6875000020484094, -7.188101187500001821 ) ) ;
#7711=CARTESIAN_POINT ( 'NONE',  ( 2.977408999572650927, 24.74999999795161543, -7.188101187500000933 ) ) ;
#7718=CARTESIAN_POINT ( 'NONE',  ( -7.188101187500000044, 102.0312500020483810, 0.000000000000000000 ) ) ;
#7722=EDGE_LOOP ( 'NONE', ( #46689, #39045, #53972, #24072 ) ) ;
#7730=CARTESIAN_POINT ( 'NONE',  ( -1.469576158976823947E-15, 1.125000000000000222, 8.000000000000000000 ) ) ;
#7737=CARTESIAN_POINT ( 'NONE',  ( 0.000000000000000000, 125.0000000000000000, 0.000000000000000000 ) ) ;
#7740=CARTESIAN_POINT ( 'NONE',  ( -3.313708498984760276, 7.781249995903221972, -8.000000000000000000 ) ) ;
#7744=CARTESIAN_POINT ( 'NONE',  ( -8.000000000000001776, 5.156249995903221084, 3.313708498984759387 ) ) ;
#7747=CARTESIAN_POINT ( 'NONE',  ( -5.082755093536324154, 113.8437500020483810, 5.082755093536326818 ) ) ;
#7776=CARTESIAN_POINT ( 'NONE',  ( 5.082755093536324154, 11.15624999795161187, 5.082755093536326818 ) ) ;
#7794=CARTESIAN_POINT ( 'NONE',  ( -5.656854249492381470, 23.43750000000000355, 5.656854249492379694 ) ) ;
#7796=ORIENTED_EDGE ( 'NONE', *, *, #10768, .T. ) ;
#7805=CARTESIAN_POINT ( 'NONE',  ( 5.082755093536325930, 8.156249997951611874, -5.082755093536325930 ) ) ;
#7807=CARTESIAN_POINT ( 'NONE',  ( -7.188101187500000044, 117.0312500020483810, 0.000000000000000000 ) ) ;
#7812=ORIENTED_EDGE ( 'NONE', *, *, #7512, .F. ) ;
#7818=CARTESIAN_POINT ( 'NONE',  ( 5.656854249492378806, 23.81250000000000355, 5.656854249492381470 ) ) ;
#7832=CARTESIAN_POINT ( 'NONE',  ( -5.082755093536324154, 91.71875000204838102, 5.082755093536326818 ) ) ;
#7856=EDGE_CURVE ( 'NONE', #25866, #23857, #63064, .T. ) ;
#7866=CYLINDRICAL_SURFACE ( 'NONE', #14697, 8.000000000000000000 ) ;
#7879=ORIENTED_EDGE ( 'NONE', *, *, #7688, .F. ) ;
#7881=CARTESIAN_POINT ( 'NONE',  ( -3.313708498984762052, 96.40625000409677625, -8.000000000000000000 ) ) ;
#7889=CARTESIAN_POINT ( 'NONE',  ( 7.188101187500001821, 99.50000000204838102, -2.977408999572651371 ) ) ;
#7893=ORIENTED_EDGE ( 'NONE', *, *, #39361, .F. ) ;
#7908=CARTESIAN_POINT ( 'NONE',  ( 5.656854249492378806, 4.124999995903220196, 5.656854249492381470 ) ) ;
#7910=CARTESIAN_POINT ( 'NONE',  ( -2.977408999572654480, 12.37499999795161010, 7.188101187499999156 ) ) ;
#7913=CARTESIAN_POINT ( 'NONE',  ( -5.082755093536325930, 110.8437500020483810, -5.082755093536325930 ) ) ;
#7935=CARTESIAN_POINT ( 'NONE',  ( 7.188101187500000044, 105.4062500020483810, -8.802885111219163269E-16 ) ) ;
#7940=CARTESIAN_POINT ( 'NONE',  ( 2.977408999572650039, 107.5625000020483810, -7.188101187500001821 ) ) ;
#7947=CARTESIAN_POINT ( 'NONE',  ( -8.000000000000000000, 0.6562500000000001110, -3.313708498984762496 ) ) ;
#7951=LINE ( 'NONE', #54353, #41100 ) ;
#7953=CARTESIAN_POINT ( 'NONE',  ( 8.000000000000000000, 15.00000000000000355, 0.000000000000000000 ) ) ;
#7968=CARTESIAN_POINT ( 'NONE',  ( 8.000000000000000000, 12.00000000000000178, 0.000000000000000000 ) ) ;
#7969=CARTESIAN_POINT ( 'NONE',  ( -3.313708498984761608, 106.7187500000000000, -8.000000000000000000 ) ) ;
#7970=CARTESIAN_POINT ( 'NONE',  ( 2.977408999572650927, 5.249999997951610986, -7.188101187500001821 ) ) ;
#7972=CARTESIAN_POINT ( 'NONE',  ( -5.656854249492378806, 113.3750000040967763, 5.656854249492381470 ) ) ;
#7985=ORIENTED_EDGE ( 'NONE', *, *, #27632, .F. ) ;
#7987=CARTESIAN_POINT ( 'NONE',  ( 5.656854249492378806, 26.62499999590322375, 5.656854249492381470 ) ) ;
#7993=CARTESIAN_POINT ( 'NONE',  ( 5.656854249492381470, 115.0625000000000000, 5.656854249492379694 ) ) ;
#7997=CARTESIAN_POINT ( 'NONE',  ( -5.656854249492381470, 14.24999999590322375, 5.656854249492379694 ) ) ;
#8018=CARTESIAN_POINT ( 'NONE',  ( -1.469576158976823947E-15, 3.937499995903220640, 8.000000000000000000 ) ) ;
#8024=CARTESIAN_POINT ( 'NONE',  ( -7.188101187499999156, 92.75000000204839523, 2.977408999572654924 ) ) ;
#8053=CARTESIAN_POINT ( 'NONE',  ( 5.082755093536324154, 16.78124999795161543, 5.082755093536326818 ) ) ;
#8057=CARTESIAN_POINT ( 'NONE',  ( -5.082755093536326818, 10.78124999795161187, 5.082755093536325042 ) ) ;
#8070=CARTESIAN_POINT ( 'NONE',  ( -5.082755093536324154, 112.3437500020483810, 5.082755093536326818 ) ) ;
#8071=EDGE_CURVE ( 'NONE', #5359, #49924, #61755, .T. ) ;
#8074=ORIENTED_EDGE ( 'NONE', *, *, #39840, .F. ) ;
#8075=CARTESIAN_POINT ( 'NONE',  ( -2.977408999572654480, 25.49999999795161187, 7.188101187499999156 ) ) ;
#8081=CARTESIAN_POINT ( 'NONE',  ( 1.320432766682874540E-15, 96.40625000204838102, 7.188101187500000044 ) ) ;
#8085=ORIENTED_EDGE ( 'NONE', *, *, #62476, .F. ) ;
#8094=DIRECTION ( 'NONE',  ( 0.000000000000000000, 0.000000000000000000, 1.000000000000000000 ) ) ;
#8105=CARTESIAN_POINT ( 'NONE',  ( -3.313708498984744732, 8.343749995903223748, 8.000000000000019540 ) ) ;
#8106=EDGE_CURVE ( 'NONE', #64023, #5844, #47613, .T. ) ;
#8110=CARTESIAN_POINT ( 'NONE',  ( -4.528114470331722430, 124.6731747980935836, -6.389158183658611101 ) ) ;
#8112=CARTESIAN_POINT ( 'NONE',  ( 1.320432766682874540E-15, 108.0312500020483810, 7.188101187500000044 ) ) ;
#8129=FACE_BOUND ( 'NONE', #34453, .T. ) ;
#8141=CARTESIAN_POINT ( 'NONE',  ( -1.320432766682874540E-15, 12.46874999795161187, 7.188101187500000044 ) ) ;
#8145=CARTESIAN_POINT ( 'NONE',  ( 1.347111479062088405E-15, 75.00000000000000000, -11.00000000000000000 ) ) ;
#8157=CARTESIAN_POINT ( 'NONE',  ( 3.313708498984762052, 22.78125000000000355, -8.000000000000000000 ) ) ;
#8168=CARTESIAN_POINT ( 'NONE',  ( 4.401442555609581635E-16, 6.843749997951611874, -7.188101187500000044 ) ) ;
#8170=CARTESIAN_POINT ( 'NONE',  ( 2.977408999572654480, 116.0000000020483810, 7.188101187499999156 ) ) ;
#8179=CARTESIAN_POINT ( 'NONE',  ( 0.000000000000000000, 125.0000000000000000, 8.000000000000000000 ) ) ;
#8183=CARTESIAN_POINT ( 'NONE',  ( 3.313708498984765161, 99.96875000000000000, 7.999999999999998224 ) ) ;
#8196=CARTESIAN_POINT ( 'NONE',  ( 5.082755093536325930, 26.53124999795161543, -5.082755093536325930 ) ) ;
#8198=CARTESIAN_POINT ( 'NONE',  ( 7.188101187500000044, 90.78125000204838102, -8.802885111219163269E-16 ) ) ;
#8209=CARTESIAN_POINT ( 'NONE',  ( 0.000000000000000000, 125.0000000000000000, 0.000000000000000000 ) ) ;
#8212=ORIENTED_EDGE ( 'NONE', *, *, #51085, .T. ) ;
#8223=CARTESIAN_POINT ( 'NONE',  ( 1.320432766682874540E-15, 90.40625000204838102, 7.188101187500000044 ) ) ;
#8243=CARTESIAN_POINT ( 'NONE',  ( 5.656854249492379694, 96.12500000409677625, -5.656854249492380582 ) ) ;
#8249=CYLINDRICAL_SURFACE ( 'NONE', #46302, 8.000000000000000000 ) ;
#8250=CARTESIAN_POINT ( 'NONE',  ( -4.401442555609581635E-16, 99.78125000204838102, -7.188101187500000044 ) ) ;
#8257=CARTESIAN_POINT ( 'NONE',  ( -4.898587196589412829E-16, 100.8125000040967763, -8.000000000000000000 ) ) ;
#8272=EDGE_CURVE ( 'NONE', #20088, #55604, #5906, .T. ) ;
#8275=CARTESIAN_POINT ( 'NONE',  ( -5.656854249492379694, 1.874999995903220196, -5.656854249492380582 ) ) ;
#8277=CARTESIAN_POINT ( 'NONE',  ( -2.977408999572650039, 11.81249999795161187, -7.188101187500001821 ) ) ;
#8280=CARTESIAN_POINT ( 'NONE',  ( -7.188101187499999156, 111.1250000020483810, 2.977408999572654924 ) ) ;
#8299=CARTESIAN_POINT ( 'NONE',  ( -5.082755093536325930, 102.9687500020483810, -5.082755093536325930 ) ) ;
#8306=CARTESIAN_POINT ( 'NONE',  ( -5.082755093536325930, 106.3437500020483810, -5.082755093536325930 ) ) ;
#8322=AXIS2_PLACEMENT_3D ( 'NONE', #20233, #25887, #60233 ) ;
#8329=ORIENTED_EDGE ( 'NONE', *, *, #73944, .F. ) ;
#8331=CARTESIAN_POINT ( 'NONE',  ( 7.188101187499999156, 27.74999999795161543, 2.977408999572654924 ) ) ;
#8332=CARTESIAN_POINT ( 'NONE',  ( 3.313708498984760720, 117.2187500040968047, -8.000000000000000000 ) ) ;
#8356=EDGE_CURVE ( 'NONE', #12358, #41332, #55363, .T. ) ;
#8358=CARTESIAN_POINT ( 'NONE',  ( -3.313708498984762052, 111.2187500000000142, -8.000000000000000000 ) ) ;
#8363=CARTESIAN_POINT ( 'NONE',  ( -1.469576158976823947E-15, 23.43749999590322020, 8.000000000000000000 ) ) ;
#8375=CARTESIAN_POINT ( 'NONE',  ( 1.469576158976823947E-15, 100.0625000040967763, 8.000000000000000000 ) ) ;
#8387=CARTESIAN_POINT ( 'NONE',  ( 7.188101187500002709, 121.8125000020483810, 2.977408999572649151 ) ) ;
#8392=CARTESIAN_POINT ( 'NONE',  ( 7.188101187500001821, 93.50000000204838102, -2.977408999572651371 ) ) ;
#8421=CARTESIAN_POINT ( 'NONE',  ( -7.188101187500002709, 19.31249999795161543, 2.977408999572649151 ) ) ;
#8424=CARTESIAN_POINT ( 'NONE',  ( -1.320432766682874540E-15, 13.96874999795161187, 7.188101187500000044 ) ) ;
#8435=CARTESIAN_POINT ( 'NONE',  ( 7.188101187500001821, 108.5000000020483810, -2.977408999572651371 ) ) ;
#8439=CARTESIAN_POINT ( 'NONE',  ( -1.320432766682874540E-15, 21.09374999795161543, 7.188101187500000044 ) ) ;
#8447=CARTESIAN_POINT ( 'NONE',  ( 7.188101187500001821, 95.37500000204839523, -2.977408999572651371 ) ) ;
#8451=AXIS2_PLACEMENT_3D ( 'NONE', #64419, #12716, #54209 ) ;
#8459=CARTESIAN_POINT ( 'NONE',  ( -7.683012701892240059, 124.8169872981077901, 0.000000000000000000 ) ) ;
#8471=EDGE_CURVE ( 'NONE', #11312, #49646, #37955, .T. ) ;
#8478=CARTESIAN_POINT ( 'NONE',  ( 7.188101187500000044, 111.4062500020483810, -8.802885111219163269E-16 ) ) ;
#8484=ORIENTED_EDGE ( 'NONE', *, *, #63473, .T. ) ;
#8508=CARTESIAN_POINT ( 'NONE',  ( 7.188101187500000044, 14.34374999795161187, 0.000000000000000000 ) ) ;
#8517=CARTESIAN_POINT ( 'NONE',  ( -2.977408999572654480, 5.999999997951610098, 7.188101187499999156 ) ) ;
#8521=CONICAL_SURFACE ( 'NONE', #18171, 8.000000000000000000, 0.7853981633974552734 ) ;
#8527=CARTESIAN_POINT ( 'NONE',  ( -5.656854249492381470, 21.93750000000000355, 5.656854249492379694 ) ) ;
#8537=CARTESIAN_POINT ( 'NONE',  ( -7.188101187500000933, 2.624999997951609654, -2.977408999572651371 ) ) ;
#8541=CARTESIAN_POINT ( 'NONE',  ( -4.401442555609581635E-16, 113.6562500020483952, -7.188101187500000044 ) ) ;
#8542=AXIS2_PLACEMENT_3D ( 'NONE', #34312, #22585, #6380 ) ;
#8556=CARTESIAN_POINT ( 'NONE',  ( -4.898587196589412829E-16, 100.6249999999999858, -8.000000000000000000 ) ) ;
#8571=CARTESIAN_POINT ( 'NONE',  ( -4.401442555609581635E-16, 94.15625000204838102, -7.188101187500000044 ) ) ;
#8595=CARTESIAN_POINT ( 'NONE',  ( 5.082755093536326818, 90.59375000204839523, 5.082755093536325042 ) ) ;
#8604=CARTESIAN_POINT ( 'NONE',  ( 3.313708498984761608, 15.09374999590322020, -8.000000000000000000 ) ) ;
#8607=CARTESIAN_POINT ( 'NONE',  ( 3.313708498984761608, 3.093749995903220196, -8.000000000000000000 ) ) ;
#8615=( BOUNDED_CURVE ( )  B_SPLINE_CURVE ( 2, ( #22147, #74589, #4446, #51572, #5195, #27437, #28192, #45175, #68188 ),
 .UNSPECIFIED., .F., .F. ) 
 B_SPLINE_CURVE_WITH_KNOTS ( ( 3, 2, 2, 2, 3 ),
 ( 0.1145833333333333981, 0.1197916666666667407, 0.1250000000000000833, 0.1302083333333334259, 0.1354166666666667407 ),
 .UNSPECIFIED. ) 
 CURVE ( )  GEOMETRIC_REPRESENTATION_ITEM ( )  RATIONAL_B_SPLINE_CURVE ( ( 0.9999999999999990008, 0.9238795325112877377, 1.000000000000000000, 0.9238795325112867385, 1.000000000000000000, 0.9238795325112867385, 1.000000000000000000, 0.9238795325112855172, 1.000000000000001110 ) ) 
 REPRESENTATION_ITEM ( '' )  );
#8620=CARTESIAN_POINT ( 'NONE',  ( -3.313708498984762496, 96.96875000409677625, 7.999999999999998224 ) ) ;
#8631=CARTESIAN_POINT ( 'NONE',  ( 7.188101187500002709, 91.81250000204839523, 2.977408999572649151 ) ) ;
#8649=CARTESIAN_POINT ( 'NONE',  ( 0.000000000000000000, 125.0000000000000000, 0.000000000000000000 ) ) ;
#8653=CARTESIAN_POINT ( 'NONE',  ( -3.313708498984760720, 1.781249995903220418, -8.000000000000000000 ) ) ;
#8655=CARTESIAN_POINT ( 'NONE',  ( -7.188101187500001821, 11.99999999795161187, -2.977408999572651371 ) ) ;
#8658=CARTESIAN_POINT ( 'NONE',  ( -7.188101187499999156, 112.6250000020483810, 2.977408999572654924 ) ) ;
#8676=CARTESIAN_POINT ( 'NONE',  ( 7.188101187500000933, 102.5000000020483810, -2.977408999572651371 ) ) ;
#8679=CARTESIAN_POINT ( 'NONE',  ( 2.506878452759003562, 0.3721089088409397228, -7.479669363585287556 ) ) ;
#8682=CARTESIAN_POINT ( 'NONE',  ( 7.188101187500000044, 105.7812500020483810, -8.802885111219163269E-16 ) ) ;
#8686=DIRECTION ( 'NONE',  ( 0.000000000000000000, 0.000000000000000000, 1.000000000000000000 ) ) ;
#8709=CARTESIAN_POINT ( 'NONE',  ( -1.320432766682874540E-15, 6.093749997951610986, 7.188101187500000044 ) ) ;
#8710=CARTESIAN_POINT ( 'NONE',  ( 1.469576158976823947E-15, 116.5625000040967763, 8.000000000000000000 ) ) ;
#8739=CARTESIAN_POINT ( 'NONE',  ( -8.000000000000000000, 110.0000000000000000, 0.000000000000000000 ) ) ;
#8746=CARTESIAN_POINT ( 'NONE',  ( 4.898587196589412829E-16, 19.68749999590322020, -8.000000000000000000 ) ) ;
#8749=CARTESIAN_POINT ( 'NONE',  ( 3.313708498984873518, 113.6562500040967763, 7.999999999999890754 ) ) ;
#8759=CARTESIAN_POINT ( 'NONE',  ( -4.898587196589412829E-16, 106.8125000040967763, -8.000000000000000000 ) ) ;
#8769=CARTESIAN_POINT ( 'NONE',  ( 7.188101187500000933, 120.5000000020483810, -2.977408999572651371 ) ) ;
#8774=CARTESIAN_POINT ( 'NONE',  ( -5.082755093536325930, 90.96875000204838102, -5.082755093536325930 ) ) ;
#8804=CARTESIAN_POINT ( 'NONE',  ( -7.188101187500001821, 23.62499999795161543, -2.977408999572651371 ) ) ;
#8807=CARTESIAN_POINT ( 'NONE',  ( -1.320432766682874540E-15, 15.46874999795161187, 7.188101187500000044 ) ) ;
#8817=CARTESIAN_POINT ( 'NONE',  ( 2.977408999572650039, 111.6875000020483810, -7.188101187500001821 ) ) ;
#8822=CARTESIAN_POINT ( 'NONE',  ( 7.188101187499999156, 27.37499999795161543, 2.977408999572654924 ) ) ;
#8829=CARTESIAN_POINT ( 'NONE',  ( -4.401442555609581635E-16, 95.65625000204838102, -7.188101187500000044 ) ) ;
#8835=CARTESIAN_POINT ( 'NONE',  ( 1.469576158976823947E-15, 92.56250000409677625, 8.000000000000000000 ) ) ;
#8840=FACE_OUTER_BOUND ( 'NONE', #64222, .T. ) ;
#8860=CARTESIAN_POINT ( 'NONE',  ( -5.082755093536325930, 111.9687500020483810, -5.082755093536325930 ) ) ;
#8873=FACE_OUTER_BOUND ( 'NONE', #12901, .T. ) ;
#8878=DIRECTION ( 'NONE',  ( -0.000000000000000000, 1.000000000000000000, -0.000000000000000000 ) ) ;
#8885=CARTESIAN_POINT ( 'NONE',  ( -7.188101187500000933, 19.49999999795161898, -2.977408999572651371 ) ) ;
#8893=CARTESIAN_POINT ( 'NONE',  ( -8.000000000000000000, 98.09375000409680467, -3.313708498984761164 ) ) ;
#8894=CARTESIAN_POINT ( 'NONE',  ( 2.977408999572650927, 0.7499999979516099868, -7.188101187500001821 ) ) ;
#8913=CARTESIAN_POINT ( 'NONE',  ( -2.977408999572650039, 9.937499997951610098, -7.188101187500000933 ) ) ;
#8917=CARTESIAN_POINT ( 'NONE',  ( -7.188101187500001821, 113.9375000020483952, -2.977408999572650483 ) ) ;
#8927=CARTESIAN_POINT ( 'NONE',  ( 3.313708498984802020, 19.59374999590321664, -7.999999999999958256 ) ) ;
#8930=CARTESIAN_POINT ( 'NONE',  ( 0.000000000000000000, 125.0000000000000000, 8.000000000000000000 ) ) ;
#8932=CARTESIAN_POINT ( 'NONE',  ( -7.999999999999998224, 95.09375000000001421, 3.313708498984766493 ) ) ;
#8946=CARTESIAN_POINT ( 'NONE',  ( 2.977408999572654480, 93.50000000204838102, 7.188101187499999156 ) ) ;
#8951=CARTESIAN_POINT ( 'NONE',  ( -8.000000000000000000, 96.50000000000000000, 0.000000000000000000 ) ) ;
#8956=CARTESIAN_POINT ( 'NONE',  ( 7.188101187500000044, 21.46874999795161543, 0.000000000000000000 ) ) ;
#8972=CARTESIAN_POINT ( 'NONE',  ( -7.188101187499999156, 91.62500000204838102, 2.977408999572654924 ) ) ;
#8994=CARTESIAN_POINT ( 'NONE',  ( 8.000000000000001776, 95.84375000409677625, 3.313708498984759387 ) ) ;
#9003=EDGE_LOOP ( 'NONE', ( #43742, #64553, #17626, #9619 ) ) ;
#9005=CARTESIAN_POINT ( 'NONE',  ( -2.977408999572650927, 90.87500000204838102, -7.188101187500001821 ) ) ;
#9011=EDGE_CURVE ( 'NONE', #28769, #49646, #14789, .T. ) ;
#9027=CARTESIAN_POINT ( 'NONE',  ( 3.313708498984762496, 4.031249995903220196, 7.999999999999998224 ) ) ;
#9029=CARTESIAN_POINT ( 'NONE',  ( 2.977408999572650927, 13.12499999795161187, -7.188101187500001821 ) ) ;
#9033=CARTESIAN_POINT ( 'NONE',  ( 2.977408999572650039, 112.0625000020483810, -7.188101187500000933 ) ) ;
#9042=ORIENTED_EDGE ( 'NONE', *, *, #2908, .F. ) ;
#9051=CARTESIAN_POINT ( 'NONE',  ( -5.082755093536325930, 99.96875000204838102, -5.082755093536325930 ) ) ;
#9058=CARTESIAN_POINT ( 'NONE',  ( -4.401442555609581635E-16, 107.6562500020483810, -7.188101187500000044 ) ) ;
#9062=( BOUNDED_CURVE ( )  B_SPLINE_CURVE ( 2, ( #64712, #47353, #623, #41699, #5895, #59064, #29276, #57585, #18320 ),
 .UNSPECIFIED., .F., .F. ) 
 B_SPLINE_CURVE_WITH_KNOTS ( ( 3, 2, 2, 2, 3 ),
 ( 0.3750000000000000000, 0.3819444444444444198, 0.3888888888888888395, 0.3958333333333332593, 0.4027777777777776791 ),
 .UNSPECIFIED. ) 
 CURVE ( )  GEOMETRIC_REPRESENTATION_ITEM ( )  RATIONAL_B_SPLINE_CURVE ( ( 1.000000000000000000, 0.9238795325112867385, 1.000000000000000000, 0.9238795325112867385, 1.000000000000000000, 0.9238795325112867385, 1.000000000000000000, 0.9238795325112879597, 0.9999999999999987788 ) ) 
 REPRESENTATION_ITEM ( '' )  );
#9065=ORIENTED_EDGE ( 'NONE', *, *, #2124, .F. ) ;
#9069=CYLINDRICAL_SURFACE ( 'NONE', #24246, 8.000000000000000000 ) ;
#9077=CARTESIAN_POINT ( 'NONE',  ( 0.000000000000000000, 125.0000000000000000, 0.000000000000000000 ) ) ;
#9078=CARTESIAN_POINT ( 'NONE',  ( -7.999999999999998224, 122.2812500040967905, 3.313708498984766049 ) ) ;
#9086=CARTESIAN_POINT ( 'NONE',  ( 7.188101187499999156, 10.87499999795161187, 2.977408999572654924 ) ) ;
#9088=CARTESIAN_POINT ( 'NONE',  ( 8.000000000000000000, 118.4375000040967763, -9.797174393178825657E-16 ) ) ;
#9092=DIRECTION ( 'NONE',  ( -0.000000000000000000, 1.000000000000000000, -0.000000000000000000 ) ) ;
#9093=AXIS2_PLACEMENT_3D ( 'NONE', #54377, #9092, #1944 ) ;
#9104=ORIENTED_EDGE ( 'NONE', *, *, #69176, .T. ) ;
#9112=CARTESIAN_POINT ( 'NONE',  ( -7.999999999999998224, 110.0937499999999858, 3.313708498984766493 ) ) ;
#9118=CARTESIAN_POINT ( 'NONE',  ( 4.898587196589412829E-16, 18.18749999590322020, -8.000000000000000000 ) ) ;
#9140=CARTESIAN_POINT ( 'NONE',  ( 7.188101187500000933, 119.0000000020483810, -2.977408999572651371 ) ) ;
#9146=CARTESIAN_POINT ( 'NONE',  ( 7.188101187500000044, 93.40625000204838102, -8.802885111219163269E-16 ) ) ;
#9172=CARTESIAN_POINT ( 'NONE',  ( 2.977408999572650927, 20.24999999795161898, -7.188101187500001821 ) ) ;
#9175=CARTESIAN_POINT ( 'NONE',  ( -1.320432766682874540E-15, 19.96874999795161543, 7.188101187500000044 ) ) ;
#9179=DIRECTION ( 'NONE',  ( -0.000000000000000000, 1.000000000000000000, -0.000000000000000000 ) ) ;
#9186=CARTESIAN_POINT ( 'NONE',  ( -5.082755093536325930, 111.9687500020483810, -5.082755093536325930 ) ) ;
#9190=CARTESIAN_POINT ( 'NONE',  ( 4.898587196589412829E-16, 4.875000000000000888, -8.000000000000000000 ) ) ;
#9194=CARTESIAN_POINT ( 'NONE',  ( 9.797174393178825657E-16, 125.0000000000000000, -8.000000000000000000 ) ) ;
#9198=CARTESIAN_POINT ( 'NONE',  ( -7.188101187500001821, 95.93750000204839523, -2.977408999572650483 ) ) ;
#9230=CARTESIAN_POINT ( 'NONE',  ( 5.082755093536325042, 111.5937500020483810, -5.082755093536325930 ) ) ;
#9240=CARTESIAN_POINT ( 'NONE',  ( -4.898587196589412829E-16, 99.12499999999998579, -8.000000000000000000 ) ) ;
#9245=CARTESIAN_POINT ( 'NONE',  ( 1.469576158976823947E-15, 93.87499999999998579, 8.000000000000000000 ) ) ;
#9257=CARTESIAN_POINT ( 'NONE',  ( 7.188101187499999156, 17.24999999795162253, 2.977408999572654924 ) ) ;
#9265=CARTESIAN_POINT ( 'NONE',  ( -2.977408999572650039, 3.937499997951610986, -7.188101187500001821 ) ) ;
#9268=CARTESIAN_POINT ( 'NONE',  ( 7.188101187500000044, 0.8437499979516099868, 0.000000000000000000 ) ) ;
#9284=CARTESIAN_POINT ( 'NONE',  ( -7.188101187500000044, 10.21874999795161187, -8.802885111219163269E-16 ) ) ;
#9289=CARTESIAN_POINT ( 'NONE',  ( 7.188101187500000044, 111.7812500020483810, -8.802885111219163269E-16 ) ) ;
#9304=CARTESIAN_POINT ( 'NONE',  ( -8.000000000000000000, 94.90624999999998579, -3.313708498984761608 ) ) ;
#9313=EDGE_CURVE ( 'NONE', #33538, #5844, #41146, .T. ) ;
#9323=FACE_OUTER_BOUND ( 'NONE', #7263, .T. ) ;
#9331=CARTESIAN_POINT ( 'NONE',  ( -2.977408999572654480, 17.99999999795161898, 7.188101187499999156 ) ) ;
#9341=CARTESIAN_POINT ( 'NONE',  ( 3.313708498984777595, 121.7187500040967620, -7.999999999999983125 ) ) ;
#9346=CARTESIAN_POINT ( 'NONE',  ( -5.656854249492381470, 21.74999999590322375, 5.656854249492379694 ) ) ;
#9366=CARTESIAN_POINT ( 'NONE',  ( 3.313708498984762496, 8.718750000000000000, 7.999999999999998224 ) ) ;
#9368=CARTESIAN_POINT ( 'NONE',  ( -8.000000000000000000, 89.18750000409677625, 0.000000000000000000 ) ) ;
#9380=CARTESIAN_POINT ( 'NONE',  ( -2.977408999572651815, 89.93750000204840944, 7.188101187500000933 ) ) ;
#9403=CARTESIAN_POINT ( 'NONE',  ( -1.469576158976823947E-15, 8.437499995903221972, 8.000000000000000000 ) ) ;
#9407=CARTESIAN_POINT ( 'NONE',  ( -5.082755093536325042, 11.90624999795161010, -5.082755093536325930 ) ) ;
#9409=CARTESIAN_POINT ( 'NONE',  ( -3.313708498984815343, 105.2187500000000000, -7.999999999999944933 ) ) ;
#9410=CARTESIAN_POINT ( 'NONE',  ( 7.188101187500000933, 110.3750000020484094, -2.977408999572651371 ) ) ;
#9430=CARTESIAN_POINT ( 'NONE',  ( -7.188101187500000044, 98.65625000204838102, 0.000000000000000000 ) ) ;
#9438=CARTESIAN_POINT ( 'NONE',  ( 2.977408999572654480, 102.5000000020483810, 7.188101187499999156 ) ) ;
#9455=VERTEX_POINT ( 'NONE', #53206 ) ;
#9463=ORIENTED_EDGE ( 'NONE', *, *, #38256, .T. ) ;
#9465=CARTESIAN_POINT ( 'NONE',  ( 5.082755093536325930, 8.156249997951611874, -5.082755093536325930 ) ) ;
#9466=CARTESIAN_POINT ( 'NONE',  ( -5.656854249492378806, 114.8750000040967905, 5.656854249492381470 ) ) ;
#9479=CARTESIAN_POINT ( 'NONE',  ( -1.469576158976823947E-15, 16.12500000000000355, 8.000000000000000000 ) ) ;
#9495=CARTESIAN_POINT ( 'NONE',  ( 3.313708498984765161, 110.4687500000000000, 7.999999999999998224 ) ) ;
#9499=CARTESIAN_POINT ( 'NONE',  ( 5.656854249492378806, 19.31250000000000355, 5.656854249492381470 ) ) ;
#9502=CARTESIAN_POINT ( 'NONE',  ( 3.313708498984762496, 22.03124999590322375, 7.999999999999998224 ) ) ;
#9517=CARTESIAN_POINT ( 'NONE',  ( -5.656854249492380582, 107.0000000040967763, -5.656854249492380582 ) ) ;
#9526=CARTESIAN_POINT ( 'NONE',  ( 5.082755093536326818, 120.2187500020483952, 5.082755093536325042 ) ) ;
#9530=EDGE_CURVE ( 'NONE', #41332, #33110, #15052, .T. ) ;
#9532=CARTESIAN_POINT ( 'NONE',  ( 2.977408999572654480, 91.62500000204838102, 7.188101187499999156 ) ) ;
#9536=EDGE_LOOP ( 'NONE', ( #21225, #7796, #50705, #56140 ) ) ;
#9545=CARTESIAN_POINT ( 'NONE',  ( -1.469576158976823947E-15, 5.625000000000000888, 8.000000000000000000 ) ) ;
#9558=CARTESIAN_POINT ( 'NONE',  ( 5.082755093536324154, 18.28124999795161187, 5.082755093536326818 ) ) ;
#9560=CARTESIAN_POINT ( 'NONE',  ( 0.000000000000000000, 75.00000000000000000, 0.000000000000000000 ) ) ;
#9561=CARTESIAN_POINT ( 'NONE',  ( -7.188101187500001821, 17.99999999795161898, -2.977408999572651371 ) ) ;
#9569=ADVANCED_FACE ( 'NONE', ( #27873 ), #49770, .T. ) ;
#9585=CARTESIAN_POINT ( 'NONE',  ( 5.082755093536325042, 92.46875000204838102, -5.082755093536325930 ) ) ;
#9590=CARTESIAN_POINT ( 'NONE',  ( 7.999999999999998224, 11.90625000000000355, 3.313708498984766049 ) ) ;
#9600=CARTESIAN_POINT ( 'NONE',  ( 1.469576158976823947E-15, 113.5625000040967905, 8.000000000000000000 ) ) ;
#9613=CARTESIAN_POINT ( 'NONE',  ( -7.188101187499999156, 109.2500000020483952, 2.977408999572654924 ) ) ;
#9617=CARTESIAN_POINT ( 'NONE',  ( 1.469576158976823947E-15, 110.3750000000000000, 8.000000000000000000 ) ) ;
#9619=ORIENTED_EDGE ( 'NONE', *, *, #9313, .F. ) ;
#9624=CARTESIAN_POINT ( 'NONE',  ( 0.000000000000000000, 125.0000000000000000, 8.000000000000000000 ) ) ;
#9626=ORIENTED_EDGE ( 'NONE', *, *, #36970, .T. ) ;
#9631=CARTESIAN_POINT ( 'NONE',  ( -3.313708498984816231, 95.28124999999998579, 7.999999999999943157 ) ) ;
#9635=( BOUNDED_CURVE ( )  B_SPLINE_CURVE ( 2, ( #67948, #4957, #69066, #17370, #63392, #10610, #56642, #27959, #6066 ),
 .UNSPECIFIED., .F., .F. ) 
 B_SPLINE_CURVE_WITH_KNOTS ( ( 3, 2, 2, 2, 3 ),
 ( 0.7395833333333334814, 0.7447916666666667407, 0.7500000000000001110, 0.7552083333333334814, 0.7604166666666667407 ),
 .UNSPECIFIED. ) 
 CURVE ( )  GEOMETRIC_REPRESENTATION_ITEM ( )  RATIONAL_B_SPLINE_CURVE ( ( 0.9999999999999983347, 0.9238795325112884038, 1.000000000000000000, 0.9238795325112867385, 1.000000000000000000, 0.9238795325112867385, 1.000000000000000000, 0.9238795325112850731, 1.000000000000001554 ) ) 
 REPRESENTATION_ITEM ( '' )  );
#9636=CARTESIAN_POINT ( 'NONE',  ( -7.999999999999998224, 110.0937499999999858, 3.313708498984766049 ) ) ;
#9640=CARTESIAN_POINT ( 'NONE',  ( 7.188101187500000044, 17.34374999795161543, 0.000000000000000000 ) ) ;
#9649=CARTESIAN_POINT ( 'NONE',  ( -5.082755093536326818, 2.906249997951610098, 5.082755093536325042 ) ) ;
#9653=ORIENTED_EDGE ( 'NONE', *, *, #13403, .T. ) ;
#9668=CARTESIAN_POINT ( 'NONE',  ( 5.082755093536324154, 13.78124999795161010, 5.082755093536326818 ) ) ;
#9672=CARTESIAN_POINT ( 'NONE',  ( -7.188101187500001821, 110.9375000020483810, -2.977408999572650483 ) ) ;
#9682=CARTESIAN_POINT ( 'NONE',  ( -1.469576158976823947E-15, 18.93749999590322020, 8.000000000000000000 ) ) ;
#9687=CARTESIAN_POINT ( 'NONE',  ( 3.313708498984760720, 94.53125000000001421, -8.000000000000000000 ) ) ;
#9693=CARTESIAN_POINT ( 'NONE',  ( -1.469576158976823947E-15, 13.12500000000000355, 8.000000000000000000 ) ) ;
#9701=DIRECTION ( 'NONE',  ( 0.000000000000000000, 0.000000000000000000, 1.000000000000000000 ) ) ;
#9708=VERTEX_POINT ( 'NONE', #6371 ) ;
#9709=CARTESIAN_POINT ( 'NONE',  ( 4.401442555609581635E-16, 21.84374999795161543, -7.188101187500000044 ) ) ;
#9713=VERTEX_POINT ( 'NONE', #29377 ) ;
#9744=CARTESIAN_POINT ( 'NONE',  ( 5.656854249492380582, 18.18750000000000355, -5.656854249492380582 ) ) ;
#9746=CARTESIAN_POINT ( 'NONE',  ( 4.898587196589412829E-16, 9.375000000000001776, -8.000000000000000000 ) ) ;
#9749=VECTOR ( 'NONE', #17678, 1000.000000000000000 ) ;
#9750=CARTESIAN_POINT ( 'NONE',  ( 5.656854249492381470, 91.25000000409677625, 5.656854249492379694 ) ) ;
#9759=CARTESIAN_POINT ( 'NONE',  ( -5.082755093536325930, 93.96875000204838102, -5.082755093536325930 ) ) ;
#9781=CARTESIAN_POINT ( 'NONE',  ( -1.469576158976823947E-15, 9.937499995903220196, 8.000000000000000000 ) ) ;
#9784=CARTESIAN_POINT ( 'NONE',  ( 7.188101187500001821, 17.43749999795161543, -2.977408999572650483 ) ) ;
#9787=CARTESIAN_POINT ( 'NONE',  ( 5.082755093536326818, 102.5937500020483810, 5.082755093536325042 ) ) ;
#9797=LINE ( 'NONE', #56571, #47109 ) ;
#9804=CARTESIAN_POINT ( 'NONE',  ( -7.188101187500000933, 100.0625000020483810, -2.977408999572650483 ) ) ;
#9810=CARTESIAN_POINT ( 'NONE',  ( -7.188101187500000044, 103.5312500020483810, 0.000000000000000000 ) ) ;
#9816=DIRECTION ( 'NONE',  ( -0.000000000000000000, 1.000000000000000000, -0.000000000000000000 ) ) ;
#9821=DIRECTION ( 'NONE',  ( -0.000000000000000000, 1.000000000000000000, -0.000000000000000000 ) ) ;
#9826=CARTESIAN_POINT ( 'NONE',  ( 5.656854249492380582, 20.99999999590322375, -5.656854249492380582 ) ) ;
#9836=CARTESIAN_POINT ( 'NONE',  ( -5.082755093536326818, 5.906249997951610986, 5.082755093536325042 ) ) ;
#9837=CARTESIAN_POINT ( 'NONE',  ( -8.000000000000000000, 111.6875000040967905, 0.000000000000000000 ) ) ;
#9845=ORIENTED_EDGE ( 'NONE', *, *, #24394, .T. ) ;
#9855=ORIENTED_EDGE ( 'NONE', *, *, #6114, .T. ) ;
#9863=CARTESIAN_POINT ( 'NONE',  ( 1.469576158976823947E-15, 105.8750000000000000, 8.000000000000000000 ) ) ;
#9866=EDGE_LOOP ( 'NONE', ( #69993, #21675, #57527, #43714, #25649 ) ) ;
#9867=CARTESIAN_POINT ( 'NONE',  ( 7.999999999999998224, 19.40625000000000355, 3.313708498984766049 ) ) ;
#9870=CARTESIAN_POINT ( 'NONE',  ( -1.469576158976823947E-15, 20.43749999590322375, 8.000000000000000000 ) ) ;
#9871=( BOUNDED_CURVE ( )  B_SPLINE_CURVE ( 2, ( #39785, #44711, #61319, #26602, #27345, #50361, #21685, #3990, #49624 ),
 .UNSPECIFIED., .F., .F. ) 
 B_SPLINE_CURVE_WITH_KNOTS ( ( 3, 2, 2, 2, 3 ),
 ( 0.7395833333333334814, 0.7447916666666667407, 0.7500000000000001110, 0.7552083333333334814, 0.7604166666666667407 ),
 .UNSPECIFIED. ) 
 CURVE ( )  GEOMETRIC_REPRESENTATION_ITEM ( )  RATIONAL_B_SPLINE_CURVE ( ( 0.9999999999999983347, 0.9238795325112884038, 1.000000000000000000, 0.9238795325112867385, 1.000000000000000000, 0.9238795325112867385, 1.000000000000000000, 0.9238795325112850731, 1.000000000000001554 ) ) 
 REPRESENTATION_ITEM ( '' )  );
#9873=CARTESIAN_POINT ( 'NONE',  ( 7.188101187500002709, 119.1875000020483952, 2.977408999572649151 ) ) ;
#9892=CARTESIAN_POINT ( 'NONE',  ( 7.188101187500002709, 117.3125000020483952, 2.977408999572649151 ) ) ;
#9897=CARTESIAN_POINT ( 'NONE',  ( -7.188101187499999156, 120.1250000020483952, 2.977408999572654924 ) ) ;
#9919=B_SPLINE_CURVE_WITH_KNOTS ( 'NONE', 1,
 ( #67932, #39263 ),
 .UNSPECIFIED., .F., .F.,
 ( 2, 2 ),
 ( 0.000000000000000000, 1.000000000000000000 ),
 .UNSPECIFIED. ) ;
#9920=CARTESIAN_POINT ( 'NONE',  ( -2.977408999572650039, 20.43749999795161187, -7.188101187500001821 ) ) ;
#9923=CARTESIAN_POINT ( 'NONE',  ( 4.401442555609581635E-16, 17.71874999795161187, -7.188101187500000044 ) ) ;
#9928=CARTESIAN_POINT ( 'NONE',  ( 0.000000000000000000, 125.0000000000000000, 8.000000000000000000 ) ) ;
#9950=CARTESIAN_POINT ( 'NONE',  ( -8.000000000000000000, 123.5000000000000000, 0.000000000000000000 ) ) ;
#9954=CARTESIAN_POINT ( 'NONE',  ( 4.898587196589412829E-16, 9.187499995903221972, -8.000000000000000000 ) ) ;
#9969=DIRECTION ( 'NONE',  ( -0.000000000000000000, 1.000000000000000000, -0.000000000000000000 ) ) ;
#9981=CARTESIAN_POINT ( 'NONE',  ( 2.977408999572654480, 102.1250000020483810, 7.188101187499999156 ) ) ;
#10009=CARTESIAN_POINT ( 'NONE',  ( 7.188101187500000044, 15.84374999795161365, 0.000000000000000000 ) ) ;
#10018=CARTESIAN_POINT ( 'NONE',  ( 5.082755093536324154, 4.781249997951610986, 5.082755093536326818 ) ) ;
#10021=CARTESIAN_POINT ( 'NONE',  ( -5.082755093536326818, 1.781249997951610098, 5.082755093536325042 ) ) ;
#10032=CARTESIAN_POINT ( 'NONE',  ( -1.469576158976823947E-15, 23.62500000000000355, 8.000000000000000000 ) ) ;
#10034=CARTESIAN_POINT ( 'NONE',  ( 7.188101187500000044, 9.468749997951610098, 0.000000000000000000 ) ) ;
#10039=CARTESIAN_POINT ( 'NONE',  ( -4.401442555609581635E-16, 115.1562500020483810, -7.188101187500000044 ) ) ;
#10042=CARTESIAN_POINT ( 'NONE',  ( -4.898587196589412829E-16, 105.1250000000000000, -8.000000000000000000 ) ) ;
#10043=ORIENTED_EDGE ( 'NONE', *, *, #10370, .F. ) ;
#10053=CARTESIAN_POINT ( 'NONE',  ( -5.656854249492380582, 94.81250000000000000, -5.656854249492380582 ) ) ;
#10068=CARTESIAN_POINT ( 'NONE',  ( -7.188101187499999156, 119.7500000020483810, 2.977408999572654924 ) ) ;
#10073=DIRECTION ( 'NONE',  ( -0.000000000000000000, 1.000000000000000000, -0.000000000000000000 ) ) ;
#10077=CARTESIAN_POINT ( 'NONE',  ( 4.401442555609581635E-16, 18.84374999795161187, -7.188101187500000044 ) ) ;
#10078=CARTESIAN_POINT ( 'NONE',  ( -5.656854249492380582, 108.5000000040967763, -5.656854249492380582 ) ) ;
#10100=ORIENTED_EDGE ( 'NONE', *, *, #67238, .T. ) ;
#10102=LINE ( 'NONE', #4822, #24347 ) ;
#10112=CARTESIAN_POINT ( 'NONE',  ( -1.469576158976823947E-15, 14.62500000000000178, 8.000000000000000000 ) ) ;
#10114=CARTESIAN_POINT ( 'NONE',  ( 1.469576158976823947E-15, 94.06250000409677625, 8.000000000000000000 ) ) ;
#10116=AXIS2_PLACEMENT_3D ( 'NONE', #43125, #50282, #14071 ) ;
#10124=CARTESIAN_POINT ( 'NONE',  ( -7.188101187499999156, 91.25000000204838102, 2.977408999572654924 ) ) ;
#10132=ORIENTED_EDGE ( 'NONE', *, *, #29784, .F. ) ;
#10146=CARTESIAN_POINT ( 'NONE',  ( -5.656854249492379694, 6.374999995903221084, -5.656854249492380582 ) ) ;
#10150=CARTESIAN_POINT ( 'NONE',  ( -7.188101187500000044, 18.09374999795161187, -8.802885111219163269E-16 ) ) ;
#10152=CARTESIAN_POINT ( 'NONE',  ( -8.000000000000000000, 105.5000000000000000, 0.000000000000000000 ) ) ;
#10153=CARTESIAN_POINT ( 'NONE',  ( 1.320432766682874540E-15, 105.4062500020483810, 7.188101187500000044 ) ) ;
#10163=ORIENTED_EDGE ( 'NONE', *, *, #19393, .F. ) ;
#10172=CARTESIAN_POINT ( 'NONE',  ( -2.977408999572650927, 99.87500000204838102, -7.188101187500000933 ) ) ;
#10179=CARTESIAN_POINT ( 'NONE',  ( -5.082755093536325930, 103.3437500020483668, -5.082755093536325930 ) ) ;
#10180=AXIS2_PLACEMENT_3D ( 'NONE', #41567, #35913, #42292 ) ;
#10183=( BOUNDED_CURVE ( )  B_SPLINE_CURVE ( 2, ( #7389, #1006, #70027, #12662, #1375, #65079, #53781, #30760, #1737 ),
 .UNSPECIFIED., .F., .F. ) 
 B_SPLINE_CURVE_WITH_KNOTS ( ( 3, 2, 2, 2, 3 ),
 ( 0.4270833333333332593, 0.4322916666666666297, 0.4374999999999998890, 0.4427083333333332038, 0.4479166666666665741 ),
 .UNSPECIFIED. ) 
 CURVE ( )  GEOMETRIC_REPRESENTATION_ITEM ( )  RATIONAL_B_SPLINE_CURVE ( ( 1.000000000000000888, 0.9238795325112859613, 1.000000000000000000, 0.9238795325112867385, 1.000000000000000000, 0.9238795325112867385, 1.000000000000000000, 0.9238795325112884038, 0.9999999999999983347 ) ) 
 REPRESENTATION_ITEM ( '' )  );
#10203=ORIENTED_EDGE ( 'NONE', *, *, #57385, .F. ) ;
#10206=CARTESIAN_POINT ( 'NONE',  ( -2.977408999572650039, 6.937499997951610986, -7.188101187500001821 ) ) ;
#10207=CARTESIAN_POINT ( 'NONE',  ( 5.656854249492381470, 110.7500000040967763, 5.656854249492379694 ) ) ;
#10233=CARTESIAN_POINT ( 'NONE',  ( 8.000000000000000000, 107.8437500000000000, -3.313708498984762496 ) ) ;
#10240=CARTESIAN_POINT ( 'NONE',  ( 7.999999999999998224, 26.71874999590322375, 3.313708498984766493 ) ) ;
#10242=CARTESIAN_POINT ( 'NONE',  ( 7.188101187500000044, 120.7812500020483810, -8.802885111219163269E-16 ) ) ;
#10264=CARTESIAN_POINT ( 'NONE',  ( -7.188101187500000933, 115.0625000020483810, -2.977408999572650483 ) ) ;
#10268=EDGE_CURVE ( 'NONE', #52001, #60988, #20065, .T. ) ;
#10270=CARTESIAN_POINT ( 'NONE',  ( 7.188101187500002709, 123.6875000020484094, 2.977408999572649151 ) ) ;
#10279=LINE ( 'NONE', #56683, #21259 ) ;
#10281=ADVANCED_FACE ( 'NONE', ( #72129 ), #2735, .T. ) ;
#10294=VERTEX_POINT ( 'NONE', #20443 ) ;
#10295=CARTESIAN_POINT ( 'NONE',  ( 7.188101187499999156, 27.37499999795161187, 2.977408999572654924 ) ) ;
#10298=CARTESIAN_POINT ( 'NONE',  ( -2.977408999572654480, 18.37499999795161187, 7.188101187499999156 ) ) ;
#10312=ORIENTED_EDGE ( 'NONE', *, *, #23603, .T. ) ;
#10320=EDGE_CURVE ( 'NONE', #69933, #73724, #43459, .T. ) ;
#10321=CARTESIAN_POINT ( 'NONE',  ( -5.656854249492380582, 123.3125000000000000, -5.656854249492380582 ) ) ;
#10346=DIRECTION ( 'NONE',  ( 0.000000000000000000, 0.000000000000000000, 1.000000000000000000 ) ) ;
#10348=FACE_OUTER_BOUND ( 'NONE', #47276, .T. ) ;
#10352=CARTESIAN_POINT ( 'NONE',  ( 7.188101187500000044, 105.4062500020483810, -8.802885111219163269E-16 ) ) ;
#10369=CARTESIAN_POINT ( 'NONE',  ( 8.000000000000001776, 116.8437500040967905, 3.313708498984759387 ) ) ;
#10370=EDGE_CURVE ( 'NONE', #66034, #29121, #62166, .T. ) ;
#10378=CARTESIAN_POINT ( 'NONE',  ( -1.320432766682874540E-15, 19.96874999795161543, 7.188101187500000044 ) ) ;
#10386=CARTESIAN_POINT ( 'NONE',  ( 5.082755093536325930, 11.15624999795161187, -5.082755093536325930 ) ) ;
#10398=ORIENTED_EDGE ( 'NONE', *, *, #71055, .T. ) ;
#10403=CARTESIAN_POINT ( 'NONE',  ( -3.313708498984805573, 22.03125000000000000, 7.999999999999956479 ) ) ;
#10405=CARTESIAN_POINT ( 'NONE',  ( -7.188101187500002709, 11.81249999795161187, 2.977408999572649151 ) ) ;
#10408=CARTESIAN_POINT ( 'NONE',  ( -2.977408999572651815, 103.8125000020483952, 7.188101187500000933 ) ) ;
#10424=CARTESIAN_POINT ( 'NONE',  ( -4.898587196589412829E-16, 90.12500000000000000, -8.000000000000000000 ) ) ;
#10426=CARTESIAN_POINT ( 'NONE',  ( 8.000000000000000000, 98.74999999999998579, -9.797174393178825657E-16 ) ) ;
#10438=CARTESIAN_POINT ( 'NONE',  ( 5.082755093536326818, 120.2187500020483952, 5.082755093536325042 ) ) ;
#10447=CARTESIAN_POINT ( 'NONE',  ( 2.977408999572651815, 18.18749999795161187, 7.188101187500000933 ) ) ;
#10464=CARTESIAN_POINT ( 'NONE',  ( 5.656854249492379694, 115.4375000000000000, -5.656854249492380582 ) ) ;
#10482=CARTESIAN_POINT ( 'NONE',  ( -8.000000000000001776, 12.84375000000000178, 3.313708498984759387 ) ) ;
#10486=CARTESIAN_POINT ( 'NONE',  ( -8.000000000000000000, 90.68750000409677625, 0.000000000000000000 ) ) ;
#10501=( BOUNDED_CURVE ( )  B_SPLINE_CURVE ( 2, ( #31333, #43774, #48678, #20005, #15092 ),
 .UNSPECIFIED., .F., .F. ) 
 B_SPLINE_CURVE_WITH_KNOTS ( ( 3, 2, 3 ),
 ( 0.000000000000000000, 0.006944444444444445794, 0.01388888888888889159 ),
 .UNSPECIFIED. ) 
 CURVE ( )  GEOMETRIC_REPRESENTATION_ITEM ( )  RATIONAL_B_SPLINE_CURVE ( ( 1.000000000000000000, 0.9238795325112867385, 1.000000000000000000, 0.9238795325112867385, 1.000000000000000000 ) ) 
 REPRESENTATION_ITEM ( '' )  );
#10519=CARTESIAN_POINT ( 'NONE',  ( 8.000000000000000000, 8.906249995903221972, -3.313708498984761608 ) ) ;
#10522=CARTESIAN_POINT ( 'NONE',  ( 7.188101187500001821, 20.43749999795161187, -2.977408999572650483 ) ) ;
#10525=CARTESIAN_POINT ( 'NONE',  ( 2.977408999572654480, 107.0000000020483810, 7.188101187499999156 ) ) ;
#10543=CARTESIAN_POINT ( 'NONE',  ( 5.082755093536325042, 96.59375000204838102, -5.082755093536325930 ) ) ;
#10550=CARTESIAN_POINT ( 'NONE',  ( 7.188101187500001821, 104.3750000020483952, -2.977408999572651371 ) ) ;
#10559=CARTESIAN_POINT ( 'NONE',  ( 8.000000000000000000, 16.50000000000000355, 0.000000000000000000 ) ) ;
#10573=EDGE_LOOP ( 'NONE', ( #24785, #31253, #44161, #14218 ) ) ;
#10575=CARTESIAN_POINT ( 'NONE',  ( 7.188101187500001821, 12.56249999795161365, -2.977408999572650483 ) ) ;
#10576=CARTESIAN_POINT ( 'NONE',  ( -3.313708498984762496, 108.9687500040967905, 7.999999999999998224 ) ) ;
#10579=ADVANCED_FACE ( 'NONE', ( #2859 ), #30055, .T. ) ;
#10586=CARTESIAN_POINT ( 'NONE',  ( -7.188101187499999156, 107.7500000020483810, 2.977408999572654924 ) ) ;
#10602=CARTESIAN_POINT ( 'NONE',  ( -8.000000000000000000, 111.5000000000000000, 0.000000000000000000 ) ) ;
#10605=CARTESIAN_POINT ( 'NONE',  ( 3.313708498984765161, 104.4687500000000000, 7.999999999999998224 ) ) ;
#10610=CARTESIAN_POINT ( 'NONE',  ( -8.000000000000000000, 97.90625000000000000, -3.313708498984761164 ) ) ;
#10612=CARTESIAN_POINT ( 'NONE',  ( -1.469576158976823947E-15, 24.93749999590322375, 8.000000000000000000 ) ) ;
#10614=CARTESIAN_POINT ( 'NONE',  ( 5.082755093536325042, 122.4687500020483952, -5.082755093536325930 ) ) ;
#10634=CARTESIAN_POINT ( 'NONE',  ( -7.188101187499999156, 112.2500000020483952, 2.977408999572654924 ) ) ;
#10639=CARTESIAN_POINT ( 'NONE',  ( -5.082755093536325930, 122.8437500020483952, -5.082755093536325930 ) ) ;
#10648=CARTESIAN_POINT ( 'NONE',  ( -3.313708498984719864, 18.46875000000000000, -8.000000000000040856 ) ) ;
#10651=ORIENTED_EDGE ( 'NONE', *, *, #4462, .T. ) ;
#10654=CYLINDRICAL_SURFACE ( 'NONE', #54450, 8.000000000000000000 ) ;
#10657=EDGE_LOOP ( 'NONE', ( #24976, #10203, #43677, #26538 ) ) ;
#10661=CARTESIAN_POINT ( 'NONE',  ( -3.313708498984765161, 1.031250000000000000, 7.999999999999998224 ) ) ;
#10662=CARTESIAN_POINT ( 'NONE',  ( -3.313708498984681672, 110.4687500040967763, 8.000000000000078160 ) ) ;
#10665=CARTESIAN_POINT ( 'NONE',  ( -7.188101187500002709, 25.68749999795162253, 2.977408999572649151 ) ) ;
#10667=AXIS2_PLACEMENT_3D ( 'NONE', #28619, #68985, #51632 ) ;
#10677=LINE ( 'NONE', #17070, #35704 ) ;
#10681=ORIENTED_EDGE ( 'NONE', *, *, #31191, .T. ) ;
#10682=CARTESIAN_POINT ( 'NONE',  ( 1.469576158976823947E-15, 104.5625000040967763, 8.000000000000000000 ) ) ;
#10689=CARTESIAN_POINT ( 'NONE',  ( -5.656854249492380582, 124.8125000000000000, -5.656854249492380582 ) ) ;
#10698=CARTESIAN_POINT ( 'NONE',  ( 3.313708498984720308, 13.59374999590322552, -8.000000000000040856 ) ) ;
#10712=DIRECTION ( 'NONE',  ( 0.000000000000000000, 0.000000000000000000, 1.000000000000000000 ) ) ;
#10713=DIRECTION ( 'NONE',  ( -0.000000000000000000, 1.000000000000000000, -0.000000000000000000 ) ) ;
#10715=( BOUNDED_CURVE ( )  B_SPLINE_CURVE ( 2, ( #29633, #23224, #17562, #982, #6993, #46972, #5512, #23594, #47343 ),
 .UNSPECIFIED., .F., .F. ) 
 B_SPLINE_CURVE_WITH_KNOTS ( ( 3, 2, 2, 2, 3 ),
 ( 0.1562500000000001110, 0.1614583333333334536, 0.1666666666666667407, 0.1718750000000000833, 0.1770833333333334259 ),
 .UNSPECIFIED. ) 
 CURVE ( )  GEOMETRIC_REPRESENTATION_ITEM ( )  RATIONAL_B_SPLINE_CURVE ( ( 0.9999999999999983347, 0.9238795325112884038, 1.000000000000000000, 0.9238795325112867385, 1.000000000000000000, 0.9238795325112867385, 1.000000000000000000, 0.9238795325112855172, 1.000000000000001110 ) ) 
 REPRESENTATION_ITEM ( '' )  );
#10718=CARTESIAN_POINT ( 'NONE',  ( 7.188101187500001821, 104.0000000020483810, -2.977408999572651371 ) ) ;
#10721=CARTESIAN_POINT ( 'NONE',  ( 7.692636802427458953, 0.1926368024274620616, -0.5153151192473633957 ) ) ;
#10733=FACE_OUTER_BOUND ( 'NONE', #48043, .T. ) ;
#10739=( BOUNDED_CURVE ( )  B_SPLINE_CURVE ( 2, ( #41696, #1354, #1720, #30010, #42053, #65060, #986, #13371, #620 ),
 .UNSPECIFIED., .F., .F. ) 
 B_SPLINE_CURVE_WITH_KNOTS ( ( 3, 2, 2, 2, 3 ),
 ( 0.3854166666666665741, 0.3906249999999998890, 0.3958333333333332038, 0.4010416666666665741, 0.4062499999999998890 ),
 .UNSPECIFIED. ) 
 CURVE ( )  GEOMETRIC_REPRESENTATION_ITEM ( )  RATIONAL_B_SPLINE_CURVE ( ( 1.000000000000001554, 0.9238795325112850731, 1.000000000000000000, 0.9238795325112867385, 1.000000000000000000, 0.9238795325112867385, 1.000000000000000000, 0.9238795325112884038, 0.9999999999999983347 ) ) 
 REPRESENTATION_ITEM ( '' )  );
#10744=CARTESIAN_POINT ( 'NONE',  ( 5.082755093536324154, 23.15624999795161543, 5.082755093536326818 ) ) ;
#10753=CARTESIAN_POINT ( 'NONE',  ( 7.188101187499999156, 10.87499999795161187, 2.977408999572654924 ) ) ;
#10768=EDGE_CURVE ( 'NONE', #50397, #35571, #4729, .T. ) ;
#10771=CARTESIAN_POINT ( 'NONE',  ( 5.082755093536324154, 16.78124999795161543, 5.082755093536326818 ) ) ;
#10775=CARTESIAN_POINT ( 'NONE',  ( -5.082755093536325930, 107.8437500020483810, -5.082755093536325930 ) ) ;
#10795=CARTESIAN_POINT ( 'NONE',  ( -5.656854249492381470, 5.437500000000000888, 5.656854249492379694 ) ) ;
#10798=CARTESIAN_POINT ( 'NONE',  ( 3.313708498984711426, 118.1562500040967905, 8.000000000000053291 ) ) ;
#10801=CARTESIAN_POINT ( 'NONE',  ( -8.000000000000000000, 20.25000000000000355, -9.797174393178825657E-16 ) ) ;
#10808=CARTESIAN_POINT ( 'NONE',  ( -7.188101187500000044, 121.1562500020483810, 0.000000000000000000 ) ) ;
#10812=CARTESIAN_POINT ( 'NONE',  ( -5.656854249492379694, 12.56250000000000178, -5.656854249492380582 ) ) ;
#10814=ORIENTED_EDGE ( 'NONE', *, *, #35420, .T. ) ;
#10815=DIRECTION ( 'NONE',  ( -0.000000000000000000, 1.000000000000000000, -0.000000000000000000 ) ) ;
#10816=CARTESIAN_POINT ( 'NONE',  ( 7.188101187500000044, 25.96874999795161543, 0.000000000000000000 ) ) ;
#10831=CARTESIAN_POINT ( 'NONE',  ( -5.656854249492379694, 27.37499999590322375, -5.656854249492380582 ) ) ;
#10834=CARTESIAN_POINT ( 'NONE',  ( -1.469576158976823947E-15, 4.125000000000000888, 8.000000000000000000 ) ) ;
#10838=CARTESIAN_POINT ( 'NONE',  ( -7.188101187500000933, 4.499999997951610098, -2.977408999572651371 ) ) ;
#10844=CARTESIAN_POINT ( 'NONE',  ( -4.898587196589412829E-16, 115.8125000040967763, -8.000000000000000000 ) ) ;
#10854=CARTESIAN_POINT ( 'NONE',  ( -3.313708498984760720, 15.46875000000000533, -8.000000000000000000 ) ) ;
#10856=CARTESIAN_POINT ( 'NONE',  ( -3.313708498984762052, 91.90625000409677625, -8.000000000000000000 ) ) ;
#10859=ADVANCED_FACE ( 'NONE', ( #13156 ), #64119, .T. ) ;
#10862=VERTEX_POINT ( 'NONE', #58473 ) ;
#10873=CARTESIAN_POINT ( 'NONE',  ( 9.797174393178825657E-16, 125.0000000000000000, -8.000000000000000000 ) ) ;
#10880=EDGE_CURVE ( 'NONE', #34923, #24630, #47127, .T. ) ;
#10893=CARTESIAN_POINT ( 'NONE',  ( 8.000000000000000000, 11.81249999590322197, 0.000000000000000000 ) ) ;
#10896=CARTESIAN_POINT ( 'NONE',  ( -7.188101187500002709, 16.68749999795161543, 2.977408999572649151 ) ) ;
#10899=CARTESIAN_POINT ( 'NONE',  ( 7.188101187500000933, 101.3750000020483952, -2.977408999572651371 ) ) ;
#10908=VERTEX_POINT ( 'NONE', #54661 ) ;
#10914=CARTESIAN_POINT ( 'NONE',  ( -4.850062511589670794E-16, 124.5792468245269475, -7.920753175473082663 ) ) ;
#10916=CARTESIAN_POINT ( 'NONE',  ( -5.082755093536324154, 94.34375000204838102, 5.082755093536326818 ) ) ;
#10922=CARTESIAN_POINT ( 'NONE',  ( 1.320432766682874540E-15, 100.9062500020483810, 7.188101187500000044 ) ) ;
#10931=CARTESIAN_POINT ( 'NONE',  ( 5.656854249492378806, 16.31250000000000355, 5.656854249492381470 ) ) ;
#10936=CARTESIAN_POINT ( 'NONE',  ( -1.469576158976823947E-15, 8.625000000000000000, 8.000000000000000000 ) ) ;
#10950=CARTESIAN_POINT ( 'NONE',  ( -2.977408999572654480, 13.49999999795161187, 7.188101187499999156 ) ) ;
#10951=CARTESIAN_POINT ( 'NONE',  ( -5.656854249492380582, 110.0000000040967763, -5.656854249492380582 ) ) ;
#10962=CARTESIAN_POINT ( 'NONE',  ( 2.977408999572650039, 102.6875000020483810, -7.188101187500001821 ) ) ;
#10971=CARTESIAN_POINT ( 'NONE',  ( 5.656854249492381470, 91.25000000409677625, 5.656854249492379694 ) ) ;
#10978=CARTESIAN_POINT ( 'NONE',  ( -8.000000000000000000, 108.5000000000000000, 0.000000000000000000 ) ) ;
#10984=CARTESIAN_POINT ( 'NONE',  ( 5.656854249492380582, 26.99999999590322375, -5.656854249492380582 ) ) ;
#10985=AXIS2_PLACEMENT_3D ( 'NONE', #73653, #61959, #39330 ) ;
#10987=CARTESIAN_POINT ( 'NONE',  ( -7.188101187499999156, 120.1250000020484094, 2.977408999572654924 ) ) ;
#11008=CARTESIAN_POINT ( 'NONE',  ( 7.188101187500002709, 114.3125000020483668, 2.977408999572649151 ) ) ;
#11015=CARTESIAN_POINT ( 'NONE',  ( -2.977408999572651815, 120.3125000020483668, 7.188101187500000933 ) ) ;
#11019=VERTEX_POINT ( 'NONE', #71610 ) ;
#11039=EDGE_LOOP ( 'NONE', ( #6708, #38418, #46396, #73797 ) ) ;
#11040=CARTESIAN_POINT ( 'NONE',  ( 8.000000000000000000, -1.084202172485504434E-16, 0.000000000000000000 ) ) ;
#11041=CARTESIAN_POINT ( 'NONE',  ( -7.999999999999998224, 107.0937500000000142, 3.313708498984766049 ) ) ;
#11044=CARTESIAN_POINT ( 'NONE',  ( -5.082755093536326818, 21.28124999795161543, 5.082755093536325042 ) ) ;
#11052=VECTOR ( 'NONE', #10073, 1000.000000000000000 ) ;
#11070=CARTESIAN_POINT ( 'NONE',  ( 7.188101187500002709, 90.68750000204838102, 2.977408999572649151 ) ) ;
#11097=EDGE_CURVE ( 'NONE', #45475, #31249, #45564, .T. ) ;
#11101=CARTESIAN_POINT ( 'NONE',  ( 7.188101187500001821, 102.5000000020483810, -2.977408999572651371 ) ) ;
#11113=CARTESIAN_POINT ( 'NONE',  ( -5.656854249492381470, 0.9375000000000001110, 5.656854249492379694 ) ) ;
#11121=CARTESIAN_POINT ( 'NONE',  ( 8.000000000000000000, 106.5312500040968189, -3.313708498984762496 ) ) ;
#11122=AXIS2_PLACEMENT_3D ( 'NONE', #70666, #64642, #8686 ) ;
#11126=CARTESIAN_POINT ( 'NONE',  ( 7.188101187500000933, 21.93749999795161187, -2.977408999572650483 ) ) ;
#11134=CARTESIAN_POINT ( 'NONE',  ( 4.401442555609581635E-16, 8.343749997951611874, -7.188101187500000044 ) ) ;
#11138=CARTESIAN_POINT ( 'NONE',  ( -7.188101187500001821, 7.499999997951610986, -2.977408999572651371 ) ) ;
#11151=CARTESIAN_POINT ( 'NONE',  ( -1.320432766682874540E-15, 19.59374999795161543, 7.188101187500000044 ) ) ;
#11155=CARTESIAN_POINT ( 'NONE',  ( -4.401442555609581635E-16, 109.1562500020483810, -7.188101187500000044 ) ) ;
#11161=ORIENTED_EDGE ( 'NONE', *, *, #56540, .F. ) ;
#11185=CARTESIAN_POINT ( 'NONE',  ( 2.977408999572650039, 119.1875000020483810, -7.188101187500001821 ) ) ;
#11192=CARTESIAN_POINT ( 'NONE',  ( -5.082755093536326818, 25.40624999795161543, 5.082755093536325042 ) ) ;
#11207=CARTESIAN_POINT ( 'NONE',  ( -8.000000000000000000, 27.46874999590322375, -3.313708498984762496 ) ) ;
#11214=CARTESIAN_POINT ( 'NONE',  ( -5.082755093536326818, 7.781249997951610986, 5.082755093536325042 ) ) ;
#11219=CARTESIAN_POINT ( 'NONE',  ( 5.656854249492381470, 115.2500000040967905, 5.656854249492379694 ) ) ;
#11231=CARTESIAN_POINT ( 'NONE',  ( 4.898587196589412829E-16, 18.37500000000000355, -8.000000000000000000 ) ) ;
#11232=ORIENTED_EDGE ( 'NONE', *, *, #16301, .T. ) ;
#11233=VECTOR ( 'NONE', #65661, 1000.000000000000000 ) ;
#11234=CARTESIAN_POINT ( 'NONE',  ( 5.082755093536325042, 120.5937500020483952, -5.082755093536325930 ) ) ;
#11241=CARTESIAN_POINT ( 'NONE',  ( 5.082755093536325930, 2.156249997951610098, -5.082755093536325930 ) ) ;
#11243=CARTESIAN_POINT ( 'NONE',  ( -7.188101187500000044, 123.0312500020483810, 0.000000000000000000 ) ) ;
#11254=ORIENTED_EDGE ( 'NONE', *, *, #55753, .T. ) ;
#11263=CARTESIAN_POINT ( 'NONE',  ( -3.313708498984654138, 114.7812500000000142, 8.000000000000106581 ) ) ;
#11264=CARTESIAN_POINT ( 'NONE',  ( 5.656854249492379694, 101.9375000000000000, -5.656854249492380582 ) ) ;
#11268=CARTESIAN_POINT ( 'NONE',  ( 5.082755093536325930, 19.03124999795161543, -5.082755093536325930 ) ) ;
#11270=CARTESIAN_POINT ( 'NONE',  ( 0.000000000000000000, 125.0000000000000000, 0.000000000000000000 ) ) ;
#11271=CARTESIAN_POINT ( 'NONE',  ( -2.977408999572652260, 102.3125000020483952, 7.188101187500000044 ) ) ;
#11278=( BOUNDED_CURVE ( )  B_SPLINE_CURVE ( 2, ( #68306, #72856, #55887, #22642, #39641, #62638, #10971, #21161, #34006 ),
 .UNSPECIFIED., .F., .F. ) 
 B_SPLINE_CURVE_WITH_KNOTS ( ( 3, 2, 2, 2, 3 ),
 ( 0.8854166666666669627, 0.8906250000000003331, 0.8958333333333337034, 0.9010416666666668517, 0.9062500000000002220 ),
 .UNSPECIFIED. ) 
 CURVE ( )  GEOMETRIC_REPRESENTATION_ITEM ( )  RATIONAL_B_SPLINE_CURVE ( ( 0.9999999999999951150, 0.9238795325112916235, 1.000000000000000000, 0.9238795325112867385, 1.000000000000000000, 0.9238795325112867385, 1.000000000000000000, 0.9238795325112835188, 1.000000000000003331 ) ) 
 REPRESENTATION_ITEM ( '' )  );
#11283=AXIS2_PLACEMENT_3D ( 'NONE', #66368, #60713, #15798 ) ;
#11289=CARTESIAN_POINT ( 'NONE',  ( -7.188101187500000044, 92.65625000204838102, 0.000000000000000000 ) ) ;
#11296=CARTESIAN_POINT ( 'NONE',  ( -7.188101187499999156, 96.12500000204836681, 2.977408999572654924 ) ) ;
#11306=LINE ( 'NONE', #41091, #67623 ) ;
#11312=VERTEX_POINT ( 'NONE', #68951 ) ;
#11314=VECTOR ( 'NONE', #73304, 1000.000000000000000 ) ;
#11321=CARTESIAN_POINT ( 'NONE',  ( -5.082755093536326818, 11.90624999795161010, 5.082755093536325042 ) ) ;
#11322=CARTESIAN_POINT ( 'NONE',  ( 8.000000000000000000, 112.5312500040967905, -3.313708498984762496 ) ) ;
#11331=CARTESIAN_POINT ( 'NONE',  ( -7.188101187500001821, 104.5625000020483668, -2.977408999572650483 ) ) ;
#11345=EDGE_CURVE ( 'NONE', #832, #66991, #63281, .T. ) ;
#11347=CARTESIAN_POINT ( 'NONE',  ( -8.000000000000000000, 104.0000000000000000, 0.000000000000000000 ) ) ;
#11353=CARTESIAN_POINT ( 'NONE',  ( 3.313708498984762052, 24.09374999590322020, -8.000000000000000000 ) ) ;
#11355=CARTESIAN_POINT ( 'NONE',  ( -5.082755093536325930, 124.3437500020483952, -5.082755093536325930 ) ) ;
#11363=CARTESIAN_POINT ( 'NONE',  ( 8.000000000000000000, 122.8437500000000000, -3.313708498984762496 ) ) ;
#11367=CARTESIAN_POINT ( 'NONE',  ( -1.469576158976823947E-15, 26.43749999590322375, 8.000000000000000000 ) ) ;
#11375=CARTESIAN_POINT ( 'NONE',  ( 8.000000000000000000, 7.312499995903221084, 0.000000000000000000 ) ) ;
#11376=CARTESIAN_POINT ( 'NONE',  ( -5.082755093536325930, 110.4687500020483810, -5.082755093536325930 ) ) ;
#11381=CARTESIAN_POINT ( 'NONE',  ( -2.977408999572650927, 116.7500000020483810, -7.188101187500001821 ) ) ;
#11382=CARTESIAN_POINT ( 'NONE',  ( -3.313708498984744732, 14.34374999590322552, 8.000000000000019540 ) ) ;
#11407=CARTESIAN_POINT ( 'NONE',  ( -7.188101187500000044, 25.21874999795161543, -8.802885111219163269E-16 ) ) ;
#11410=CARTESIAN_POINT ( 'NONE',  ( 4.401442555609581635E-16, 25.21874999795161543, -7.188101187500000044 ) ) ;
#11418=ORIENTED_EDGE ( 'NONE', *, *, #2410, .F. ) ;
#11422=DIRECTION ( 'NONE',  ( 0.000000000000000000, 0.000000000000000000, 1.000000000000000000 ) ) ;
#11427=DIRECTION ( 'NONE',  ( 0.000000000000000000, 0.000000000000000000, 1.000000000000000000 ) ) ;
#11435=CARTESIAN_POINT ( 'NONE',  ( 5.656854249492381470, 122.5625000000000000, 5.656854249492379694 ) ) ;
#11443=CARTESIAN_POINT ( 'NONE',  ( 3.313708498984761608, 6.093749995903221084, -8.000000000000000000 ) ) ;
#11456=ORIENTED_EDGE ( 'NONE', *, *, #26854, .T. ) ;
#11463=CARTESIAN_POINT ( 'NONE',  ( 0.000000000000000000, 125.0000000000000000, 0.000000000000000000 ) ) ;
#11469=CARTESIAN_POINT ( 'NONE',  ( 7.188101187500001821, 105.5000000020483810, -2.977408999572651371 ) ) ;
#11478=LINE ( 'NONE', #57887, #33948 ) ;
#11486=CARTESIAN_POINT ( 'NONE',  ( -8.000000000000000000, 100.9062500000000000, -3.313708498984761164 ) ) ;
#11492=CARTESIAN_POINT ( 'NONE',  ( -2.977408999572650039, 23.81249999795161543, -7.188101187500000933 ) ) ;
#11493=( BOUNDED_CURVE ( )  B_SPLINE_CURVE ( 1, ( #37807, #25710 ),
 .UNSPECIFIED., .F., .F. ) 
 B_SPLINE_CURVE_WITH_KNOTS ( ( 2, 2 ),
 ( 0.000000000000000000, 1.000000000000000000 ),
 .UNSPECIFIED. ) 
 CURVE ( )  GEOMETRIC_REPRESENTATION_ITEM ( )  RATIONAL_B_SPLINE_CURVE ( ( 0.9660722070829144137, 0.9660722070829144137 ) ) 
 REPRESENTATION_ITEM ( '' )  );
#11501=CARTESIAN_POINT ( 'NONE',  ( 5.082755093536324154, 7.781249997951611874, 5.082755093536326818 ) ) ;
#11504=CARTESIAN_POINT ( 'NONE',  ( 2.977408999572651815, 5.062499997951609210, 7.188101187500000933 ) ) ;
#11520=EDGE_LOOP ( 'NONE', ( #55968, #58846, #10100, #37231 ) ) ;
#11521=CARTESIAN_POINT ( 'NONE',  ( 5.082755093536325930, 15.65624999795161365, -5.082755093536325930 ) ) ;
#11524=CARTESIAN_POINT ( 'NONE',  ( -7.188101187500000044, 106.5312500020483810, 0.000000000000000000 ) ) ;
#11527=DIRECTION ( 'NONE',  ( -0.000000000000000000, 1.000000000000000000, -0.000000000000000000 ) ) ;
#11539=CARTESIAN_POINT ( 'NONE',  ( -3.313708498984762052, 90.21874999999998579, -8.000000000000000000 ) ) ;
#11549=LINE ( 'NONE', #5899, #70193 ) ;
#11551=CARTESIAN_POINT ( 'NONE',  ( 5.082755093536326818, 123.2187500020483952, 5.082755093536325042 ) ) ;
#11560=CARTESIAN_POINT ( 'NONE',  ( -7.188101187500001821, 26.62499999795161543, -2.977408999572651371 ) ) ;
#11580=CARTESIAN_POINT ( 'NONE',  ( 5.082755093536324154, 6.656249997951610986, 5.082755093536326818 ) ) ;
#11584=CARTESIAN_POINT ( 'NONE',  ( 3.313708498984763828, 123.2187500040967763, -7.999999999999996447 ) ) ;
#11585=CARTESIAN_POINT ( 'NONE',  ( 3.313708498984711426, 98.65625000409679046, 8.000000000000053291 ) ) ;
#11595=EDGE_CURVE ( 'NONE', #1389, #73500, #35384, .T. ) ;
#11597=CARTESIAN_POINT ( 'NONE',  ( 7.999999999999998224, 16.40625000000000355, 3.313708498984766493 ) ) ;
#11600=CARTESIAN_POINT ( 'NONE',  ( 5.082755093536325042, 123.5937500020483952, -5.082755093536325930 ) ) ;
#11607=CARTESIAN_POINT ( 'NONE',  ( 2.977408999572652260, 1.687499997951610098, 7.188101187500000044 ) ) ;
#11638=CARTESIAN_POINT ( 'NONE',  ( -2.977408999572650039, 25.31249999795161543, -7.188101187500001821 ) ) ;
#11640=DIRECTION ( 'NONE',  ( 0.000000000000000000, 0.000000000000000000, 1.000000000000000000 ) ) ;
#11641=CARTESIAN_POINT ( 'NONE',  ( -2.977408999572650927, 98.75000000204838102, -7.188101187500000933 ) ) ;
#11657=CARTESIAN_POINT ( 'NONE',  ( 2.977408999572654480, 94.62500000204838102, 7.188101187499999156 ) ) ;
#11662=CARTESIAN_POINT ( 'NONE',  ( -7.188101187500001821, 97.43750000204839523, -2.977408999572650483 ) ) ;
#11667=ORIENTED_EDGE ( 'NONE', *, *, #45373, .F. ) ;
#11686=CARTESIAN_POINT ( 'NONE',  ( -2.977408999572650039, 15.93749999795161543, -7.188101187500001821 ) ) ;
#11687=CARTESIAN_POINT ( 'NONE',  ( -8.000000000000000000, 104.0937500040967905, -3.313708498984761608 ) ) ;
#11697=CARTESIAN_POINT ( 'NONE',  ( -2.977408999572651815, 103.4375000020483668, 7.188101187500000933 ) ) ;
#11698=CARTESIAN_POINT ( 'NONE',  ( -5.656854249492381470, 15.74999999590322197, 5.656854249492379694 ) ) ;
#11699=ORIENTED_EDGE ( 'NONE', *, *, #44091, .F. ) ;
#11703=( BOUNDED_CURVE ( )  B_SPLINE_CURVE ( 2, ( #33276, #17009, #27971, #11363, #50975, #27588, #40035, #57398, #5706 ),
 .UNSPECIFIED., .F., .F. ) 
 B_SPLINE_CURVE_WITH_KNOTS ( ( 3, 2, 2, 2, 3 ),
 ( 0.05208333333333337034, 0.05729166666666669905, 0.06250000000000004163, 0.06770833333333337034, 0.07291666666666671293 ),
 .UNSPECIFIED. ) 
 CURVE ( )  GEOMETRIC_REPRESENTATION_ITEM ( )  RATIONAL_B_SPLINE_CURVE ( ( 0.9999999999999994449, 0.9238795325112872936, 1.000000000000000000, 0.9238795325112867385, 1.000000000000000000, 0.9238795325112867385, 1.000000000000000000, 0.9238795325112861834, 1.000000000000000666 ) ) 
 REPRESENTATION_ITEM ( '' )  );
#11704=ORIENTED_EDGE ( 'NONE', *, *, #882, .F. ) ;
#11713=CARTESIAN_POINT ( 'NONE',  ( 8.000000000000000000, 101.8437499999999858, -3.313708498984762496 ) ) ;
#11721=CARTESIAN_POINT ( 'NONE',  ( -3.313708498984760720, 24.28124999590322020, -8.000000000000000000 ) ) ;
#11724=CARTESIAN_POINT ( 'NONE',  ( -5.082755093536324154, 118.7187500020483810, 5.082755093536326818 ) ) ;
#11737=ORIENTED_EDGE ( 'NONE', *, *, #56350, .F. ) ;
#11744=DIRECTION ( 'NONE',  ( -0.000000000000000000, 1.000000000000000000, -0.000000000000000000 ) ) ;
#11746=CARTESIAN_POINT ( 'NONE',  ( 5.082755093536325042, 111.5937500020483810, -5.082755093536325930 ) ) ;
#11752=CARTESIAN_POINT ( 'NONE',  ( 2.977408999572650039, 115.0625000020483952, -7.188101187500001821 ) ) ;
#11753=CARTESIAN_POINT ( 'NONE',  ( -3.313708498984800688, 13.78124999590322552, -7.999999999999958256 ) ) ;
#11766=ORIENTED_EDGE ( 'NONE', *, *, #14207, .T. ) ;
#11775=CARTESIAN_POINT ( 'NONE',  ( -8.000000000000000000, 6.656250000000000888, -3.313708498984762496 ) ) ;
#11776=CARTESIAN_POINT ( 'NONE',  ( 1.469576158976823947E-15, 110.5625000040967905, 8.000000000000000000 ) ) ;
#11778=CARTESIAN_POINT ( 'NONE',  ( -7.188101187500002709, 24.18749999795161543, 2.977408999572649151 ) ) ;
#11779=CARTESIAN_POINT ( 'NONE',  ( 8.000000000000000000, 119.9375000040967763, -9.797174393178825657E-16 ) ) ;
#11803=CARTESIAN_POINT ( 'NONE',  ( 1.469576158976823947E-15, 116.3750000000000000, 8.000000000000000000 ) ) ;
#11837=CARTESIAN_POINT ( 'NONE',  ( 2.977408999572650039, 98.18750000204838102, -7.188101187500001821 ) ) ;
#11850=CARTESIAN_POINT ( 'NONE',  ( 4.898587196589412829E-16, 4.875000000000000888, -8.000000000000000000 ) ) ;
#11861=CARTESIAN_POINT ( 'NONE',  ( -7.188101187500002709, 25.68749999795162253, 2.977408999572649151 ) ) ;
#11869=CARTESIAN_POINT ( 'NONE',  ( 7.188101187499999156, 6.374999997951610986, 2.977408999572654924 ) ) ;
#11872=CARTESIAN_POINT ( 'NONE',  ( -1.320432766682874540E-15, 4.968749997951610986, 7.188101187500000044 ) ) ;
#11886=CARTESIAN_POINT ( 'NONE',  ( 5.082755093536326818, 118.7187500020483810, 5.082755093536325042 ) ) ;
#11890=CARTESIAN_POINT ( 'NONE',  ( 5.082755093536324154, 18.28124999795161187, 5.082755093536326818 ) ) ;
#11895=CARTESIAN_POINT ( 'NONE',  ( 5.082755093536326818, 104.0937500020483810, 5.082755093536325042 ) ) ;
#11918=ORIENTED_EDGE ( 'NONE', *, *, #29775, .T. ) ;
#11924=CARTESIAN_POINT ( 'NONE',  ( 1.320432766682874540E-15, 115.5312500020483952, 7.188101187500000044 ) ) ;
#11943=DIRECTION ( 'NONE',  ( 0.000000000000000000, 0.000000000000000000, 1.000000000000000000 ) ) ;
#11953=CARTESIAN_POINT ( 'NONE',  ( 3.313708498984873518, 114.9687500000000142, 7.999999999999890754 ) ) ;
#11957=CARTESIAN_POINT ( 'NONE',  ( 7.188101187500000044, 8.343749997951611874, 0.000000000000000000 ) ) ;
#11961=ORIENTED_EDGE ( 'NONE', *, *, #2410, .T. ) ;
#11962=CARTESIAN_POINT ( 'NONE',  ( 8.000000000000000000, 123.0312500040967905, -3.313708498984762496 ) ) ;
#11975=CARTESIAN_POINT ( 'NONE',  ( 3.313708498984762052, 15.28125000000000355, -8.000000000000000000 ) ) ;
#11977=CARTESIAN_POINT ( 'NONE',  ( 7.188101187500001821, 120.5000000020483810, -2.977408999572651371 ) ) ;
#11986=CARTESIAN_POINT ( 'NONE',  ( -5.082755093536325930, 122.8437500020483952, -5.082755093536325930 ) ) ;
#12006=CARTESIAN_POINT ( 'NONE',  ( -8.000000000000000000, 114.4062500000000000, -3.313708498984761164 ) ) ;
#12011=CARTESIAN_POINT ( 'NONE',  ( 7.188101187500000044, 23.34374999795161543, 0.000000000000000000 ) ) ;
#12013=CARTESIAN_POINT ( 'NONE',  ( -7.188101187500000044, 97.53125000204838102, 0.000000000000000000 ) ) ;
#12023=LINE ( 'NONE', #17302, #9749 ) ;
#12029=CARTESIAN_POINT ( 'NONE',  ( -5.082755093536325930, 92.46875000204838102, -5.082755093536325930 ) ) ;
#12034=CARTESIAN_POINT ( 'NONE',  ( -7.188101187499999156, 97.62500000204836681, 2.977408999572654924 ) ) ;
#12051=( BOUNDED_CURVE ( )  B_SPLINE_CURVE ( 2, ( #44114, #51255, #38084, #27123, #61833, #56186, #44483, #33189, #22574 ),
 .UNSPECIFIED., .F., .F. ) 
 B_SPLINE_CURVE_WITH_KNOTS ( ( 3, 2, 2, 2, 3 ),
 ( 0.2638888888888888951, 0.2708333333333333148, 0.2777777777777777346, 0.2847222222222221544, 0.2916666666666666297 ),
 .UNSPECIFIED. ) 
 CURVE ( )  GEOMETRIC_REPRESENTATION_ITEM ( )  RATIONAL_B_SPLINE_CURVE ( ( 1.000000000000000000, 0.9238795325112867385, 1.000000000000000000, 0.9238795325112867385, 1.000000000000000000, 0.9238795325112867385, 1.000000000000000000, 0.9238795325112872936, 0.9999999999999994449 ) ) 
 REPRESENTATION_ITEM ( '' )  );
#12057=CARTESIAN_POINT ( 'NONE',  ( 8.000000000000000000, 106.5312500040967905, -3.313708498984762496 ) ) ;
#12063=ORIENTED_EDGE ( 'NONE', *, *, #16301, .F. ) ;
#12064=CARTESIAN_POINT ( 'NONE',  ( -4.898587196589412829E-16, 112.8125000040967905, -8.000000000000000000 ) ) ;
#12065=CARTESIAN_POINT ( 'NONE',  ( -2.977408999572650927, 104.3750000020483952, -7.188101187500001821 ) ) ;
#12073=ORIENTED_EDGE ( 'NONE', *, *, #64674, .T. ) ;
#12078=FACE_OUTER_BOUND ( 'NONE', #5303, .T. ) ;
#12082=CARTESIAN_POINT ( 'NONE',  ( -3.313708498984762052, 100.7187499999999858, -8.000000000000000000 ) ) ;
#12087=CARTESIAN_POINT ( 'NONE',  ( 2.977408999572650927, 4.124999997951610986, -7.188101187500001821 ) ) ;
#12090=CARTESIAN_POINT ( 'NONE',  ( 5.082755093536325042, 117.9687500020483810, -5.082755093536325930 ) ) ;
#12094=CARTESIAN_POINT ( 'NONE',  ( -5.656854249492378806, 90.68750000000000000, 5.656854249492381470 ) ) ;
#12111=CARTESIAN_POINT ( 'NONE',  ( 5.082755093536325042, 113.0937500020483810, -5.082755093536325930 ) ) ;
#12116=CARTESIAN_POINT ( 'NONE',  ( 7.188101187500002709, 116.1875000020483952, 2.977408999572649151 ) ) ;
#12128=EDGE_CURVE ( 'NONE', #5844, #32408, #16319, .T. ) ;
#12142=CARTESIAN_POINT ( 'NONE',  ( -8.000000000000000000, 6.750000000000000888, -9.797174393178825657E-16 ) ) ;
#12143=CARTESIAN_POINT ( 'NONE',  ( -8.000000000000000000, 11.15625000000000178, -3.313708498984762496 ) ) ;
#12144=CARTESIAN_POINT ( 'NONE',  ( 5.082755093536325930, 23.53124999795161543, -5.082755093536325930 ) ) ;
#12146=CARTESIAN_POINT ( 'NONE',  ( 8.000000000000000000, 122.9375000040967905, -9.797174393178825657E-16 ) ) ;
#12163=ORIENTED_EDGE ( 'NONE', *, *, #15375, .F. ) ;
#12171=CARTESIAN_POINT ( 'NONE',  ( -4.898587196589412829E-16, 115.6250000000000000, -8.000000000000000000 ) ) ;
#12175=CARTESIAN_POINT ( 'NONE',  ( 5.656854249492378806, 16.12499999590322375, 5.656854249492381470 ) ) ;
#12177=CARTESIAN_POINT ( 'NONE',  ( 5.656854249492378806, 11.62499999590322197, 5.656854249492381470 ) ) ;
#12198=CARTESIAN_POINT ( 'NONE',  ( -7.188101187500000044, 100.1562500020483810, 0.000000000000000000 ) ) ;
#12213=CARTESIAN_POINT ( 'NONE',  ( 0.000000000000000000, 125.0000000000000000, 0.000000000000000000 ) ) ;
#12219=CARTESIAN_POINT ( 'NONE',  ( -5.656854249492380582, 112.8125000000000000, -5.656854249492380582 ) ) ;
#12224=CARTESIAN_POINT ( 'NONE',  ( 4.401442555609581635E-16, 25.21874999795161543, -7.188101187500000044 ) ) ;
#12233=CARTESIAN_POINT ( 'NONE',  ( -7.188101187500000044, 17.71874999795161187, -8.802885111219163269E-16 ) ) ;
#12236=CARTESIAN_POINT ( 'NONE',  ( -7.188101187500002709, 4.687499997951610986, 2.977408999572649151 ) ) ;
#12249=CARTESIAN_POINT ( 'NONE',  ( -4.401442555609581635E-16, 117.7812500020483810, -7.188101187500000044 ) ) ;
#12255=CARTESIAN_POINT ( 'NONE',  ( -5.082755093536325042, 19.03124999795161543, -5.082755093536325930 ) ) ;
#12260=CARTESIAN_POINT ( 'NONE',  ( 1.320432766682874540E-15, 97.90625000204839523, 7.188101187500000044 ) ) ;
#12263=CARTESIAN_POINT ( 'NONE',  ( -4.898587196589412829E-16, 111.3125000040967905, -8.000000000000000000 ) ) ;
#12270=CARTESIAN_POINT ( 'NONE',  ( -3.313708498984765161, 14.53125000000000178, 7.999999999999998224 ) ) ;
#12292=CARTESIAN_POINT ( 'NONE',  ( -7.188101187500001821, 115.0625000020483952, -2.977408999572650483 ) ) ;
#12302=CARTESIAN_POINT ( 'NONE',  ( 4.401442555609581635E-16, 23.34374999795161543, -7.188101187500000044 ) ) ;
#12313=DIRECTION ( 'NONE',  ( -0.000000000000000000, 1.000000000000000000, -0.000000000000000000 ) ) ;
#12318=ORIENTED_EDGE ( 'NONE', *, *, #61021, .F. ) ;
#12325=CARTESIAN_POINT ( 'NONE',  ( 7.188101187500000933, 5.437499997951610098, -2.977408999572650483 ) ) ;
#12329=CARTESIAN_POINT ( 'NONE',  ( 8.000000000000001776, 98.84375000409680467, 3.313708498984759387 ) ) ;
#12341=CARTESIAN_POINT ( 'NONE',  ( -8.000000000000000000, 18.75000000000000355, -9.797174393178825657E-16 ) ) ;
#12343=CARTESIAN_POINT ( 'NONE',  ( -5.082755093536324154, 119.8437500020483810, 5.082755093536326818 ) ) ;
#12352=CARTESIAN_POINT ( 'NONE',  ( 5.082755093536325042, 119.4687500020483810, -5.082755093536325930 ) ) ;
#12358=VERTEX_POINT ( 'NONE', #30368 ) ;
#12370=CARTESIAN_POINT ( 'NONE',  ( -1.469576158976823947E-15, 20.62500000000000355, 8.000000000000000000 ) ) ;
#12376=CARTESIAN_POINT ( 'NONE',  ( -7.188101187500001821, 20.99999999795161898, -2.977408999572651371 ) ) ;
#12378=CARTESIAN_POINT ( 'NONE',  ( -7.188101187500000933, 97.43750000204839523, -2.977408999572650483 ) ) ;
#12390=CARTESIAN_POINT ( 'NONE',  ( 0.000000000000000000, 125.0000000000000000, 8.000000000000000000 ) ) ;
#12395=DIRECTION ( 'NONE',  ( -0.000000000000000000, 1.000000000000000000, -0.000000000000000000 ) ) ;
#12401=CARTESIAN_POINT ( 'NONE',  ( 7.188101187500002709, 95.18750000204838102, 2.977408999572649151 ) ) ;
#12419=CARTESIAN_POINT ( 'NONE',  ( -8.000000000000001776, 3.656249995903220640, 3.313708498984759387 ) ) ;
#12421=CARTESIAN_POINT ( 'NONE',  ( 5.656854249492379694, 106.6250000040967763, -5.656854249492380582 ) ) ;
#12426=CARTESIAN_POINT ( 'NONE',  ( 0.000000000000000000, 125.0000000000000000, 0.000000000000000000 ) ) ;
#12429=CARTESIAN_POINT ( 'NONE',  ( 2.977408999572654480, 105.1250000020483668, 7.188101187499999156 ) ) ;
#12430=CARTESIAN_POINT ( 'NONE',  ( -5.656854249492378806, 92.37500000409677625, 5.656854249492381470 ) ) ;
#12434=ADVANCED_FACE ( 'NONE', ( #52643 ), #51899, .T. ) ;
#12450=CARTESIAN_POINT ( 'NONE',  ( -7.999999999999998224, 98.09375000000001421, 3.313708498984766493 ) ) ;
#12456=CARTESIAN_POINT ( 'NONE',  ( -5.082755093536326818, 3.281249997951610542, 5.082755093536325042 ) ) ;
#12459=CARTESIAN_POINT ( 'NONE',  ( -7.188101187500000933, 118.4375000020483952, -2.977408999572650483 ) ) ;
#12470=CARTESIAN_POINT ( 'NONE',  ( -8.000000000000000000, 96.40625000000000000, -3.313708498984761164 ) ) ;
#12478=CARTESIAN_POINT ( 'NONE',  ( 2.977408999572650039, 104.1875000020483810, -7.188101187500000933 ) ) ;
#12484=CARTESIAN_POINT ( 'NONE',  ( -5.082755093536324154, 115.7187500020483810, 5.082755093536326818 ) ) ;
#12487=VECTOR ( 'NONE', #59273, 1000.000000000000000 ) ;
#12509=CARTESIAN_POINT ( 'NONE',  ( -5.656854249492381470, 3.937500000000000888, 5.656854249492379694 ) ) ;
#12511=CARTESIAN_POINT ( 'NONE',  ( -5.082755093536325042, 2.531249997951610542, -5.082755093536325930 ) ) ;
#12512=CARTESIAN_POINT ( 'NONE',  ( 5.656854249492379694, 123.1250000040967905, -5.656854249492380582 ) ) ;
#12527=AXIS2_PLACEMENT_3D ( 'NONE', #37108, #60110, #25765 ) ;
#12539=CARTESIAN_POINT ( 'NONE',  ( 8.000000000000001776, 115.1562500000000000, 3.313708498984759387 ) ) ;
#12545=CARTESIAN_POINT ( 'NONE',  ( 3.313708498984762052, 15.09374999590322020, -8.000000000000000000 ) ) ;
#12547=CARTESIAN_POINT ( 'NONE',  ( 7.999999999999998224, 11.71874999590322197, 3.313708498984766049 ) ) ;
#12558=CARTESIAN_POINT ( 'NONE',  ( 4.898587196589412829E-16, 10.68749999590322020, -8.000000000000000000 ) ) ;
#12560=VECTOR ( 'NONE', #27459, 1000.000000000000000 ) ;
#12564=EDGE_CURVE ( 'NONE', #61043, #63531, #67463, .T. ) ;
#12570=CARTESIAN_POINT ( 'NONE',  ( -5.082755093536325930, 96.96875000204838102, -5.082755093536325930 ) ) ;
#12576=VERTEX_POINT ( 'NONE', #8459 ) ;
#12587=CARTESIAN_POINT ( 'NONE',  ( 4.898587196589412829E-16, 18.18749999590322020, -8.000000000000000000 ) ) ;
#12601=CARTESIAN_POINT ( 'NONE',  ( -5.082755093536326818, 17.90624999795161187, 5.082755093536325042 ) ) ;
#12604=CARTESIAN_POINT ( 'NONE',  ( -5.082755093536325042, 5.906249997951610986, -5.082755093536325930 ) ) ;
#12615=CARTESIAN_POINT ( 'NONE',  ( 7.188101187500002709, 117.3125000020483810, 2.977408999572649151 ) ) ;
#12619=CARTESIAN_POINT ( 'NONE',  ( -5.082755093536325042, 23.53124999795161543, -5.082755093536325930 ) ) ;
#12620=EDGE_LOOP ( 'NONE', ( #27361, #26318, #6945, #42792 ) ) ;
#12623=CARTESIAN_POINT ( 'NONE',  ( 7.188101187500002709, 101.1875000020483810, 2.977408999572649151 ) ) ;
#12632=VECTOR ( 'NONE', #15315, 1000.000000000000000 ) ;
#12633=CARTESIAN_POINT ( 'NONE',  ( -1.469576158976823947E-15, 14.62500000000000178, 8.000000000000000000 ) ) ;
#12651=ADVANCED_FACE ( 'NONE', ( #8840 ), #53752, .T. ) ;
#12653=CARTESIAN_POINT ( 'NONE',  ( 1.320432766682874540E-15, 112.5312500020483952, 7.188101187500000044 ) ) ;
#12655=CARTESIAN_POINT ( 'NONE',  ( -4.898587196589412829E-16, 117.3125000040967763, -8.000000000000000000 ) ) ;
#12658=CARTESIAN_POINT ( 'NONE',  ( -8.000000000000000000, 24.46874999590322375, -3.313708498984762496 ) ) ;
#12660=CARTESIAN_POINT ( 'NONE',  ( 1.469576158976823947E-15, 122.3750000000000000, 8.000000000000000000 ) ) ;
#12662=CARTESIAN_POINT ( 'NONE',  ( 8.000000000000000000, 109.3437499999999858, -3.313708498984762496 ) ) ;
#12670=FACE_OUTER_BOUND ( 'NONE', #14790, .T. ) ;
#12681=CARTESIAN_POINT ( 'NONE',  ( -5.082755093536326818, 13.78124999795161187, 5.082755093536325042 ) ) ;
#12690=CARTESIAN_POINT ( 'NONE',  ( 1.469576158976823947E-15, 94.06250000409677625, 8.000000000000000000 ) ) ;
#12700=CARTESIAN_POINT ( 'NONE',  ( -3.313708498984760720, 21.46875000000000355, -8.000000000000000000 ) ) ;
#12712=CARTESIAN_POINT ( 'NONE',  ( -2.977408999572650927, 116.7500000020483810, -7.188101187500001821 ) ) ;
#12716=DIRECTION ( 'NONE',  ( -0.000000000000000000, 1.000000000000000000, -0.000000000000000000 ) ) ;
#12740=CARTESIAN_POINT ( 'NONE',  ( 2.977408999572651815, 26.06249999795161543, 7.188101187500000933 ) ) ;
#12743=CARTESIAN_POINT ( 'NONE',  ( -5.082755093536324154, 100.7187500020483810, 5.082755093536326818 ) ) ;
#12764=CARTESIAN_POINT ( 'NONE',  ( -4.401442555609581635E-16, 94.15625000204838102, -7.188101187500000044 ) ) ;
#12775=CARTESIAN_POINT ( 'NONE',  ( 0.000000000000000000, 125.0000000000000000, 8.000000000000000000 ) ) ;
#12781=CARTESIAN_POINT ( 'NONE',  ( -1.469576158976823947E-15, 3.937499995903220640, 8.000000000000000000 ) ) ;
#12783=CONICAL_SURFACE ( 'NONE', #28412, 7.500000000000020428, 0.7853981633974552734 ) ;
#12784=CARTESIAN_POINT ( 'NONE',  ( -8.000000000000000000, 105.6875000040967763, 0.000000000000000000 ) ) ;
#12796=CARTESIAN_POINT ( 'NONE',  ( 2.977408999572650039, 98.18750000204838102, -7.188101187500001821 ) ) ;
#12797=CARTESIAN_POINT ( 'NONE',  ( -3.313708498984870410, 92.46875000409679046, 7.999999999999890754 ) ) ;
#12804=ORIENTED_EDGE ( 'NONE', *, *, #12564, .T. ) ;
#12817=CARTESIAN_POINT ( 'NONE',  ( -5.082755093536326818, 4.781249997951610986, 5.082755093536325042 ) ) ;
#12820=CARTESIAN_POINT ( 'NONE',  ( 2.977408999572650039, 118.0625000020483952, -7.188101187500000933 ) ) ;
#12839=CARTESIAN_POINT ( 'NONE',  ( -2.977408999572650927, 104.3750000020483952, -7.188101187500000933 ) ) ;
#12844=CARTESIAN_POINT ( 'NONE',  ( 5.082755093536325042, 111.9687500020483810, -5.082755093536325930 ) ) ;
#12850=DIRECTION ( 'NONE',  ( -0.000000000000000000, 1.000000000000000000, -0.000000000000000000 ) ) ;
#12871=CARTESIAN_POINT ( 'NONE',  ( -3.313708498984765161, 4.031250000000000888, 7.999999999999998224 ) ) ;
#12873=CARTESIAN_POINT ( 'NONE',  ( -2.977408999572654480, 1.499999997951610542, 7.188101187499999156 ) ) ;
#12874=CARTESIAN_POINT ( 'NONE',  ( -8.000000000000000000, 119.1875000040967763, 0.000000000000000000 ) ) ;
#12880=ORIENTED_EDGE ( 'NONE', *, *, #35464, .F. ) ;
#12886=CARTESIAN_POINT ( 'NONE',  ( 4.898587196589412829E-16, 13.68749999590322375, -8.000000000000000000 ) ) ;
#12891=ORIENTED_EDGE ( 'NONE', *, *, #48476, .F. ) ;
#12899=CARTESIAN_POINT ( 'NONE',  ( -5.656854249492378806, 120.6875000000000000, 5.656854249492381470 ) ) ;
#12901=EDGE_LOOP ( 'NONE', ( #12318, #13528, #47726, #24206 ) ) ;
#12902=( BOUNDED_CURVE ( )  B_SPLINE_CURVE ( 2, ( #38544, #61546, #55899, #4212, #43057, #51707, #51336, #23405, #40024 ),
 .UNSPECIFIED., .F., .F. ) 
 B_SPLINE_CURVE_WITH_KNOTS ( ( 3, 2, 2, 2, 3 ),
 ( 0.5729166666666666297, 0.5781250000000000000, 0.5833333333333333703, 0.5885416666666666297, 0.5937500000000000000 ),
 .UNSPECIFIED. ) 
 CURVE ( )  GEOMETRIC_REPRESENTATION_ITEM ( )  RATIONAL_B_SPLINE_CURVE ( ( 1.000000000000000000, 0.9238795325112867385, 1.000000000000000000, 0.9238795325112867385, 1.000000000000000000, 0.9238795325112867385, 1.000000000000000000, 0.9238795325112867385, 1.000000000000000000 ) ) 
 REPRESENTATION_ITEM ( '' )  );
#12905=CARTESIAN_POINT ( 'NONE',  ( -5.656854249492381470, 12.74999999590322197, 5.656854249492379694 ) ) ;
#12916=CARTESIAN_POINT ( 'NONE',  ( -7.999999999999998224, 99.78125000409676204, 3.313708498984766049 ) ) ;
#12931=CARTESIAN_POINT ( 'NONE',  ( -5.082755093536324154, 97.34375000204838102, 5.082755093536326818 ) ) ;
#12955=DIRECTION ( 'NONE',  ( 0.000000000000000000, -1.000000000000000000, 0.000000000000000000 ) ) ;
#12960=CARTESIAN_POINT ( 'NONE',  ( -7.188101187500000044, 13.21874999795161187, -8.802885111219163269E-16 ) ) ;
#12962=CARTESIAN_POINT ( 'NONE',  ( -7.999999999999998224, 117.7812500040967763, 3.313708498984766049 ) ) ;
#12963=CARTESIAN_POINT ( 'NONE',  ( 7.188101187500000044, 14.34374999795161187, 0.000000000000000000 ) ) ;
#12976=CARTESIAN_POINT ( 'NONE',  ( -5.082755093536324154, 115.3437500020483810, 5.082755093536326818 ) ) ;
#12977=LINE ( 'NONE', #36014, #71756 ) ;
#12980=CARTESIAN_POINT ( 'NONE',  ( -7.188101187500000044, 25.21874999795161543, -8.802885111219163269E-16 ) ) ;
#12986=CARTESIAN_POINT ( 'NONE',  ( 2.977408999572650039, 100.0625000020483952, -7.188101187500001821 ) ) ;
#13005=DIRECTION ( 'NONE',  ( 0.000000000000000000, 0.000000000000000000, 1.000000000000000000 ) ) ;
#13014=CARTESIAN_POINT ( 'NONE',  ( 0.000000000000000000, 0.5000000000000004441, 8.000000000000000000 ) ) ;
#13016=CARTESIAN_POINT ( 'NONE',  ( -5.082755093536324154, 116.8437500020483810, 5.082755093536326818 ) ) ;
#13034=DIRECTION ( 'NONE',  ( 0.000000000000000000, 0.000000000000000000, 1.000000000000000000 ) ) ;
#13041=CARTESIAN_POINT ( 'NONE',  ( 8.000000000000000000, 22.50000000000000355, 0.000000000000000000 ) ) ;
#13044=CARTESIAN_POINT ( 'NONE',  ( 4.401442555609581635E-16, 14.71874999795161187, -7.188101187500000044 ) ) ;
#13053=DIRECTION ( 'NONE',  ( -0.000000000000000000, 1.000000000000000000, -0.000000000000000000 ) ) ;
#13056=CYLINDRICAL_SURFACE ( 'NONE', #23233, 8.000000000000000000 ) ;
#13062=CARTESIAN_POINT ( 'NONE',  ( 5.656854249492380582, 25.68750000000000711, -5.656854249492380582 ) ) ;
#13074=CARTESIAN_POINT ( 'NONE',  ( 7.188101187499999156, 4.874999997951610986, 2.977408999572654924 ) ) ;
#13076=CARTESIAN_POINT ( 'NONE',  ( -5.082755093536324154, 115.7187500020483810, 5.082755093536326818 ) ) ;
#13080=FACE_OUTER_BOUND ( 'NONE', #25412, .T. ) ;
#13102=CARTESIAN_POINT ( 'NONE',  ( 2.977408999572650927, 25.12499999795161187, -7.188101187500001821 ) ) ;
#13104=CARTESIAN_POINT ( 'NONE',  ( -2.977408999572650927, 95.75000000204838102, -7.188101187500000933 ) ) ;
#13127=CARTESIAN_POINT ( 'NONE',  ( -5.082755093536325930, 89.84375000204839523, -5.082755093536325930 ) ) ;
#13138=CARTESIAN_POINT ( 'NONE',  ( -1.469576158976823947E-15, 2.437499995903220196, 8.000000000000000000 ) ) ;
#13143=( BOUNDED_CURVE ( )  B_SPLINE_CURVE ( 2, ( #53878, #70126, #53509, #59177, #6748 ),
 .UNSPECIFIED., .F., .F. ) 
 B_SPLINE_CURVE_WITH_KNOTS ( ( 3, 2, 3 ),
 ( 0.000000000000000000, 0.005208333333333336514, 0.01041666666666667303 ),
 .UNSPECIFIED. ) 
 CURVE ( )  GEOMETRIC_REPRESENTATION_ITEM ( )  RATIONAL_B_SPLINE_CURVE ( ( 1.000000000000000000, 0.9238795325112867385, 1.000000000000000000, 0.9238795325112866275, 1.000000000000000000 ) ) 
 REPRESENTATION_ITEM ( '' )  );
#13148=CARTESIAN_POINT ( 'NONE',  ( -5.656854249492378806, 101.3750000040967905, 5.656854249492381470 ) ) ;
#13156=FACE_OUTER_BOUND ( 'NONE', #9536, .T. ) ;
#13160=CARTESIAN_POINT ( 'NONE',  ( 7.188101187500002709, 99.31250000204839523, 2.977408999572649151 ) ) ;
#13165=CARTESIAN_POINT ( 'NONE',  ( -3.313708498984815343, 103.9062500040968047, -7.999999999999944933 ) ) ;
#13178=LINE ( 'NONE', #36214, #20283 ) ;
#13182=CARTESIAN_POINT ( 'NONE',  ( -2.977408999572650039, 2.812499997951610542, -7.188101187500001821 ) ) ;
#13185=CARTESIAN_POINT ( 'NONE',  ( -5.082755093536324154, 114.2187500020483810, 5.082755093536326818 ) ) ;
#13194=CARTESIAN_POINT ( 'NONE',  ( 5.656854249492381470, 112.0625000000000000, 5.656854249492379694 ) ) ;
#13205=CARTESIAN_POINT ( 'NONE',  ( 7.188101187500000933, 108.5000000020483810, -2.977408999572651371 ) ) ;
#13212=CARTESIAN_POINT ( 'NONE',  ( 7.188101187500001821, 107.3750000020484094, -2.977408999572651371 ) ) ;
#13219=CARTESIAN_POINT ( 'NONE',  ( -5.656854249492381470, 6.749999995903220196, 5.656854249492379694 ) ) ;
#13220=CARTESIAN_POINT ( 'NONE',  ( 1.469576158976823947E-15, 107.3750000000000000, 8.000000000000000000 ) ) ;
#13232=EDGE_CURVE ( 'NONE', #32201, #60988, #49159, .T. ) ;
#13240=CARTESIAN_POINT ( 'NONE',  ( 7.999999999999998224, 5.906250000000000000, 3.313708498984766493 ) ) ;
#13242=CARTESIAN_POINT ( 'NONE',  ( 4.401442555609581635E-16, 3.843749997951610098, -7.188101187500000044 ) ) ;
#13243=CARTESIAN_POINT ( 'NONE',  ( 5.656854249492381470, 122.7500000040967905, 5.656854249492379694 ) ) ;
#13266=CARTESIAN_POINT ( 'NONE',  ( -3.313708498984762496, 117.7812500000000000, 7.999999999999998224 ) ) ;
#13269=CARTESIAN_POINT ( 'NONE',  ( -1.469576158976823947E-15, 17.43749999590322375, 8.000000000000000000 ) ) ;
#13295=VECTOR ( 'NONE', #68584, 1000.000000000000000 ) ;
#13298=CARTESIAN_POINT ( 'NONE',  ( -7.188101187499999156, 95.75000000204836681, 2.977408999572654924 ) ) ;
#13325=CARTESIAN_POINT ( 'NONE',  ( -2.977408999572654480, 16.49999999795161543, 7.188101187499999156 ) ) ;
#13329=CARTESIAN_POINT ( 'NONE',  ( -1.320432766682874540E-15, 12.46874999795161187, 7.188101187500000044 ) ) ;
#13332=CARTESIAN_POINT ( 'NONE',  ( 0.000000000000000000, 0.000000000000000000, 0.000000000000000000 ) ) ;
#13340=CARTESIAN_POINT ( 'NONE',  ( 7.188101187500001821, 119.0000000020483810, -2.977408999572651371 ) ) ;
#13343=ORIENTED_EDGE ( 'NONE', *, *, #70067, .F. ) ;
#13344=CARTESIAN_POINT ( 'NONE',  ( -5.082755093536326818, 23.90624999795161543, 5.082755093536325042 ) ) ;
#13350=CARTESIAN_POINT ( 'NONE',  ( 7.188101187500002709, 99.68750000204838102, 2.977408999572649151 ) ) ;
#13352=CARTESIAN_POINT ( 'NONE',  ( -5.656854249492380582, 89.00000000409677625, -5.656854249492380582 ) ) ;
#13371=CARTESIAN_POINT ( 'NONE',  ( 3.313708498984819339, 110.4687500000000000, 7.999999999999943157 ) ) ;
#13383=CARTESIAN_POINT ( 'NONE',  ( -4.401442555609581635E-16, 114.7812500020483952, -7.188101187500000044 ) ) ;
#13390=DIRECTION ( 'NONE',  ( 0.000000000000000000, 0.000000000000000000, 1.000000000000000000 ) ) ;
#13403=EDGE_CURVE ( 'NONE', #24477, #14040, #39288, .T. ) ;
#13408=CARTESIAN_POINT ( 'NONE',  ( 7.999999999999998224, 22.40625000000000355, 3.313708498984766049 ) ) ;
#13412=CARTESIAN_POINT ( 'NONE',  ( 7.188101187499999156, 11.24999999795161187, 2.977408999572654924 ) ) ;
#13415=ORIENTED_EDGE ( 'NONE', *, *, #32678, .T. ) ;
#13428=CARTESIAN_POINT ( 'NONE',  ( 8.000000000000000000, 22.59375000000000355, -3.313708498984761608 ) ) ;
#13440=CARTESIAN_POINT ( 'NONE',  ( 7.188101187500000044, 7.968749997951610986, 0.000000000000000000 ) ) ;
#13443=CARTESIAN_POINT ( 'NONE',  ( 2.977408999572650039, 116.5625000020483810, -7.188101187500001821 ) ) ;
#13454=ORIENTED_EDGE ( 'NONE', *, *, #29775, .F. ) ;
#13464=CARTESIAN_POINT ( 'NONE',  ( 1.469576158976823947E-15, 99.87499999999998579, 8.000000000000000000 ) ) ;
#13471=CARTESIAN_POINT ( 'NONE',  ( -7.188101187500000044, 93.03125000204836681, 0.000000000000000000 ) ) ;
#13491=EDGE_CURVE ( 'NONE', #69151, #22422, #20807, .T. ) ;
#13494=CARTESIAN_POINT ( 'NONE',  ( 7.188101187500001821, 92.37500000204839523, -2.977408999572651371 ) ) ;
#13503=DIRECTION ( 'NONE',  ( -0.000000000000000000, 1.000000000000000000, -0.000000000000000000 ) ) ;
#13511=CARTESIAN_POINT ( 'NONE',  ( 7.999999999999998224, 17.90625000000000355, 3.313708498984766049 ) ) ;
#13514=CARTESIAN_POINT ( 'NONE',  ( -3.313708498984762052, 99.40625000409676204, -8.000000000000000000 ) ) ;
#13515=VECTOR ( 'NONE', #60927, 1000.000000000000000 ) ;
#13520=DIRECTION ( 'NONE',  ( -0.000000000000000000, 1.000000000000000000, -0.000000000000000000 ) ) ;
#13524=CARTESIAN_POINT ( 'NONE',  ( 7.188101187500000044, 99.40625000204838102, -8.802885111219163269E-16 ) ) ;
#13525=CARTESIAN_POINT ( 'NONE',  ( 5.656854249492378806, 16.12499999590322375, 5.656854249492381470 ) ) ;
#13528=ORIENTED_EDGE ( 'NONE', *, *, #22351, .F. ) ;
#13542=( BOUNDED_CURVE ( )  B_SPLINE_CURVE ( 2, ( #55340, #49281, #7818, #31193, #59869, #43627, #2899, #42133, #37607 ),
 .UNSPECIFIED., .F., .F. ) 
 B_SPLINE_CURVE_WITH_KNOTS ( ( 3, 2, 2, 2, 3 ),
 ( 0.8750000000000000000, 0.8819444444444444198, 0.8888888888888888395, 0.8958333333333332593, 0.9027777777777776791 ),
 .UNSPECIFIED. ) 
 CURVE ( )  GEOMETRIC_REPRESENTATION_ITEM ( )  RATIONAL_B_SPLINE_CURVE ( ( 1.000000000000000000, 0.9238795325112867385, 1.000000000000000000, 0.9238795325112867385, 1.000000000000000000, 0.9238795325112867385, 1.000000000000000000, 0.9238795325112879597, 0.9999999999999987788 ) ) 
 REPRESENTATION_ITEM ( '' )  );
#13544=CARTESIAN_POINT ( 'NONE',  ( -1.469576158976823947E-15, 5.437499995903221084, 8.000000000000000000 ) ) ;
#13548=CARTESIAN_POINT ( 'NONE',  ( 7.188101187499999156, 6.749999997951610986, 2.977408999572654924 ) ) ;
#13551=CARTESIAN_POINT ( 'NONE',  ( 5.082755093536326818, 108.5937500020483810, 5.082755093536325042 ) ) ;
#13572=CARTESIAN_POINT ( 'NONE',  ( -7.188101187499999156, 107.7500000020483810, 2.977408999572654924 ) ) ;
#13576=( BOUNDED_CURVE ( )  B_SPLINE_CURVE ( 2, ( #63436, #10648, #29118, #33679, #27618, #34428, #62687, #17414, #5368 ),
 .UNSPECIFIED., .F., .F. ) 
 B_SPLINE_CURVE_WITH_KNOTS ( ( 3, 2, 2, 2, 3 ),
 ( 0.6805555555555554692, 0.6874999999999998890, 0.6944444444444443088, 0.7013888888888887285, 0.7083333333333332593 ),
 .UNSPECIFIED. ) 
 CURVE ( )  GEOMETRIC_REPRESENTATION_ITEM ( )  RATIONAL_B_SPLINE_CURVE ( ( 1.000000000000001110, 0.9238795325112855172, 1.000000000000000000, 0.9238795325112867385, 1.000000000000000000, 0.9238795325112867385, 1.000000000000000000, 0.9238795325112879597, 0.9999999999999987788 ) ) 
 REPRESENTATION_ITEM ( '' )  );
#13579=CARTESIAN_POINT ( 'NONE',  ( 7.188101187500000044, 110.2812500020483810, -8.802885111219163269E-16 ) ) ;
#13587=CARTESIAN_POINT ( 'NONE',  ( -3.979266480698733677, 0.4999999999999095723, -6.940132439340586323 ) ) ;
#13591=CARTESIAN_POINT ( 'NONE',  ( 2.977408999572650927, 1.124999997951610098, -7.188101187500000933 ) ) ;
#13605=CARTESIAN_POINT ( 'NONE',  ( -3.313708498984760720, 12.46875000000000178, -8.000000000000000000 ) ) ;
#13607=CARTESIAN_POINT ( 'NONE',  ( -2.977408999572654480, 4.499999997951610986, 7.188101187499999156 ) ) ;
#13608=CARTESIAN_POINT ( 'NONE',  ( -7.999999999999998224, 114.7812500040967763, 3.313708498984766493 ) ) ;
#13610=CARTESIAN_POINT ( 'NONE',  ( -8.000000000000000000, 6.656250000000000888, -3.313708498984762496 ) ) ;
#13620=FACE_OUTER_BOUND ( 'NONE', #56416, .T. ) ;
#13632=CARTESIAN_POINT ( 'NONE',  ( 5.656854249492381470, 104.5625000000000000, 5.656854249492379694 ) ) ;
#13634=CARTESIAN_POINT ( 'NONE',  ( -5.656854249492380582, 114.3125000000000000, -5.656854249492380582 ) ) ;
#13638=CARTESIAN_POINT ( 'NONE',  ( 8.000000000000000000, 17.90624999590322375, -3.313708498984761608 ) ) ;
#13658=CARTESIAN_POINT ( 'NONE',  ( -5.082755093536325930, 122.4687500020483952, -5.082755093536325930 ) ) ;
#13659=CARTESIAN_POINT ( 'NONE',  ( 1.469576158976823947E-15, 119.3750000000000000, 8.000000000000000000 ) ) ;
#13664=CARTESIAN_POINT ( 'NONE',  ( 1.926045908305006327, 89.22060438569889129, -7.188101187499999156 ) ) ;
#13670=( BOUNDED_CURVE ( )  B_SPLINE_CURVE ( 2, ( #785, #23768, #2152, #19488, #46772, #59503, #42130, #30818, #69056 ),
 .UNSPECIFIED., .F., .F. ) 
 B_SPLINE_CURVE_WITH_KNOTS ( ( 3, 2, 2, 2, 3 ),
 ( 0.09722222222222220989, 0.1041666666666666574, 0.1111111111111111049, 0.1180555555555555525, 0.1250000000000000000 ),
 .UNSPECIFIED. ) 
 CURVE ( )  GEOMETRIC_REPRESENTATION_ITEM ( )  RATIONAL_B_SPLINE_CURVE ( ( 1.000000000000000222, 0.9238795325112866275, 1.000000000000000000, 0.9238795325112867385, 1.000000000000000000, 0.9238795325112867385, 1.000000000000000000, 0.9238795325112867385, 1.000000000000000000 ) ) 
 REPRESENTATION_ITEM ( '' )  );
#13686=CARTESIAN_POINT ( 'NONE',  ( 1.469576158976823947E-15, 120.8750000000000000, 8.000000000000000000 ) ) ;
#13690=CARTESIAN_POINT ( 'NONE',  ( 7.188101187500001821, 17.06249999795161543, -2.977408999572650483 ) ) ;
#13692=CARTESIAN_POINT ( 'NONE',  ( 0.3459307087059793062, 124.5729800877406461, -7.927019912259368972 ) ) ;
#13693=CARTESIAN_POINT ( 'NONE',  ( -2.977408999572654480, 9.374999997951610098, 7.188101187499999156 ) ) ;
#13700=EDGE_CURVE ( 'NONE', #67076, #33995, #21738, .T. ) ;
#13704=CARTESIAN_POINT ( 'NONE',  ( 5.082755093536326818, 112.7187500020483810, 5.082755093536325042 ) ) ;
#13707=EDGE_LOOP ( 'NONE', ( #40429, #19341, #23683, #11456 ) ) ;
#13709=CARTESIAN_POINT ( 'NONE',  ( 7.188101187500000933, 24.56249999795161543, -2.977408999572650483 ) ) ;
#13715=CARTESIAN_POINT ( 'NONE',  ( -2.977408999572651815, 100.8125000020484094, 7.188101187500000933 ) ) ;
#13743=CARTESIAN_POINT ( 'NONE',  ( -7.692623880995575369, 124.8073761190044166, -0.5146232510360394530 ) ) ;
#13746=CARTESIAN_POINT ( 'NONE',  ( 5.082755093536326818, 111.2187500020483810, 5.082755093536325042 ) ) ;
#13750=CARTESIAN_POINT ( 'NONE',  ( 4.898587196589412829E-16, 25.87500000000000711, -8.000000000000000000 ) ) ;
#13772=CARTESIAN_POINT ( 'NONE',  ( -2.977408999572650039, 10.31249999795161187, -7.188101187500000933 ) ) ;
#13780=CARTESIAN_POINT ( 'NONE',  ( -3.313708498984707429, 97.90625000409677625, -8.000000000000055067 ) ) ;
#13791=CARTESIAN_POINT ( 'NONE',  ( -5.656854249492381470, 24.93750000000000355, 5.656854249492379694 ) ) ;
#13803=CARTESIAN_POINT ( 'NONE',  ( 5.082755093536324154, 6.281249997951610986, 5.082755093536326818 ) ) ;
#13805=CARTESIAN_POINT ( 'NONE',  ( 5.082755093536326818, 116.0937500020483810, 5.082755093536325042 ) ) ;
#13818=CARTESIAN_POINT ( 'NONE',  ( 8.000000000000000000, 97.34375000000000000, -3.313708498984762496 ) ) ;
#13829=CARTESIAN_POINT ( 'NONE',  ( 7.188101187500000044, 27.84374999795161543, 0.000000000000000000 ) ) ;
#13831=CARTESIAN_POINT ( 'NONE',  ( 1.320432766682874540E-15, 91.90625000204838102, 7.188101187500000044 ) ) ;
#13856=CARTESIAN_POINT ( 'NONE',  ( -4.401442555609581635E-16, 92.65625000204838102, -7.188101187500000044 ) ) ;
#13879=EDGE_CURVE ( 'NONE', #59499, #72853, #5896, .T. ) ;
#13880=CARTESIAN_POINT ( 'NONE',  ( -8.000000000000000000, 96.68750000409679046, 0.000000000000000000 ) ) ;
#13891=CARTESIAN_POINT ( 'NONE',  ( -7.188101187499999156, 100.2500000020483952, 2.977408999572654924 ) ) ;
#13912=CARTESIAN_POINT ( 'NONE',  ( 8.000000000000000000, 1.312499995903220196, 0.000000000000000000 ) ) ;
#13914=CARTESIAN_POINT ( 'NONE',  ( -1.320432766682874540E-15, 9.468749997951610098, 7.188101187500000044 ) ) ;
#13916=CARTESIAN_POINT ( 'NONE',  ( -1.469576158976823947E-15, 11.62500000000000178, 8.000000000000000000 ) ) ;
#13917=CARTESIAN_POINT ( 'NONE',  ( -5.082755093536325930, 107.8437500020483810, -5.082755093536325930 ) ) ;
#13936=CARTESIAN_POINT ( 'NONE',  ( 1.320432766682874540E-15, 108.0312500020483810, 7.188101187500000044 ) ) ;
#13942=CARTESIAN_POINT ( 'NONE',  ( 7.188101187500002709, 108.6875000020483952, 2.977408999572649151 ) ) ;
#13966=CARTESIAN_POINT ( 'NONE',  ( -8.000000000000000000, 11.15625000000000178, -3.313708498984762496 ) ) ;
#13969=CARTESIAN_POINT ( 'NONE',  ( 7.188101187500001821, 5.062499997951610098, -2.977408999572650483 ) ) ;
#13970=CARTESIAN_POINT ( 'NONE',  ( 5.656854249492379694, 117.1250000040967905, -5.656854249492380582 ) ) ;
#13973=CYLINDRICAL_SURFACE ( 'NONE', #9093, 8.000000000000000000 ) ;
#13998=CARTESIAN_POINT ( 'NONE',  ( -7.999999999999998224, 113.0937500000000000, 3.313708498984766493 ) ) ;
#14001=ORIENTED_EDGE ( 'NONE', *, *, #67751, .T. ) ;
#14005=CARTESIAN_POINT ( 'NONE',  ( 4.898587196589412829E-16, 22.68749999590322375, -8.000000000000000000 ) ) ;
#14010=CARTESIAN_POINT ( 'NONE',  ( 1.469576158976823947E-15, 115.0625000040967905, 8.000000000000000000 ) ) ;
#14015=CARTESIAN_POINT ( 'NONE',  ( 9.797174393178825657E-16, 125.0000000000000000, -8.000000000000000000 ) ) ;
#14027=CARTESIAN_POINT ( 'NONE',  ( 7.188101187500000044, 121.9062500020483810, -8.802885111219163269E-16 ) ) ;
#14033=CARTESIAN_POINT ( 'NONE',  ( -5.082755093536325930, 93.96875000204838102, -5.082755093536325930 ) ) ;
#14040=VERTEX_POINT ( 'NONE', #58695 ) ;
#14051=DIRECTION ( 'NONE',  ( 0.000000000000000000, 0.000000000000000000, 1.000000000000000000 ) ) ;
#14063=CARTESIAN_POINT ( 'NONE',  ( -5.082755093536326818, 20.90624999795161543, 5.082755093536325042 ) ) ;
#14067=CARTESIAN_POINT ( 'NONE',  ( 7.188101187500001821, 11.43749999795161010, -2.977408999572650483 ) ) ;
#14071=DIRECTION ( 'NONE',  ( -0.4999969897303749300, 0.000000000000000000, 0.8660271417574413322 ) ) ;
#14079=CARTESIAN_POINT ( 'NONE',  ( -2.977408999572651815, 109.4375000020483810, 7.188101187500000933 ) ) ;
#14084=CARTESIAN_POINT ( 'NONE',  ( -7.188101187500000933, 20.62499999795161543, -2.977408999572651371 ) ) ;
#14091=CARTESIAN_POINT ( 'NONE',  ( -5.082755093536324154, 96.21875000204838102, 5.082755093536326818 ) ) ;
#14120=CARTESIAN_POINT ( 'NONE',  ( -7.514277766361627364, 124.7823509838186169, -1.778518646698914241 ) ) ;
#14123=CARTESIAN_POINT ( 'NONE',  ( 7.188101187500001821, 107.0000000020483810, -2.977408999572651371 ) ) ;
#14130=CARTESIAN_POINT ( 'NONE',  ( -4.898587196589412829E-16, 93.31250000409677625, -8.000000000000000000 ) ) ;
#14151=CARTESIAN_POINT ( 'NONE',  ( 2.977408999572652260, 14.06249999795161365, 7.188101187500000044 ) ) ;
#14162=CARTESIAN_POINT ( 'NONE',  ( 7.188101187500001821, 0.5624999979516098758, -2.977408999572650483 ) ) ;
#14170=CARTESIAN_POINT ( 'NONE',  ( 5.656854249492380582, 21.18750000000000355, -5.656854249492380582 ) ) ;
#14180=CARTESIAN_POINT ( 'NONE',  ( -1.320432766682874540E-15, 7.593749997951611874, 7.188101187500000044 ) ) ;
#14182=CARTESIAN_POINT ( 'NONE',  ( 7.188101187500002709, 111.6875000020483810, 2.977408999572649151 ) ) ;
#14196=CARTESIAN_POINT ( 'NONE',  ( -8.000000000000000000, 97.90625000000000000, -3.313708498984761608 ) ) ;
#14207=EDGE_CURVE ( 'NONE', #20933, #27944, #48705, .T. ) ;
#14209=CARTESIAN_POINT ( 'NONE',  ( 7.188101187499999156, 27.74999999795161543, 2.977408999572654924 ) ) ;
#14211=CARTESIAN_POINT ( 'NONE',  ( 2.977408999572654480, 95.00000000204838102, 7.188101187499999156 ) ) ;
#14212=CYLINDRICAL_SURFACE ( 'NONE', #50654, 8.000000000000000000 ) ;
#14218=ORIENTED_EDGE ( 'NONE', *, *, #18195, .T. ) ;
#14226=CARTESIAN_POINT ( 'NONE',  ( -3.313708498984762496, 102.7812499999999858, 7.999999999999998224 ) ) ;
#14227=CARTESIAN_POINT ( 'NONE',  ( 5.656854249492380582, 23.99999999590322375, -5.656854249492380582 ) ) ;
#14236=CARTESIAN_POINT ( 'NONE',  ( -2.977408999572650927, 91.25000000204838102, -7.188101187500001821 ) ) ;
#14251=CARTESIAN_POINT ( 'NONE',  ( 0.000000000000000000, 125.0000000000000000, 0.000000000000000000 ) ) ;
#14260=CARTESIAN_POINT ( 'NONE',  ( -5.656854249492380582, 98.00000000409677625, -5.656854249492380582 ) ) ;
#14269=CARTESIAN_POINT ( 'NONE',  ( 1.320432766682874540E-15, 96.03125000204838102, 7.188101187500000044 ) ) ;
#14273=AXIS2_PLACEMENT_3D ( 'NONE', #46638, #47004, #11943 ) ;
#14291=CARTESIAN_POINT ( 'NONE',  ( 7.999999999999998224, 4.218749995903220196, 3.313708498984766493 ) ) ;
#14293=CARTESIAN_POINT ( 'NONE',  ( 7.188101187500001821, 9.937499997951610098, -2.977408999572650483 ) ) ;
#14296=CARTESIAN_POINT ( 'NONE',  ( -4.401442555609581635E-16, 110.6562500020483810, -7.188101187500000044 ) ) ;
#14306=ORIENTED_EDGE ( 'NONE', *, *, #14207, .F. ) ;
#14315=CARTESIAN_POINT ( 'NONE',  ( 5.082755093536326818, 102.2187500020483810, 5.082755093536325042 ) ) ;
#14323=CARTESIAN_POINT ( 'NONE',  ( 7.188101187500000044, 107.2812500020483810, -8.802885111219163269E-16 ) ) ;
#14327=( BOUNDED_CURVE ( )  B_SPLINE_CURVE ( 2, ( #57580, #5890, #22468, #247, #52650, #46607, #10795, #6266, #68880 ),
 .UNSPECIFIED., .F., .F. ) 
 B_SPLINE_CURVE_WITH_KNOTS ( ( 3, 2, 2, 2, 3 ),
 ( 0.1805555555555555525, 0.1875000000000000000, 0.1944444444444444198, 0.2013888888888888673, 0.2083333333333333148 ),
 .UNSPECIFIED. ) 
 CURVE ( )  GEOMETRIC_REPRESENTATION_ITEM ( )  RATIONAL_B_SPLINE_CURVE ( ( 1.000000000000000000, 0.9238795325112867385, 1.000000000000000000, 0.9238795325112867385, 1.000000000000000000, 0.9238795325112867385, 1.000000000000000000, 0.9238795325112870716, 0.9999999999999996669 ) ) 
 REPRESENTATION_ITEM ( '' )  );
#14335=CARTESIAN_POINT ( 'NONE',  ( -1.320432766682874540E-15, 1.968749997951610320, 7.188101187500000044 ) ) ;
#14341=ORIENTED_EDGE ( 'NONE', *, *, #36982, .T. ) ;
#14343=FACE_OUTER_BOUND ( 'NONE', #9003, .T. ) ;
#14353=CARTESIAN_POINT ( 'NONE',  ( -7.188101187500001821, 8.624999997951611874, -2.977408999572651371 ) ) ;
#14354=CARTESIAN_POINT ( 'NONE',  ( -4.898587196589412829E-16, 114.3125000040967905, -8.000000000000000000 ) ) ;
#14375=CARTESIAN_POINT ( 'NONE',  ( 1.469576158976823947E-15, 104.3750000000000000, 8.000000000000000000 ) ) ;
#14378=CARTESIAN_POINT ( 'NONE',  ( 5.656854249492381470, 112.0625000000000000, 5.656854249492379694 ) ) ;
#14381=ORIENTED_EDGE ( 'NONE', *, *, #69806, .F. ) ;
#14385=CARTESIAN_POINT ( 'NONE',  ( -5.656854249492381470, 20.24999999590322375, 5.656854249492379694 ) ) ;
#14408=CARTESIAN_POINT ( 'NONE',  ( 5.082755093536326818, 123.2187500020483952, 5.082755093536325042 ) ) ;
#14414=CARTESIAN_POINT ( 'NONE',  ( -7.188101187500000044, 89.65625000204838102, 0.000000000000000000 ) ) ;
#14425=CARTESIAN_POINT ( 'NONE',  ( 3.313708498984760276, 103.5312500000000000, -8.000000000000000000 ) ) ;
#14439=CARTESIAN_POINT ( 'NONE',  ( -2.977408999572650039, 23.43749999795161898, -7.188101187500001821 ) ) ;
#14442=CARTESIAN_POINT ( 'NONE',  ( -7.188101187500000044, 9.093749997951611874, -8.802885111219163269E-16 ) ) ;
#14454=CARTESIAN_POINT ( 'NONE',  ( -4.401442555609581635E-16, 108.7812500020483810, -7.188101187500000044 ) ) ;
#14465=CARTESIAN_POINT ( 'NONE',  ( -7.188101187500000044, 91.53125000204836681, 0.000000000000000000 ) ) ;
#14468=CARTESIAN_POINT ( 'NONE',  ( 0.000000000000000000, 125.0000000000000000, 0.000000000000000000 ) ) ;
#14472=CARTESIAN_POINT ( 'NONE',  ( -1.469576158976823947E-15, 11.62500000000000178, 8.000000000000000000 ) ) ;
#14490=CARTESIAN_POINT ( 'NONE',  ( -8.000000000000000000, 115.9999999999999858, 0.000000000000000000 ) ) ;
#14492=EDGE_CURVE ( 'NONE', #3547, #28168, #39958, .T. ) ;
#14495=CARTESIAN_POINT ( 'NONE',  ( 7.188101187500001821, 110.0000000020483668, -2.977408999572651371 ) ) ;
#14504=CARTESIAN_POINT ( 'NONE',  ( 7.999999999999998224, 26.90625000000000355, 3.313708498984766049 ) ) ;
#14523=CARTESIAN_POINT ( 'NONE',  ( 2.977408999572652260, 17.06249999795161543, 7.188101187500000044 ) ) ;
#14525=ADVANCED_FACE ( 'NONE', ( #10348 ), #56374, .T. ) ;
#14531=CARTESIAN_POINT ( 'NONE',  ( 7.188101187500000044, 4.968749997951610986, 0.000000000000000000 ) ) ;
#14550=CARTESIAN_POINT ( 'NONE',  ( -5.082755093536325042, 7.031249997951611874, -5.082755093536325930 ) ) ;
#14556=CARTESIAN_POINT ( 'NONE',  ( -5.082755093536324154, 114.2187500020483810, 5.082755093536326818 ) ) ;
#14557=AXIS2_PLACEMENT_3D ( 'NONE', #8209, #19517, #70842 ) ;
#14573=CARTESIAN_POINT ( 'NONE',  ( 8.000000000000000000, 91.25000000000000000, -9.797174393178825657E-16 ) ) ;
#14580=CARTESIAN_POINT ( 'NONE',  ( 3.313708498984800688, 118.7187500040967905, -7.999999999999958256 ) ) ;
#14587=CARTESIAN_POINT ( 'NONE',  ( -5.082755093536324154, 90.21875000204838102, 5.082755093536326818 ) ) ;
#14594=ORIENTED_EDGE ( 'NONE', *, *, #57275, .T. ) ;
#14597=CARTESIAN_POINT ( 'NONE',  ( -7.188101187500000044, 20.71874999795161543, -8.802885111219163269E-16 ) ) ;
#14602=ORIENTED_EDGE ( 'NONE', *, *, #34723, .F. ) ;
#14613=CARTESIAN_POINT ( 'NONE',  ( 2.977408999572654480, 93.50000000204838102, 7.188101187499999156 ) ) ;
#14634=CARTESIAN_POINT ( 'NONE',  ( 1.469576158976823947E-15, 98.56250000409677625, 8.000000000000000000 ) ) ;
#14641=AXIS2_PLACEMENT_3D ( 'NONE', #51147, #57193, #22460 ) ;
#14644=CARTESIAN_POINT ( 'NONE',  ( 5.082755093536325042, 95.09375000204838102, -5.082755093536325930 ) ) ;
#14665=( BOUNDED_CURVE ( )  B_SPLINE_CURVE ( 2, ( #2924, #38758, #21750, #72706, #44034, #67042, #49306, #4794, #54992 ),
 .UNSPECIFIED., .F., .F. ) 
 B_SPLINE_CURVE_WITH_KNOTS ( ( 3, 2, 2, 2, 3 ),
 ( 0.8854166666666669627, 0.8906250000000003331, 0.8958333333333337034, 0.9010416666666668517, 0.9062500000000002220 ),
 .UNSPECIFIED. ) 
 CURVE ( )  GEOMETRIC_REPRESENTATION_ITEM ( )  RATIONAL_B_SPLINE_CURVE ( ( 0.9999999999999951150, 0.9238795325112916235, 1.000000000000000000, 0.9238795325112867385, 1.000000000000000000, 0.9238795325112867385, 1.000000000000000000, 0.9238795325112835188, 1.000000000000003331 ) ) 
 REPRESENTATION_ITEM ( '' )  );
#14668=CARTESIAN_POINT ( 'NONE',  ( -5.082755093536326818, 13.78124999795161187, 5.082755093536325042 ) ) ;
#14671=CARTESIAN_POINT ( 'NONE',  ( 0.000000000000000000, 125.0000000000000000, 0.000000000000000000 ) ) ;
#14672=CARTESIAN_POINT ( 'NONE',  ( -7.188101187500000044, 111.0312500020483810, 0.000000000000000000 ) ) ;
#14682=ORIENTED_EDGE ( 'NONE', *, *, #7002, .T. ) ;
#14683=DIRECTION ( 'NONE',  ( -0.000000000000000000, 1.000000000000000000, -0.000000000000000000 ) ) ;
#14690=CARTESIAN_POINT ( 'NONE',  ( -5.082755093536324154, 98.84375000204838102, 5.082755093536326818 ) ) ;
#14697=AXIS2_PLACEMENT_3D ( 'NONE', #23731, #35075, #6398 ) ;
#14698=CARTESIAN_POINT ( 'NONE',  ( 2.977408999572654480, 111.5000000020483810, 7.188101187499999156 ) ) ;
#14710=CARTESIAN_POINT ( 'NONE',  ( 7.188101187500000044, 2.343749997951610098, 0.000000000000000000 ) ) ;
#14717=CARTESIAN_POINT ( 'NONE',  ( 0.000000000000000000, 55.00000000000000000, 8.000000000000000000 ) ) ;
#14722=ORIENTED_EDGE ( 'NONE', *, *, #2908, .T. ) ;
#14725=CARTESIAN_POINT ( 'NONE',  ( 5.082755093536325930, 9.656249997951610098, -5.082755093536325930 ) ) ;
#14726=CARTESIAN_POINT ( 'NONE',  ( -5.656854249492380582, 116.0000000040967905, -5.656854249492380582 ) ) ;
#14736=CARTESIAN_POINT ( 'NONE',  ( 1.469576158976823947E-15, 95.37499999999998579, 8.000000000000000000 ) ) ;
#14751=AXIS2_PLACEMENT_3D ( 'NONE', #29951, #52964, #14051 ) ;
#14752=CARTESIAN_POINT ( 'NONE',  ( -5.656854249492378806, 111.6875000000000000, 5.656854249492381470 ) ) ;
#14758=CARTESIAN_POINT ( 'NONE',  ( -8.000000000000001776, 20.15624999590322375, 3.313708498984759387 ) ) ;
#14780=CARTESIAN_POINT ( 'NONE',  ( 4.898587196589412829E-16, 4.687499995903220196, -8.000000000000000000 ) ) ;
#14781=CARTESIAN_POINT ( 'NONE',  ( -2.977408999572652260, 119.9375000020483952, 7.188101187500000044 ) ) ;
#14786=CARTESIAN_POINT ( 'NONE',  ( -7.188101187500001821, 124.4375000020483810, -2.977408999572650483 ) ) ;
#14789=LINE ( 'NONE', #21947, #39016 ) ;
#14790=EDGE_LOOP ( 'NONE', ( #69317, #24000, #45151, #57372, #32471, #44444, #44745, #64839 ) ) ;
#14792=( BOUNDED_CURVE ( )  B_SPLINE_CURVE ( 2, ( #66272, #14580, #45130, #67776, #32714, #61366, #33834, #10798, #44763 ),
 .UNSPECIFIED., .F., .F. ) 
 B_SPLINE_CURVE_WITH_KNOTS ( ( 3, 2, 2, 2, 3 ),
 ( 0.1354166666666667407, 0.1406250000000000833, 0.1458333333333334259, 0.1510416666666667684, 0.1562500000000001110 ),
 .UNSPECIFIED. ) 
 CURVE ( )  GEOMETRIC_REPRESENTATION_ITEM ( )  RATIONAL_B_SPLINE_CURVE ( ( 0.9999999999999987788, 0.9238795325112879597, 1.000000000000000000, 0.9238795325112867385, 1.000000000000000000, 0.9238795325112867385, 1.000000000000000000, 0.9238795325112850731, 1.000000000000001554 ) ) 
 REPRESENTATION_ITEM ( '' )  );
#14814=CARTESIAN_POINT ( 'NONE',  ( 5.082755093536325930, 21.65624999795161543, -5.082755093536325930 ) ) ;
#14816=CARTESIAN_POINT ( 'NONE',  ( -5.082755093536326818, 19.78124999795161543, 5.082755093536325042 ) ) ;
#14819=PLANE ( 'NONE',  #10116 ) ;
#14828=CARTESIAN_POINT ( 'NONE',  ( -7.188101187500001821, 109.0625000020483810, -2.977408999572650483 ) ) ;
#14839=CARTESIAN_POINT ( 'NONE',  ( -4.401442555609581635E-16, 92.65625000204838102, -7.188101187500000044 ) ) ;
#14841=EDGE_CURVE ( 'NONE', #36620, #46386, #9797, .T. ) ;
#14851=CARTESIAN_POINT ( 'NONE',  ( 8.000000000000000000, 108.0312500040967905, -3.313708498984762496 ) ) ;
#14866=CYLINDRICAL_SURFACE ( 'NONE', #69751, 8.000000000000000000 ) ;
#14871=CARTESIAN_POINT ( 'NONE',  ( 7.188101187500001821, 108.5000000020483810, -2.977408999572651371 ) ) ;
#14878=VERTEX_POINT ( 'NONE', #73167 ) ;
#14880=CARTESIAN_POINT ( 'NONE',  ( -3.313708498984816231, 99.78124999999997158, 7.999999999999943157 ) ) ;
#14887=CARTESIAN_POINT ( 'NONE',  ( -4.898587196589412829E-16, 117.1250000000000000, -8.000000000000000000 ) ) ;
#14888=CARTESIAN_POINT ( 'NONE',  ( -8.000000000000000000, 95.00000000000000000, 0.000000000000000000 ) ) ;
#14898=CARTESIAN_POINT ( 'NONE',  ( 5.082755093536325930, 20.53124999795161543, -5.082755093536325930 ) ) ;
#14901=ORIENTED_EDGE ( 'NONE', *, *, #10880, .F. ) ;
#14907=CARTESIAN_POINT ( 'NONE',  ( 4.401442555609581635E-16, 3.843749997951610098, -7.188101187500000044 ) ) ;
#14910=CARTESIAN_POINT ( 'NONE',  ( 5.082755093536325930, 1.031249997951609876, -5.082755093536325930 ) ) ;
#14924=CARTESIAN_POINT ( 'NONE',  ( 7.188101187500000933, 9.562499997951608322, -2.977408999572650483 ) ) ;
#14928=CARTESIAN_POINT ( 'NONE',  ( 5.082755093536325042, 114.9687500020483810, -5.082755093536325930 ) ) ;
#14943=DIRECTION ( 'NONE',  ( -0.000000000000000000, 1.000000000000000000, -0.000000000000000000 ) ) ;
#14945=CARTESIAN_POINT ( 'NONE',  ( 8.000000000000000000, 92.84375000000000000, -3.313708498984762496 ) ) ;
#14970=CARTESIAN_POINT ( 'NONE',  ( 2.977408999572650927, 20.24999999795161898, -7.188101187500001821 ) ) ;
#15006=( BOUNDED_CURVE ( )  B_SPLINE_CURVE ( 2, ( #20255, #38380, #55740, #66665, #43276, #38008, #10078, #71943, #4419 ),
 .UNSPECIFIED., .F., .F. ) 
 B_SPLINE_CURVE_WITH_KNOTS ( ( 3, 2, 2, 2, 3 ),
 ( 0.4062499999999998890, 0.4114583333333332038, 0.4166666666666666297, 0.4218749999999999445, 0.4270833333333332593 ),
 .UNSPECIFIED. ) 
 CURVE ( )  GEOMETRIC_REPRESENTATION_ITEM ( )  RATIONAL_B_SPLINE_CURVE ( ( 1.000000000000001554, 0.9238795325112850731, 1.000000000000000000, 0.9238795325112867385, 1.000000000000000000, 0.9238795325112867385, 1.000000000000000000, 0.9238795325112875156, 0.9999999999999992228 ) ) 
 REPRESENTATION_ITEM ( '' )  );
#15010=CARTESIAN_POINT ( 'NONE',  ( -3.313708498984762496, 89.46875000409677625, 7.999999999999998224 ) ) ;
#15022=CARTESIAN_POINT ( 'NONE',  ( 1.320432766682874540E-15, 94.53125000204836681, 7.188101187500000044 ) ) ;
#15029=CARTESIAN_POINT ( 'NONE',  ( 1.469576158976823947E-15, 101.5625000040967763, 8.000000000000000000 ) ) ;
#15044=CARTESIAN_POINT ( 'NONE',  ( 8.000000000000000000, 7.406249995903221972, -3.313708498984761608 ) ) ;
#15046=CARTESIAN_POINT ( 'NONE',  ( 7.188101187499999156, 12.74999999795161187, 2.977408999572654924 ) ) ;
#15050=CARTESIAN_POINT ( 'NONE',  ( 7.188101187500000933, 107.3750000020483952, -2.977408999572651371 ) ) ;
#15052=LINE ( 'NONE', #20716, #67926 ) ;
#15066=LINE ( 'NONE', #3766, #41975 ) ;
#15067=CARTESIAN_POINT ( 'NONE',  ( 3.313708498984802020, 25.59374999590322375, -7.999999999999958256 ) ) ;
#15068=CARTESIAN_POINT ( 'NONE',  ( 5.082755093536326818, 97.71875000204838102, 5.082755093536325042 ) ) ;
#15074=CARTESIAN_POINT ( 'NONE',  ( 7.188101187500000044, 104.2812500020483810, -8.802885111219163269E-16 ) ) ;
#15085=CARTESIAN_POINT ( 'NONE',  ( -7.188101187500002709, 3.187499997951610542, 2.977408999572649151 ) ) ;
#15091=EDGE_CURVE ( 'NONE', #3980, #832, #35082, .T. ) ;
#15092=CARTESIAN_POINT ( 'NONE',  ( 4.898587196589412829E-16, 1.687499995903220196, -8.000000000000000000 ) ) ;
#15096=ADVANCED_FACE ( 'NONE', ( #28258 ), #73905, .F. ) ;
#15101=CARTESIAN_POINT ( 'NONE',  ( -2.977408999572650039, 8.437499997951611874, -7.188101187500001821 ) ) ;
#15103=CARTESIAN_POINT ( 'NONE',  ( 5.656854249492379694, 115.6250000040967905, -5.656854249492380582 ) ) ;
#15108=VECTOR ( 'NONE', #1690, 1000.000000000000000 ) ;
#15113=ORIENTED_EDGE ( 'NONE', *, *, #34298, .F. ) ;
#15130=CARTESIAN_POINT ( 'NONE',  ( 1.469576158976823947E-15, 111.8750000000000000, 8.000000000000000000 ) ) ;
#15136=CARTESIAN_POINT ( 'NONE',  ( -5.656854249492379694, 21.37499999590322375, -5.656854249492380582 ) ) ;
#15143=CARTESIAN_POINT ( 'NONE',  ( -7.999999999999998224, 114.7812500040967763, 3.313708498984766049 ) ) ;
#15161=CARTESIAN_POINT ( 'NONE',  ( -2.977408999572650927, 114.8750000020483810, -7.188101187500000933 ) ) ;
#15168=CARTESIAN_POINT ( 'NONE',  ( 7.188101187500001821, 90.50000000204840944, -2.977408999572651371 ) ) ;
#15182=EDGE_CURVE ( 'NONE', #66596, #60057, #12023, .T. ) ;
#15186=EDGE_CURVE ( 'NONE', #31074, #4353, #39581, .T. ) ;
#15195=CARTESIAN_POINT ( 'NONE',  ( -1.320432766682874540E-15, 19.59374999795161543, 7.188101187500000044 ) ) ;
#15198=CARTESIAN_POINT ( 'NONE',  ( 5.082755093536325930, 17.53124999795161543, -5.082755093536325930 ) ) ;
#15201=DIRECTION ( 'NONE',  ( 0.000000000000000000, 0.000000000000000000, 1.000000000000000000 ) ) ;
#15219=CARTESIAN_POINT ( 'NONE',  ( 1.320432766682874540E-15, 94.90625000204838102, 7.188101187500000044 ) ) ;
#15233=CARTESIAN_POINT ( 'NONE',  ( 9.797174393178825657E-16, 125.0000000000000000, -8.000000000000000000 ) ) ;
#15247=CARTESIAN_POINT ( 'NONE',  ( 2.977408999572654480, 109.6250000020483952, 7.188101187499999156 ) ) ;
#15273=CARTESIAN_POINT ( 'NONE',  ( -2.977408999572650039, 19.31249999795161543, -7.188101187500000933 ) ) ;
#15280=CARTESIAN_POINT ( 'NONE',  ( 2.977408999572650927, 3.749999997951610542, -7.188101187500001821 ) ) ;
#15297=CARTESIAN_POINT ( 'NONE',  ( -1.320432766682874540E-15, 10.59374999795161187, 7.188101187500000044 ) ) ;
#15302=CARTESIAN_POINT ( 'NONE',  ( -7.188101187499999156, 109.6250000020483952, 2.977408999572654924 ) ) ;
#15315=DIRECTION ( 'NONE',  ( -0.000000000000000000, 1.000000000000000000, -0.000000000000000000 ) ) ;
#15316=CARTESIAN_POINT ( 'NONE',  ( -5.656854249492378806, 96.68750000000000000, 5.656854249492381470 ) ) ;
#15343=CARTESIAN_POINT ( 'NONE',  ( -5.082755093536325042, 19.03124999795161543, -5.082755093536325930 ) ) ;
#15348=DIRECTION ( 'NONE',  ( -0.000000000000000000, 1.000000000000000000, -0.000000000000000000 ) ) ;
#15354=CARTESIAN_POINT ( 'NONE',  ( -4.898587196589412829E-16, 121.8125000040967763, -8.000000000000000000 ) ) ;
#15359=EDGE_CURVE ( 'NONE', #24466, #32974, #35785, .T. ) ;
#15370=CARTESIAN_POINT ( 'NONE',  ( -1.469576158976823947E-15, 21.93749999590322375, 8.000000000000000000 ) ) ;
#15375=EDGE_CURVE ( 'NONE', #62362, #30042, #52760, .T. ) ;
#15380=CARTESIAN_POINT ( 'NONE',  ( -3.313708498984765161, 14.53125000000000178, 7.999999999999998224 ) ) ;
#15382=CARTESIAN_POINT ( 'NONE',  ( -5.656854249492380582, 92.00000000409677625, -5.656854249492380582 ) ) ;
#15390=CARTESIAN_POINT ( 'NONE',  ( 9.797174393178825657E-16, 125.0000000000000000, -8.000000000000000000 ) ) ;
#15393=CARTESIAN_POINT ( 'NONE',  ( -2.977408999572651815, 94.43750000204838102, 7.188101187500000933 ) ) ;
#15412=CARTESIAN_POINT ( 'NONE',  ( 3.313708498984762052, 9.093749995903223748, -8.000000000000000000 ) ) ;
#15415=AXIS2_PLACEMENT_3D ( 'NONE', #50881, #33932, #55438 ) ;
#15416=CARTESIAN_POINT ( 'NONE',  ( 7.188101187499999156, 15.74999999795161543, 2.977408999572654924 ) ) ;
#15418=DIRECTION ( 'NONE',  ( -0.000000000000000000, 1.000000000000000000, -0.000000000000000000 ) ) ;
#15419=CARTESIAN_POINT ( 'NONE',  ( -2.977408999572650927, 103.2500000020483810, -7.188101187500000933 ) ) ;
#15427=CARTESIAN_POINT ( 'NONE',  ( 5.656854249492378806, 20.81250000000000355, 5.656854249492381470 ) ) ;
#15432=CARTESIAN_POINT ( 'NONE',  ( -8.000000000000000000, 19.96874999590322020, -3.313708498984762496 ) ) ;
#15439=CARTESIAN_POINT ( 'NONE',  ( 7.188101187500002709, 102.3125000020483952, 2.977408999572649151 ) ) ;
#15447=CARTESIAN_POINT ( 'NONE',  ( 2.977408999572650039, 103.0625000020483810, -7.188101187500001821 ) ) ;
#15466=CARTESIAN_POINT ( 'NONE',  ( 7.594050593750000466, 0.2343749989758049379, 0.000000000000000000 ) ) ;
#15469=ADVANCED_FACE ( 'NONE', ( #59171 ), #30849, .T. ) ;
#15474=CARTESIAN_POINT ( 'NONE',  ( -5.082755093536325042, 11.53124999795161010, -5.082755093536325930 ) ) ;
#15475=CARTESIAN_POINT ( 'NONE',  ( -8.000000000000000000, 110.1875000040967905, 0.000000000000000000 ) ) ;
#15500=EDGE_CURVE ( 'NONE', #17357, #31653, #69449, .T. ) ;
#15502=CARTESIAN_POINT ( 'NONE',  ( 3.313708498984765161, 107.4687500000000000, 7.999999999999998224 ) ) ;
#15508=CARTESIAN_POINT ( 'NONE',  ( -5.656854249492379694, 18.37499999590322020, -5.656854249492380582 ) ) ;
#15510=CARTESIAN_POINT ( 'NONE',  ( 5.082755093536326818, 119.0937500020483810, 5.082755093536325042 ) ) ;
#15522=CARTESIAN_POINT ( 'NONE',  ( -8.000000000000001776, 26.15624999590322730, 3.313708498984759387 ) ) ;
#15531=CARTESIAN_POINT ( 'NONE',  ( -5.082755093536324154, 118.3437500020483810, 5.082755093536326818 ) ) ;
#15537=CARTESIAN_POINT ( 'NONE',  ( -2.977408999572650927, 121.2500000020483952, -7.188101187500001821 ) ) ;
#15552=( BOUNDED_CURVE ( )  B_SPLINE_CURVE ( 2, ( #65048, #42407, #65425, #29996, #69620, #41685, #30729, #12270, #12633 ),
 .UNSPECIFIED., .F., .F. ) 
 B_SPLINE_CURVE_WITH_KNOTS ( ( 3, 2, 2, 2, 3 ),
 ( 0.5138888888888888395, 0.5208333333333333703, 0.5277777777777777901, 0.5347222222222222099, 0.5416666666666666297 ),
 .UNSPECIFIED. ) 
 CURVE ( )  GEOMETRIC_REPRESENTATION_ITEM ( )  RATIONAL_B_SPLINE_CURVE ( ( 1.000000000000000000, 0.9238795325112867385, 1.000000000000000000, 0.9238795325112867385, 1.000000000000000000, 0.9238795325112867385, 1.000000000000000000, 0.9238795325112867385, 1.000000000000000000 ) ) 
 REPRESENTATION_ITEM ( '' )  );
#15562=CARTESIAN_POINT ( 'NONE',  ( 7.188101187499999156, 18.37499999795161187, 2.977408999572654924 ) ) ;
#15565=CARTESIAN_POINT ( 'NONE',  ( 7.188101187499999156, 17.24999999795162253, 2.977408999572654924 ) ) ;
#15570=CARTESIAN_POINT ( 'NONE',  ( 0.000000000000000000, 125.0000000000000000, 0.000000000000000000 ) ) ;
#15579=CARTESIAN_POINT ( 'NONE',  ( 3.313708498984815343, 94.71875000409676204, -7.999999999999944933 ) ) ;
#15591=CARTESIAN_POINT ( 'NONE',  ( 2.977408999572650039, 97.06250000204838102, -7.188101187500001821 ) ) ;
#15600=CARTESIAN_POINT ( 'NONE',  ( 4.898587196589412829E-16, 22.87500000000000355, -8.000000000000000000 ) ) ;
#15611=CARTESIAN_POINT ( 'NONE',  ( 1.469576158976823947E-15, 109.0625000040967905, 8.000000000000000000 ) ) ;
#15620=CARTESIAN_POINT ( 'NONE',  ( 5.082755093536326818, 103.7187500020483810, 5.082755093536325042 ) ) ;
#15645=CARTESIAN_POINT ( 'NONE',  ( -7.188101187500000044, 18.09374999795161187, -8.802885111219163269E-16 ) ) ;
#15648=ORIENTED_EDGE ( 'NONE', *, *, #25302, .T. ) ;
#15654=CARTESIAN_POINT ( 'NONE',  ( -2.977408999572654480, 4.499999997951610986, 7.188101187499999156 ) ) ;
#15657=CARTESIAN_POINT ( 'NONE',  ( -2.977408999572650039, 1.312499997951610098, -7.188101187500001821 ) ) ;
#15670=EDGE_CURVE ( 'NONE', #4192, #61043, #15006, .T. ) ;
#15674=CARTESIAN_POINT ( 'NONE',  ( -2.977408999572654480, 10.49999999795161010, 7.188101187499999156 ) ) ;
#15679=CARTESIAN_POINT ( 'NONE',  ( -2.977408999572650927, 110.7500000020483668, -7.188101187500001821 ) ) ;
#15682=CARTESIAN_POINT ( 'NONE',  ( -8.000000000000000000, 111.5937500040967905, -3.313708498984761164 ) ) ;
#15695=CARTESIAN_POINT ( 'NONE',  ( 5.656854249492381470, 94.06250000000000000, 5.656854249492379694 ) ) ;
#15701=FACE_OUTER_BOUND ( 'NONE', #69866, .T. ) ;
#15703=CARTESIAN_POINT ( 'NONE',  ( -8.000000000000000000, 20.15625000000000355, -3.313708498984762496 ) ) ;
#15704=EDGE_CURVE ( 'NONE', #69862, #4108, #44036, .T. ) ;
#15708=DIRECTION ( 'NONE',  ( -0.000000000000000000, 1.000000000000000000, -0.000000000000000000 ) ) ;
#15716=FACE_OUTER_BOUND ( 'NONE', #42555, .T. ) ;
#15717=CARTESIAN_POINT ( 'NONE',  ( -7.188101187500000044, 17.71874999795161187, -8.802885111219163269E-16 ) ) ;
#15740=ORIENTED_EDGE ( 'NONE', *, *, #40052, .T. ) ;
#15750=CARTESIAN_POINT ( 'NONE',  ( -5.656854249492379694, 14.06250000000000178, -5.656854249492380582 ) ) ;
#15754=CARTESIAN_POINT ( 'NONE',  ( 5.656854249492381470, 89.75000000409677625, 5.656854249492379694 ) ) ;
#15767=CARTESIAN_POINT ( 'NONE',  ( 2.977408999572654480, 91.62500000204838102, 7.188101187499999156 ) ) ;
#15768=CYLINDRICAL_SURFACE ( 'NONE', #72358, 8.000000000000000000 ) ;
#15772=( BOUNDED_CURVE ( )  B_SPLINE_CURVE ( 2, ( #33092, #62103, #44759, #49668, #10426, #56089, #16066, #20612, #67772 ),
 .UNSPECIFIED., .F., .F. ) 
 B_SPLINE_CURVE_WITH_KNOTS ( ( 3, 2, 2, 2, 3 ),
 ( 0.7187500000000001110, 0.7239583333333334814, 0.7291666666666667407, 0.7343750000000001110, 0.7395833333333334814 ),
 .UNSPECIFIED. ) 
 CURVE ( )  GEOMETRIC_REPRESENTATION_ITEM ( )  RATIONAL_B_SPLINE_CURVE ( ( 0.9999999999999983347, 0.9238795325112884038, 1.000000000000000000, 0.9238795325112867385, 1.000000000000000000, 0.9238795325112867385, 1.000000000000000000, 0.9238795325112850731, 1.000000000000001554 ) ) 
 REPRESENTATION_ITEM ( '' )  );
#15786=FACE_OUTER_BOUND ( 'NONE', #44299, .T. ) ;
#15790=CARTESIAN_POINT ( 'NONE',  ( -8.000000000000001776, 8.156249995903221972, 3.313708498984759387 ) ) ;
#15793=CARTESIAN_POINT ( 'NONE',  ( -2.977408999572650039, 17.81249999795161543, -7.188101187500001821 ) ) ;
#15796=CARTESIAN_POINT ( 'NONE',  ( 7.188101187500000933, 105.8750000020483668, -2.977408999572651371 ) ) ;
#15798=DIRECTION ( 'NONE',  ( 0.000000000000000000, 0.000000000000000000, 1.000000000000000000 ) ) ;
#15807=CARTESIAN_POINT ( 'NONE',  ( 4.898587196589412829E-16, 22.68749999590322375, -8.000000000000000000 ) ) ;
#15813=CARTESIAN_POINT ( 'NONE',  ( -5.082755093536324154, 100.3437500020483810, 5.082755093536326818 ) ) ;
#15819=CARTESIAN_POINT ( 'NONE',  ( 1.320432766682874540E-15, 102.4062500020483810, 7.188101187500000044 ) ) ;
#15832=CARTESIAN_POINT ( 'NONE',  ( 4.898587196589412829E-16, 9.375000000000001776, -8.000000000000000000 ) ) ;
#15845=CARTESIAN_POINT ( 'NONE',  ( -7.188101187500000044, 10.21874999795161187, -8.802885111219163269E-16 ) ) ;
#15846=CARTESIAN_POINT ( 'NONE',  ( -4.898587196589412829E-16, 111.3125000040967905, -8.000000000000000000 ) ) ;
#15863=ORIENTED_EDGE ( 'NONE', *, *, #44122, .T. ) ;
#15864=( BOUNDED_CURVE ( )  B_SPLINE_CURVE ( 2, ( #1120, #24831, #24473, #35079, #34710, #65194, #752, #58091, #35809 ),
 .UNSPECIFIED., .F., .F. ) 
 B_SPLINE_CURVE_WITH_KNOTS ( ( 3, 2, 2, 2, 3 ),
 ( 0.3472222222222222099, 0.3541666666666666852, 0.3611111111111111049, 0.3680555555555555802, 0.3750000000000000000 ),
 .UNSPECIFIED. ) 
 CURVE ( )  GEOMETRIC_REPRESENTATION_ITEM ( )  RATIONAL_B_SPLINE_CURVE ( ( 1.000000000000000000, 0.9238795325112867385, 1.000000000000000000, 0.9238795325112867385, 1.000000000000000000, 0.9238795325112867385, 1.000000000000000000, 0.9238795325112867385, 1.000000000000000000 ) ) 
 REPRESENTATION_ITEM ( '' )  );
#15873=CARTESIAN_POINT ( 'NONE',  ( 8.000000000000001776, 103.1562500000000142, 3.313708498984759387 ) ) ;
#15878=CARTESIAN_POINT ( 'NONE',  ( 8.000000000000000000, 19.50000000000000355, 0.000000000000000000 ) ) ;
#15881=CARTESIAN_POINT ( 'NONE',  ( -8.000000000000000000, 26.06249999590322375, -9.797174393178825657E-16 ) ) ;
#15883=CARTESIAN_POINT ( 'NONE',  ( 1.320432766682874540E-15, 123.4062500020483810, 7.188101187500000044 ) ) ;
#15897=ORIENTED_EDGE ( 'NONE', *, *, #37012, .F. ) ;
#15904=CARTESIAN_POINT ( 'NONE',  ( -5.082755093536324154, 116.8437500020483810, 5.082755093536326818 ) ) ;
#15910=CARTESIAN_POINT ( 'NONE',  ( 5.082755093536325042, 117.9687500020483810, -5.082755093536325930 ) ) ;
#15933=EDGE_LOOP ( 'NONE', ( #72455, #14381, #14341, #60762 ) ) ;
#15934=CARTESIAN_POINT ( 'NONE',  ( -1.320432766682874540E-15, 25.59374999795161543, 7.188101187500000044 ) ) ;
#15937=CARTESIAN_POINT ( 'NONE',  ( -5.082755093536326818, 18.28124999795161187, 5.082755093536325042 ) ) ;
#15942=EDGE_CURVE ( 'NONE', #64958, #9708, #67578, .T. ) ;
#15964=CARTESIAN_POINT ( 'NONE',  ( 7.188101187500001821, 90.87500000204838102, -2.977408999572651371 ) ) ;
#15973=CARTESIAN_POINT ( 'NONE',  ( 0.000000000000000000, 125.0000000000000000, 0.000000000000000000 ) ) ;
#15994=CARTESIAN_POINT ( 'NONE',  ( 2.977408999572650039, 104.1875000020483668, -7.188101187500001821 ) ) ;
#16007=ORIENTED_EDGE ( 'NONE', *, *, #26577, .T. ) ;
#16010=CARTESIAN_POINT ( 'NONE',  ( 4.898587196589412829E-16, 6.187499995903221084, -8.000000000000000000 ) ) ;
#16012=CARTESIAN_POINT ( 'NONE',  ( -5.656854249492381470, 18.74999999590322020, 5.656854249492379694 ) ) ;
#16020=CARTESIAN_POINT ( 'NONE',  ( 7.188101187500000933, 18.93749999795161543, -2.977408999572650483 ) ) ;
#16027=CARTESIAN_POINT ( 'NONE',  ( 7.188101187500001821, 11.06249999795161187, -2.977408999572650483 ) ) ;
#16030=CARTESIAN_POINT ( 'NONE',  ( 5.082755093536324154, 2.156249997951610098, 5.082755093536326818 ) ) ;
#16044=CARTESIAN_POINT ( 'NONE',  ( -2.977408999572654480, 11.99999999795161187, 7.188101187499999156 ) ) ;
#16049=CARTESIAN_POINT ( 'NONE',  ( -2.977408999572651815, 106.8125000020484094, 7.188101187500000933 ) ) ;
#16064=CARTESIAN_POINT ( 'NONE',  ( -8.000000000000000000, 91.90625000000000000, -3.313708498984761608 ) ) ;
#16066=CARTESIAN_POINT ( 'NONE',  ( 5.656854249492381470, 98.56250000000000000, 5.656854249492379694 ) ) ;
#16076=CARTESIAN_POINT ( 'NONE',  ( -4.401442555609581635E-16, 123.7812500020483810, -7.188101187500000044 ) ) ;
#16084=CARTESIAN_POINT ( 'NONE',  ( 4.401442555609581635E-16, 17.34374999795161187, -7.188101187500000044 ) ) ;
#16099=EDGE_CURVE ( 'NONE', #35953, #54549, #10183, .T. ) ;
#16103=( BOUNDED_CURVE ( )  B_SPLINE_CURVE ( 2, ( #33035, #3224, #26211, #9636, #48856, #72631, #26593, #49231, #20180 ),
 .UNSPECIFIED., .F., .F. ) 
 B_SPLINE_CURVE_WITH_KNOTS ( ( 3, 2, 2, 2, 3 ),
 ( 0.4062499999999998890, 0.4114583333333332038, 0.4166666666666666297, 0.4218749999999999445, 0.4270833333333332593 ),
 .UNSPECIFIED. ) 
 CURVE ( )  GEOMETRIC_REPRESENTATION_ITEM ( )  RATIONAL_B_SPLINE_CURVE ( ( 1.000000000000001554, 0.9238795325112850731, 1.000000000000000000, 0.9238795325112867385, 1.000000000000000000, 0.9238795325112867385, 1.000000000000000000, 0.9238795325112875156, 0.9999999999999992228 ) ) 
 REPRESENTATION_ITEM ( '' )  );
#16118=CARTESIAN_POINT ( 'NONE',  ( -1.469576158976823947E-15, 10.12500000000000178, 8.000000000000000000 ) ) ;
#16120=CARTESIAN_POINT ( 'NONE',  ( -8.000000000000000000, 93.59375000409679046, -3.313708498984761608 ) ) ;
#16129=CARTESIAN_POINT ( 'NONE',  ( -4.401442555609581635E-16, 93.78125000204836681, -7.188101187500000044 ) ) ;
#16138=ORIENTED_EDGE ( 'NONE', *, *, #15186, .T. ) ;
#16147=CARTESIAN_POINT ( 'NONE',  ( -8.000000000000000000, 114.4999999999999858, 0.000000000000000000 ) ) ;
#16148=CARTESIAN_POINT ( 'NONE',  ( 3.313708498984815343, 102.0312499999999574, -7.999999999999944933 ) ) ;
#16150=CARTESIAN_POINT ( 'NONE',  ( 4.898587196589412829E-16, 10.68749999590322020, -8.000000000000000000 ) ) ;
#16154=CARTESIAN_POINT ( 'NONE',  ( 2.977408999572651815, 20.06249999795161543, 7.188101187500000933 ) ) ;
#16157=CARTESIAN_POINT ( 'NONE',  ( 7.188101187500002709, 102.6875000020483810, 2.977408999572649151 ) ) ;
#16174=CARTESIAN_POINT ( 'NONE',  ( 5.082755093536326818, 91.71875000204838102, 5.082755093536325042 ) ) ;
#16181=CARTESIAN_POINT ( 'NONE',  ( -4.401442555609581635E-16, 104.6562500020483810, -7.188101187500000044 ) ) ;
#16209=CARTESIAN_POINT ( 'NONE',  ( -1.320432766682874540E-15, 16.59374999795161543, 7.188101187500000044 ) ) ;
#16211=CARTESIAN_POINT ( 'NONE',  ( -8.000000000000000000, 107.1875000040967905, 0.000000000000000000 ) ) ;
#16222=CARTESIAN_POINT ( 'NONE',  ( 5.082755093536326818, 108.2187500020483810, 5.082755093536325042 ) ) ;
#16239=CARTESIAN_POINT ( 'NONE',  ( -8.000000000000000000, 106.9062500000000000, -3.313708498984761608 ) ) ;
#16242=CARTESIAN_POINT ( 'NONE',  ( 3.313708498984762496, 1.218750000000000222, 7.999999999999998224 ) ) ;
#16244=CARTESIAN_POINT ( 'NONE',  ( -1.320432766682874540E-15, 1.968749997951610320, 7.188101187500000044 ) ) ;
#16246=CARTESIAN_POINT ( 'NONE',  ( 7.188101187500002709, 123.6875000020483952, 2.977408999572649151 ) ) ;
#16250=CARTESIAN_POINT ( 'NONE',  ( -5.656854249492380582, 114.5000000040967763, -5.656854249492380582 ) ) ;
#16268=CARTESIAN_POINT ( 'NONE',  ( 5.082755093536325042, 117.5937500020483810, -5.082755093536325930 ) ) ;
#16273=CARTESIAN_POINT ( 'NONE',  ( 5.082755093536326818, 122.0937500020483952, 5.082755093536325042 ) ) ;
#16274=CARTESIAN_POINT ( 'NONE',  ( -8.000000000000000000, 13.96874999590322375, -3.313708498984762496 ) ) ;
#16288=VECTOR ( 'NONE', #66804, 1000.000000000000000 ) ;
#16297=CARTESIAN_POINT ( 'NONE',  ( 2.977408999572651815, 25.68749999795162253, 7.188101187500000933 ) ) ;
#16300=CARTESIAN_POINT ( 'NONE',  ( 2.977408999572651815, 17.06249999795161543, 7.188101187500000933 ) ) ;
#16301=EDGE_CURVE ( 'NONE', #49646, #54702, #61294, .T. ) ;
#16304=( BOUNDED_CURVE ( )  B_SPLINE_CURVE ( 2, ( #55568, #14425, #37459, #60457, #28000, #28368, #23079, #56305, #57055 ),
 .UNSPECIFIED., .F., .F. ) 
 B_SPLINE_CURVE_WITH_KNOTS ( ( 3, 2, 2, 2, 3 ),
 ( 0.5937500000000000000, 0.5989583333333333703, 0.6041666666666666297, 0.6093750000000000000, 0.6145833333333333703 ),
 .UNSPECIFIED. ) 
 CURVE ( )  GEOMETRIC_REPRESENTATION_ITEM ( )  RATIONAL_B_SPLINE_CURVE ( ( 1.000000000000000000, 0.9238795325112867385, 1.000000000000000000, 0.9238795325112867385, 1.000000000000000000, 0.9238795325112867385, 1.000000000000000000, 0.9238795325112867385, 1.000000000000000000 ) ) 
 REPRESENTATION_ITEM ( '' )  );
#16319=( BOUNDED_CURVE ( )  B_SPLINE_CURVE ( 2, ( #35652, #40564, #6973, #29982, #1333, #24315, #47326, #69608, #17923 ),
 .UNSPECIFIED., .F., .F. ) 
 B_SPLINE_CURVE_WITH_KNOTS ( ( 3, 2, 2, 2, 3 ),
 ( 0.4861111111111111049, 0.4930555555555555802, 0.5000000000000000000, 0.5069444444444444198, 0.5138888888888888395 ),
 .UNSPECIFIED. ) 
 CURVE ( )  GEOMETRIC_REPRESENTATION_ITEM ( )  RATIONAL_B_SPLINE_CURVE ( ( 1.000000000000000000, 0.9238795325112867385, 1.000000000000000000, 0.9238795325112867385, 1.000000000000000000, 0.9238795325112867385, 1.000000000000000000, 0.9238795325112867385, 1.000000000000000000 ) ) 
 REPRESENTATION_ITEM ( '' )  );
#16326=CARTESIAN_POINT ( 'NONE',  ( 8.000000000000000000, 124.3437500000000000, -3.313708498984762496 ) ) ;
#16330=CIRCLE ( 'NONE', #58547, 11.00000000000000000 ) ;
#16334=CARTESIAN_POINT ( 'NONE',  ( 8.000000000000000000, 13.31249999590322375, 0.000000000000000000 ) ) ;
#16354=CARTESIAN_POINT ( 'NONE',  ( -4.401442555609581635E-16, 101.2812500020483810, -7.188101187500000044 ) ) ;
#16365=CARTESIAN_POINT ( 'NONE',  ( -5.656854249492380582, 99.31250000000000000, -5.656854249492380582 ) ) ;
#16372=CARTESIAN_POINT ( 'NONE',  ( -5.656854249492379694, 18.37499999590322020, -5.656854249492380582 ) ) ;
#16381=CARTESIAN_POINT ( 'NONE',  ( -2.977408999572654480, 25.87499999795161543, 7.188101187499999156 ) ) ;
#16389=CARTESIAN_POINT ( 'NONE',  ( -2.977408999572650039, 9.937499997951610098, -7.188101187500001821 ) ) ;
#16393=CARTESIAN_POINT ( 'NONE',  ( -5.082755093536325042, 2.906249997951610542, -5.082755093536325930 ) ) ;
#16397=CIRCLE ( 'NONE', #46507, 8.000000000000000000 ) ;
#16408=CARTESIAN_POINT ( 'NONE',  ( 4.898587196589412829E-16, 21.37500000000000355, -8.000000000000000000 ) ) ;
#16411=CARTESIAN_POINT ( 'NONE',  ( 7.188101187500000044, 10.96874999795161187, 0.000000000000000000 ) ) ;
#16415=CARTESIAN_POINT ( 'NONE',  ( 7.188101187500000044, 104.2812500020483810, -8.802885111219163269E-16 ) ) ;
#16418=DIRECTION ( 'NONE',  ( 0.000000000000000000, 0.000000000000000000, 1.000000000000000000 ) ) ;
#16446=CARTESIAN_POINT ( 'NONE',  ( 7.188101187500000044, 121.9062500020483810, -8.802885111219163269E-16 ) ) ;
#16454=EDGE_CURVE ( 'NONE', #832, #2971, #72421, .T. ) ;
#16456=CARTESIAN_POINT ( 'NONE',  ( -2.977408999572654480, 25.49999999795161898, 7.188101187499999156 ) ) ;
#16474=DIRECTION ( 'NONE',  ( -0.000000000000000000, 1.000000000000000000, -0.000000000000000000 ) ) ;
#16477=CARTESIAN_POINT ( 'NONE',  ( -7.188101187500000933, 7.499999997951610986, -2.977408999572651371 ) ) ;
#16478=EDGE_CURVE ( 'NONE', #50841, #28168, #11478, .T. ) ;
#16483=CARTESIAN_POINT ( 'NONE',  ( -5.656854249492379694, 1.874999995903220196, -5.656854249492380582 ) ) ;
#16492=CARTESIAN_POINT ( 'NONE',  ( 3.313708498984762496, 19.21875000000000000, 7.999999999999998224 ) ) ;
#16496=CARTESIAN_POINT ( 'NONE',  ( -3.313708498984762496, 92.46875000409679046, 7.999999999999998224 ) ) ;
#16499=ORIENTED_EDGE ( 'NONE', *, *, #14841, .F. ) ;
#16515=ORIENTED_EDGE ( 'NONE', *, *, #60484, .T. ) ;
#16527=CARTESIAN_POINT ( 'NONE',  ( 5.656854249492378806, 10.12499999590322020, 5.656854249492381470 ) ) ;
#16528=VERTEX_POINT ( 'NONE', #59723 ) ;
#16530=CARTESIAN_POINT ( 'NONE',  ( 5.082755093536324154, 17.15624999795161543, 5.082755093536326818 ) ) ;
#16533=CARTESIAN_POINT ( 'NONE',  ( -7.188101187499999156, 102.1250000020483810, 2.977408999572654924 ) ) ;
#16551=CARTESIAN_POINT ( 'NONE',  ( 1.320432766682874540E-15, 94.53125000204836681, 7.188101187500000044 ) ) ;
#16558=CARTESIAN_POINT ( 'NONE',  ( -7.188101187500001821, 104.9375000020483810, -2.977408999572650483 ) ) ;
#16575=ORIENTED_EDGE ( 'NONE', *, *, #47622, .T. ) ;
#16580=ORIENTED_EDGE ( 'NONE', *, *, #1596, .T. ) ;
#16584=CARTESIAN_POINT ( 'NONE',  ( -2.977408999572650039, 14.43749999795161365, -7.188101187500001821 ) ) ;
#16585=CARTESIAN_POINT ( 'NONE',  ( -3.313708498984762496, 111.9687500040967905, 7.999999999999998224 ) ) ;
#16593=CARTESIAN_POINT ( 'NONE',  ( -5.082755093536325930, 102.9687500020483810, -5.082755093536325930 ) ) ;
#16598=ADVANCED_FACE ( 'NONE', ( #59358 ), #65372, .T. ) ;
#16612=CARTESIAN_POINT ( 'NONE',  ( 5.656854249492381470, 104.5625000000000000, 5.656854249492379694 ) ) ;
#16616=CARTESIAN_POINT ( 'NONE',  ( 5.656854249492378806, 1.312500000000000222, 5.656854249492381470 ) ) ;
#16618=CARTESIAN_POINT ( 'NONE',  ( 7.188101187500001821, 2.437499997951610542, -2.977408999572650483 ) ) ;
#16620=CARTESIAN_POINT ( 'NONE',  ( -2.977408999572650927, 124.2500000020484094, -7.188101187500000933 ) ) ;
#16641=CARTESIAN_POINT ( 'NONE',  ( -5.082755093536324154, 109.3437500020483810, 5.082755093536326818 ) ) ;
#16646=CARTESIAN_POINT ( 'NONE',  ( -7.188101187500000044, 123.0312500020483810, 0.000000000000000000 ) ) ;
#16647=CARTESIAN_POINT ( 'NONE',  ( -5.656854249492378806, 120.8750000040967905, 5.656854249492381470 ) ) ;
#16660=( BOUNDED_CURVE ( )  B_SPLINE_CURVE ( 2, ( #2831, #27321, #4331, #61296, #3966 ),
 .UNSPECIFIED., .F., .F. ) 
 B_SPLINE_CURVE_WITH_KNOTS ( ( 3, 2, 3 ),
 ( 0.9861111111111110494, 0.9930555555555555802, 1.000000000000000000 ),
 .UNSPECIFIED. ) 
 CURVE ( )  GEOMETRIC_REPRESENTATION_ITEM ( )  RATIONAL_B_SPLINE_CURVE ( ( 1.000000000000001110, 0.9238795325112855172, 1.000000000000000000, 0.9238795325112867385, 1.000000000000000000 ) ) 
 REPRESENTATION_ITEM ( '' )  );
#16661=AXIS2_PLACEMENT_3D ( 'NONE', #11270, #62946, #11640 ) ;
#16667=ORIENTED_EDGE ( 'NONE', *, *, #21816, .F. ) ;
#16671=CARTESIAN_POINT ( 'NONE',  ( -7.188101187500001821, 25.12499999795161187, -2.977408999572651371 ) ) ;
#16672=CARTESIAN_POINT ( 'NONE',  ( -3.313708498984762496, 107.2812500000000000, 7.999999999999998224 ) ) ;
#16675=CARTESIAN_POINT ( 'NONE',  ( -7.188101187500000044, 21.09374999795161543, -8.802885111219163269E-16 ) ) ;
#16693=CARTESIAN_POINT ( 'NONE',  ( 0.000000000000000000, 125.0000000000000000, 8.000000000000000000 ) ) ;
#16698=CARTESIAN_POINT ( 'NONE',  ( -3.313708498984762052, 121.7187500000000000, -8.000000000000000000 ) ) ;
#16707=CARTESIAN_POINT ( 'NONE',  ( 3.313708498984762496, 5.531249995903220196, 7.999999999999998224 ) ) ;
#16713=CARTESIAN_POINT ( 'NONE',  ( 4.898587196589412829E-16, 7.687499995903221084, -8.000000000000000000 ) ) ;
#16717=EDGE_LOOP ( 'NONE', ( #66935, #23934, #61245, #21597 ) ) ;
#16730=CARTESIAN_POINT ( 'NONE',  ( -7.188101187500001821, 104.5625000020483668, -2.977408999572650483 ) ) ;
#16733=CARTESIAN_POINT ( 'NONE',  ( 7.454948327196666114, 0.2228442467353887457, -2.032657377778160690 ) ) ;
#16750=ORIENTED_EDGE ( 'NONE', *, *, #9011, .F. ) ;
#16751=CARTESIAN_POINT ( 'NONE',  ( 3.313708498984706985, 106.7187500040967763, -8.000000000000055067 ) ) ;
#16755=CARTESIAN_POINT ( 'NONE',  ( 7.188101187500000044, 26.34374999795161543, 0.000000000000000000 ) ) ;
#16759=ORIENTED_EDGE ( 'NONE', *, *, #15704, .T. ) ;
#16764=CARTESIAN_POINT ( 'NONE',  ( -7.188101187500001821, 7.124999997951610098, -2.977408999572651371 ) ) ;
#16767=CARTESIAN_POINT ( 'NONE',  ( 7.188101187500001821, 3.937499997951610986, -2.977408999572650483 ) ) ;
#16773=FACE_OUTER_BOUND ( 'NONE', #26116, .T. ) ;
#16784=CARTESIAN_POINT ( 'NONE',  ( -7.188101187500000933, 17.62499999795161187, -2.977408999572651371 ) ) ;
#16788=CARTESIAN_POINT ( 'NONE',  ( -2.977408999572650927, 104.7500000020483810, -7.188101187500001821 ) ) ;
#16798=DIRECTION ( 'NONE',  ( -0.000000000000000000, -1.000000000000000000, -0.000000000000000000 ) ) ;
#16814=APPLICATION_CONTEXT ( 'automotive_design' ) ;
#16820=CARTESIAN_POINT ( 'NONE',  ( 5.082755093536326818, 121.7187500020483952, 5.082755093536325042 ) ) ;
#16830=CARTESIAN_POINT ( 'NONE',  ( -2.977408999572654480, 26.99999999795161187, 7.188101187499999156 ) ) ;
#16853=CARTESIAN_POINT ( 'NONE',  ( -1.320432766682874540E-15, 6.468749997951610098, 7.188101187500000044 ) ) ;
#16858=CARTESIAN_POINT ( 'NONE',  ( 8.000000000000000000, 115.5312500040968047, -3.313708498984762496 ) ) ;
#16868=CARTESIAN_POINT ( 'NONE',  ( -5.656854249492381470, 18.93750000000000355, 5.656854249492379694 ) ) ;
#16872=CARTESIAN_POINT ( 'NONE',  ( -4.898587196589412829E-16, 88.81250000409677625, -8.000000000000000000 ) ) ;
#16888=CARTESIAN_POINT ( 'NONE',  ( -2.977408999572650927, 122.7500000020483952, -7.188101187500001821 ) ) ;
#16905=CARTESIAN_POINT ( 'NONE',  ( -3.313708498984770934, 2.531250000000000000, 7.999999999999992895 ) ) ;
#16915=CARTESIAN_POINT ( 'NONE',  ( 5.082755093536324154, 18.65624999795161187, 5.082755093536326818 ) ) ;
#16918=CARTESIAN_POINT ( 'NONE',  ( -4.401442555609581635E-16, 106.1562500020483810, -7.188101187500000044 ) ) ;
#16935=CARTESIAN_POINT ( 'NONE',  ( -5.082755093536324154, 92.84375000204838102, 5.082755093536326818 ) ) ;
#16942=CARTESIAN_POINT ( 'NONE',  ( 5.082755093536325042, 98.46875000204838102, -5.082755093536325930 ) ) ;
#16955=CARTESIAN_POINT ( 'NONE',  ( 3.313708498984761608, 9.281250000000001776, -8.000000000000000000 ) ) ;
#16960=AXIS2_PLACEMENT_3D ( 'NONE', #34221, #57222, #45888 ) ;
#16961=VERTEX_POINT ( 'NONE', #63434 ) ;
#16967=CARTESIAN_POINT ( 'NONE',  ( 7.188101187499999156, 12.37499999795161010, 2.977408999572654924 ) ) ;
#16968=CARTESIAN_POINT ( 'NONE',  ( -3.313708498984762052, 108.4062500040967905, -8.000000000000000000 ) ) ;
#16977=CARTESIAN_POINT ( 'NONE',  ( -7.188101187500001821, 106.0625000020483668, -2.977408999572650483 ) ) ;
#16979=CARTESIAN_POINT ( 'NONE',  ( 4.898587196589412829E-16, 15.18749999590322197, -8.000000000000000000 ) ) ;
#16982=ORIENTED_EDGE ( 'NONE', *, *, #12128, .T. ) ;
#16993=CARTESIAN_POINT ( 'NONE',  ( 5.656854249492381470, 106.0625000000000000, 5.656854249492379694 ) ) ;
#16999=CARTESIAN_POINT ( 'NONE',  ( 4.898587196589412829E-16, 25.68749999590322375, -8.000000000000000000 ) ) ;
#17002=CARTESIAN_POINT ( 'NONE',  ( -4.401442555609581635E-16, 119.6562500020483810, -7.188101187500000044 ) ) ;
#17009=CARTESIAN_POINT ( 'NONE',  ( 3.313708498984777595, 123.0312499999999858, -7.999999999999983125 ) ) ;
#17023=CARTESIAN_POINT ( 'NONE',  ( -2.977408999572652260, 113.9375000020483952, 7.188101187500000044 ) ) ;
#17028=CARTESIAN_POINT ( 'NONE',  ( -7.188101187500000044, 121.5312500020483810, 0.000000000000000000 ) ) ;
#17055=CARTESIAN_POINT ( 'NONE',  ( 7.188101187499999156, 24.37499999795161543, 2.977408999572654924 ) ) ;
#17059=CARTESIAN_POINT ( 'NONE',  ( 5.082755093536324154, 23.15624999795161543, 5.082755093536326818 ) ) ;
#17070=CARTESIAN_POINT ( 'NONE',  ( 7.594050593750000466, 28.07812499692741781, 0.000000000000000000 ) ) ;
#17074=EDGE_LOOP ( 'NONE', ( #18934, #28969, #61545, #34280 ) ) ;
#17082=CARTESIAN_POINT ( 'NONE',  ( 1.469576158976823947E-15, 123.8750000000000000, 8.000000000000000000 ) ) ;
#17104=DIRECTION ( 'NONE',  ( 0.000000000000000000, 0.000000000000000000, 1.000000000000000000 ) ) ;
#17107=DIRECTION ( 'NONE',  ( 0.000000000000000000, 0.000000000000000000, 1.000000000000000000 ) ) ;
#17113=CARTESIAN_POINT ( 'NONE',  ( 5.082755093536326818, 100.7187500020483810, 5.082755093536325042 ) ) ;
#17127=CARTESIAN_POINT ( 'NONE',  ( 3.313708498984761608, 4.781250000000000888, -8.000000000000000000 ) ) ;
#17130=CARTESIAN_POINT ( 'NONE',  ( -7.999999999999998224, 101.0937500000000142, 3.313708498984766049 ) ) ;
#17137=CARTESIAN_POINT ( 'NONE',  ( -5.082755093536326818, 27.28124999795161543, 5.082755093536325042 ) ) ;
#17141=LINE ( 'NONE', #52234, #762 ) ;
#17148=CARTESIAN_POINT ( 'NONE',  ( -1.320432766682874540E-15, 7.593749997951611874, 7.188101187500000044 ) ) ;
#17151=CARTESIAN_POINT ( 'NONE',  ( 5.082755093536325930, 7.031249997951610986, -5.082755093536325930 ) ) ;
#17168=CARTESIAN_POINT ( 'NONE',  ( 7.188101187500000933, 20.06249999795161543, -2.977408999572650483 ) ) ;
#17171=CARTESIAN_POINT ( 'NONE',  ( 7.188101187500002709, 105.6875000020483952, 2.977408999572649151 ) ) ;
#17194=ORIENTED_EDGE ( 'NONE', *, *, #45223, .F. ) ;
#17202=CARTESIAN_POINT ( 'NONE',  ( -2.977408999572650927, 123.8750000020483810, -7.188101187500001821 ) ) ;
#17211=CARTESIAN_POINT ( 'NONE',  ( 7.188101187499999156, 25.87499999795161543, 2.977408999572654924 ) ) ;
#17232=CARTESIAN_POINT ( 'NONE',  ( -7.188101187500002709, 4.687499997951610986, 2.977408999572649151 ) ) ;
#17248=CARTESIAN_POINT ( 'NONE',  ( 5.656854249492378806, 16.31250000000000355, 5.656854249492381470 ) ) ;
#17251=CARTESIAN_POINT ( 'NONE',  ( -2.977408999572650927, 120.8750000020483810, -7.188101187500001821 ) ) ;
#17260=CARTESIAN_POINT ( 'NONE',  ( -7.188101187500002709, 1.312499997951610098, 2.977408999572649151 ) ) ;
#17264=CARTESIAN_POINT ( 'NONE',  ( 7.188101187500000044, 122.2812500020483810, -8.802885111219163269E-16 ) ) ;
#17276=ORIENTED_EDGE ( 'NONE', *, *, #34100, .T. ) ;
#17290=CARTESIAN_POINT ( 'NONE',  ( 2.977408999572650927, 23.62499999795161543, -7.188101187500001821 ) ) ;
#17293=CARTESIAN_POINT ( 'NONE',  ( 7.188101187500000933, 99.87500000204838102, -2.977408999572651371 ) ) ;
#17302=CARTESIAN_POINT ( 'NONE',  ( 0.000000000000000000, 125.0000000000000000, 8.000000000000000000 ) ) ;
#17308=CARTESIAN_POINT ( 'NONE',  ( 2.977408999572654480, 91.62500000204836681, 7.188101187499999156 ) ) ;
#17314=CARTESIAN_POINT ( 'NONE',  ( 7.188101187500002709, 99.68750000204838102, 2.977408999572649151 ) ) ;
#17317=EDGE_CURVE ( 'NONE', #29688, #61043, #7951, .T. ) ;
#17332=EDGE_CURVE ( 'NONE', #22422, #61351, #4453, .T. ) ;
#17336=VERTEX_POINT ( 'NONE', #29954 ) ;
#17338=CARTESIAN_POINT ( 'NONE',  ( -2.977408999572654480, 11.99999999795161187, 7.188101187499999156 ) ) ;
#17339=CARTESIAN_POINT ( 'NONE',  ( -8.000000000000000000, 101.0937500040968047, -3.313708498984761608 ) ) ;
#17350=CARTESIAN_POINT ( 'NONE',  ( -8.000000000000000000, 24.75000000000000355, -9.797174393178825657E-16 ) ) ;
#17351=CARTESIAN_POINT ( 'NONE',  ( 2.977408999572650039, 105.6875000020483952, -7.188101187500001821 ) ) ;
#17353=CARTESIAN_POINT ( 'NONE',  ( -5.656854249492379694, 15.37499999590322197, -5.656854249492380582 ) ) ;
#17357=VERTEX_POINT ( 'NONE', #35260 ) ;
#17367=CARTESIAN_POINT ( 'NONE',  ( 5.656854249492381470, 100.0625000000000000, 5.656854249492379694 ) ) ;
#17370=CARTESIAN_POINT ( 'NONE',  ( -7.999999999999998224, 98.09375000000001421, 3.313708498984766049 ) ) ;
#17372=CARTESIAN_POINT ( 'NONE',  ( 5.656854249492378806, 25.12499999590322375, 5.656854249492381470 ) ) ;
#17376=CARTESIAN_POINT ( 'NONE',  ( -2.977408999572652260, 117.3125000020483952, 7.188101187500000044 ) ) ;
#17380=CARTESIAN_POINT ( 'NONE',  ( -8.000000000000000000, 90.50000000000000000, 0.000000000000000000 ) ) ;
#17395=CARTESIAN_POINT ( 'NONE',  ( 5.656854249492380582, 7.499999995903221084, -5.656854249492380582 ) ) ;
#17396=CARTESIAN_POINT ( 'NONE',  ( -2.977408999572650927, 110.3750000020484094, -7.188101187500000933 ) ) ;
#17402=CARTESIAN_POINT ( 'NONE',  ( 7.188101187500000044, 114.7812500020483952, -8.802885111219163269E-16 ) ) ;
#17403=CARTESIAN_POINT ( 'NONE',  ( -4.898587196589412829E-16, 120.3125000040967763, -8.000000000000000000 ) ) ;
#17414=CARTESIAN_POINT ( 'NONE',  ( -3.313708498984805573, 19.03125000000000000, 7.999999999999956479 ) ) ;
#17419=FACE_OUTER_BOUND ( 'NONE', #60494, .T. ) ;
#17427=CARTESIAN_POINT ( 'NONE',  ( 3.313708498984762052, 1.781250000000000444, -8.000000000000000000 ) ) ;
#17430=CARTESIAN_POINT ( 'NONE',  ( 7.188101187500001821, 21.93749999795161543, -2.977408999572650483 ) ) ;
#17431=CARTESIAN_POINT ( 'NONE',  ( 5.656854249492381470, 119.7500000040967905, 5.656854249492379694 ) ) ;
#17455=CARTESIAN_POINT ( 'NONE',  ( 8.000000000000001776, 124.1562499999999858, 3.313708498984759387 ) ) ;
#17464=CARTESIAN_POINT ( 'NONE',  ( -4.898587196589412829E-16, 97.62499999999998579, -8.000000000000000000 ) ) ;
#17490=CARTESIAN_POINT ( 'NONE',  ( 7.188101187500000044, 96.40625000204838102, -8.802885111219163269E-16 ) ) ;
#17507=CARTESIAN_POINT ( 'NONE',  ( -4.898587196589412829E-16, 117.3125000040967763, -8.000000000000000000 ) ) ;
#17514=CARTESIAN_POINT ( 'NONE',  ( -2.977408999572650039, 22.31249999795161543, -7.188101187500000933 ) ) ;
#17522=CARTESIAN_POINT ( 'NONE',  ( -7.188101187500000044, 10.21874999795161187, -8.802885111219163269E-16 ) ) ;
#17525=CARTESIAN_POINT ( 'NONE',  ( 7.188101187500001821, 6.937499997951610098, -2.977408999572650483 ) ) ;
#17537=CARTESIAN_POINT ( 'NONE',  ( 1.320432766682874540E-15, 117.0312500020483810, 7.188101187500000044 ) ) ;
#17542=CARTESIAN_POINT ( 'NONE',  ( -7.188101187500000044, 17.71874999795161187, -8.802885111219163269E-16 ) ) ;
#17547=CARTESIAN_POINT ( 'NONE',  ( -5.082755093536325930, 104.8437500020483810, -5.082755093536325930 ) ) ;
#17553=( BOUNDED_CURVE ( )  B_SPLINE_CURVE ( 2, ( #22669, #44958, #39297, #27975, #32912, #15522, #45688, #21188, #11367 ),
 .UNSPECIFIED., .F., .F. ) 
 B_SPLINE_CURVE_WITH_KNOTS ( ( 3, 2, 2, 2, 3 ),
 ( 0.9027777777777776791, 0.9097222222222220989, 0.9166666666666665186, 0.9236111111111110494, 0.9305555555555554692 ),
 .UNSPECIFIED. ) 
 CURVE ( )  GEOMETRIC_REPRESENTATION_ITEM ( )  RATIONAL_B_SPLINE_CURVE ( ( 1.000000000000001110, 0.9238795325112855172, 1.000000000000000000, 0.9238795325112867385, 1.000000000000000000, 0.9238795325112867385, 1.000000000000000000, 0.9238795325112879597, 0.9999999999999987788 ) ) 
 REPRESENTATION_ITEM ( '' )  );
#17562=CARTESIAN_POINT ( 'NONE',  ( -5.656854249492378806, 119.1875000000000000, 5.656854249492381470 ) ) ;
#17578=CARTESIAN_POINT ( 'NONE',  ( -7.188101187500000044, 124.1562500020483810, 0.000000000000000000 ) ) ;
#17585=ORIENTED_EDGE ( 'NONE', *, *, #56540, .T. ) ;
#17587=CARTESIAN_POINT ( 'NONE',  ( -3.979266480698733677, 0.4999999999999095723, -6.940132439340585435 ) ) ;
#17609=CARTESIAN_POINT ( 'NONE',  ( -7.188101187500000044, 7.593749997951610986, -8.802885111219163269E-16 ) ) ;
#17614=CARTESIAN_POINT ( 'NONE',  ( 1.469576158976823947E-15, 98.56250000409677625, 8.000000000000000000 ) ) ;
#17625=CARTESIAN_POINT ( 'NONE',  ( -3.313708498984765161, 20.53125000000001066, 7.999999999999998224 ) ) ;
#17626=ORIENTED_EDGE ( 'NONE', *, *, #12128, .F. ) ;
#17627=CARTESIAN_POINT ( 'NONE',  ( -7.188101187499999156, 121.2500000020483952, 2.977408999572654924 ) ) ;
#17633=CARTESIAN_POINT ( 'NONE',  ( 2.977408999572650927, 0.7499999979516099868, -7.188101187500000933 ) ) ;
#17637=FACE_OUTER_BOUND ( 'NONE', #66908, .T. ) ;
#17646=( BOUNDED_CURVE ( )  B_SPLINE_CURVE ( 2, ( #70129, #57326, #41079, #52402, #68629, #62968, #18436, #46360, #46726 ),
 .UNSPECIFIED., .F., .F. ) 
 B_SPLINE_CURVE_WITH_KNOTS ( ( 3, 2, 2, 2, 3 ),
 ( 0.3437499999999998335, 0.3489583333333331483, 0.3541666666666665186, 0.3593749999999998335, 0.3645833333333331483 ),
 .UNSPECIFIED. ) 
 CURVE ( )  GEOMETRIC_REPRESENTATION_ITEM ( )  RATIONAL_B_SPLINE_CURVE ( ( 1.000000000000002442, 0.9238795325112842960, 1.000000000000000000, 0.9238795325112867385, 1.000000000000000000, 0.9238795325112867385, 1.000000000000000000, 0.9238795325112891810, 0.9999999999999975575 ) ) 
 REPRESENTATION_ITEM ( '' )  );
#17664=CARTESIAN_POINT ( 'NONE',  ( -7.188101187500002709, 24.18749999795161543, 2.977408999572649151 ) ) ;
#17667=CARTESIAN_POINT ( 'NONE',  ( 1.320432766682874540E-15, 96.40625000204838102, 7.188101187500000044 ) ) ;
#17678=DIRECTION ( 'NONE',  ( -0.000000000000000000, 1.000000000000000000, -0.000000000000000000 ) ) ;
#17683=CARTESIAN_POINT ( 'NONE',  ( -7.188101187499999156, 94.25000000204838102, 2.977408999572654924 ) ) ;
#17689=CARTESIAN_POINT ( 'NONE',  ( 7.188101187500001821, 96.87500000204836681, -2.977408999572651371 ) ) ;
#17700=VECTOR ( 'NONE', #16798, 1000.000000000000000 ) ;
#17713=CARTESIAN_POINT ( 'NONE',  ( -4.898587196589412829E-16, 103.8125000040967763, -8.000000000000000000 ) ) ;
#17721=CARTESIAN_POINT ( 'NONE',  ( -8.000000000000001776, 24.84375000000000355, 3.313708498984759387 ) ) ;
#17722=CARTESIAN_POINT ( 'NONE',  ( -7.188101187500000044, 101.6562500020483810, 0.000000000000000000 ) ) ;
#17740=CARTESIAN_POINT ( 'NONE',  ( 5.656854249492381470, 103.0625000000000000, 5.656854249492379694 ) ) ;
#17748=CARTESIAN_POINT ( 'NONE',  ( -7.188101187500000044, 4.593749997951610098, -8.802885111219163269E-16 ) ) ;
#17751=CARTESIAN_POINT ( 'NONE',  ( 7.188101187500000933, 116.3750000020483810, -2.977408999572651371 ) ) ;
#17759=CARTESIAN_POINT ( 'NONE',  ( -8.000000000000001776, 9.843750000000000000, 3.313708498984759387 ) ) ;
#17771=CARTESIAN_POINT ( 'NONE',  ( 1.320432766682874540E-15, 114.0312500020483952, 7.188101187500000044 ) ) ;
#17779=CARTESIAN_POINT ( 'NONE',  ( 7.188101187500002709, 113.1875000020483810, 2.977408999572649151 ) ) ;
#17786=LINE ( 'NONE', #7217, #12487 ) ;
#17797=CARTESIAN_POINT ( 'NONE',  ( 0.000000000000000000, 125.0000000000000000, 0.000000000000000000 ) ) ;
#17803=EDGE_LOOP ( 'NONE', ( #37795, #38145, #30585, #47566, #37784 ) ) ;
#17805=CARTESIAN_POINT ( 'NONE',  ( -8.000000000000001776, 3.843750000000000888, 3.313708498984759387 ) ) ;
#17807=CARTESIAN_POINT ( 'NONE',  ( 4.401442555609581635E-16, 26.71874999795161543, -7.188101187500000044 ) ) ;
#17834=CARTESIAN_POINT ( 'NONE',  ( -3.313708498984762052, 118.7187499999999858, -8.000000000000000000 ) ) ;
#17839=CARTESIAN_POINT ( 'NONE',  ( -5.656854249492379694, 13.87499999590322375, -5.656854249492380582 ) ) ;
#17842=CARTESIAN_POINT ( 'NONE',  ( 5.656854249492381470, 97.06250000000000000, 5.656854249492379694 ) ) ;
#17852=ORIENTED_EDGE ( 'NONE', *, *, #42405, .T. ) ;
#17858=CARTESIAN_POINT ( 'NONE',  ( 3.313708498984761608, 4.593749995903220196, -8.000000000000000000 ) ) ;
#17859=CARTESIAN_POINT ( 'NONE',  ( -5.656854249492378806, 116.3750000040967905, 5.656854249492381470 ) ) ;
#17862=VECTOR ( 'NONE', #1724, 1000.000000000000000 ) ;
#17864=CARTESIAN_POINT ( 'NONE',  ( 5.082755093536325042, 95.09375000204838102, -5.082755093536325930 ) ) ;
#17867=CARTESIAN_POINT ( 'NONE',  ( 5.836461775160671550, 0.2934486527655157939, -5.189590606809809437 ) ) ;
#17879=VECTOR ( 'NONE', #31202, 1000.000000000000000 ) ;
#17883=ORIENTED_EDGE ( 'NONE', *, *, #27362, .T. ) ;
#17889=CARTESIAN_POINT ( 'NONE',  ( -5.082755093536325042, 22.40624999795161543, -5.082755093536325930 ) ) ;
#17899=CARTESIAN_POINT ( 'NONE',  ( 7.188101187500001821, 12.56249999795161365, -2.977408999572650483 ) ) ;
#17902=CARTESIAN_POINT ( 'NONE',  ( -5.082755093536325042, 7.406249997951610986, -5.082755093536325930 ) ) ;
#17915=CARTESIAN_POINT ( 'NONE',  ( -2.977408999572651815, 113.9375000020483952, 7.188101187500000933 ) ) ;
#17918=ORIENTED_EDGE ( 'NONE', *, *, #36982, .F. ) ;
#17920=CARTESIAN_POINT ( 'NONE',  ( 7.188101187500000933, 17.06249999795161543, -2.977408999572650483 ) ) ;
#17923=CARTESIAN_POINT ( 'NONE',  ( 4.898587196589412829E-16, 13.87500000000000178, -8.000000000000000000 ) ) ;
#17926=CARTESIAN_POINT ( 'NONE',  ( 7.188101187500000044, 99.78125000204838102, -8.802885111219163269E-16 ) ) ;
#17929=CARTESIAN_POINT ( 'NONE',  ( -8.000000000000000000, 89.18750000409677625, 0.000000000000000000 ) ) ;
#17954=CARTESIAN_POINT ( 'NONE',  ( 7.188101187500000044, 117.4062500020483810, -8.802885111219163269E-16 ) ) ;
#17967=CARTESIAN_POINT ( 'NONE',  ( -1.469576158976823947E-15, 25.12500000000000355, 8.000000000000000000 ) ) ;
#17984=CARTESIAN_POINT ( 'NONE',  ( 7.188101187499999156, 3.749999997951610542, 2.977408999572654924 ) ) ;
#17989=CARTESIAN_POINT ( 'NONE',  ( 5.656854249492381470, 98.75000000409677625, 5.656854249492379694 ) ) ;
#18000=ADVANCED_FACE ( 'NONE', ( #68735 ), #43497, .T. ) ;
#18003=CARTESIAN_POINT ( 'NONE',  ( -8.000000000000000000, 15.65625000000000355, -3.313708498984762496 ) ) ;
#18007=CARTESIAN_POINT ( 'NONE',  ( 2.977408999572650039, 123.6875000020484094, -7.188101187500001821 ) ) ;
#18016=CARTESIAN_POINT ( 'NONE',  ( -2.977408999572650927, 121.2500000020483952, -7.188101187500001821 ) ) ;
#18037=LINE ( 'NONE', #60522, #44093 ) ;
#18043=CARTESIAN_POINT ( 'NONE',  ( 4.401442555609581635E-16, 22.21874999795161543, -7.188101187500000044 ) ) ;
#18045=CARTESIAN_POINT ( 'NONE',  ( -7.188101187500000933, 100.4375000020483810, -2.977408999572650483 ) ) ;
#18061=CARTESIAN_POINT ( 'NONE',  ( 3.594044162775203777, 89.15552387383502264, -6.225081946264263699 ) ) ;
#18066=CARTESIAN_POINT ( 'NONE',  ( 2.977408999572650039, 97.06250000204838102, -7.188101187500001821 ) ) ;
#18077=ADVANCED_FACE ( 'NONE', ( #17419 ), #10654, .T. ) ;
#18091=CARTESIAN_POINT ( 'NONE',  ( 8.000000000000000000, 106.4375000040967763, -9.797174393178825657E-16 ) ) ;
#18101=CARTESIAN_POINT ( 'NONE',  ( 7.188101187500000044, 106.9062500020483810, -8.802885111219163269E-16 ) ) ;
#18119=CARTESIAN_POINT ( 'NONE',  ( 5.656854249492381470, 101.5625000000000000, 5.656854249492379694 ) ) ;
#18125=CARTESIAN_POINT ( 'NONE',  ( 7.188101187500001821, 6.937499997951610098, -2.977408999572650483 ) ) ;
#18128=CARTESIAN_POINT ( 'NONE',  ( 7.188101187500000044, 114.7812500020483952, -8.802885111219163269E-16 ) ) ;
#18149=CARTESIAN_POINT ( 'NONE',  ( 7.188101187500002709, 105.3125000020483810, 2.977408999572649151 ) ) ;
#18154=CARTESIAN_POINT ( 'NONE',  ( -2.977408999572651815, 117.3125000020483810, 7.188101187500000933 ) ) ;
#18160=DIRECTION ( 'NONE',  ( -0.000000000000000000, 1.000000000000000000, -0.000000000000000000 ) ) ;
#18167=CARTESIAN_POINT ( 'NONE',  ( 4.898587196589412829E-16, 15.37500000000000355, -8.000000000000000000 ) ) ;
#18171=AXIS2_PLACEMENT_3D ( 'NONE', #56461, #38744, #4402 ) ;
#18172=CARTESIAN_POINT ( 'NONE',  ( 8.000000000000000000, 20.90624999590322375, -3.313708498984761164 ) ) ;
#18178=ORIENTED_EDGE ( 'NONE', *, *, #62454, .T. ) ;
#18180=CARTESIAN_POINT ( 'NONE',  ( 3.313708498984762052, 7.781250000000001776, -8.000000000000000000 ) ) ;
#18182=CARTESIAN_POINT ( 'NONE',  ( 5.082755093536324154, 1.781249997951610098, 5.082755093536326818 ) ) ;
#18183=CARTESIAN_POINT ( 'NONE',  ( 8.000000000000000000, 120.0312500040967763, -3.313708498984762496 ) ) ;
#18192=VECTOR ( 'NONE', #40321, 1000.000000000000000 ) ;
#18195=EDGE_CURVE ( 'NONE', #2977, #45738, #19847, .T. ) ;
#18208=CARTESIAN_POINT ( 'NONE',  ( -3.313708498984762052, 120.2187500000000000, -8.000000000000000000 ) ) ;
#18215=CARTESIAN_POINT ( 'NONE',  ( 8.000000000000000000, 16.40624999590322375, -3.313708498984761608 ) ) ;
#18238=CARTESIAN_POINT ( 'NONE',  ( -2.977408999572650927, 99.87500000204838102, -7.188101187500001821 ) ) ;
#18251=CARTESIAN_POINT ( 'NONE',  ( 0.000000000000000000, 125.0000000000000000, 0.000000000000000000 ) ) ;
#18269=CARTESIAN_POINT ( 'NONE',  ( 2.977408999572651815, 16.68749999795161543, 7.188101187500000933 ) ) ;
#18272=CARTESIAN_POINT ( 'NONE',  ( 5.082755093536324154, 5.156249997951610098, 5.082755093536326818 ) ) ;
#18286=CARTESIAN_POINT ( 'NONE',  ( -7.188101187500000044, 113.6562500020483810, 0.000000000000000000 ) ) ;
#18290=CARTESIAN_POINT ( 'NONE',  ( 2.977408999572652260, 25.68749999795162253, 7.188101187500000044 ) ) ;
#18295=CARTESIAN_POINT ( 'NONE',  ( 7.188101187500002709, 102.6875000020483810, 2.977408999572649151 ) ) ;
#18303=AXIS2_PLACEMENT_3D ( 'NONE', #34075, #68746, #51026 ) ;
#18315=CARTESIAN_POINT ( 'NONE',  ( -5.656854249492378806, 117.6875000000000000, 5.656854249492381470 ) ) ;
#18320=CARTESIAN_POINT ( 'NONE',  ( 4.898587196589412829E-16, 10.87500000000000178, -8.000000000000000000 ) ) ;
#18325=CARTESIAN_POINT ( 'NONE',  ( -7.188101187499999156, 116.7500000020483810, 2.977408999572654924 ) ) ;
#18330=CARTESIAN_POINT ( 'NONE',  ( 4.898587196589412829E-16, 24.18749999590322375, -8.000000000000000000 ) ) ;
#18331=ORIENTED_EDGE ( 'NONE', *, *, #34911, .F. ) ;
#18357=CARTESIAN_POINT ( 'NONE',  ( -7.188101187500000044, 15.09374999795161187, -8.802885111219163269E-16 ) ) ;
#18375=CARTESIAN_POINT ( 'NONE',  ( -3.313708498984765161, 22.03125000000000355, 7.999999999999998224 ) ) ;
#18378=CARTESIAN_POINT ( 'NONE',  ( -5.082755093536325930, 123.9687500020483952, -5.082755093536325930 ) ) ;
#18385=CARTESIAN_POINT ( 'NONE',  ( 7.188101187500000044, 1.968749997951610320, 0.000000000000000000 ) ) ;
#18389=CARTESIAN_POINT ( 'NONE',  ( 2.977408999572654480, 120.5000000020483810, 7.188101187499999156 ) ) ;
#18399=CARTESIAN_POINT ( 'NONE',  ( 8.000000000000000000, 104.9375000040967763, -9.797174393178825657E-16 ) ) ;
#18414=CARTESIAN_POINT ( 'NONE',  ( 2.977408999572651815, 24.56249999795161543, 7.188101187500000933 ) ) ;
#18416=CARTESIAN_POINT ( 'NONE',  ( 1.320432766682874540E-15, 97.90625000204839523, 7.188101187500000044 ) ) ;
#18424=CARTESIAN_POINT ( 'NONE',  ( 1.469576158976823947E-15, 119.5625000040967763, 8.000000000000000000 ) ) ;
#18426=DIRECTION ( 'NONE',  ( -0.000000000000000000, 1.000000000000000000, -0.000000000000000000 ) ) ;
#18431=CARTESIAN_POINT ( 'NONE',  ( 3.999980467337267864, 125.0000000000000000, -6.928214507426884161 ) ) ;
#18436=CARTESIAN_POINT ( 'NONE',  ( 5.656854249492381470, 110.7500000040967763, 5.656854249492379694 ) ) ;
#18439=CARTESIAN_POINT ( 'NONE',  ( 2.977408999572650039, 95.56250000204838102, -7.188101187500001821 ) ) ;
#18444=ORIENTED_EDGE ( 'NONE', *, *, #10768, .F. ) ;
#18459=CARTESIAN_POINT ( 'NONE',  ( -5.656854249492379694, 3.374999995903220640, -5.656854249492380582 ) ) ;
#18461=CARTESIAN_POINT ( 'NONE',  ( -5.656854249492380582, 104.0000000040967905, -5.656854249492380582 ) ) ;
#18462=VECTOR ( 'NONE', #51371, 1000.000000000000000 ) ;
#18470=CARTESIAN_POINT ( 'NONE',  ( -7.188101187499999156, 95.75000000204836681, 2.977408999572654924 ) ) ;
#18471=CARTESIAN_POINT ( 'NONE',  ( 4.898587196589412829E-16, 16.68749999590322375, -8.000000000000000000 ) ) ;
#18476=CARTESIAN_POINT ( 'NONE',  ( -8.000000000000000000, 104.1875000040967763, 0.000000000000000000 ) ) ;
#18477=EDGE_CURVE ( 'NONE', #31066, #3802, #50551, .T. ) ;
#18480=ORIENTED_EDGE ( 'NONE', *, *, #74600, .T. ) ;
#18494=CARTESIAN_POINT ( 'NONE',  ( -5.082755093536326818, 7.781249997951610986, 5.082755093536325042 ) ) ;
#18497=CARTESIAN_POINT ( 'NONE',  ( 2.977408999572650039, 115.0625000020483810, -7.188101187500000933 ) ) ;
#18498=CARTESIAN_POINT ( 'NONE',  ( 4.898587196589412829E-16, 6.375000000000000888, -8.000000000000000000 ) ) ;
#18505=CARTESIAN_POINT ( 'NONE',  ( -5.656854249492379694, 9.562500000000001776, -5.656854249492380582 ) ) ;
#18519=CARTESIAN_POINT ( 'NONE',  ( -7.188101187500000933, 106.0625000020483668, -2.977408999572650483 ) ) ;
#18524=CARTESIAN_POINT ( 'NONE',  ( 2.977408999572650039, 113.5625000020483668, -7.188101187500001821 ) ) ;
#18533=CARTESIAN_POINT ( 'NONE',  ( -8.000000000000000000, 108.5000000000000000, 0.000000000000000000 ) ) ;
#18545=( BOUNDED_CURVE ( )  B_SPLINE_CURVE ( 2, ( #42624, #55456, #65639, #42990, #71660, #49401, #59982, #15067, #61100 ),
 .UNSPECIFIED., .F., .F. ) 
 B_SPLINE_CURVE_WITH_KNOTS ( ( 3, 2, 2, 2, 3 ),
 ( 0.8750000000000000000, 0.8819444444444444198, 0.8888888888888888395, 0.8958333333333332593, 0.9027777777777776791 ),
 .UNSPECIFIED. ) 
 CURVE ( )  GEOMETRIC_REPRESENTATION_ITEM ( )  RATIONAL_B_SPLINE_CURVE ( ( 1.000000000000000000, 0.9238795325112867385, 1.000000000000000000, 0.9238795325112867385, 1.000000000000000000, 0.9238795325112867385, 1.000000000000000000, 0.9238795325112879597, 0.9999999999999987788 ) ) 
 REPRESENTATION_ITEM ( '' )  );
#18548=ORIENTED_EDGE ( 'NONE', *, *, #55893, .T. ) ;
#18551=CARTESIAN_POINT ( 'NONE',  ( 3.313708498984762496, 5.718750000000000888, 7.999999999999998224 ) ) ;
#18553=CARTESIAN_POINT ( 'NONE',  ( -1.320432766682874540E-15, 1.593749997951610098, 7.188101187500000044 ) ) ;
#18578=CARTESIAN_POINT ( 'NONE',  ( 1.469576158976823947E-15, 119.3750000000000000, 8.000000000000000000 ) ) ;
#18581=ORIENTED_EDGE ( 'NONE', *, *, #69806, .T. ) ;
#18583=CARTESIAN_POINT ( 'NONE',  ( 8.000000000000000000, 13.40624999590322375, -3.313708498984761608 ) ) ;
#18594=CARTESIAN_POINT ( 'NONE',  ( -3.313708498984762496, 99.96875000409676204, 7.999999999999998224 ) ) ;
#18605=CARTESIAN_POINT ( 'NONE',  ( 8.000000000000000000, 4.312499995903220196, 0.000000000000000000 ) ) ;
#18606=CARTESIAN_POINT ( 'NONE',  ( -7.188101187500000044, 121.1562500020483810, 0.000000000000000000 ) ) ;
#18611=CARTESIAN_POINT ( 'NONE',  ( 2.977408999572654480, 94.62500000204838102, 7.188101187499999156 ) ) ;
#18614=CARTESIAN_POINT ( 'NONE',  ( 5.117192270959802336, 0.3122852236289677674, -5.908609428792219731 ) ) ;
#18642=CARTESIAN_POINT ( 'NONE',  ( -5.082755093536326818, 14.90624999795161187, 5.082755093536325042 ) ) ;
#18645=CARTESIAN_POINT ( 'NONE',  ( 4.401442555609581635E-16, 13.21874999795161187, -7.188101187500000044 ) ) ;
#18657=CARTESIAN_POINT ( 'NONE',  ( 7.188101187500002709, 115.8125000020484094, 2.977408999572649151 ) ) ;
#18661=CARTESIAN_POINT ( 'NONE',  ( -7.188101187500000044, 22.21874999795161187, -8.802885111219163269E-16 ) ) ;
#18667=CARTESIAN_POINT ( 'NONE',  ( -2.977408999572651815, 102.3125000020483810, 7.188101187500000933 ) ) ;
#18670=CARTESIAN_POINT ( 'NONE',  ( -3.313708498984761608, 88.90625000409677625, -8.000000000000000000 ) ) ;
#18690=CARTESIAN_POINT ( 'NONE',  ( 0.000000000000000000, 125.0000000000000000, 8.000000000000000000 ) ) ;
#18699=CARTESIAN_POINT ( 'NONE',  ( -2.977408999572651815, 115.4375000020483810, 7.188101187500000933 ) ) ;
#18706=CARTESIAN_POINT ( 'NONE',  ( 5.656854249492381470, 92.75000000409677625, 5.656854249492379694 ) ) ;
#18722=ADVANCED_FACE ( 'NONE', ( #44628 ), #61972, .T. ) ;
#18727=CARTESIAN_POINT ( 'NONE',  ( 7.188101187499999156, 14.24999999795161187, 2.977408999572654924 ) ) ;
#18732=CARTESIAN_POINT ( 'NONE',  ( 5.656854249492379694, 123.1250000040967905, -5.656854249492380582 ) ) ;
#18734=CARTESIAN_POINT ( 'NONE',  ( 0.000000000000000000, 125.0000000000000000, 0.000000000000000000 ) ) ;
#18745=CARTESIAN_POINT ( 'NONE',  ( -3.313708498984760720, 25.96875000000001066, -8.000000000000000000 ) ) ;
#18754=CARTESIAN_POINT ( 'NONE',  ( 4.401442555609581635E-16, 3.843749997951610098, -7.188101187500000044 ) ) ;
#18757=CARTESIAN_POINT ( 'NONE',  ( -7.188101187500001821, 115.4375000020483810, -2.977408999572650483 ) ) ;
#18760=EDGE_CURVE ( 'NONE', #69933, #43418, #2628, .T. ) ;
#18771=CARTESIAN_POINT ( 'NONE',  ( 1.469576158976823947E-15, 104.5625000040967763, 8.000000000000000000 ) ) ;
#18773=DIRECTION ( 'NONE',  ( 0.000000000000000000, 0.000000000000000000, 1.000000000000000000 ) ) ;
#18785=CARTESIAN_POINT ( 'NONE',  ( -5.082755093536326818, 24.28124999795161543, 5.082755093536325042 ) ) ;
#18788=CARTESIAN_POINT ( 'NONE',  ( -7.188101187499999156, 96.12500000204838102, 2.977408999572654924 ) ) ;
#18810=CARTESIAN_POINT ( 'NONE',  ( 2.977408999572654480, 92.00000000204838102, 7.188101187499999156 ) ) ;
#18816=EDGE_CURVE ( 'NONE', #51832, #64185, #45002, .T. ) ;
#18825=VERTEX_POINT ( 'NONE', #68005 ) ;
#18830=CARTESIAN_POINT ( 'NONE',  ( 3.313708498984760720, 105.2187500040967905, -8.000000000000000000 ) ) ;
#18837=CARTESIAN_POINT ( 'NONE',  ( 0.000000000000000000, 125.0000000000000000, 0.000000000000000000 ) ) ;
#18838=CARTESIAN_POINT ( 'NONE',  ( 5.082755093536325042, 98.09375000204838102, -5.082755093536325930 ) ) ;
#18841=CARTESIAN_POINT ( 'NONE',  ( 8.000000000000000000, 120.0312500040967905, -3.313708498984762496 ) ) ;
#18861=CARTESIAN_POINT ( 'NONE',  ( 7.188101187500001821, 3.937499997951610986, -2.977408999572650483 ) ) ;
#18864=CARTESIAN_POINT ( 'NONE',  ( -5.082755093536324154, 117.2187500020483810, 5.082755093536326818 ) ) ;
#18885=CARTESIAN_POINT ( 'NONE',  ( -7.188101187500000933, 104.5625000020483810, -2.977408999572650483 ) ) ;
#18891=CARTESIAN_POINT ( 'NONE',  ( 7.188101187500002709, 117.6875000020484094, 2.977408999572649151 ) ) ;
#18897=CARTESIAN_POINT ( 'NONE',  ( 0.000000000000000000, 125.0000000000000000, 0.000000000000000000 ) ) ;
#18913=ORIENTED_EDGE ( 'NONE', *, *, #63218, .T. ) ;
#18914=CARTESIAN_POINT ( 'NONE',  ( -3.313708498984765161, 5.531250000000000888, 7.999999999999998224 ) ) ;
#18916=CARTESIAN_POINT ( 'NONE',  ( -5.082755093536326818, 2.906249997951610098, 5.082755093536325042 ) ) ;
#18917=CARTESIAN_POINT ( 'NONE',  ( -5.656854249492380582, 122.0000000040967905, -5.656854249492380582 ) ) ;
#18920=ADVANCED_FACE ( 'NONE', ( #24573 ), #47403, .T. ) ;
#18930=DIRECTION ( 'NONE',  ( -0.000000000000000000, 1.000000000000000000, -0.000000000000000000 ) ) ;
#18934=ORIENTED_EDGE ( 'NONE', *, *, #10320, .F. ) ;
#18937=CARTESIAN_POINT ( 'NONE',  ( -4.898587196589412829E-16, 123.3125000040967905, -8.000000000000000000 ) ) ;
#18942=CARTESIAN_POINT ( 'NONE',  ( -5.656854249492380582, 120.3125000000000000, -5.656854249492380582 ) ) ;
#18944=ADVANCED_FACE ( 'NONE', ( #17637 ), #53148, .T. ) ;
#18948=CARTESIAN_POINT ( 'NONE',  ( -5.656854249492381470, 17.24999999590322375, 5.656854249492379694 ) ) ;
#18963=ORIENTED_EDGE ( 'NONE', *, *, #5242, .F. ) ;
#18970=CARTESIAN_POINT ( 'NONE',  ( -7.188101187500000933, 121.0625000020483810, -2.977408999572650483 ) ) ;
#18974=CARTESIAN_POINT ( 'NONE',  ( -5.082755093536324154, 98.84375000204838102, 5.082755093536326818 ) ) ;
#18985=CARTESIAN_POINT ( 'NONE',  ( 0.000000000000000000, 125.0000000000000000, 0.000000000000000000 ) ) ;
#18990=CARTESIAN_POINT ( 'NONE',  ( -8.000000000000000000, 113.0000000000000000, 0.000000000000000000 ) ) ;
#19002=CARTESIAN_POINT ( 'NONE',  ( 7.188101187500000044, 13.96874999795161187, 0.000000000000000000 ) ) ;
#19004=CARTESIAN_POINT ( 'NONE',  ( 1.377103048673011143, 124.5535323524340896, -7.833776318515874415 ) ) ;
#19005=CARTESIAN_POINT ( 'NONE',  ( 7.188101187499999156, 9.749999997951611874, 2.977408999572654924 ) ) ;
#19018=CARTESIAN_POINT ( 'NONE',  ( 1.320432766682874540E-15, 114.0312500020483952, 7.188101187500000044 ) ) ;
#19022=CARTESIAN_POINT ( 'NONE',  ( 7.188101187499999156, 22.87499999795161543, 2.977408999572654924 ) ) ;
#19028=CARTESIAN_POINT ( 'NONE',  ( -2.977408999572650927, 98.75000000204838102, -7.188101187500001821 ) ) ;
#19051=ORIENTED_EDGE ( 'NONE', *, *, #61420, .T. ) ;
#19060=CARTESIAN_POINT ( 'NONE',  ( 2.977408999572650039, 116.1875000020483952, -7.188101187500001821 ) ) ;
#19082=CARTESIAN_POINT ( 'NONE',  ( 4.898587196589412829E-16, 22.87500000000000355, -8.000000000000000000 ) ) ;
#19086=CARTESIAN_POINT ( 'NONE',  ( -5.082755093536325042, 11.90624999795161010, -5.082755093536325930 ) ) ;
#19090=CARTESIAN_POINT ( 'NONE',  ( 9.797174393178825657E-16, 125.0000000000000000, -8.000000000000000000 ) ) ;
#19093=ADVANCED_FACE ( 'NONE', ( #27764 ), #45124, .T. ) ;
#19102=CARTESIAN_POINT ( 'NONE',  ( 5.656854249492380582, 22.68750000000000355, -5.656854249492380582 ) ) ;
#19113=CARTESIAN_POINT ( 'NONE',  ( 7.188101187499999156, 7.874999997951610986, 2.977408999572654924 ) ) ;
#19115=CARTESIAN_POINT ( 'NONE',  ( -5.082755093536324154, 118.7187500020483810, 5.082755093536326818 ) ) ;
#19144=CARTESIAN_POINT ( 'NONE',  ( 7.188101187500002709, 93.68750000204838102, 2.977408999572649151 ) ) ;
#19168=CARTESIAN_POINT ( 'NONE',  ( -7.188101187500000044, 91.53125000204836681, 0.000000000000000000 ) ) ;
#19173=ORIENTED_EDGE ( 'NONE', *, *, #28766, .F. ) ;
#19189=CARTESIAN_POINT ( 'NONE',  ( -1.469576158976823947E-15, 17.62500000000000000, 8.000000000000000000 ) ) ;
#19191=CARTESIAN_POINT ( 'NONE',  ( 5.656854249492379694, 97.62500000409677625, -5.656854249492380582 ) ) ;
#19201=CARTESIAN_POINT ( 'NONE',  ( -4.401442555609581635E-16, 96.78125000204838102, -7.188101187500000044 ) ) ;
#19222=CARTESIAN_POINT ( 'NONE',  ( -8.000000000000000000, 5.062499995903221084, -9.797174393178825657E-16 ) ) ;
#19224=CARTESIAN_POINT ( 'NONE',  ( -2.977408999572654480, 3.374999997951610986, 7.188101187499999156 ) ) ;
#19227=CARTESIAN_POINT ( 'NONE',  ( 7.188101187500000933, 108.8750000020483952, -2.977408999572651371 ) ) ;
#19232=FACE_OUTER_BOUND ( 'NONE', #32931, .T. ) ;
#19236=ORIENTED_EDGE ( 'NONE', *, *, #56605, .F. ) ;
#19244=CARTESIAN_POINT ( 'NONE',  ( -2.977408999572650927, 107.3750000020483952, -7.188101187500000933 ) ) ;
#19250=CARTESIAN_POINT ( 'NONE',  ( 7.188101187500001821, 105.8750000020483952, -2.977408999572651371 ) ) ;
#19262=CARTESIAN_POINT ( 'NONE',  ( 7.999999999999998224, 14.90625000000000355, 3.313708498984766049 ) ) ;
#19276=CARTESIAN_POINT ( 'NONE',  ( 8.000000000000000000, 3.093750000000001332, -3.313708498984761608 ) ) ;
#19277=CARTESIAN_POINT ( 'NONE',  ( -3.313708498984719864, 10.96874999999999822, -8.000000000000040856 ) ) ;
#19278=CARTESIAN_POINT ( 'NONE',  ( 5.082755093536325930, 5.156249997951610986, -5.082755093536325930 ) ) ;
#19279=CARTESIAN_POINT ( 'NONE',  ( 8.000000000000000000, 114.0312500040967763, -3.313708498984762496 ) ) ;
#19281=CARTESIAN_POINT ( 'NONE',  ( -5.656854249492381470, 6.937500000000000888, 5.656854249492379694 ) ) ;
#19304=CARTESIAN_POINT ( 'NONE',  ( 8.000000000000000000, 110.8437499999999858, -3.313708498984762496 ) ) ;
#19308=CARTESIAN_POINT ( 'NONE',  ( 5.656854249492380582, 13.49999999590322375, -5.656854249492380582 ) ) ;
#19333=EDGE_CURVE ( 'NONE', #21298, #48333, #11703, .T. ) ;
#19336=CARTESIAN_POINT ( 'NONE',  ( 2.977408999572654480, 93.12500000204836681, 7.188101187499999156 ) ) ;
#19341=ORIENTED_EDGE ( 'NONE', *, *, #25602, .F. ) ;
#19362=CARTESIAN_POINT ( 'NONE',  ( 4.401442555609581635E-16, 15.84374999795161365, -7.188101187500000044 ) ) ;
#19365=CARTESIAN_POINT ( 'NONE',  ( -3.313708498984720308, 117.4062500040967763, -8.000000000000040856 ) ) ;
#19366=CARTESIAN_POINT ( 'NONE',  ( -2.977408999572650039, 14.81249999795161543, -7.188101187500001821 ) ) ;
#19377=CARTESIAN_POINT ( 'NONE',  ( -7.188101187500001821, 112.0625000020483810, -2.977408999572650483 ) ) ;
#19381=CARTESIAN_POINT ( 'NONE',  ( -7.188101187500002709, 22.31249999795161187, 2.977408999572649151 ) ) ;
#19387=CARTESIAN_POINT ( 'NONE',  ( 2.977408999572654480, 102.5000000020483810, 7.188101187499999156 ) ) ;
#19393=EDGE_CURVE ( 'NONE', #40745, #72853, #34879, .T. ) ;
#19420=CARTESIAN_POINT ( 'NONE',  ( 1.320432766682874540E-15, 114.0312500020483952, 7.188101187500000044 ) ) ;
#19444=EDGE_CURVE ( 'NONE', #7158, #10862, #50707, .T. ) ;
#19450=CARTESIAN_POINT ( 'NONE',  ( -7.188101187500002709, 10.68749999795161187, 2.977408999572649151 ) ) ;
#19459=CARTESIAN_POINT ( 'NONE',  ( -7.999999999999998224, 98.28125000409677625, 3.313708498984766049 ) ) ;
#19467=CARTESIAN_POINT ( 'NONE',  ( -8.000000000000000000, 24.75000000000000355, -9.797174393178825657E-16 ) ) ;
#19478=CARTESIAN_POINT ( 'NONE',  ( -1.320432766682874540E-15, 3.093749997951610542, 7.188101187500000044 ) ) ;
#19480=CARTESIAN_POINT ( 'NONE',  ( -5.082755093536325930, 118.3437500020483810, -5.082755093536325930 ) ) ;
#19488=CARTESIAN_POINT ( 'NONE',  ( 7.999999999999998224, 2.906250000000000888, 3.313708498984766049 ) ) ;
#19492=CARTESIAN_POINT ( 'NONE',  ( -8.000000000000000000, 99.49999999999998579, 0.000000000000000000 ) ) ;
#19502=DIRECTION ( 'NONE',  ( -0.000000000000000000, 1.000000000000000000, -0.000000000000000000 ) ) ;
#19508=CARTESIAN_POINT ( 'NONE',  ( -7.188101187500000044, 94.53125000204836681, 0.000000000000000000 ) ) ;
#19517=DIRECTION ( 'NONE',  ( -0.000000000000000000, 1.000000000000000000, -0.000000000000000000 ) ) ;
#19524=CARTESIAN_POINT ( 'NONE',  ( -8.000000000000000000, 102.4062500000000000, -3.313708498984761164 ) ) ;
#19525=CARTESIAN_POINT ( 'NONE',  ( 7.188101187500000044, 27.84374999795161543, 0.000000000000000000 ) ) ;
#19531=CARTESIAN_POINT ( 'NONE',  ( 4.898587196589412829E-16, 1.687499995903220196, -8.000000000000000000 ) ) ;
#19555=CARTESIAN_POINT ( 'NONE',  ( -3.313708498984762052, 97.90625000409677625, -8.000000000000000000 ) ) ;
#19565=CARTESIAN_POINT ( 'NONE',  ( 7.188101187500002709, 100.8125000020484094, 2.977408999572649151 ) ) ;
#19584=CARTESIAN_POINT ( 'NONE',  ( 5.656854249492380582, 2.999999995903220196, -5.656854249492380582 ) ) ;
#19587=CARTESIAN_POINT ( 'NONE',  ( -7.188101187500002709, 12.18749999795161187, 2.977408999572649151 ) ) ;
#19590=CARTESIAN_POINT ( 'NONE',  ( -7.188101187499999156, 108.1250000020483810, 2.977408999572654924 ) ) ;
#19596=DIRECTION ( 'NONE',  ( 0.000000000000000000, 1.000000000000000000, 0.000000000000000000 ) ) ;
#19612=CARTESIAN_POINT ( 'NONE',  ( -5.082755093536325930, 107.4687500020483810, -5.082755093536325930 ) ) ;
#19618=CARTESIAN_POINT ( 'NONE',  ( -5.082755093536324154, 109.7187500020483810, 5.082755093536326818 ) ) ;
#19620=EDGE_LOOP ( 'NONE', ( #57350, #11961 ) ) ;
#19644=CARTESIAN_POINT ( 'NONE',  ( -8.000000000000001776, 11.34375000000000000, 3.313708498984759387 ) ) ;
#19646=CARTESIAN_POINT ( 'NONE',  ( 2.977408999572650927, 2.249999997951610098, -7.188101187500001821 ) ) ;
#19647=CARTESIAN_POINT ( 'NONE',  ( -3.313708498984762496, 114.9687500040967905, 7.999999999999998224 ) ) ;
#19666=CARTESIAN_POINT ( 'NONE',  ( 5.656854249492380582, 26.99999999590322375, -5.656854249492380582 ) ) ;
#19672=CARTESIAN_POINT ( 'NONE',  ( 5.656854249492379694, 112.4375000000000000, -5.656854249492380582 ) ) ;
#19677=CARTESIAN_POINT ( 'NONE',  ( -8.000000000000000000, 21.56249999590322375, -9.797174393178825657E-16 ) ) ;
#19700=CARTESIAN_POINT ( 'NONE',  ( 7.188101187500002709, 123.3125000020483810, 2.977408999572649151 ) ) ;
#19701=DIRECTION ( 'NONE',  ( 0.000000000000000000, 0.000000000000000000, 1.000000000000000000 ) ) ;
#19705=CARTESIAN_POINT ( 'NONE',  ( -7.188101187500001821, 91.06250000204838102, -2.977408999572650483 ) ) ;
#19736=CARTESIAN_POINT ( 'NONE',  ( 7.188101187499999156, 22.87499999795161187, 2.977408999572654924 ) ) ;
#19739=CARTESIAN_POINT ( 'NONE',  ( -1.320432766682874540E-15, 9.468749997951610098, 7.188101187500000044 ) ) ;
#19741=( BOUNDED_CURVE ( )  B_SPLINE_CURVE ( 2, ( #61392, #55374, #50812, #45156, #62497, #55748, #3680, #49703, #33861 ),
 .UNSPECIFIED., .F., .F. ) 
 B_SPLINE_CURVE_WITH_KNOTS ( ( 3, 2, 2, 2, 3 ),
 ( 0.1770833333333334259, 0.1822916666666667407, 0.1875000000000001110, 0.1927083333333334814, 0.1979166666666667962 ),
 .UNSPECIFIED. ) 
 CURVE ( )  GEOMETRIC_REPRESENTATION_ITEM ( )  RATIONAL_B_SPLINE_CURVE ( ( 0.9999999999999987788, 0.9238795325112879597, 1.000000000000000000, 0.9238795325112867385, 1.000000000000000000, 0.9238795325112867385, 1.000000000000000000, 0.9238795325112847401, 1.000000000000001998 ) ) 
 REPRESENTATION_ITEM ( '' )  );
#19752=CARTESIAN_POINT ( 'NONE',  ( -2.977408999572650927, 113.3750000020483810, -7.188101187500001821 ) ) ;
#19756=CARTESIAN_POINT ( 'NONE',  ( 2.977408999572652260, 22.68749999795161187, 7.188101187500000044 ) ) ;
#19764=CARTESIAN_POINT ( 'NONE',  ( 2.977408999572654480, 92.00000000204838102, 7.188101187499999156 ) ) ;
#19793=CARTESIAN_POINT ( 'NONE',  ( -5.082755093536325930, 110.4687500020483810, -5.082755093536325930 ) ) ;
#19809=DIRECTION ( 'NONE',  ( -0.000000000000000000, 1.000000000000000000, -0.000000000000000000 ) ) ;
#19819=CARTESIAN_POINT ( 'NONE',  ( -2.977408999572650039, 11.81249999795161187, -7.188101187500000933 ) ) ;
#19836=CARTESIAN_POINT ( 'NONE',  ( -8.000000000000001776, 24.84375000000000355, 3.313708498984759387 ) ) ;
#19838=ORIENTED_EDGE ( 'NONE', *, *, #1599, .F. ) ;
#19847=( BOUNDED_CURVE ( )  B_SPLINE_CURVE ( 2, ( #43394, #65662, #32092, #9078, #26404, #1932, #71686, #3046, #60375 ),
 .UNSPECIFIED., .F., .F. ) 
 B_SPLINE_CURVE_WITH_KNOTS ( ( 3, 2, 2, 2, 3 ),
 ( 0.03125000000000002082, 0.03645833333333335646, 0.04166666666666669211, 0.04687500000000002776, 0.05208333333333337034 ),
 .UNSPECIFIED. ) 
 CURVE ( )  GEOMETRIC_REPRESENTATION_ITEM ( )  RATIONAL_B_SPLINE_CURVE ( ( 0.9999999999999996669, 0.9238795325112870716, 1.000000000000000000, 0.9238795325112867385, 1.000000000000000000, 0.9238795325112867385, 1.000000000000000000, 0.9238795325112861834, 1.000000000000000444 ) ) 
 REPRESENTATION_ITEM ( '' )  );
#19848=CARTESIAN_POINT ( 'NONE',  ( -2.977408999572650039, 6.937499997951611874, -7.188101187500000933 ) ) ;
#19853=CARTESIAN_POINT ( 'NONE',  ( 1.320432766682874540E-15, 109.9062500020483810, 7.188101187500000044 ) ) ;
#19865=CARTESIAN_POINT ( 'NONE',  ( 1.469576158976823947E-15, 102.8750000000000000, 8.000000000000000000 ) ) ;
#19878=DIRECTION ( 'NONE',  ( -0.000000000000000000, 1.000000000000000000, -0.000000000000000000 ) ) ;
#19880=CARTESIAN_POINT ( 'NONE',  ( -2.977408999572652260, 93.31250000204838102, 7.188101187500000044 ) ) ;
#19885=CARTESIAN_POINT ( 'NONE',  ( -3.313708498984707429, 96.21875000000000000, -8.000000000000055067 ) ) ;
#19890=CARTESIAN_POINT ( 'NONE',  ( -5.656854249492381470, 9.749999995903220196, 5.656854249492379694 ) ) ;
#19897=CARTESIAN_POINT ( 'NONE',  ( 4.898587196589412829E-16, 24.18749999590322375, -8.000000000000000000 ) ) ;
#19898=CARTESIAN_POINT ( 'NONE',  ( 8.000000000000000000, 121.4375000040967763, -9.797174393178825657E-16 ) ) ;
#19911=VERTEX_POINT ( 'NONE', #47780 ) ;
#19913=CARTESIAN_POINT ( 'NONE',  ( 8.000000000000000000, 14.90624999590322197, -3.313708498984761164 ) ) ;
#19925=CARTESIAN_POINT ( 'NONE',  ( 3.313708498984765161, 100.1562500040967905, 7.999999999999998224 ) ) ;
#19933=ORIENTED_EDGE ( 'NONE', *, *, #21942, .F. ) ;
#19935=CARTESIAN_POINT ( 'NONE',  ( 7.188101187500002709, 96.31250000204838102, 2.977408999572649151 ) ) ;
#19955=CARTESIAN_POINT ( 'NONE',  ( -8.000000000000000000, 90.59375000409677625, -3.313708498984761164 ) ) ;
#19956=EDGE_CURVE ( 'NONE', #69918, #29891, #57558, .T. ) ;
#19958=( BOUNDED_CURVE ( )  B_SPLINE_CURVE ( 2, ( #41905, #53609, #1200, #47192, #18533, #35891, #58908, #30221, #53239 ),
 .UNSPECIFIED., .F., .F. ) 
 B_SPLINE_CURVE_WITH_KNOTS ( ( 3, 2, 2, 2, 3 ),
 ( 0.4479166666666665741, 0.4531249999999998890, 0.4583333333333332038, 0.4635416666666665741, 0.4687499999999998890 ),
 .UNSPECIFIED. ) 
 CURVE ( )  GEOMETRIC_REPRESENTATION_ITEM ( )  RATIONAL_B_SPLINE_CURVE ( ( 1.000000000000001554, 0.9238795325112850731, 1.000000000000000000, 0.9238795325112867385, 1.000000000000000000, 0.9238795325112867385, 1.000000000000000000, 0.9238795325112884038, 0.9999999999999983347 ) ) 
 REPRESENTATION_ITEM ( '' )  );
#19959=CARTESIAN_POINT ( 'NONE',  ( 4.898587196589412829E-16, 1.687499995903220196, -8.000000000000000000 ) ) ;
#19961=CARTESIAN_POINT ( 'NONE',  ( 7.188101187500000044, 12.84374999795161187, 0.000000000000000000 ) ) ;
#19964=CARTESIAN_POINT ( 'NONE',  ( -4.401442555609581635E-16, 112.1562500020483952, -7.188101187500000044 ) ) ;
#19982=CARTESIAN_POINT ( 'NONE',  ( 7.188101187500002709, 99.31250000204838102, 2.977408999572649151 ) ) ;
#19988=CARTESIAN_POINT ( 'NONE',  ( -4.401442555609581635E-16, 110.6562500020483810, -7.188101187500000044 ) ) ;
#19993=ORIENTED_EDGE ( 'NONE', *, *, #65427, .T. ) ;
#19999=CARTESIAN_POINT ( 'NONE',  ( 7.188101187500000933, 0.9374999979516102089, -2.977408999572650483 ) ) ;
#20005=CARTESIAN_POINT ( 'NONE',  ( 3.313708498984760276, 1.593749995903220196, -8.000000000000001776 ) ) ;
#20012=CARTESIAN_POINT ( 'NONE',  ( -7.188101187500000044, 7.218749997951610986, -8.802885111219163269E-16 ) ) ;
#20013=CARTESIAN_POINT ( 'NONE',  ( -3.313708498984762496, 117.9687500040968047, 7.999999999999998224 ) ) ;
#20023=CARTESIAN_POINT ( 'NONE',  ( -8.000000000000000000, 15.75000000000000355, -9.797174393178825657E-16 ) ) ;
#20037=CARTESIAN_POINT ( 'NONE',  ( 8.000000000000000000, 110.7500000000000000, -9.797174393178825657E-16 ) ) ;
#20041=CARTESIAN_POINT ( 'NONE',  ( -8.000000000000000000, 23.06249999590322020, -9.797174393178825657E-16 ) ) ;
#20044=CARTESIAN_POINT ( 'NONE',  ( 8.000000000000000000, 121.2500000000000000, -9.797174393178825657E-16 ) ) ;
#20054=CARTESIAN_POINT ( 'NONE',  ( -8.000000000000000000, 99.59375000409679046, -3.313708498984761164 ) ) ;
#20064=CARTESIAN_POINT ( 'NONE',  ( -7.188101187500000933, 122.5625000020483668, -2.977408999572650483 ) ) ;
#20065=LINE ( 'NONE', #42343, #43856 ) ;
#20068=VECTOR ( 'NONE', #6023, 1000.000000000000000 ) ;
#20071=CARTESIAN_POINT ( 'NONE',  ( -2.977408999572650927, 90.87500000204838102, -7.188101187500001821 ) ) ;
#20088=VERTEX_POINT ( 'NONE', #1093 ) ;
#20090=CARTESIAN_POINT ( 'NONE',  ( 5.656854249492380582, 22.49999999590322375, -5.656854249492380582 ) ) ;
#20103=CARTESIAN_POINT ( 'NONE',  ( 7.188101187500000044, 19.96874999795161543, 0.000000000000000000 ) ) ;
#20107=CARTESIAN_POINT ( 'NONE',  ( -2.977408999572654480, 10.87499999795161187, 7.188101187499999156 ) ) ;
#20119=CARTESIAN_POINT ( 'NONE',  ( 1.320432766682874540E-15, 111.0312500020483810, 7.188101187500000044 ) ) ;
#20130=CARTESIAN_POINT ( 'NONE',  ( -5.082755093536325930, 95.84375000204838102, -5.082755093536325930 ) ) ;
#20158=CARTESIAN_POINT ( 'NONE',  ( -2.977408999572650927, 110.3750000020484094, -7.188101187500001821 ) ) ;
#20172=DIRECTION ( 'NONE',  ( -1.000000000000000000, 0.000000000000000000, -0.000000000000000000 ) ) ;
#20180=CARTESIAN_POINT ( 'NONE',  ( -4.898587196589412829E-16, 109.6250000000000000, -8.000000000000000000 ) ) ;
#20184=CARTESIAN_POINT ( 'NONE',  ( 7.188101187499999156, 20.24999999795161898, 2.977408999572654924 ) ) ;
#20192=CARTESIAN_POINT ( 'NONE',  ( -7.188101187500001821, 1.124999997951610098, -2.977408999572651371 ) ) ;
#20212=CARTESIAN_POINT ( 'NONE',  ( -5.082755093536325042, 5.531249997951610986, -5.082755093536325930 ) ) ;
#20217=CARTESIAN_POINT ( 'NONE',  ( -7.188101187500001821, 112.4375000020483810, -2.977408999572650483 ) ) ;
#20231=CARTESIAN_POINT ( 'NONE',  ( 3.313708498984765161, 92.46874999999998579, 7.999999999999998224 ) ) ;
#20233=CARTESIAN_POINT ( 'NONE',  ( 0.000000000000000000, 125.0000000000000000, 0.000000000000000000 ) ) ;
#20238=ORIENTED_EDGE ( 'NONE', *, *, #29592, .F. ) ;
#20243=CARTESIAN_POINT ( 'NONE',  ( 4.401442555609581635E-16, 26.71874999795161543, -7.188101187500000044 ) ) ;
#20245=CARTESIAN_POINT ( 'NONE',  ( 2.977408999572654480, 90.50000000204839523, 7.188101187499999156 ) ) ;
#20255=CARTESIAN_POINT ( 'NONE',  ( 1.469576158976823947E-15, 109.0625000040967905, 8.000000000000000000 ) ) ;
#20269=CARTESIAN_POINT ( 'NONE',  ( -7.188101187500000044, 90.03125000204838102, 0.000000000000000000 ) ) ;
#20283=VECTOR ( 'NONE', #47886, 1000.000000000000000 ) ;
#20292=( BOUNDED_CURVE ( )  B_SPLINE_CURVE ( 2, ( #51975, #23668, #40276, #57268, #35380, #58026, #22536, #63276, #5954 ),
 .UNSPECIFIED., .F., .F. ) 
 B_SPLINE_CURVE_WITH_KNOTS ( ( 3, 2, 2, 2, 3 ),
 ( 0.2916666666666666297, 0.2986111111111110494, 0.3055555555555555247, 0.3124999999999999445, 0.3194444444444443643 ),
 .UNSPECIFIED. ) 
 CURVE ( )  GEOMETRIC_REPRESENTATION_ITEM ( )  RATIONAL_B_SPLINE_CURVE ( ( 1.000000000000000666, 0.9238795325112861834, 1.000000000000000000, 0.9238795325112867385, 1.000000000000000000, 0.9238795325112867385, 1.000000000000000000, 0.9238795325112872936, 0.9999999999999994449 ) ) 
 REPRESENTATION_ITEM ( '' )  );
#20295=CARTESIAN_POINT ( 'NONE',  ( -8.000000000000000000, 99.59375000409679046, -3.313708498984761608 ) ) ;
#20301=EDGE_LOOP ( 'NONE', ( #71321, #21621, #4820, #60507 ) ) ;
#20303=CARTESIAN_POINT ( 'NONE',  ( -5.082755093536325930, 92.46875000204838102, -5.082755093536325930 ) ) ;
#20326=CARTESIAN_POINT ( 'NONE',  ( -8.000000000000000000, 3.468749995903220196, -3.313708498984762496 ) ) ;
#20329=CARTESIAN_POINT ( 'NONE',  ( 4.401442555609581635E-16, 13.21874999795161187, -7.188101187500000044 ) ) ;
#20332=CARTESIAN_POINT ( 'NONE',  ( 7.188101187500002709, 110.1875000020483810, 2.977408999572649151 ) ) ;
#20334=DIRECTION ( 'NONE',  ( -0.000000000000000000, 1.000000000000000000, -0.000000000000000000 ) ) ;
#20350=CARTESIAN_POINT ( 'NONE',  ( 5.082755093536325042, 101.0937500020483810, -5.082755093536325930 ) ) ;
#20357=CARTESIAN_POINT ( 'NONE',  ( 1.320432766682874540E-15, 111.4062500020483810, 7.188101187500000044 ) ) ;
#20368=CARTESIAN_POINT ( 'NONE',  ( 2.977408999572650927, 2.624999997951610542, -7.188101187500000933 ) ) ;
#20386=CARTESIAN_POINT ( 'NONE',  ( 2.977408999572650927, 6.749999997951611874, -7.188101187500001821 ) ) ;
#20388=CARTESIAN_POINT ( 'NONE',  ( 8.000000000000001776, 115.3437500040967763, 3.313708498984759387 ) ) ;
#20396=CARTESIAN_POINT ( 'NONE',  ( -4.898587196589412829E-16, 96.12499999999998579, -8.000000000000000000 ) ) ;
#20407=CARTESIAN_POINT ( 'NONE',  ( 3.313708498984721640, 26.53124999590322020, 8.000000000000039080 ) ) ;
#20413=CARTESIAN_POINT ( 'NONE',  ( -7.999999999999998224, 111.5937499999999858, 3.313708498984766493 ) ) ;
#20418=CARTESIAN_POINT ( 'NONE',  ( -8.000000000000000000, 21.46874999590322375, -3.313708498984762496 ) ) ;
#20439=CARTESIAN_POINT ( 'NONE',  ( -1.469576158976823947E-15, 25.12500000000000355, 8.000000000000000000 ) ) ;
#20442=CARTESIAN_POINT ( 'NONE',  ( 5.082755093536326818, 118.7187500020483810, 5.082755093536325042 ) ) ;
#20443=CARTESIAN_POINT ( 'NONE',  ( 4.898587196589412829E-16, 18.18749999590322020, -8.000000000000000000 ) ) ;
#20447=CARTESIAN_POINT ( 'NONE',  ( 7.188101187500000044, 91.90625000204838102, -8.802885111219163269E-16 ) ) ;
#20459=EDGE_LOOP ( 'NONE', ( #3051, #45378, #39712, #60951 ) ) ;
#20470=CARTESIAN_POINT ( 'NONE',  ( 2.977408999572651815, 19.68749999795161543, 7.188101187500000933 ) ) ;
#20473=CARTESIAN_POINT ( 'NONE',  ( 7.188101187499999156, 18.74999999795161898, 2.977408999572654924 ) ) ;
#20483=AXIS2_PLACEMENT_3D ( 'NONE', #18251, #6570, #555 ) ;
#20487=CARTESIAN_POINT ( 'NONE',  ( -4.401442555609581635E-16, 110.2812500020483810, -7.188101187500000044 ) ) ;
#20488=EDGE_CURVE ( 'NONE', #9455, #31077, #51133, .T. ) ;
#20489=CARTESIAN_POINT ( 'NONE',  ( 8.000000000000000000, 94.53125000409676204, -3.313708498984762496 ) ) ;
#20500=CARTESIAN_POINT ( 'NONE',  ( -5.082755093536325930, 92.84375000204838102, -5.082755093536325930 ) ) ;
#20523=CARTESIAN_POINT ( 'NONE',  ( 3.313708498984706985, 109.7187500040968047, -8.000000000000055067 ) ) ;
#20534=CARTESIAN_POINT ( 'NONE',  ( -2.977408999572650927, 108.8750000020483810, -7.188101187500001821 ) ) ;
#20543=CARTESIAN_POINT ( 'NONE',  ( 9.797174393178825657E-16, 125.0000000000000000, -8.000000000000000000 ) ) ;
#20545=DIRECTION ( 'NONE',  ( -0.000000000000000000, 1.000000000000000000, -0.000000000000000000 ) ) ;
#20554=LINE ( 'NONE', #32651, #13515 ) ;
#20556=CYLINDRICAL_SURFACE ( 'NONE', #45758, 8.000000000000000000 ) ;
#20563=CARTESIAN_POINT ( 'NONE',  ( -7.188101187500000933, 16.49999999795161543, -2.977408999572651371 ) ) ;
#20572=CARTESIAN_POINT ( 'NONE',  ( -7.188101187500001821, 5.624999997951611874, -2.977408999572651371 ) ) ;
#20590=CARTESIAN_POINT ( 'NONE',  ( 2.977408999572652260, 13.68749999795161187, 7.188101187500000044 ) ) ;
#20594=CARTESIAN_POINT ( 'NONE',  ( -4.401442555609581635E-16, 110.6562500020483810, -7.188101187500000044 ) ) ;
#20605=CARTESIAN_POINT ( 'NONE',  ( 8.000000000000000000, 19.40624999590322375, -3.313708498984761164 ) ) ;
#20610=CARTESIAN_POINT ( 'NONE',  ( 8.000000000000001776, 95.65625000000002842, 3.313708498984759387 ) ) ;
#20612=CARTESIAN_POINT ( 'NONE',  ( 3.313708498984711426, 98.46875000000001421, 8.000000000000053291 ) ) ;
#20618=ORIENTED_EDGE ( 'NONE', *, *, #52512, .F. ) ;
#20627=CARTESIAN_POINT ( 'NONE',  ( 3.594042629939374400, 89.53052393364181683, -6.225082831242716885 ) ) ;
#20637=CARTESIAN_POINT ( 'NONE',  ( 2.977408999572650927, 18.74999999795161898, -7.188101187500001821 ) ) ;
#20671=CARTESIAN_POINT ( 'NONE',  ( 4.898587196589412829E-16, 18.37500000000000355, -8.000000000000000000 ) ) ;
#20674=CARTESIAN_POINT ( 'NONE',  ( 3.313708498984765161, 98.65625000409679046, 7.999999999999998224 ) ) ;
#20685=CARTESIAN_POINT ( 'NONE',  ( 2.977408999572650039, 92.18750000204838102, -7.188101187500001821 ) ) ;
#20699=CARTESIAN_POINT ( 'NONE',  ( -5.656854249492380582, 105.5000000040967905, -5.656854249492380582 ) ) ;
#20708=CARTESIAN_POINT ( 'NONE',  ( -8.000000000000001776, 5.156249995903220196, 3.313708498984759387 ) ) ;
#20710=CARTESIAN_POINT ( 'NONE',  ( 7.188101187499999156, 11.24999999795161187, 2.977408999572654924 ) ) ;
#20714=CARTESIAN_POINT ( 'NONE',  ( -4.401442555609581635E-16, 107.6562500020483810, -7.188101187500000044 ) ) ;
#20716=CARTESIAN_POINT ( 'NONE',  ( 0.000000000000000000, 125.0000000000000000, 8.000000000000000000 ) ) ;
#20732=CARTESIAN_POINT ( 'NONE',  ( 7.188101187500000933, 98.00000000204838102, -2.977408999572651371 ) ) ;
#20739=CARTESIAN_POINT ( 'NONE',  ( 5.082755093536326818, 110.0937500020483810, 5.082755093536325042 ) ) ;
#20751=CARTESIAN_POINT ( 'NONE',  ( -5.082755093536325042, 2.906249997951610542, -5.082755093536325930 ) ) ;
#20763=ORIENTED_EDGE ( 'NONE', *, *, #61637, .T. ) ;
#20766=CARTESIAN_POINT ( 'NONE',  ( 4.401442555609581635E-16, 8.343749997951611874, -7.188101187500000044 ) ) ;
#20767=CARTESIAN_POINT ( 'NONE',  ( 3.313708498984765161, 115.1562500040967763, 7.999999999999998224 ) ) ;
#20796=CARTESIAN_POINT ( 'NONE',  ( -3.313708498984762052, 112.7187499999999858, -8.000000000000000000 ) ) ;
#20800=CARTESIAN_POINT ( 'NONE',  ( 4.898587196589412829E-16, 19.87500000000000355, -8.000000000000000000 ) ) ;
#20801=CARTESIAN_POINT ( 'NONE',  ( -5.656854249492379694, 19.87499999590322020, -5.656854249492380582 ) ) ;
#20807=LINE ( 'NONE', #25950, #49582 ) ;
#20825=CARTESIAN_POINT ( 'NONE',  ( 1.320432766682874540E-15, 115.5312500020483952, 7.188101187500000044 ) ) ;
#20830=CARTESIAN_POINT ( 'NONE',  ( 5.082755093536325042, 123.9687500020483952, -5.082755093536325930 ) ) ;
#20855=CARTESIAN_POINT ( 'NONE',  ( -2.977408999572650039, 18.93749999795161187, -7.188101187500001821 ) ) ;
#20858=CARTESIAN_POINT ( 'NONE',  ( 5.082755093536325930, 19.03124999795161543, -5.082755093536325930 ) ) ;
#20862=FACE_OUTER_BOUND ( 'NONE', #42506, .T. ) ;
#20870=CARTESIAN_POINT ( 'NONE',  ( -4.898587196589412829E-16, 94.81250000409677625, -8.000000000000000000 ) ) ;
#20882=CARTESIAN_POINT ( 'NONE',  ( 2.977408999572654480, 96.50000000204838102, 7.188101187499999156 ) ) ;
#20888=CARTESIAN_POINT ( 'NONE',  ( 5.656854249492379694, 94.43750000000000000, -5.656854249492380582 ) ) ;
#20903=ORIENTED_EDGE ( 'NONE', *, *, #11097, .F. ) ;
#20906=EDGE_CURVE ( 'NONE', #48510, #55947, #53738, .T. ) ;
#20913=CARTESIAN_POINT ( 'NONE',  ( -2.977408999572651815, 109.4375000020483810, 7.188101187500000933 ) ) ;
#20922=LINE ( 'NONE', #9624, #62971 ) ;
#20927=CARTESIAN_POINT ( 'NONE',  ( -5.656854249492380582, 93.31249999999998579, -5.656854249492380582 ) ) ;
#20933=VERTEX_POINT ( 'NONE', #3166 ) ;
#20939=CARTESIAN_POINT ( 'NONE',  ( 7.188101187500000933, 17.43749999795161543, -2.977408999572650483 ) ) ;
#20947=CARTESIAN_POINT ( 'NONE',  ( -1.320432766682874540E-15, 3.093749997951610542, 7.188101187500000044 ) ) ;
#20950=CARTESIAN_POINT ( 'NONE',  ( 2.977408999572650927, 1.124999997951610098, -7.188101187500001821 ) ) ;
#20963=CARTESIAN_POINT ( 'NONE',  ( -5.656854249492380582, 103.8125000000000000, -5.656854249492380582 ) ) ;
#20966=CARTESIAN_POINT ( 'NONE',  ( 5.082755093536325930, 14.15624999795161187, -5.082755093536325930 ) ) ;
#20969=CARTESIAN_POINT ( 'NONE',  ( 7.188101187500000044, 110.2812500020483810, -8.802885111219163269E-16 ) ) ;
#20979=VECTOR ( 'NONE', #52068, 999.9999999999998863 ) ;
#20984=ORIENTED_EDGE ( 'NONE', *, *, #23603, .F. ) ;
#20985=CARTESIAN_POINT ( 'NONE',  ( -3.313708498984762496, 92.28124999999998579, 7.999999999999998224 ) ) ;
#21007=ORIENTED_EDGE ( 'NONE', *, *, #46641, .F. ) ;
#21009=CYLINDRICAL_SURFACE ( 'NONE', #5042, 8.000000000000000000 ) ;
#21010=CARTESIAN_POINT ( 'NONE',  ( -7.188101187500000044, 22.21874999795161187, -8.802885111219163269E-16 ) ) ;
#21015=ORIENTED_EDGE ( 'NONE', *, *, #27362, .F. ) ;
#21046=CARTESIAN_POINT ( 'NONE',  ( 8.000000000000000000, 18.00000000000000355, 0.000000000000000000 ) ) ;
#21047=CARTESIAN_POINT ( 'NONE',  ( -8.000000000000000000, 14.25000000000000178, -9.797174393178825657E-16 ) ) ;
#21050=CARTESIAN_POINT ( 'NONE',  ( -7.999999999999998224, 92.28125000409679046, 3.313708498984766493 ) ) ;
#21051=EDGE_CURVE ( 'NONE', #70312, #31825, #55979, .T. ) ;
#21059=ORIENTED_EDGE ( 'NONE', *, *, #50549, .T. ) ;
#21061=CARTESIAN_POINT ( 'NONE',  ( 5.082755093536325042, 92.09375000204838102, -5.082755093536325930 ) ) ;
#21082=CARTESIAN_POINT ( 'NONE',  ( -8.000000000000000000, 90.68750000409677625, 0.000000000000000000 ) ) ;
#21085=CARTESIAN_POINT ( 'NONE',  ( 3.313708498984762052, 7.593749995903221972, -8.000000000000000000 ) ) ;
#21088=CARTESIAN_POINT ( 'NONE',  ( -5.082755093536326818, 10.78124999795161187, 5.082755093536325042 ) ) ;
#21091=CARTESIAN_POINT ( 'NONE',  ( -7.999999999999998224, 105.5937500000000000, 3.313708498984766049 ) ) ;
#21092=CARTESIAN_POINT ( 'NONE',  ( 5.082755093536326818, 104.0937500020483810, 5.082755093536325042 ) ) ;
#21110=CYLINDRICAL_SURFACE ( 'NONE', #49134, 8.000000000000000000 ) ;
#21111=CARTESIAN_POINT ( 'NONE',  ( 5.082755093536326818, 99.21875000204838102, 5.082755093536325042 ) ) ;
#21117=CARTESIAN_POINT ( 'NONE',  ( -2.977408999572651815, 105.3125000020483668, 7.188101187500000933 ) ) ;
#21122=CARTESIAN_POINT ( 'NONE',  ( -3.313708498984765161, 1.031250000000000000, 7.999999999999998224 ) ) ;
#21140=CARTESIAN_POINT ( 'NONE',  ( -2.977408999572650039, 11.43749999795161010, -7.188101187500001821 ) ) ;
#21141=CARTESIAN_POINT ( 'NONE',  ( -7.999999999999998224, 107.2812500040967620, 3.313708498984766493 ) ) ;
#21161=CARTESIAN_POINT ( 'NONE',  ( 3.313708498984657247, 91.15625000409677625, 8.000000000000106581 ) ) ;
#21167=CARTESIAN_POINT ( 'NONE',  ( -5.656854249492378806, 107.1874999999999858, 5.656854249492381470 ) ) ;
#21173=CARTESIAN_POINT ( 'NONE',  ( 8.000000000000000000, 19.31249999590322020, 0.000000000000000000 ) ) ;
#21176=CARTESIAN_POINT ( 'NONE',  ( 5.656854249492381470, 121.0625000000000000, 5.656854249492379694 ) ) ;
#21188=CARTESIAN_POINT ( 'NONE',  ( -3.313708498984805573, 26.34374999590322020, 7.999999999999956479 ) ) ;
#21194=DIRECTION ( 'NONE',  ( -0.7071067811865525687, -0.7071067811865425767, -0.000000000000000000 ) ) ;
#21197=CARTESIAN_POINT ( 'NONE',  ( 1.320432766682874540E-15, 120.0312500020483810, 7.188101187500000044 ) ) ;
#21203=CARTESIAN_POINT ( 'NONE',  ( -5.082755093536325930, 118.3437500020483810, -5.082755093536325930 ) ) ;
#21225=ORIENTED_EDGE ( 'NONE', *, *, #40075, .F. ) ;
#21230=CARTESIAN_POINT ( 'NONE',  ( 4.401442555609581635E-16, 20.34374999795161543, -7.188101187500000044 ) ) ;
#21233=CARTESIAN_POINT ( 'NONE',  ( -2.977408999572650039, 17.81249999795161543, -7.188101187500001821 ) ) ;
#21255=CARTESIAN_POINT ( 'NONE',  ( 7.188101187500002709, 95.18750000204838102, 2.977408999572649151 ) ) ;
#21259=VECTOR ( 'NONE', #57430, 1000.000000000000000 ) ;
#21285=CARTESIAN_POINT ( 'NONE',  ( -7.188101187499999156, 101.7500000020483810, 2.977408999572654924 ) ) ;
#21298=VERTEX_POINT ( 'NONE', #7253 ) ;
#21304=CARTESIAN_POINT ( 'NONE',  ( -3.313708498984765161, 18.84374999590322020, 7.999999999999998224 ) ) ;
#21311=FACE_OUTER_BOUND ( 'NONE', #4256, .T. ) ;
#21314=CARTESIAN_POINT ( 'NONE',  ( 5.082755093536324154, 15.65624999795161365, 5.082755093536326818 ) ) ;
#21320=DIRECTION ( 'NONE',  ( -0.000000000000000000, 1.000000000000000000, -0.000000000000000000 ) ) ;
#21324=CARTESIAN_POINT ( 'NONE',  ( -7.188101187500002709, 2.812499997951610098, 2.977408999572649151 ) ) ;
#21342=CARTESIAN_POINT ( 'NONE',  ( -7.188101187500002709, 8.812499997951611874, 2.977408999572649151 ) ) ;
#21346=CARTESIAN_POINT ( 'NONE',  ( -7.188101187499999156, 114.1250000020483952, 2.977408999572654924 ) ) ;
#21349=ORIENTED_EDGE ( 'NONE', *, *, #15500, .F. ) ;
#21352=CARTESIAN_POINT ( 'NONE',  ( 5.656854249492381470, 106.0625000000000000, 5.656854249492379694 ) ) ;
#21358=CARTESIAN_POINT ( 'NONE',  ( -4.898587196589412829E-16, 91.62499999999998579, -8.000000000000000000 ) ) ;
#21372=CARTESIAN_POINT ( 'NONE',  ( 1.469576158976823947E-15, 90.87500000000000000, 8.000000000000000000 ) ) ;
#21377=CARTESIAN_POINT ( 'NONE',  ( 4.898587196589412829E-16, 12.37500000000000178, -8.000000000000000000 ) ) ;
#21382=CARTESIAN_POINT ( 'NONE',  ( -2.977408999572650039, 17.43749999795161187, -7.188101187500001821 ) ) ;
#21386=ORIENTED_EDGE ( 'NONE', *, *, #11595, .F. ) ;
#21387=EDGE_CURVE ( 'NONE', #29800, #56053, #21833, .T. ) ;
#21390=CARTESIAN_POINT ( 'NONE',  ( -1.469576158976823947E-15, 17.62500000000000000, 8.000000000000000000 ) ) ;
#21393=CARTESIAN_POINT ( 'NONE',  ( 8.000000000000001776, 121.3437500040967763, 3.313708498984759387 ) ) ;
#21405=VERTEX_POINT ( 'NONE', #18937 ) ;
#21407=DIRECTION ( 'NONE',  ( 8.659560562354994488E-17, -0.7071067811865425767, 0.7071067811865525687 ) ) ;
#21419=CARTESIAN_POINT ( 'NONE',  ( 4.898587196589412829E-16, 12.37500000000000178, -8.000000000000000000 ) ) ;
#21421=CARTESIAN_POINT ( 'NONE',  ( -3.313708498984762052, 93.40625000409677625, -8.000000000000000000 ) ) ;
#21425=EDGE_CURVE ( 'NONE', #28769, #50841, #34439, .T. ) ;
#21433=CARTESIAN_POINT ( 'NONE',  ( 2.977408999572650039, 93.68750000204838102, -7.188101187500001821 ) ) ;
#21448=DIRECTION ( 'NONE',  ( -0.000000000000000000, 1.000000000000000000, -0.000000000000000000 ) ) ;
#21455=CARTESIAN_POINT ( 'NONE',  ( -8.000000000000000000, 8.062499995903221972, -9.797174393178825657E-16 ) ) ;
#21459=CARTESIAN_POINT ( 'NONE',  ( -2.977408999572650039, 19.31249999795161543, -7.188101187500001821 ) ) ;
#21461=CYLINDRICAL_SURFACE ( 'NONE', #25048, 8.000000000000000000 ) ;
#21462=CARTESIAN_POINT ( 'NONE',  ( -4.401442555609581635E-16, 101.6562500020483810, -7.188101187500000044 ) ) ;
#21481=CARTESIAN_POINT ( 'NONE',  ( -5.082755093536325930, 96.96875000204838102, -5.082755093536325930 ) ) ;
#21489=CARTESIAN_POINT ( 'NONE',  ( 2.977408999572650039, 104.5625000020483668, -7.188101187500001821 ) ) ;
#21494=ORIENTED_EDGE ( 'NONE', *, *, #45013, .F. ) ;
#21514=CARTESIAN_POINT ( 'NONE',  ( 7.188101187500000044, 9.468749997951610098, 0.000000000000000000 ) ) ;
#21515=CARTESIAN_POINT ( 'NONE',  ( -8.000000000000000000, 108.5937500040967905, -3.313708498984761608 ) ) ;
#21526=ORIENTED_EDGE ( 'NONE', *, *, #28863, .T. ) ;
#21538=CARTESIAN_POINT ( 'NONE',  ( -5.656854249492380582, 111.3125000000000000, -5.656854249492380582 ) ) ;
#21540=CARTESIAN_POINT ( 'NONE',  ( 8.000000000000000000, 104.7500000000000000, -9.797174393178825657E-16 ) ) ;
#21546=CARTESIAN_POINT ( 'NONE',  ( 3.313708498984762496, 28.03124999590322020, 7.999999999999998224 ) ) ;
#21548=CARTESIAN_POINT ( 'NONE',  ( -7.188101187500000933, 124.4375000020483810, -2.977408999572650483 ) ) ;
#21549=CARTESIAN_POINT ( 'NONE',  ( 8.000000000000000000, 121.3437500000000000, -3.313708498984762496 ) ) ;
#21561=CARTESIAN_POINT ( 'NONE',  ( 8.000000000000000000, 101.9375000040967763, -9.797174393178825657E-16 ) ) ;
#21568=CARTESIAN_POINT ( 'NONE',  ( -7.188101187500000933, 118.0625000020483952, -2.977408999572650483 ) ) ;
#21574=CARTESIAN_POINT ( 'NONE',  ( 2.977408999572654480, 122.0000000020483668, 7.188101187499999156 ) ) ;
#21597=ORIENTED_EDGE ( 'NONE', *, *, #70627, .T. ) ;
#21598=CARTESIAN_POINT ( 'NONE',  ( -8.000000000000000000, 2.156250000000000444, -3.313708498984762496 ) ) ;
#21601=CARTESIAN_POINT ( 'NONE',  ( 7.188101187500000044, 20.34374999795161543, 0.000000000000000000 ) ) ;
#21605=( BOUNDED_CURVE ( )  B_SPLINE_CURVE ( 2, ( #25568, #37661, #48581, #71591, #60278, #19913, #67070, #8604, #25938 ),
 .UNSPECIFIED., .F., .F. ) 
 B_SPLINE_CURVE_WITH_KNOTS ( ( 3, 2, 2, 2, 3 ),
 ( 0.4861111111111111605, 0.4930555555555556357, 0.5000000000000000000, 0.5069444444444444198, 0.5138888888888888395 ),
 .UNSPECIFIED. ) 
 CURVE ( )  GEOMETRIC_REPRESENTATION_ITEM ( )  RATIONAL_B_SPLINE_CURVE ( ( 0.9999999999999994449, 0.9238795325112872936, 1.000000000000000000, 0.9238795325112867385, 1.000000000000000000, 0.9238795325112867385, 1.000000000000000000, 0.9238795325112867385, 1.000000000000000000 ) ) 
 REPRESENTATION_ITEM ( '' )  );
#21619=CARTESIAN_POINT ( 'NONE',  ( -7.188101187500000044, 26.71874999795161543, -8.802885111219163269E-16 ) ) ;
#21621=ORIENTED_EDGE ( 'NONE', *, *, #72345, .T. ) ;
#21626=CARTESIAN_POINT ( 'NONE',  ( 2.977408999572654480, 90.50000000204840944, 7.188101187499999156 ) ) ;
#21629=ORIENTED_EDGE ( 'NONE', *, *, #34414, .F. ) ;
#21633=CARTESIAN_POINT ( 'NONE',  ( 5.656854249492378806, 11.81250000000000178, 5.656854249492381470 ) ) ;
#21636=CARTESIAN_POINT ( 'NONE',  ( -4.898587196589412829E-16, 88.81250000409677625, -8.000000000000000000 ) ) ;
#21646=CARTESIAN_POINT ( 'NONE',  ( -5.656854249492381470, 17.43750000000000000, 5.656854249492379694 ) ) ;
#21650=CARTESIAN_POINT ( 'NONE',  ( 3.594044162775203777, 89.15552387383502264, -6.225081946264263699 ) ) ;
#21656=CARTESIAN_POINT ( 'NONE',  ( -7.188101187500001821, 106.0625000020483668, -2.977408999572650483 ) ) ;
#21662=EDGE_LOOP ( 'NONE', ( #23215, #70754, #35055, #37314, #41854, #53838, #12063, #16750 ) ) ;
#21668=ORIENTED_EDGE ( 'NONE', *, *, #35527, .T. ) ;
#21675=ORIENTED_EDGE ( 'NONE', *, *, #65683, .T. ) ;
#21677=CARTESIAN_POINT ( 'NONE',  ( 1.469576158976823947E-15, 106.0625000040967763, 8.000000000000000000 ) ) ;
#21681=CARTESIAN_POINT ( 'NONE',  ( -7.188101187500000044, 19.59374999795161543, -8.802885111219163269E-16 ) ) ;
#21685=CARTESIAN_POINT ( 'NONE',  ( -5.656854249492380582, 96.50000000409677625, -5.656854249492380582 ) ) ;
#21690=CARTESIAN_POINT ( 'NONE',  ( 7.188101187499999156, 9.374999997951610098, 2.977408999572654924 ) ) ;
#21705=CARTESIAN_POINT ( 'NONE',  ( 5.656854249492380582, 6.187500000000000888, -5.656854249492380582 ) ) ;
#21707=CARTESIAN_POINT ( 'NONE',  ( -7.188101187500000933, 11.62499999795160832, -2.977408999572651371 ) ) ;
#21711=CARTESIAN_POINT ( 'NONE',  ( 5.082755093536325042, 108.9687500020483810, -5.082755093536325930 ) ) ;
#21727=CARTESIAN_POINT ( 'NONE',  ( -5.656854249492380582, 93.31249999999998579, -5.656854249492380582 ) ) ;
#21738=LINE ( 'NONE', #40217, #42361 ) ;
#21742=CARTESIAN_POINT ( 'NONE',  ( 7.188101187500000044, 123.4062500020483810, -8.802885111219163269E-16 ) ) ;
#21747=CARTESIAN_POINT ( 'NONE',  ( -1.469576158976823947E-15, 13.12500000000000355, 8.000000000000000000 ) ) ;
#21750=CARTESIAN_POINT ( 'NONE',  ( 5.656854249492379694, 92.93749999999998579, -5.656854249492380582 ) ) ;
#21751=CARTESIAN_POINT ( 'NONE',  ( 7.188101187500000044, 19.96874999795161543, 0.000000000000000000 ) ) ;
#21785=CARTESIAN_POINT ( 'NONE',  ( 5.656854249492378806, 10.31250000000000178, 5.656854249492381470 ) ) ;
#21787=CARTESIAN_POINT ( 'NONE',  ( -5.656854249492380582, 93.50000000409677625, -5.656854249492380582 ) ) ;
#21798=CARTESIAN_POINT ( 'NONE',  ( -4.401442555609581635E-16, 92.28125000204836681, -7.188101187500000044 ) ) ;
#21816=EDGE_CURVE ( 'NONE', #31249, #4353, #11278, .T. ) ;
#21820=CARTESIAN_POINT ( 'NONE',  ( 8.000000000000000000, 7.312499995903221084, 0.000000000000000000 ) ) ;
#21823=CARTESIAN_POINT ( 'NONE',  ( -7.188101187500001821, 16.49999999795161543, -2.977408999572651371 ) ) ;
#21826=CARTESIAN_POINT ( 'NONE',  ( -7.188101187500000044, 103.5312500020483810, 0.000000000000000000 ) ) ;
#21833=( BOUNDED_CURVE ( )  B_SPLINE_CURVE ( 2, ( #23483, #6147, #46495, #47232, #40843, #30628, #6518, #70617, #63851 ),
 .UNSPECIFIED., .F., .F. ) 
 B_SPLINE_CURVE_WITH_KNOTS ( ( 3, 2, 2, 2, 3 ),
 ( 0.7604166666666667407, 0.7656250000000001110, 0.7708333333333334814, 0.7760416666666667407, 0.7812500000000001110 ),
 .UNSPECIFIED. ) 
 CURVE ( )  GEOMETRIC_REPRESENTATION_ITEM ( )  RATIONAL_B_SPLINE_CURVE ( ( 0.9999999999999983347, 0.9238795325112884038, 1.000000000000000000, 0.9238795325112867385, 1.000000000000000000, 0.9238795325112867385, 1.000000000000000000, 0.9238795325112850731, 1.000000000000001554 ) ) 
 REPRESENTATION_ITEM ( '' )  );
#21845=CARTESIAN_POINT ( 'NONE',  ( -2.977408999572650927, 92.37500000204838102, -7.188101187500000933 ) ) ;
#21853=CARTESIAN_POINT ( 'NONE',  ( -5.082755093536324154, 103.7187500020483810, 5.082755093536326818 ) ) ;
#21855=CARTESIAN_POINT ( 'NONE',  ( -2.712922267096666396, 0.4730691518507174065, -7.505356363334990455 ) ) ;
#21871=DIRECTION ( 'NONE',  ( 0.000000000000000000, 0.000000000000000000, 1.000000000000000000 ) ) ;
#21882=CARTESIAN_POINT ( 'NONE',  ( -7.188101187500000044, 16.21874999795161543, -8.802885111219163269E-16 ) ) ;
#21883=CARTESIAN_POINT ( 'NONE',  ( -5.656854249492378806, 108.8750000040967763, 5.656854249492381470 ) ) ;
#21891=CARTESIAN_POINT ( 'NONE',  ( 5.082755093536326818, 109.7187500020483810, 5.082755093536325042 ) ) ;
#21907=CARTESIAN_POINT ( 'NONE',  ( 3.313708498984765161, 108.9687500000000000, 7.999999999999998224 ) ) ;
#21910=CARTESIAN_POINT ( 'NONE',  ( 3.313708498984761608, 1.781250000000000222, -8.000000000000000000 ) ) ;
#21913=CARTESIAN_POINT ( 'NONE',  ( -7.188101187500000044, 1.593749997951610320, -8.802885111219163269E-16 ) ) ;
#21915=CARTESIAN_POINT ( 'NONE',  ( 7.188101187500002709, 120.6875000020483952, 2.977408999572649151 ) ) ;
#21919=CARTESIAN_POINT ( 'NONE',  ( -3.313708498984869966, 114.4062500040967763, -7.999999999999892530 ) ) ;
#21928=CARTESIAN_POINT ( 'NONE',  ( 5.656854249492381470, 101.7500000040967905, 5.656854249492379694 ) ) ;
#21929=VERTEX_POINT ( 'NONE', #53841 ) ;
#21937=CARTESIAN_POINT ( 'NONE',  ( -7.188101187500000044, 115.1562500020483810, 0.000000000000000000 ) ) ;
#21942=EDGE_CURVE ( 'NONE', #24630, #31077, #13670, .T. ) ;
#21944=CARTESIAN_POINT ( 'NONE',  ( 5.082755093536326818, 120.5937500020483952, 5.082755093536325042 ) ) ;
#21947=CARTESIAN_POINT ( 'NONE',  ( 0.000000000000000000, 125.0000000000000000, 8.000000000000000000 ) ) ;
#21958=( BOUNDED_CURVE ( )  B_SPLINE_CURVE ( 2, ( #15600, #55991, #51427, #5791, #68779, #34478, #22747, #39737, #40111 ),
 .UNSPECIFIED., .F., .F. ) 
 B_SPLINE_CURVE_WITH_KNOTS ( ( 3, 2, 2, 2, 3 ),
 ( 0.8472222222222222099, 0.8541666666666666297, 0.8611111111111111605, 0.8680555555555555802, 0.8750000000000000000 ),
 .UNSPECIFIED. ) 
 CURVE ( )  GEOMETRIC_REPRESENTATION_ITEM ( )  RATIONAL_B_SPLINE_CURVE ( ( 1.000000000000000000, 0.9238795325112867385, 1.000000000000000000, 0.9238795325112867385, 1.000000000000000000, 0.9238795325112867385, 1.000000000000000000, 0.9238795325112867385, 1.000000000000000000 ) ) 
 REPRESENTATION_ITEM ( '' )  );
#21963=EDGE_CURVE ( 'NONE', #54549, #4192, #42504, .T. ) ;
#21969=ORIENTED_EDGE ( 'NONE', *, *, #15670, .T. ) ;
#21970=CARTESIAN_POINT ( 'NONE',  ( 5.082755093536324154, 27.28124999795161543, 5.082755093536326818 ) ) ;
#21973=CARTESIAN_POINT ( 'NONE',  ( -7.188101187500000044, 15.09374999795161187, -8.802885111219163269E-16 ) ) ;
#21979=DIRECTION ( 'NONE',  ( -0.000000000000000000, 1.000000000000000000, -0.000000000000000000 ) ) ;
#22000=CARTESIAN_POINT ( 'NONE',  ( -3.313708498984762496, 122.2812500000000000, 7.999999999999998224 ) ) ;
#22028=CARTESIAN_POINT ( 'NONE',  ( -2.977408999572651815, 101.9375000020483810, 7.188101187500000933 ) ) ;
#22038=ORIENTED_EDGE ( 'NONE', *, *, #26049, .T. ) ;
#22041=CARTESIAN_POINT ( 'NONE',  ( 5.656854249492378806, 4.312500000000000000, 5.656854249492381470 ) ) ;
#22047=DIRECTION ( 'NONE',  ( -0.000000000000000000, 1.000000000000000000, -0.000000000000000000 ) ) ;
#22050=CARTESIAN_POINT ( 'NONE',  ( -7.188101187500000933, 22.49999999795161187, -2.977408999572651371 ) ) ;
#22058=CARTESIAN_POINT ( 'NONE',  ( 2.977408999572651815, 9.187499997951610098, 7.188101187500000933 ) ) ;
#22078=CARTESIAN_POINT ( 'NONE',  ( 7.188101187499999156, 9.374999997951610098, 2.977408999572654924 ) ) ;
#22084=CARTESIAN_POINT ( 'NONE',  ( -7.188101187500000044, 105.0312500020483810, 0.000000000000000000 ) ) ;
#22085=DIRECTION ( 'NONE',  ( 0.000000000000000000, -1.000000000000000000, 0.000000000000000000 ) ) ;
#22099=DIRECTION ( 'NONE',  ( -0.000000000000000000, 1.000000000000000000, -0.000000000000000000 ) ) ;
#22107=CARTESIAN_POINT ( 'NONE',  ( -5.656854249492381470, 20.43750000000000355, 5.656854249492379694 ) ) ;
#22113=CARTESIAN_POINT ( 'NONE',  ( -7.188101187499999156, 121.2500000020483952, 2.977408999572654924 ) ) ;
#22121=CARTESIAN_POINT ( 'NONE',  ( 7.188101187500000044, 24.46874999795161543, 0.000000000000000000 ) ) ;
#22147=CARTESIAN_POINT ( 'NONE',  ( 1.469576158976823947E-15, 120.8750000000000000, 8.000000000000000000 ) ) ;
#22157=CARTESIAN_POINT ( 'NONE',  ( 5.656854249492380582, 9.187500000000001776, -5.656854249492380582 ) ) ;
#22160=CARTESIAN_POINT ( 'NONE',  ( 8.000000000000001776, 94.34375000409679046, 3.313708498984759387 ) ) ;
#22161=CARTESIAN_POINT ( 'NONE',  ( -4.898587196589412829E-16, 115.8125000040967763, -8.000000000000000000 ) ) ;
#22171=CARTESIAN_POINT ( 'NONE',  ( -4.898587196589412829E-16, 120.1250000000000000, -8.000000000000000000 ) ) ;
#22172=CARTESIAN_POINT ( 'NONE',  ( -7.188101187500001821, 121.4375000020483668, -2.977408999572650483 ) ) ;
#22173=EDGE_CURVE ( 'NONE', #1217, #73206, #1147, .T. ) ;
#22195=CARTESIAN_POINT ( 'NONE',  ( 3.313708498984762052, 6.093749995903220196, -8.000000000000000000 ) ) ;
#22198=CARTESIAN_POINT ( 'NONE',  ( 2.977408999572650927, 16.12499999795161187, -7.188101187500001821 ) ) ;
#22201=CARTESIAN_POINT ( 'NONE',  ( 2.977408999572650039, 103.0625000020483810, -7.188101187500000933 ) ) ;
#22217=CARTESIAN_POINT ( 'NONE',  ( 7.188101187500000044, 96.40625000204838102, -8.802885111219163269E-16 ) ) ;
#22223=CARTESIAN_POINT ( 'NONE',  ( 7.188101187500001821, 99.87500000204838102, -2.977408999572651371 ) ) ;
#22225=CARTESIAN_POINT ( 'NONE',  ( -2.381929342090383095, 0.4663230313613501155, -7.609644401983861606 ) ) ;
#22234=CARTESIAN_POINT ( 'NONE',  ( -4.898587196589412829E-16, 121.8125000040967763, -8.000000000000000000 ) ) ;
#22248=CARTESIAN_POINT ( 'NONE',  ( 7.188101187500001821, 15.56249999795161365, -2.977408999572650483 ) ) ;
#22249=CARTESIAN_POINT ( 'NONE',  ( 1.469576158976823947E-15, 109.0625000040967905, 8.000000000000000000 ) ) ;
#22257=CARTESIAN_POINT ( 'NONE',  ( 5.082755093536326818, 102.2187500020483810, 5.082755093536325042 ) ) ;
#22261=CARTESIAN_POINT ( 'NONE',  ( -3.313708498984744732, 123.2187500000000142, -8.000000000000019540 ) ) ;
#22276=CYLINDRICAL_SURFACE ( 'NONE', #65115, 8.000000000000000000 ) ;
#22278=CARTESIAN_POINT ( 'NONE',  ( -3.313708498984762052, 106.7187500000000000, -8.000000000000000000 ) ) ;
#22281=CARTESIAN_POINT ( 'NONE',  ( 4.898587196589412829E-16, 1.875000000000000444, -8.000000000000000000 ) ) ;
#22283=CARTESIAN_POINT ( 'NONE',  ( -5.656854249492381470, 24.74999999590322375, 5.656854249492379694 ) ) ;
#22285=CARTESIAN_POINT ( 'NONE',  ( 1.320432766682874540E-15, 120.4062500020483810, 7.188101187500000044 ) ) ;
#22304=CARTESIAN_POINT ( 'NONE',  ( 1.320432766682874540E-15, 112.5312500020483952, 7.188101187500000044 ) ) ;
#22309=CARTESIAN_POINT ( 'NONE',  ( 5.082755093536325042, 122.4687500020483952, -5.082755093536325930 ) ) ;
#22332=CARTESIAN_POINT ( 'NONE',  ( 7.188101187500001821, 24.56249999795161543, -2.977408999572650483 ) ) ;
#22335=CARTESIAN_POINT ( 'NONE',  ( 7.188101187500000044, 24.84374999795161543, 0.000000000000000000 ) ) ;
#22351=EDGE_CURVE ( 'NONE', #16528, #54702, #62095, .T. ) ;
#22360=CARTESIAN_POINT ( 'NONE',  ( -8.000000000000000000, 123.4062500000000142, -3.313708498984761608 ) ) ;
#22391=CARTESIAN_POINT ( 'NONE',  ( 7.188101187500001821, 101.0000000020483810, -2.977408999572651371 ) ) ;
#22411=CARTESIAN_POINT ( 'NONE',  ( 1.469576158976823947E-15, 101.3750000000000000, 8.000000000000000000 ) ) ;
#22418=CARTESIAN_POINT ( 'NONE',  ( 7.188101187500000933, 23.43749999795161187, -2.977408999572650483 ) ) ;
#22422=VERTEX_POINT ( 'NONE', #33448 ) ;
#22427=CARTESIAN_POINT ( 'NONE',  ( -5.082755093536326818, 11.90624999795161010, 5.082755093536325042 ) ) ;
#22430=CARTESIAN_POINT ( 'NONE',  ( -4.898587196589412829E-16, 114.1250000000000000, -8.000000000000000000 ) ) ;
#22431=CARTESIAN_POINT ( 'NONE',  ( -7.188101187500002709, 3.187499997951610098, 2.977408999572649151 ) ) ;
#22441=VECTOR ( 'NONE', #19502, 1000.000000000000000 ) ;
#22446=CARTESIAN_POINT ( 'NONE',  ( -2.977408999572654480, 19.49999999795161898, 7.188101187499999156 ) ) ;
#22450=CARTESIAN_POINT ( 'NONE',  ( 1.320432766682874540E-15, 103.9062500020483810, 7.188101187500000044 ) ) ;
#22460=DIRECTION ( 'NONE',  ( 0.000000000000000000, 0.000000000000000000, 1.000000000000000000 ) ) ;
#22468=CARTESIAN_POINT ( 'NONE',  ( -5.656854249492379694, 5.062500000000000888, -5.656854249492380582 ) ) ;
#22472=ORIENTED_EDGE ( 'NONE', *, *, #65405, .F. ) ;
#22474=CARTESIAN_POINT ( 'NONE',  ( -5.656854249492379694, 20.06250000000000355, -5.656854249492380582 ) ) ;
#22479=CARTESIAN_POINT ( 'NONE',  ( -5.082755093536324154, 121.3437500020483952, 5.082755093536326818 ) ) ;
#22489=CARTESIAN_POINT ( 'NONE',  ( 4.401442555609581635E-16, 26.34374999795161543, -7.188101187500000044 ) ) ;
#22511=CARTESIAN_POINT ( 'NONE',  ( 5.082755093536324154, 5.156249997951610098, 5.082755093536326818 ) ) ;
#22518=CARTESIAN_POINT ( 'NONE',  ( -5.656854249492381470, 2.249999995903220196, 5.656854249492379694 ) ) ;
#22524=ORIENTED_EDGE ( 'NONE', *, *, #19333, .F. ) ;
#22528=CARTESIAN_POINT ( 'NONE',  ( -8.000000000000000000, 17.25000000000000000, -9.797174393178825657E-16 ) ) ;
#22533=CARTESIAN_POINT ( 'NONE',  ( 3.313708498984765161, 89.65625000409679046, 7.999999999999998224 ) ) ;
#22536=CARTESIAN_POINT ( 'NONE',  ( -5.656854249492381470, 8.437500000000000000, 5.656854249492379694 ) ) ;
#22541=CARTESIAN_POINT ( 'NONE',  ( 5.656854249492379694, 113.9375000000000000, -5.656854249492380582 ) ) ;
#22544=CARTESIAN_POINT ( 'NONE',  ( 2.977408999572654480, 123.5000000020483952, 7.188101187499999156 ) ) ;
#22568=CARTESIAN_POINT ( 'NONE',  ( 5.656854249492378806, 11.62499999590322197, 5.656854249492381470 ) ) ;
#22572=CARTESIAN_POINT ( 'NONE',  ( 7.188101187500001821, 15.93749999795161543, -2.977408999572650483 ) ) ;
#22574=CARTESIAN_POINT ( 'NONE',  ( 4.898587196589412829E-16, 7.875000000000001776, -8.000000000000000000 ) ) ;
#22575=CARTESIAN_POINT ( 'NONE',  ( -2.977408999572652260, 106.8125000020483952, 7.188101187500000044 ) ) ;
#22585=DIRECTION ( 'NONE',  ( -0.000000000000000000, 1.000000000000000000, -0.000000000000000000 ) ) ;
#22592=CARTESIAN_POINT ( 'NONE',  ( 5.082755093536326818, 96.21875000204838102, 5.082755093536325042 ) ) ;
#22598=CARTESIAN_POINT ( 'NONE',  ( -5.082755093536324154, 94.71875000204838102, 5.082755093536326818 ) ) ;
#22623=CARTESIAN_POINT ( 'NONE',  ( -7.188101187500002709, 16.31249999795161543, 2.977408999572649151 ) ) ;
#22624=CARTESIAN_POINT ( 'NONE',  ( -4.898587196589412829E-16, 108.3125000040967905, -8.000000000000000000 ) ) ;
#22632=CARTESIAN_POINT ( 'NONE',  ( -7.188101187499999156, 106.2500000020484094, 2.977408999572654924 ) ) ;
#22635=CARTESIAN_POINT ( 'NONE',  ( -4.898587196589412829E-16, 97.81250000409677625, -8.000000000000000000 ) ) ;
#22640=ORIENTED_EDGE ( 'NONE', *, *, #27010, .F. ) ;
#22642=CARTESIAN_POINT ( 'NONE',  ( 8.000000000000000000, 91.53125000409679046, -3.313708498984762496 ) ) ;
#22650=CARTESIAN_POINT ( 'NONE',  ( 3.313708498984760720, 105.0312500000000000, -8.000000000000000000 ) ) ;
#22656=CARTESIAN_POINT ( 'NONE',  ( 5.656854249492378806, 28.12499999590322375, 5.656854249492381470 ) ) ;
#22658=CARTESIAN_POINT ( 'NONE',  ( -7.188101187500000933, 119.9375000020483952, -2.977408999572650483 ) ) ;
#22669=CARTESIAN_POINT ( 'NONE',  ( 4.898587196589412829E-16, 25.68749999590322375, -8.000000000000000000 ) ) ;
#22680=CARTESIAN_POINT ( 'NONE',  ( 1.320432766682874540E-15, 111.0312500020483810, 7.188101187500000044 ) ) ;
#22686=CARTESIAN_POINT ( 'NONE',  ( -7.188101187500000044, 118.5312500020483810, 0.000000000000000000 ) ) ;
#22707=ORIENTED_EDGE ( 'NONE', *, *, #47817, .T. ) ;
#22711=CARTESIAN_POINT ( 'NONE',  ( -3.313708498984760720, 0.4687499999999999445, -8.000000000000000000 ) ) ;
#22714=CARTESIAN_POINT ( 'NONE',  ( -7.188101187500001821, 23.99999999795161543, -2.977408999572651371 ) ) ;
#22732=ORIENTED_EDGE ( 'NONE', *, *, #25172, .T. ) ;
#22739=CARTESIAN_POINT ( 'NONE',  ( 8.000000000000000000, 124.2500000000000000, -9.797174393178825657E-16 ) ) ;
#22743=CONICAL_SURFACE ( 'NONE', #67363, 7.500000000000020428, 0.7853981633974552734 ) ;
#22747=CARTESIAN_POINT ( 'NONE',  ( -5.656854249492381470, 23.43750000000000355, 5.656854249492379694 ) ) ;
#22768=CARTESIAN_POINT ( 'NONE',  ( -5.082755093536325930, 101.4687500020483810, -5.082755093536325930 ) ) ;
#22770=FACE_OUTER_BOUND ( 'NONE', #25365, .T. ) ;
#22777=CARTESIAN_POINT ( 'NONE',  ( 0.000000000000000000, 0.5000000000000004441, 0.000000000000000000 ) ) ;
#22785=CARTESIAN_POINT ( 'NONE',  ( 3.313708498984697215, 116.6562500040967620, 8.000000000000063949 ) ) ;
#22794=CARTESIAN_POINT ( 'NONE',  ( -7.188101187500000044, 25.59374999795161543, -8.802885111219163269E-16 ) ) ;
#22798=DIRECTION ( 'NONE',  ( -0.000000000000000000, 1.000000000000000000, -0.000000000000000000 ) ) ;
#22803=CARTESIAN_POINT ( 'NONE',  ( -2.977408999572654480, 11.99999999795161187, 7.188101187499999156 ) ) ;
#22806=CARTESIAN_POINT ( 'NONE',  ( 2.977408999572650927, 7.124999997951610098, -7.188101187500001821 ) ) ;
#22825=CARTESIAN_POINT ( 'NONE',  ( 7.188101187500000933, 15.56249999795161365, -2.977408999572650483 ) ) ;
#22829=CARTESIAN_POINT ( 'NONE',  ( 1.320432766682874540E-15, 106.9062500020483810, 7.188101187500000044 ) ) ;
#22855=ORIENTED_EDGE ( 'NONE', *, *, #46697, .T. ) ;
#22864=CARTESIAN_POINT ( 'NONE',  ( 7.188101187500002709, 120.3125000020483668, 2.977408999572649151 ) ) ;
#22874=CARTESIAN_POINT ( 'NONE',  ( -2.977408999572650039, 24.93749999795161543, -7.188101187500001821 ) ) ;
#22889=CARTESIAN_POINT ( 'NONE',  ( -3.313708498984870410, 92.28124999999998579, 7.999999999999890754 ) ) ;
#22897=CARTESIAN_POINT ( 'NONE',  ( 5.082755093536325930, 4.031249997951610986, -5.082755093536325930 ) ) ;
#22901=CARTESIAN_POINT ( 'NONE',  ( 1.469576158976823947E-15, 122.5625000040967763, 8.000000000000000000 ) ) ;
#22913=CARTESIAN_POINT ( 'NONE',  ( 7.999999999999998224, 17.90625000000000355, 3.313708498984766493 ) ) ;
#22916=CARTESIAN_POINT ( 'NONE',  ( 7.188101187500000044, 121.9062500020483810, -8.802885111219163269E-16 ) ) ;
#22958=CARTESIAN_POINT ( 'NONE',  ( 2.977408999572651815, 15.56249999795161365, 7.188101187500000933 ) ) ;
#22961=CARTESIAN_POINT ( 'NONE',  ( 5.082755093536325042, 99.96875000204838102, -5.082755093536325930 ) ) ;
#22979=CARTESIAN_POINT ( 'NONE',  ( 7.188101187500000933, 93.50000000204838102, -2.977408999572651371 ) ) ;
#22986=CARTESIAN_POINT ( 'NONE',  ( -2.977408999572650927, 95.75000000204836681, -7.188101187500001821 ) ) ;
#22998=VECTOR ( 'NONE', #13053, 1000.000000000000000 ) ;
#23008=CARTESIAN_POINT ( 'NONE',  ( -7.188101187500002709, 11.81249999795161187, 2.977408999572649151 ) ) ;
#23009=CARTESIAN_POINT ( 'NONE',  ( 8.000000000000000000, 103.4375000040967763, -9.797174393178825657E-16 ) ) ;
#23019=CARTESIAN_POINT ( 'NONE',  ( 2.977408999572654480, 102.1250000020483810, 7.188101187499999156 ) ) ;
#23026=ORIENTED_EDGE ( 'NONE', *, *, #6526, .F. ) ;
#23034=CARTESIAN_POINT ( 'NONE',  ( 8.000000000000000000, 97.25000000000000000, -9.797174393178825657E-16 ) ) ;
#23038=CARTESIAN_POINT ( 'NONE',  ( 2.977408999572650927, 1.124999997951610098, -7.188101187500001821 ) ) ;
#23040=CARTESIAN_POINT ( 'NONE',  ( 5.082755093536325042, 120.9687500020483952, -5.082755093536325930 ) ) ;
#23044=CARTESIAN_POINT ( 'NONE',  ( -8.000000000000001776, 3.843750000000000888, 3.313708498984759387 ) ) ;
#23060=CARTESIAN_POINT ( 'NONE',  ( 7.999999999999998224, 7.218749995903221972, 3.313708498984766049 ) ) ;
#23061=CARTESIAN_POINT ( 'NONE',  ( 7.188101187500002709, 109.8125000020483952, 2.977408999572649151 ) ) ;
#23067=CARTESIAN_POINT ( 'NONE',  ( 7.188101187500000044, 113.2812500020483952, -8.802885111219163269E-16 ) ) ;
#23068=CARTESIAN_POINT ( 'NONE',  ( -7.999999999999998224, 120.7812500040967905, 3.313708498984766049 ) ) ;
#23079=CARTESIAN_POINT ( 'NONE',  ( 5.656854249492381470, 103.0625000000000000, 5.656854249492379694 ) ) ;
#23091=CARTESIAN_POINT ( 'NONE',  ( 7.188101187500000044, 25.96874999795161543, 0.000000000000000000 ) ) ;
#23095=CARTESIAN_POINT ( 'NONE',  ( 2.977408999572651815, 26.06249999795161543, 7.188101187500000933 ) ) ;
#23101=EDGE_LOOP ( 'NONE', ( #38897, #42931, #21526, #37939, #7460, #12891 ) ) ;
#23118=CARTESIAN_POINT ( 'NONE',  ( 8.000000000000001776, 121.1562499999999858, 3.313708498984759387 ) ) ;
#23144=CARTESIAN_POINT ( 'NONE',  ( -3.313708498984830442, 116.4687500040967763, 7.999999999999930722 ) ) ;
#23149=CARTESIAN_POINT ( 'NONE',  ( -4.401442555609581635E-16, 98.28125000204838102, -7.188101187500000044 ) ) ;
#23155=EDGE_LOOP ( 'NONE', ( #63342, #16515, #55098, #28761 ) ) ;
#23159=CARTESIAN_POINT ( 'NONE',  ( 4.898587196589412829E-16, 15.37500000000000355, -8.000000000000000000 ) ) ;
#23173=CARTESIAN_POINT ( 'NONE',  ( 2.977408999572650927, 26.62499999795161543, -7.188101187500000933 ) ) ;
#23184=CARTESIAN_POINT ( 'NONE',  ( 5.082755093536325930, 9.656249997951610098, -5.082755093536325930 ) ) ;
#23187=CARTESIAN_POINT ( 'NONE',  ( -7.188101187500001821, 5.999999997951610098, -2.977408999572651371 ) ) ;
#23204=CARTESIAN_POINT ( 'NONE',  ( -1.320432766682874540E-15, 16.59374999795161543, 7.188101187500000044 ) ) ;
#23209=CARTESIAN_POINT ( 'NONE',  ( 5.082755093536325042, 107.4687500020483952, -5.082755093536325930 ) ) ;
#23213=CARTESIAN_POINT ( 'NONE',  ( 1.469576158976823947E-15, 112.0625000040967905, 8.000000000000000000 ) ) ;
#23215=ORIENTED_EDGE ( 'NONE', *, *, #21425, .T. ) ;
#23224=CARTESIAN_POINT ( 'NONE',  ( -3.313708498984816231, 119.2812499999999858, 7.999999999999943157 ) ) ;
#23225=CARTESIAN_POINT ( 'NONE',  ( 2.143582570168941270, 90.06435469398866189, -8.000000000000000000 ) ) ;
#23231=LINE ( 'NONE', #29273, #69974 ) ;
#23233=AXIS2_PLACEMENT_3D ( 'NONE', #60572, #36095, #65854 ) ;
#23238=EDGE_CURVE ( 'NONE', #66596, #16961, #25775, .T. ) ;
#23240=CARTESIAN_POINT ( 'NONE',  ( -4.401442555609581635E-16, 122.2812500020483810, -7.188101187500000044 ) ) ;
#23249=CARTESIAN_POINT ( 'NONE',  ( -1.320432766682874540E-15, 24.09374999795161543, 7.188101187500000044 ) ) ;
#23270=CARTESIAN_POINT ( 'NONE',  ( 4.401442555609581635E-16, 7.218749997951610986, -7.188101187500000044 ) ) ;
#23285=CARTESIAN_POINT ( 'NONE',  ( -8.000000000000000000, 18.65625000000000355, -3.313708498984762496 ) ) ;
#23288=CARTESIAN_POINT ( 'NONE',  ( 7.188101187500002709, 123.3125000020483810, 2.977408999572649151 ) ) ;
#23305=ORIENTED_EDGE ( 'NONE', *, *, #52160, .F. ) ;
#23319=ORIENTED_EDGE ( 'NONE', *, *, #29592, .T. ) ;
#23325=CARTESIAN_POINT ( 'NONE',  ( 7.188101187499999156, 23.24999999795161187, 2.977408999572654924 ) ) ;
#23328=CARTESIAN_POINT ( 'NONE',  ( -5.082755093536324154, 97.71875000204838102, 5.082755093536326818 ) ) ;
#23346=CARTESIAN_POINT ( 'NONE',  ( 7.188101187500000933, 95.00000000204838102, -2.977408999572651371 ) ) ;
#23351=CARTESIAN_POINT ( 'NONE',  ( 2.977408999572650039, 98.56250000204838102, -7.188101187500001821 ) ) ;
#23376=CARTESIAN_POINT ( 'NONE',  ( 1.469576158976823947E-15, 103.0625000040967763, 8.000000000000000000 ) ) ;
#23377=( BOUNDED_CURVE ( )  B_SPLINE_CURVE ( 2, ( #68322, #21548, #11355, #16620, #33640, #45308, #73982, #38550, #5699, #16246, #61551, #27581, #15883, #38915, #50222, #39284, #62286, #5330, #50590, #61917, #32900, #73243, #10614, #34390, #56647, #51340, #73608, #44574, #4216, #4962, #28698, #33269, #27963, #57391, #59, #51712, #45677, #74348, #23040, #56268, #10242, #21915, #67587, #67213, #22285, #62653, #39655, #10987, #34020, #22658, #28332, #68692, #17002, #40028, #55905, #63030, #27205, #9873, #15510, #40400, #29820, #63773, #11724, #1538, #70548, #12459, #63398, #40766, #69440, #12820, #12090, #64149, #35128, #24144, #58870, #23786, #30187, #17376, #18864, #7181, #53205, #64883, #58143, #1165, #35489, #1888, #34764, #17751, #59241, #6450, #58501, #29453, #6807, #29079, #69071, #46051, #24518, #47156, #47523, #70188, #52832, #18497, #57766, #41870, #18128, #52462, #30558, #6072, #41506, #431, #13185, #64522, #35855, #36223, #7550, #52099, #53573, #46790, #23411, #800, #69812, #46426, #41144, #54692, #37333, #65246, #37711, #8658, #36956, #30919, #25619, #66744, #19964, #9033, #59962, #2254, #36589, #42970, #38085, #65621, #65991, #2631, #25982, #8280, #14672, #48633, #7913, #49383, #14296, #31290, #53940, #9410, #31673, #20332, #60330, #3001, #66366, #32045, #25247, #72017, #54320, #48264, #59600, #61082, #55065, #49007, #70913, #19227, #71643, #42606, #13551, #3374, #72402, #43348, #42233, #19590, #71271, #60711, #13917, #26361, #20714, #24874, #43730, #15050, #32428, #55439, #47893, #10525, #56561, #22575, #44484, #33557, #44859, #34303, #49768, #50139, #16918, #67497, #67864, #15796, #39198, #62200, #72785, #3749, #10153, #4876, #44115, #74266, #39941, #38831, #61834, #68240, #55816, #33933, #56932, #45595, #27871, #26750, #21092, #61461, #33190, #67124, #38459, #68609, #21826, #73519, #50882, #15419, #73896, #22201, #62947, #56187, #45228, #16157, #9787, #32808, #73154, #11271, #4499, #16533, #27492, #4133, #39573, #27124, #21462, #50505, #62569, #10899, #5248, #28248, #51256, #46340, #47073, #34677, #12743, #35774, #1457, #18045, #57307, #51631, #40312, #6732, #22961, #17293, #47446, #717, #1087, #58424, #74646, #41430, #29375, #52010, #41793, #45970, #29736, #11641, #24438, #52751, #23701, #35414, #64070, #24063, #57682, #70110, #18416, #68984, #23328, #5990, #12013, #12378, #69730, #63315, #64442, #41060, #69357, #28992, #58058, #70470, #52382, #58789, #17667, #348, #46706, #18788, #40685, #7099, #64802, #13104, #5618, #30107, #53124, #28618, #63686, #35046, #6369, #14211, #53858, #66653, #70832, #43643, #19508, #2915, #43265, #42147, #8571, #42526, #37249, #1809, #31587, #19144, #53492, #8946, #30475, #19880, #54235, #36877, #13471, #36510, #65160, #49297, #31958, #59519, #25903, #30837, #2544, #2170, #60245, #48920, #13831, #59885, #7832, #25165, #48182, #72314, #54983, #3290, #66280, #65540, #54608, #71189, #8198, #71933, #31210, #20245, #7470, #60623, #14587, #37626, #25535, #48548, #26276, #71558, #42886, #65905, #20627 ),
 .UNSPECIFIED., .F., .F. ) 
 B_SPLINE_CURVE_WITH_KNOTS ( ( 3, 2, 2, 2, 2, 2, 2, 2, 2, 2, 2, 2, 2, 2, 2, 2, 2, 2, 2, 2, 2, 2, 2, 2, 2, 2, 2, 2, 2, 2, 2, 2, 2, 2, 2, 2, 2, 2, 2, 2, 2, 2, 2, 2, 2, 2, 2, 2, 2, 2, 2, 2, 2, 2, 2, 2, 2, 2, 2, 2, 2, 2, 2, 2, 2, 2, 2, 2, 2, 2, 2, 2, 2, 2, 2, 2, 2, 2, 2, 2, 2, 2, 2, 2, 2, 2, 2, 2, 2, 2, 2, 2, 2, 2, 2, 2, 2, 2, 2, 2, 2, 2, 2, 2, 2, 2, 2, 2, 2, 2, 2, 2, 2, 2, 2, 2, 2, 2, 2, 2, 2, 2, 2, 2, 2, 2, 2, 2, 2, 2, 2, 2, 2, 2, 2, 2, 2, 2, 2, 2, 2, 2, 2, 2, 2, 2, 2, 2, 2, 2, 2, 2, 2, 2, 2, 2, 2, 2, 2, 2, 2, 2, 2, 2, 2, 2, 2, 2, 2, 2, 2, 2, 2, 2, 2, 2, 2, 2, 2, 2, 2, 2, 2, 2, 2, 2, 2, 3 ),
 ( 0.000000000000000000, 0.005357197731506658372, 0.01071439546301331674, 0.01607159319451997859, 0.02142879092602663349, 0.02678598865753329533, 0.03214318638903995717, 0.03750038412054661208, 0.04285758185205326698, 0.04821477958355992882, 0.05357197731506659066, 0.05892917504657324557, 0.06428637277807991435, 0.06964357050958655537, 0.07500076824109322415, 0.08035796597259987906, 0.08571516370410653396, 0.09107236143561320274, 0.09642955916711985764, 0.1017867568986265125, 0.1071439546301331813, 0.1125011523616398362, 0.1178583500931464911, 0.1232155478246531599, 0.1285727455561598287, 0.1339299432876664975, 0.1392871410191731107, 0.1446443387506797795, 0.1500015364821864483, 0.1553587342136930893, 0.1607159319451997581, 0.1660731296767064269, 0.1714303274082130679, 0.1767875251397197367, 0.1821447228712264055, 0.1875019206027330465, 0.1928591183342397153, 0.1982163160657463841, 0.2035735137972530251, 0.2089307115287596939, 0.2142879092602663627, 0.2196451069917730037, 0.2250023047232796725, 0.2303595024547863412, 0.2357167001862929823, 0.2410738979177996510, 0.2464310956493063198, 0.2517882933808129886, 0.2571454911123196574, 0.2625026888438262707, 0.2678598865753329950, 0.2732170843068396082, 0.2785742820383462215, 0.2839314797698529458, 0.2892886775013595591, 0.2946458752328662278, 0.3000030729643728966, 0.3053602706958795654, 0.3107174684273861787, 0.3160746661588929030, 0.3214318638903995162, 0.3267890616219061850, 0.3321462593534128538, 0.3375034570849195226, 0.3428606548164261358, 0.3482178525479328601, 0.3535750502794394734, 0.3589322480109461422, 0.3642894457424528110, 0.3696466434739594797, 0.3750038412054660930, 0.3803610389369728173, 0.3857182366684794306, 0.3910754343999860994, 0.3964326321314927681, 0.4017898298629994369, 0.4071470275945060502, 0.4125042253260127745, 0.4178614230575193877, 0.4232186207890260565, 0.4285758185205327253, 0.4339330162520393941, 0.4392902139835460074, 0.4446474117150527317, 0.4500046094465593449, 0.4553618071780660137, 0.4607190049095726825, 0.4660762026410793513, 0.4714334003725859645, 0.4767905981040926888, 0.4821477958355993021, 0.4875049935671059709, 0.4928621912986126397, 0.4982193890301193084, 0.5035765867616259772, 0.5089337844931326460, 0.5142909822246393148, 0.5196481799561459836, 0.5250053776876525413, 0.5303625754191592101, 0.5357197731506659899, 0.5410769708821725477, 0.5464341686136792164, 0.5517913663451858852, 0.5571485640766924430, 0.5625057618081992228, 0.5678629595397058916, 0.5732201572712124493, 0.5785773550027191181, 0.5839345527342258979, 0.5892917504657324557, 0.5946489481972391244, 0.6000061459287457932, 0.6053633436602524620, 0.6107205413917591308, 0.6160777391232657996, 0.6214349368547723573, 0.6267921345862791371, 0.6321493323177858059, 0.6375065300492923637, 0.6428637277807990325, 0.6482209255123058123, 0.6535781232438123700, 0.6589353209753190388, 0.6642925187068257076, 0.6696497164383323764, 0.6750069141698390451, 0.6803641119013457139, 0.6857213096328522717, 0.6910785073643590515, 0.6964357050958657203, 0.7017929028273722780, 0.7071501005588789468, 0.7125072982903857266, 0.7178644960218922844, 0.7232216937533989531, 0.7285788914849056219, 0.7339360892164122907, 0.7392932869479189595, 0.7446504846794256283, 0.7500076824109321860, 0.7553648801424389658, 0.7607220778739456346, 0.7660792756054521924, 0.7714364733369588611, 0.7767936710684656409, 0.7821508687999721987, 0.7875080665314788675, 0.7928652642629855363, 0.7982224619944920940, 0.8035796597259988738, 0.8089368574575055426, 0.8142940551890121004, 0.8196512529205187692, 0.8250084506520255490, 0.8303656483835321067, 0.8357228461150387755, 0.8410800438465454443, 0.8464372415780521131, 0.8517944393095587818, 0.8571516370410654506, 0.8625088347725720084, 0.8678660325040787882, 0.8732232302355854570, 0.8785804279670920147, 0.8839376256985986835, 0.8892948234301054633, 0.8946520211616120211, 0.9000092188931186898, 0.9053664166246253586, 0.9107236143561320274, 0.9160808120876386962, 0.9214380098191453650, 0.9267952075506519227, 0.9321524052821587025, 0.9375096030136653713, 0.9428668007451719291, 0.9482239984766785978, 0.9535811962081853776, 0.9589383939396919354, 0.9642955916711986042, 0.9696527894027052730, 0.9750099871342119418, 0.9803671848657186105, 0.9857243825972252793, 0.9910815803287318371, 0.9964387780602386169, 1.000000000000000000 ),
 .UNSPECIFIED. ) 
 CURVE ( )  GEOMETRIC_REPRESENTATION_ITEM ( )  RATIONAL_B_SPLINE_CURVE ( ( 1.000000000000000000, 0.9238795325112867385, 1.000000000000000000, 0.9238795325112867385, 1.000000000000000000, 0.9238795325112867385, 1.000000000000000000, 0.9238795325112867385, 1.000000000000000000, 0.9238795325112867385, 1.000000000000000000, 0.9238795325112867385, 1.000000000000000000, 0.9238795325112867385, 1.000000000000000000, 0.9238795325112867385, 1.000000000000000000, 0.9238795325112867385, 1.000000000000000000, 0.9238795325112867385, 1.000000000000000000, 0.9238795325112867385, 1.000000000000000000, 0.9238795325112867385, 1.000000000000000000, 0.9238795325112867385, 1.000000000000000000, 0.9238795325112867385, 1.000000000000000000, 0.9238795325112867385, 1.000000000000000000, 0.9238795325112867385, 1.000000000000000000, 0.9238795325112867385, 1.000000000000000000, 0.9238795325112867385, 1.000000000000000000, 0.9238795325112867385, 1.000000000000000000, 0.9238795325112867385, 1.000000000000000000, 0.9238795325112867385, 1.000000000000000000, 0.9238795325112867385, 1.000000000000000000, 0.9238795325112867385, 1.000000000000000000, 0.9238795325112867385, 1.000000000000000000, 0.9238795325112867385, 1.000000000000000000, 0.9238795325112867385, 1.000000000000000000, 0.9238795325112867385, 1.000000000000000000, 0.9238795325112867385, 1.000000000000000000, 0.9238795325112867385, 1.000000000000000000, 0.9238795325112867385, 1.000000000000000000, 0.9238795325112867385, 1.000000000000000000, 0.9238795325112867385, 1.000000000000000000, 0.9238795325112867385, 1.000000000000000000, 0.9238795325112867385, 1.000000000000000000, 0.9238795325112867385, 1.000000000000000000, 0.9238795325112867385, 1.000000000000000000, 0.9238795325112867385, 1.000000000000000000, 0.9238795325112867385, 1.000000000000000000, 0.9238795325112867385, 1.000000000000000000, 0.9238795325112867385, 1.000000000000000000, 0.9238795325112867385, 1.000000000000000000, 0.9238795325112867385, 1.000000000000000000, 0.9238795325112867385, 1.000000000000000000, 0.9238795325112867385, 1.000000000000000000, 0.9238795325112867385, 1.000000000000000000, 0.9238795325112867385, 1.000000000000000000, 0.9238795325112867385, 1.000000000000000000, 0.9238795325112867385, 1.000000000000000000, 0.9238795325112867385, 1.000000000000000000, 0.9238795325112867385, 1.000000000000000000, 0.9238795325112867385, 1.000000000000000000, 0.9238795325112867385, 1.000000000000000000, 0.9238795325112867385, 1.000000000000000000, 0.9238795325112867385, 1.000000000000000000, 0.9238795325112867385, 1.000000000000000000, 0.9238795325112867385, 1.000000000000000000, 0.9238795325112867385, 1.000000000000000000, 0.9238795325112867385, 1.000000000000000000, 0.9238795325112867385, 1.000000000000000000, 0.9238795325112867385, 1.000000000000000000, 0.9238795325112867385, 1.000000000000000000, 0.9238795325112867385, 1.000000000000000000, 0.9238795325112867385, 1.000000000000000000, 0.9238795325112867385, 1.000000000000000000, 0.9238795325112867385, 1.000000000000000000, 0.9238795325112867385, 1.000000000000000000, 0.9238795325112867385, 1.000000000000000000, 0.9238795325112867385, 1.000000000000000000, 0.9238795325112867385, 1.000000000000000000, 0.9238795325112867385, 1.000000000000000000, 0.9238795325112867385, 1.000000000000000000, 0.9238795325112867385, 1.000000000000000000, 0.9238795325112867385, 1.000000000000000000, 0.9238795325112867385, 1.000000000000000000, 0.9238795325112867385, 1.000000000000000000, 0.9238795325112867385, 1.000000000000000000, 0.9238795325112867385, 1.000000000000000000, 0.9238795325112867385, 1.000000000000000000, 0.9238795325112867385, 1.000000000000000000, 0.9238795325112867385, 1.000000000000000000, 0.9238795325112867385, 1.000000000000000000, 0.9238795325112867385, 1.000000000000000000, 0.9238795325112867385, 1.000000000000000000, 0.9238795325112867385, 1.000000000000000000, 0.9238795325112867385, 1.000000000000000000, 0.9238795325112867385, 1.000000000000000000, 0.9238795325112867385, 1.000000000000000000, 0.9238795325112867385, 1.000000000000000000, 0.9238795325112867385, 1.000000000000000000, 0.9238795325112867385, 1.000000000000000000, 0.9238795325112867385, 1.000000000000000000, 0.9238795325112867385, 1.000000000000000000, 0.9238795325112867385, 1.000000000000000000, 0.9238795325112867385, 1.000000000000000000, 0.9238795325112867385, 1.000000000000000000, 0.9238795325112867385, 1.000000000000000000, 0.9238795325112867385, 1.000000000000000000, 0.9238795325112867385, 1.000000000000000000, 0.9238795325112867385, 1.000000000000000000, 0.9238795325112867385, 1.000000000000000000, 0.9238795325112867385, 1.000000000000000000, 0.9238795325112867385, 1.000000000000000000, 0.9238795325112867385, 1.000000000000000000, 0.9238795325112867385, 1.000000000000000000, 0.9238795325112867385, 1.000000000000000000, 0.9238795325112867385, 1.000000000000000000, 0.9238795325112867385, 1.000000000000000000, 0.9238795325112867385, 1.000000000000000000, 0.9238795325112867385, 1.000000000000000000, 0.9238795325112867385, 1.000000000000000000, 0.9238795325112867385, 1.000000000000000000, 0.9238795325112867385, 1.000000000000000000, 0.9238795325112867385, 1.000000000000000000, 0.9238795325112867385, 1.000000000000000000, 0.9238795325112867385, 1.000000000000000000, 0.9238795325112867385, 1.000000000000000000, 0.9238795325112867385, 1.000000000000000000, 0.9238795325112867385, 1.000000000000000000, 0.9238795325112867385, 1.000000000000000000, 0.9238795325112867385, 1.000000000000000000, 0.9238795325112867385, 1.000000000000000000, 0.9238795325112867385, 1.000000000000000000, 0.9238795325112867385, 1.000000000000000000, 0.9238795325112867385, 1.000000000000000000, 0.9238795325112867385, 1.000000000000000000, 0.9238795325112867385, 1.000000000000000000, 0.9238795325112867385, 1.000000000000000000, 0.9238795325112867385, 1.000000000000000000, 0.9238795325112867385, 1.000000000000000000, 0.9238795325112867385, 1.000000000000000000, 0.9238795325112867385, 1.000000000000000000, 0.9238795325112867385, 1.000000000000000000, 0.9238795325112867385, 1.000000000000000000, 0.9238795325112867385, 1.000000000000000000, 0.9238795325112867385, 1.000000000000000000, 0.9238795325112867385, 1.000000000000000000, 0.9238795325112867385, 1.000000000000000000, 0.9238795325112867385, 1.000000000000000000, 0.9238795325112867385, 1.000000000000000000, 0.9238795325112867385, 1.000000000000000000, 0.9238795325112867385, 1.000000000000000000, 0.9238795325112867385, 1.000000000000000000, 0.9238795325112867385, 1.000000000000000000, 0.9238795325112867385, 1.000000000000000000, 0.9238795325112867385, 1.000000000000000000, 0.9238795325112867385, 1.000000000000000000, 0.9238795325112867385, 1.000000000000000000, 0.9238795325112867385, 1.000000000000000000, 0.9238795325112867385, 1.000000000000000000, 0.9238795325112867385, 1.000000000000000000, 0.9238795325112867385, 1.000000000000000000, 0.9238795325112867385, 1.000000000000000000, 0.9238795325112867385, 1.000000000000000000, 0.9238795325112867385, 1.000000000000000000, 0.9238795325112867385, 1.000000000000000000, 0.9238795325112867385, 1.000000000000000000, 0.9238795325112867385, 1.000000000000000000, 0.9238795325112867385, 1.000000000000000000, 0.9238795325112867385, 1.000000000000000000, 0.9238795325112867385, 1.000000000000000000, 0.9238795325112867385, 1.000000000000000000, 0.9238795325112867385, 1.000000000000000000, 0.9238795325112867385, 1.000000000000000000, 0.9238795325112867385, 1.000000000000000000, 0.9238795325112867385, 1.000000000000000000, 0.9238795325112867385, 1.000000000000000000, 0.9238795325112867385, 1.000000000000000000, 0.9238795325112867385, 1.000000000000000000, 0.9238795325112867385, 1.000000000000000000, 0.9238795325112867385, 1.000000000000000000, 0.9238795325112867385, 1.000000000000000000, 0.9238795325112867385, 1.000000000000000000, 0.9238795325112867385, 1.000000000000000000, 0.9238795325112867385, 1.000000000000000000, 0.9238795325112867385, 1.000000000000000000, 0.9238795325112867385, 1.000000000000000000, 0.9238795325112867385, 1.000000000000000000, 0.9238795325112867385, 1.000000000000000000, 0.9238795325112867385, 1.000000000000000000, 0.9238795325112867385, 1.000000000000000000, 0.9238795325112867385, 1.000000000000000000, 0.9238795325112867385, 1.000000000000000000, 0.9238795325112867385, 1.000000000000000000, 0.9238795325112867385, 1.000000000000000000, 0.9238795325112867385, 1.000000000000000000, 0.9238795325112867385, 1.000000000000000000, 0.9493985675959992765, 0.9660722070829144137 ) ) 
 REPRESENTATION_ITEM ( '' )  );
#23386=CARTESIAN_POINT ( 'NONE',  ( -2.977408999572650927, 102.8750000020483810, -7.188101187500001821 ) ) ;
#23388=CARTESIAN_POINT ( 'NONE',  ( -8.000000000000000000, 123.4062500000000142, -3.313708498984761164 ) ) ;
#23402=CARTESIAN_POINT ( 'NONE',  ( 3.313708498984765161, 98.46875000000000000, 7.999999999999998224 ) ) ;
#23405=CARTESIAN_POINT ( 'NONE',  ( -3.313708498984761608, 102.4062500040967763, -8.000000000000000000 ) ) ;
#23407=CARTESIAN_POINT ( 'NONE',  ( -2.977408999572650039, 5.812499997951610098, -7.188101187500001821 ) ) ;
#23411=CARTESIAN_POINT ( 'NONE',  ( 5.082755093536325042, 113.4687500020483810, -5.082755093536325930 ) ) ;
#23419=CARTESIAN_POINT ( 'NONE',  ( -3.313708498984760276, 9.468750000000001776, -8.000000000000000000 ) ) ;
#23423=DIRECTION ( 'NONE',  ( -0.000000000000000000, 1.000000000000000000, -0.000000000000000000 ) ) ;
#23431=CARTESIAN_POINT ( 'NONE',  ( -5.082755093536325930, 111.9687500020483810, -5.082755093536325930 ) ) ;
#23436=CARTESIAN_POINT ( 'NONE',  ( -5.082755093536325930, 115.3437500020483810, -5.082755093536325930 ) ) ;
#23462=ORIENTED_EDGE ( 'NONE', *, *, #62624, .T. ) ;
#23463=CARTESIAN_POINT ( 'NONE',  ( 8.000000000000000000, 4.500000000000000888, 0.000000000000000000 ) ) ;
#23464=CARTESIAN_POINT ( 'NONE',  ( 0.000000000000000000, 125.0000000000000000, 8.000000000000000000 ) ) ;
#23466=CARTESIAN_POINT ( 'NONE',  ( -2.977408999572654480, 22.87499999795161187, 7.188101187499999156 ) ) ;
#23467=CARTESIAN_POINT ( 'NONE',  ( -4.898587196589412829E-16, 123.3125000040967905, -8.000000000000000000 ) ) ;
#23483=CARTESIAN_POINT ( 'NONE',  ( -4.898587196589412829E-16, 96.31250000409677625, -8.000000000000000000 ) ) ;
#23488=CARTESIAN_POINT ( 'NONE',  ( -5.656854249492380582, 115.8125000000000000, -5.656854249492380582 ) ) ;
#23505=FACE_OUTER_BOUND ( 'NONE', #23155, .T. ) ;
#23521=CARTESIAN_POINT ( 'NONE',  ( 1.320432766682874540E-15, 94.53125000204836681, 7.188101187500000044 ) ) ;
#23524=CARTESIAN_POINT ( 'NONE',  ( 7.683012701892216079, 0.1830127018922207416, 0.000000000000000000 ) ) ;
#23545=CARTESIAN_POINT ( 'NONE',  ( -2.977408999572654480, 24.37499999795161543, 7.188101187499999156 ) ) ;
#23553=CARTESIAN_POINT ( 'NONE',  ( -5.082755093536325042, 17.53124999795161187, -5.082755093536325930 ) ) ;
#23555=EDGE_CURVE ( 'NONE', #21929, #38953, #32519, .T. ) ;
#23557=CARTESIAN_POINT ( 'NONE',  ( 7.188101187499999156, 5.249999997951610098, 2.977408999572654924 ) ) ;
#23569=CARTESIAN_POINT ( 'NONE',  ( 7.188101187500001821, 116.0000000020483810, -2.977408999572651371 ) ) ;
#23574=CARTESIAN_POINT ( 'NONE',  ( 2.977408999572650927, 15.74999999795161365, -7.188101187500000933 ) ) ;
#23579=CARTESIAN_POINT ( 'NONE',  ( 7.188101187500000044, 98.28125000204838102, -8.802885111219163269E-16 ) ) ;
#23594=CARTESIAN_POINT ( 'NONE',  ( -3.313708498984720308, 118.7187499999999716, -8.000000000000040856 ) ) ;
#23603=EDGE_CURVE ( 'NONE', #50120, #28645, #23377, .T. ) ;
#23610=CARTESIAN_POINT ( 'NONE',  ( -7.188101187499999156, 115.2500000020484094, 2.977408999572654924 ) ) ;
#23620=CARTESIAN_POINT ( 'NONE',  ( -1.469576158976823947E-15, 14.62500000000000178, 8.000000000000000000 ) ) ;
#23642=CARTESIAN_POINT ( 'NONE',  ( 1.469576158976823947E-15, 112.0625000040967905, 8.000000000000000000 ) ) ;
#23645=CARTESIAN_POINT ( 'NONE',  ( 7.188101187499999156, 5.249999997951610098, 2.977408999572654924 ) ) ;
#23660=AXIS2_PLACEMENT_3D ( 'NONE', #18985, #71392, #64645 ) ;
#23663=CARTESIAN_POINT ( 'NONE',  ( 3.313708498984762496, 16.21875000000000355, 7.999999999999998224 ) ) ;
#23665=CARTESIAN_POINT ( 'NONE',  ( -7.188101187500001821, 121.0625000020483668, -2.977408999572650483 ) ) ;
#23668=CARTESIAN_POINT ( 'NONE',  ( -3.313708498984740292, 7.968750000000001776, -8.000000000000021316 ) ) ;
#23671=CARTESIAN_POINT ( 'NONE',  ( 7.188101187499999156, 1.874999997951610320, 2.977408999572654924 ) ) ;
#23672=DIRECTION ( 'NONE',  ( -0.000000000000000000, 1.000000000000000000, -0.000000000000000000 ) ) ;
#23674=CARTESIAN_POINT ( 'NONE',  ( -4.401442555609581635E-16, 122.6562500020483810, -7.188101187500000044 ) ) ;
#23683=ORIENTED_EDGE ( 'NONE', *, *, #34546, .T. ) ;
#23699=CARTESIAN_POINT ( 'NONE',  ( 7.188101187500000044, 21.84374999795161543, 0.000000000000000000 ) ) ;
#23701=CARTESIAN_POINT ( 'NONE',  ( 5.082755093536325042, 98.46875000204838102, -5.082755093536325930 ) ) ;
#23717=CARTESIAN_POINT ( 'NONE',  ( -7.188101187500000044, 89.65625000204838102, 0.000000000000000000 ) ) ;
#23724=CARTESIAN_POINT ( 'NONE',  ( 1.320432766682874540E-15, 99.40625000204838102, 7.188101187500000044 ) ) ;
#23731=CARTESIAN_POINT ( 'NONE',  ( 0.000000000000000000, 125.0000000000000000, 0.000000000000000000 ) ) ;
#23739=PRODUCT_DEFINITION_FORMATION_WITH_SPECIFIED_SOURCE ( 'ANY', '', #51143, .NOT_KNOWN. ) ;
#23743=( BOUNDED_CURVE ( )  B_SPLINE_CURVE ( 2, ( #58940, #7245, #59305, #36656, #20023, #37023, #1598, #54005, #2694 ),
 .UNSPECIFIED., .F., .F. ) 
 B_SPLINE_CURVE_WITH_KNOTS ( ( 3, 2, 2, 2, 3 ),
 ( 0.5694444444444444198, 0.5763888888888888395, 0.5833333333333333703, 0.5902777777777777901, 0.5972222222222222099 ),
 .UNSPECIFIED. ) 
 CURVE ( )  GEOMETRIC_REPRESENTATION_ITEM ( )  RATIONAL_B_SPLINE_CURVE ( ( 1.000000000000000000, 0.9238795325112867385, 1.000000000000000000, 0.9238795325112867385, 1.000000000000000000, 0.9238795325112867385, 1.000000000000000000, 0.9238795325112867385, 1.000000000000000000 ) ) 
 REPRESENTATION_ITEM ( '' )  );
#23744=ADVANCED_FACE ( 'NONE', ( #45785 ), #29188, .T. ) ;
#23749=CARTESIAN_POINT ( 'NONE',  ( 1.469576158976823947E-15, 106.0625000040967763, 8.000000000000000000 ) ) ;
#23750=AXIS2_PLACEMENT_3D ( 'NONE', #64943, #18930, #54386 ) ;
#23758=CARTESIAN_POINT ( 'NONE',  ( -3.313708498984805573, 25.03125000000000000, 7.999999999999956479 ) ) ;
#23759=CARTESIAN_POINT ( 'NONE',  ( 7.188101187500001821, 104.0000000020483810, -2.977408999572651371 ) ) ;
#23765=ORIENTED_EDGE ( 'NONE', *, *, #124, .F. ) ;
#23768=CARTESIAN_POINT ( 'NONE',  ( 3.313708498984757167, 2.718750000000000000, 8.000000000000001776 ) ) ;
#23772=DIRECTION ( 'NONE',  ( -0.000000000000000000, 1.000000000000000000, -0.000000000000000000 ) ) ;
#23776=CARTESIAN_POINT ( 'NONE',  ( -5.656854249492378806, 98.18750000000000000, 5.656854249492381470 ) ) ;
#23783=CARTESIAN_POINT ( 'NONE',  ( 4.401442555609581635E-16, 5.718749997951610986, -7.188101187500000044 ) ) ;
#23786=CARTESIAN_POINT ( 'NONE',  ( 2.977408999572654480, 117.5000000020483810, 7.188101187499999156 ) ) ;
#23797=CARTESIAN_POINT ( 'NONE',  ( 3.313708498984755391, 123.9687500000000142, 8.000000000000008882 ) ) ;
#23799=CARTESIAN_POINT ( 'NONE',  ( -4.898587196589412829E-16, 96.12499999999998579, -8.000000000000000000 ) ) ;
#23807=CARTESIAN_POINT ( 'NONE',  ( 7.188101187500002709, 111.3125000020483810, 2.977408999572649151 ) ) ;
#23814=CARTESIAN_POINT ( 'NONE',  ( -7.188101187499999156, 115.6250000020483810, 2.977408999572654924 ) ) ;
#23829=CARTESIAN_POINT ( 'NONE',  ( 0.000000000000000000, 125.0000000000000000, 8.000000000000000000 ) ) ;
#23838=CARTESIAN_POINT ( 'NONE',  ( -3.313708498984765161, 8.531250000000001776, 7.999999999999998224 ) ) ;
#23840=CARTESIAN_POINT ( 'NONE',  ( 5.082755093536325930, 22.03124999795161543, -5.082755093536325930 ) ) ;
#23841=CARTESIAN_POINT ( 'NONE',  ( -8.000000000000000000, 120.5937500040967763, -3.313708498984761608 ) ) ;
#23847=ORIENTED_EDGE ( 'NONE', *, *, #57260, .F. ) ;
#23857=VERTEX_POINT ( 'NONE', #63881 ) ;
#23864=CARTESIAN_POINT ( 'NONE',  ( -8.000000000000000000, 115.9062500000000000, -3.313708498984761608 ) ) ;
#23870=CARTESIAN_POINT ( 'NONE',  ( -1.469576158976823947E-15, 14.43749999590322375, 8.000000000000000000 ) ) ;
#23872=CARTESIAN_POINT ( 'NONE',  ( 3.313708498984761608, 12.09374999590322197, -8.000000000000000000 ) ) ;
#23873=CARTESIAN_POINT ( 'NONE',  ( 5.656854249492378806, 13.12499999590322197, 5.656854249492381470 ) ) ;
#23895=CARTESIAN_POINT ( 'NONE',  ( 5.082755093536326818, 96.21875000204838102, 5.082755093536325042 ) ) ;
#23909=FACE_OUTER_BOUND ( 'NONE', #38439, .T. ) ;
#23920=ORIENTED_EDGE ( 'NONE', *, *, #35627, .F. ) ;
#23924=CARTESIAN_POINT ( 'NONE',  ( -7.188101187500000044, 16.21874999795161543, -8.802885111219163269E-16 ) ) ;
#23927=CARTESIAN_POINT ( 'NONE',  ( 5.082755093536325930, 8.531249997951611874, -5.082755093536325930 ) ) ;
#23934=ORIENTED_EDGE ( 'NONE', *, *, #2140, .F. ) ;
#23940=CARTESIAN_POINT ( 'NONE',  ( -5.082755093536325930, 117.9687500020483810, -5.082755093536325930 ) ) ;
#23945=CARTESIAN_POINT ( 'NONE',  ( -1.320432766682874540E-15, 15.09374999795161187, 7.188101187500000044 ) ) ;
#23950=CARTESIAN_POINT ( 'NONE',  ( 2.977408999572654480, 99.50000000204838102, 7.188101187499999156 ) ) ;
#23952=CARTESIAN_POINT ( 'NONE',  ( 1.469576158976823947E-15, 89.56250000409677625, 8.000000000000000000 ) ) ;
#23954=EDGE_CURVE ( 'NONE', #4200, #48510, #36381, .T. ) ;
#23971=CARTESIAN_POINT ( 'NONE',  ( 3.999985685286083115, 88.68677412680158056, -6.928211494859723985 ) ) ;
#23978=CARTESIAN_POINT ( 'NONE',  ( 2.977408999572654480, 114.1250000020483952, 7.188101187499999156 ) ) ;
#24000=ORIENTED_EDGE ( 'NONE', *, *, #14841, .T. ) ;
#24007=CARTESIAN_POINT ( 'NONE',  ( -2.977408999572650039, 14.81249999795161365, -7.188101187500000933 ) ) ;
#24024=CARTESIAN_POINT ( 'NONE',  ( -8.000000000000000000, 26.15625000000000711, -3.313708498984762496 ) ) ;
#24026=CARTESIAN_POINT ( 'NONE',  ( 2.143584681480918963, 88.75185463835309463, -8.000000000000000000 ) ) ;
#24037=CARTESIAN_POINT ( 'NONE',  ( -5.082755093536324154, 120.2187500020483952, 5.082755093536326818 ) ) ;
#24054=ORIENTED_EDGE ( 'NONE', *, *, #40997, .T. ) ;
#24055=DIRECTION ( 'NONE',  ( -0.000000000000000000, 1.000000000000000000, -0.000000000000000000 ) ) ;
#24061=CARTESIAN_POINT ( 'NONE',  ( -5.082755093536325042, 23.90624999795161543, -5.082755093536325930 ) ) ;
#24063=CARTESIAN_POINT ( 'NONE',  ( 7.188101187500002709, 98.18750000204835260, 2.977408999572649151 ) ) ;
#24072=ORIENTED_EDGE ( 'NONE', *, *, #13403, .F. ) ;
#24079=CARTESIAN_POINT ( 'NONE',  ( 8.000000000000000000, 103.4375000040967763, -9.797174393178825657E-16 ) ) ;
#24083=PRODUCT_DEFINITION_SHAPE ( 'NONE', 'NONE',  #41778 ) ;
#24085=CARTESIAN_POINT ( 'NONE',  ( 5.082755093536326818, 96.59375000204838102, 5.082755093536325042 ) ) ;
#24090=EDGE_LOOP ( 'NONE', ( #70479, #59217, #6606, #33876 ) ) ;
#24092=CARTESIAN_POINT ( 'NONE',  ( -3.313708498984782924, 122.2812500000000142, 7.999999999999979572 ) ) ;
#24105=ORIENTED_EDGE ( 'NONE', *, *, #55138, .F. ) ;
#24108=CARTESIAN_POINT ( 'NONE',  ( -3.313708498984762052, 102.4062500040967763, -8.000000000000000000 ) ) ;
#24110=CARTESIAN_POINT ( 'NONE',  ( 9.797174393178825657E-16, 125.0000000000000000, -8.000000000000000000 ) ) ;
#24117=CARTESIAN_POINT ( 'NONE',  ( -5.082755093536324154, 97.34375000204838102, 5.082755093536326818 ) ) ;
#24119=CARTESIAN_POINT ( 'NONE',  ( 1.469576158976823947E-15, 119.5625000040967763, 8.000000000000000000 ) ) ;
#24124=CARTESIAN_POINT ( 'NONE',  ( -7.999999999999998224, 104.2812500040967905, 3.313708498984766049 ) ) ;
#24141=CARTESIAN_POINT ( 'NONE',  ( 2.977408999572651815, 6.562499997951610098, 7.188101187500000933 ) ) ;
#24144=CARTESIAN_POINT ( 'NONE',  ( 7.188101187500002709, 117.6875000020484237, 2.977408999572649151 ) ) ;
#24164=DIRECTION ( 'NONE',  ( 0.000000000000000000, 0.000000000000000000, 1.000000000000000000 ) ) ;
#24166=CARTESIAN_POINT ( 'NONE',  ( -4.401442555609581635E-16, 105.7812500020483810, -7.188101187500000044 ) ) ;
#24173=CARTESIAN_POINT ( 'NONE',  ( -5.082755093536324154, 114.2187500020483810, 5.082755093536326818 ) ) ;
#24185=CARTESIAN_POINT ( 'NONE',  ( 3.313708498984762496, 14.71875000000000355, 7.999999999999998224 ) ) ;
#24197=CARTESIAN_POINT ( 'NONE',  ( 4.898587196589412829E-16, 4.875000000000000888, -8.000000000000000000 ) ) ;
#24199=CARTESIAN_POINT ( 'NONE',  ( 2.977408999572650927, 0.7499999979516099868, -7.188101187500001821 ) ) ;
#24200=CARTESIAN_POINT ( 'NONE',  ( -3.313708498984762052, 121.9062500040967763, -8.000000000000000000 ) ) ;
#24206=ORIENTED_EDGE ( 'NONE', *, *, #35268, .F. ) ;
#24216=ORIENTED_EDGE ( 'NONE', *, *, #68008, .F. ) ;
#24224=CARTESIAN_POINT ( 'NONE',  ( -7.999999999999998224, 120.5937500000000000, 3.313708498984766493 ) ) ;
#24230=CARTESIAN_POINT ( 'NONE',  ( 8.000000000000000000, 14.90624999590322375, -3.313708498984761608 ) ) ;
#24246=AXIS2_PLACEMENT_3D ( 'NONE', #33221, #9816, #43765 ) ;
#24257=CARTESIAN_POINT ( 'NONE',  ( 2.977408999572654480, 96.12500000204836681, 7.188101187499999156 ) ) ;
#24277=CARTESIAN_POINT ( 'NONE',  ( -4.898587196589412829E-16, 112.6250000000000000, -8.000000000000000000 ) ) ;
#24291=CARTESIAN_POINT ( 'NONE',  ( -5.082755093536325042, 14.53124999795161187, -5.082755093536325930 ) ) ;
#24294=CARTESIAN_POINT ( 'NONE',  ( -2.977408999572650039, 11.81249999795161187, -7.188101187500001821 ) ) ;
#24300=DIRECTION ( 'NONE',  ( 0.000000000000000000, 0.000000000000000000, -1.000000000000000000 ) ) ;
#24307=CARTESIAN_POINT ( 'NONE',  ( -7.188101187500001821, 118.0625000020483952, -2.977408999572650483 ) ) ;
#24312=CARTESIAN_POINT ( 'NONE',  ( 7.188101187500000933, 26.06249999795161543, -2.977408999572650483 ) ) ;
#24315=CARTESIAN_POINT ( 'NONE',  ( 8.000000000000000000, 13.59375000000000178, -3.313708498984761164 ) ) ;
#24318=CARTESIAN_POINT ( 'NONE',  ( -7.188101187500000044, 97.53125000204838102, 0.000000000000000000 ) ) ;
#24346=CARTESIAN_POINT ( 'NONE',  ( -2.502880839332534801, 124.6278065515491562, -7.481218951737261591 ) ) ;
#24347=VECTOR ( 'NONE', #21407, 999.9999999999998863 ) ;
#24349=CARTESIAN_POINT ( 'NONE',  ( -7.188101187499999156, 112.2500000020483952, 2.977408999572654924 ) ) ;
#24381=CARTESIAN_POINT ( 'NONE',  ( 7.188101187500000933, 11.43749999795161187, -2.977408999572650483 ) ) ;
#24385=CARTESIAN_POINT ( 'NONE',  ( 8.000000000000000000, 122.9375000040967905, -9.797174393178825657E-16 ) ) ;
#24394=EDGE_CURVE ( 'NONE', #24466, #55027, #54674, .T. ) ;
#24399=CARTESIAN_POINT ( 'NONE',  ( -3.313708498984760720, 24.46875000000000711, -8.000000000000000000 ) ) ;
#24408=CARTESIAN_POINT ( 'NONE',  ( -7.188101187500002709, 2.812499997951610098, 2.977408999572649151 ) ) ;
#24412=CARTESIAN_POINT ( 'NONE',  ( 7.188101187500000044, 119.2812500020483810, -8.802885111219163269E-16 ) ) ;
#24424=CYLINDRICAL_SURFACE ( 'NONE', #8322, 8.000000000000000000 ) ;
#24436=CARTESIAN_POINT ( 'NONE',  ( 4.401442555609581635E-16, 20.71874999795161543, -7.188101187500000044 ) ) ;
#24438=CARTESIAN_POINT ( 'NONE',  ( -4.401442555609581635E-16, 98.65625000204838102, -7.188101187500000044 ) ) ;
#24448=CARTESIAN_POINT ( 'NONE',  ( -3.313708498984781148, 9.281249995903221972, -7.999999999999981348 ) ) ;
#24454=CARTESIAN_POINT ( 'NONE',  ( 7.188101187500002709, 90.31250000204838102, 2.977408999572649151 ) ) ;
#24461=CARTESIAN_POINT ( 'NONE',  ( -7.188101187499999156, 90.12500000204836681, 2.977408999572654924 ) ) ;
#24466=VERTEX_POINT ( 'NONE', #50988 ) ;
#24467=CARTESIAN_POINT ( 'NONE',  ( -8.000000000000000000, 123.6875000040967905, 0.000000000000000000 ) ) ;
#24473=CARTESIAN_POINT ( 'NONE',  ( -5.656854249492379694, 10.87499999590322020, -5.656854249492380582 ) ) ;
#24477=VERTEX_POINT ( 'NONE', #64173 ) ;
#24484=CARTESIAN_POINT ( 'NONE',  ( 5.656854249492379694, 102.1250000040967763, -5.656854249492380582 ) ) ;
#24494=CARTESIAN_POINT ( 'NONE',  ( -5.082755093536325930, 98.46875000204838102, -5.082755093536325930 ) ) ;
#24502=ORIENTED_EDGE ( 'NONE', *, *, #39361, .T. ) ;
#24515=CARTESIAN_POINT ( 'NONE',  ( 2.977408999572651815, 8.062499997951611874, 7.188101187500000933 ) ) ;
#24518=CARTESIAN_POINT ( 'NONE',  ( -7.188101187500000044, 115.5312500020483952, 0.000000000000000000 ) ) ;
#24525=CARTESIAN_POINT ( 'NONE',  ( -8.000000000000000000, 9.656250000000001776, -3.313708498984762496 ) ) ;
#24529=ORIENTED_EDGE ( 'NONE', *, *, #18477, .T. ) ;
#24537=CARTESIAN_POINT ( 'NONE',  ( -7.188101187500000044, 106.1562500020483810, 0.000000000000000000 ) ) ;
#24542=CARTESIAN_POINT ( 'NONE',  ( 5.082755093536325042, 116.4687500020483810, -5.082755093536325930 ) ) ;
#24569=CARTESIAN_POINT ( 'NONE',  ( -3.313708498984765161, 7.031250000000000888, 7.999999999999998224 ) ) ;
#24571=CARTESIAN_POINT ( 'NONE',  ( 7.188101187500000044, 27.84374999795161543, 0.000000000000000000 ) ) ;
#24573=FACE_OUTER_BOUND ( 'NONE', #47207, .T. ) ;
#24575=CARTESIAN_POINT ( 'NONE',  ( -8.000000000000000000, 6.750000000000000888, -9.797174393178825657E-16 ) ) ;
#24593=CARTESIAN_POINT ( 'NONE',  ( 3.313708498984706985, 105.0312499999999858, -8.000000000000055067 ) ) ;
#24595=CARTESIAN_POINT ( 'NONE',  ( 8.000000000000001776, 119.6562499999999858, 3.313708498984759387 ) ) ;
#24599=CARTESIAN_POINT ( 'NONE',  ( -8.000000000000001776, 15.65624999590322197, 3.313708498984759387 ) ) ;
#24620=CARTESIAN_POINT ( 'NONE',  ( 7.188101187500000933, 123.5000000020483810, -2.977408999572651371 ) ) ;
#24624=CARTESIAN_POINT ( 'NONE',  ( 1.320432766682874540E-15, 97.53125000204838102, 7.188101187500000044 ) ) ;
#24630=VERTEX_POINT ( 'NONE', #53225 ) ;
#24641=CARTESIAN_POINT ( 'NONE',  ( 5.656854249492380582, 17.99999999590322375, -5.656854249492380582 ) ) ;
#24648=ORIENTED_EDGE ( 'NONE', *, *, #37558, .T. ) ;
#24652=CARTESIAN_POINT ( 'NONE',  ( -2.977408999572654480, 14.99999999795161187, 7.188101187499999156 ) ) ;
#24655=CARTESIAN_POINT ( 'NONE',  ( -7.188101187500001821, 14.99999999795161187, -2.977408999572651371 ) ) ;
#24659=EDGE_CURVE ( 'NONE', #54565, #47572, #69462, .T. ) ;
#24667=CARTESIAN_POINT ( 'NONE',  ( 2.977408999572654480, 117.1250000020483952, 7.188101187499999156 ) ) ;
#24672=CARTESIAN_POINT ( 'NONE',  ( 7.188101187500000933, 21.56249999795161543, -2.977408999572650483 ) ) ;
#24678=CARTESIAN_POINT ( 'NONE',  ( -7.188101187500001821, 98.93750000204838102, -2.977408999572650483 ) ) ;
#24697=CARTESIAN_POINT ( 'NONE',  ( -5.656854249492380582, 117.3125000000000000, -5.656854249492380582 ) ) ;
#24700=DIRECTION ( 'NONE',  ( 0.000000000000000000, 0.000000000000000000, 1.000000000000000000 ) ) ;
#24707=CARTESIAN_POINT ( 'NONE',  ( -3.313708498984760276, 4.781249995903220196, -8.000000000000000000 ) ) ;
#24709=CARTESIAN_POINT ( 'NONE',  ( -5.082755093536325930, 116.4687500020483810, -5.082755093536325930 ) ) ;
#24715=ORIENTED_EDGE ( 'NONE', *, *, #65509, .F. ) ;
#24734=CARTESIAN_POINT ( 'NONE',  ( 8.000000000000000000, 22.59375000000000355, -3.313708498984761164 ) ) ;
#24738=CARTESIAN_POINT ( 'NONE',  ( 7.188101187500000044, 11.34374999795161187, 0.000000000000000000 ) ) ;
#24756=CARTESIAN_POINT ( 'NONE',  ( -8.000000000000000000, 21.65625000000000000, -3.313708498984762496 ) ) ;
#24766=CARTESIAN_POINT ( 'NONE',  ( -2.977408999572654480, 7.499999997951610986, 7.188101187499999156 ) ) ;
#24768=CARTESIAN_POINT ( 'NONE',  ( -5.082755093536325930, 119.8437500020483810, -5.082755093536325930 ) ) ;
#24785=ORIENTED_EDGE ( 'NONE', *, *, #39713, .F. ) ;
#24793=CARTESIAN_POINT ( 'NONE',  ( -7.188101187500001821, 23.99999999795161543, -2.977408999572651371 ) ) ;
#24802=ADVANCED_FACE ( 'NONE', ( #55085 ), #21110, .T. ) ;
#24805=ORIENTED_EDGE ( 'NONE', *, *, #68463, .T. ) ;
#24821=CARTESIAN_POINT ( 'NONE',  ( 7.188101187500000044, 90.78125000204838102, -8.802885111219163269E-16 ) ) ;
#24831=CARTESIAN_POINT ( 'NONE',  ( -3.313708498984760276, 10.78124999590322197, -8.000000000000000000 ) ) ;
#24839=CARTESIAN_POINT ( 'NONE',  ( 1.469576158976823947E-15, 97.06250000409677625, 8.000000000000000000 ) ) ;
#24848=CARTESIAN_POINT ( 'NONE',  ( 5.082755093536325042, 101.0937500020483810, -5.082755093536325930 ) ) ;
#24849=CARTESIAN_POINT ( 'NONE',  ( 1.469576158976823947E-15, 92.56250000409677625, 8.000000000000000000 ) ) ;
#24850=CARTESIAN_POINT ( 'NONE',  ( 0.000000000000000000, 125.0000000000000000, -7.500000000000020428 ) ) ;
#24869=CARTESIAN_POINT ( 'NONE',  ( 8.000000000000000000, 4.406249995903220196, -3.313708498984761608 ) ) ;
#24871=CARTESIAN_POINT ( 'NONE',  ( 7.188101187500000044, 8.343749997951611874, 0.000000000000000000 ) ) ;
#24874=CARTESIAN_POINT ( 'NONE',  ( 2.977408999572650039, 107.5625000020483810, -7.188101187500000933 ) ) ;
#24896=CARTESIAN_POINT ( 'NONE',  ( 5.082755093536325042, 105.5937500020483810, -5.082755093536325930 ) ) ;
#24901=CARTESIAN_POINT ( 'NONE',  ( -2.977408999572650927, 106.2500000020484094, -7.188101187500001821 ) ) ;
#24927=CARTESIAN_POINT ( 'NONE',  ( -5.656854249492379694, 3.562500000000000444, -5.656854249492380582 ) ) ;
#24929=CARTESIAN_POINT ( 'NONE',  ( 7.188101187500001821, 2.062499997951610098, -2.977408999572650483 ) ) ;
#24930=CARTESIAN_POINT ( 'NONE',  ( -8.000000000000000000, 113.0937500040968047, -3.313708498984761608 ) ) ;
#24950=CARTESIAN_POINT ( 'NONE',  ( 3.313708498984802020, 27.09374999590321664, -7.999999999999958256 ) ) ;
#24956=EDGE_CURVE ( 'NONE', #41332, #61205, #18545, .T. ) ;
#24958=CARTESIAN_POINT ( 'NONE',  ( 8.000000000000001776, 116.6562500000000000, 3.313708498984759387 ) ) ;
#24963=CARTESIAN_POINT ( 'NONE',  ( 4.898587196589412829E-16, 13.68749999590322375, -8.000000000000000000 ) ) ;
#24965=CARTESIAN_POINT ( 'NONE',  ( 4.898587196589412829E-16, 12.18749999590322197, -8.000000000000000000 ) ) ;
#24976=ORIENTED_EDGE ( 'NONE', *, *, #47243, .F. ) ;
#24989=CARTESIAN_POINT ( 'NONE',  ( 7.188101187500002709, 91.81250000204839523, 2.977408999572649151 ) ) ;
#24991=LINE ( 'NONE', #25363, #33787 ) ;
#25014=CARTESIAN_POINT ( 'NONE',  ( -7.188101187500001821, 16.12499999795161187, -2.977408999572651371 ) ) ;
#25016=CARTESIAN_POINT ( 'NONE',  ( -5.656854249492380582, 117.5000000040967905, -5.656854249492380582 ) ) ;
#25017=CARTESIAN_POINT ( 'NONE',  ( 5.082755093536325930, 11.53124999795161187, -5.082755093536325930 ) ) ;
#25030=CARTESIAN_POINT ( 'NONE',  ( 1.320432766682874540E-15, 115.5312500020483952, 7.188101187500000044 ) ) ;
#25034=CARTESIAN_POINT ( 'NONE',  ( 7.188101187500000933, 23.06249999795161543, -2.977408999572650483 ) ) ;
#25035=EDGE_LOOP ( 'NONE', ( #10043, #50485, #24502, #39442 ) ) ;
#25041=CARTESIAN_POINT ( 'NONE',  ( -7.188101187500001821, 97.43750000204839523, -2.977408999572650483 ) ) ;
#25043=AXIS2_PLACEMENT_3D ( 'NONE', #5551, #28555, #51561 ) ;
#25048=AXIS2_PLACEMENT_3D ( 'NONE', #67123, #15418, #62568 ) ;
#25052=CARTESIAN_POINT ( 'NONE',  ( 0.000000000000000000, 0.000000000000000000, 0.000000000000000000 ) ) ;
#25055=CARTESIAN_POINT ( 'NONE',  ( -4.898587196589412829E-16, 90.12500000000000000, -8.000000000000000000 ) ) ;
#25059=DIRECTION ( 'NONE',  ( -0.000000000000000000, 1.000000000000000000, -0.000000000000000000 ) ) ;
#25071=CARTESIAN_POINT ( 'NONE',  ( -1.016170450681134207, 124.5980567557549250, -7.852785628585370326 ) ) ;
#25074=CARTESIAN_POINT ( 'NONE',  ( -7.188101187500000044, 118.1562500020483810, 0.000000000000000000 ) ) ;
#25092=FACE_OUTER_BOUND ( 'NONE', #40377, .T. ) ;
#25099=CARTESIAN_POINT ( 'NONE',  ( -1.469576158976823947E-15, 22.12500000000000355, 8.000000000000000000 ) ) ;
#25104=CARTESIAN_POINT ( 'NONE',  ( -7.188101187500000933, 10.49999999795161010, -2.977408999572651371 ) ) ;
#25119=CARTESIAN_POINT ( 'NONE',  ( -8.000000000000000000, 21.75000000000000355, -9.797174393178825657E-16 ) ) ;
#25132=CARTESIAN_POINT ( 'NONE',  ( -2.977408999572650039, 3.937499997951610986, -7.188101187500000933 ) ) ;
#25135=CARTESIAN_POINT ( 'NONE',  ( 5.082755093536325042, 120.9687500020483952, -5.082755093536325930 ) ) ;
#25149=CARTESIAN_POINT ( 'NONE',  ( -8.000000000000000000, 100.9999999999999858, 0.000000000000000000 ) ) ;
#25165=CARTESIAN_POINT ( 'NONE',  ( -7.188101187499999156, 91.62500000204836681, 2.977408999572654924 ) ) ;
#25172=EDGE_CURVE ( 'NONE', #27944, #14878, #725, .T. ) ;
#25176=CARTESIAN_POINT ( 'NONE',  ( 9.797174393178825657E-16, 125.0000000000000000, -8.000000000000000000 ) ) ;
#25183=CARTESIAN_POINT ( 'NONE',  ( -4.898587196589412829E-16, 102.1250000000000000, -8.000000000000000000 ) ) ;
#25185=CARTESIAN_POINT ( 'NONE',  ( 5.656854249492379694, 103.6250000040967763, -5.656854249492380582 ) ) ;
#25190=CARTESIAN_POINT ( 'NONE',  ( -7.188101187500001821, 92.93750000204839523, -2.977408999572650483 ) ) ;
#25209=ORIENTED_EDGE ( 'NONE', *, *, #70627, .F. ) ;
#25210=CARTESIAN_POINT ( 'NONE',  ( 8.000000000000000000, 99.03125000409677625, -3.313708498984762496 ) ) ;
#25213=VECTOR ( 'NONE', #70605, 1000.000000000000000 ) ;
#25223=CARTESIAN_POINT ( 'NONE',  ( 5.082755093536325042, 96.59375000204838102, -5.082755093536325930 ) ) ;
#25224=CARTESIAN_POINT ( 'NONE',  ( 7.999999999999998224, 16.21874999590322375, 3.313708498984766049 ) ) ;
#25229=ORIENTED_EDGE ( 'NONE', *, *, #49121, .F. ) ;
#25242=CARTESIAN_POINT ( 'NONE',  ( -3.313708498984760720, 4.781249995903221084, -8.000000000000000000 ) ) ;
#25244=CARTESIAN_POINT ( 'NONE',  ( -7.188101187500000044, 9.093749997951611874, -8.802885111219163269E-16 ) ) ;
#25247=CARTESIAN_POINT ( 'NONE',  ( -5.082755093536324154, 109.7187500020483810, 5.082755093536326818 ) ) ;
#25248=DIRECTION ( 'NONE',  ( -0.000000000000000000, 1.000000000000000000, -0.000000000000000000 ) ) ;
#25259=VERTEX_POINT ( 'NONE', #10834 ) ;
#25267=CARTESIAN_POINT ( 'NONE',  ( 7.188101187500000933, 104.0000000020483810, -2.977408999572651371 ) ) ;
#25273=CARTESIAN_POINT ( 'NONE',  ( 7.188101187500002709, 111.6875000020483810, 2.977408999572649151 ) ) ;
#25275=VERTEX_POINT ( 'NONE', #33869 ) ;
#25278=EDGE_LOOP ( 'NONE', ( #29641, #53008, #31167, #36467 ) ) ;
#25298=CARTESIAN_POINT ( 'NONE',  ( 8.000000000000000000, 13.59375000000000178, -3.313708498984761608 ) ) ;
#25300=CARTESIAN_POINT ( 'NONE',  ( -7.188101187500002709, 4.312499997951610986, 2.977408999572649151 ) ) ;
#25301=CARTESIAN_POINT ( 'NONE',  ( -3.313708498984762052, 115.9062500040967763, -8.000000000000000000 ) ) ;
#25302=EDGE_CURVE ( 'NONE', #73724, #30852, #34694, .T. ) ;
#25309=CARTESIAN_POINT ( 'NONE',  ( 8.000000000000000000, 95.84374999999998579, -3.313708498984762496 ) ) ;
#25325=CARTESIAN_POINT ( 'NONE',  ( -8.000000000000000000, 12.56249999590322197, -9.797174393178825657E-16 ) ) ;
#25328=CARTESIAN_POINT ( 'NONE',  ( -3.313708498984762496, 110.2812499999999858, 7.999999999999998224 ) ) ;
#25332=CARTESIAN_POINT ( 'NONE',  ( 3.313708498984762496, 20.53124999590322020, 7.999999999999998224 ) ) ;
#25335=CARTESIAN_POINT ( 'NONE',  ( 8.000000000000001776, 113.8437500040967905, 3.313708498984759387 ) ) ;
#25355=CARTESIAN_POINT ( 'NONE',  ( -7.188101187499999156, 122.7500000020483668, 2.977408999572654924 ) ) ;
#25361=CARTESIAN_POINT ( 'NONE',  ( 5.082755093536325042, 90.59375000204838102, -5.082755093536325930 ) ) ;
#25363=CARTESIAN_POINT ( 'NONE',  ( 0.000000000000000000, 125.0000000000000000, 8.000000000000000000 ) ) ;
#25365=EDGE_LOOP ( 'NONE', ( #21059, #11254, #1969, #27977 ) ) ;
#25390=EDGE_CURVE ( 'NONE', #493, #47140, #62371, .T. ) ;
#25391=CARTESIAN_POINT ( 'NONE',  ( 2.977408999572650927, 21.74999999795162253, -7.188101187500001821 ) ) ;
#25395=CARTESIAN_POINT ( 'NONE',  ( 2.977408999572650927, 13.12499999795161187, -7.188101187500001821 ) ) ;
#25400=VECTOR ( 'NONE', #66464, 1000.000000000000000 ) ;
#25407=CARTESIAN_POINT ( 'NONE',  ( -2.977408999572651815, 110.9375000020483810, 7.188101187500000933 ) ) ;
#25411=CARTESIAN_POINT ( 'NONE',  ( 4.401442555609581635E-16, 21.84374999795161543, -7.188101187500000044 ) ) ;
#25412=EDGE_LOOP ( 'NONE', ( #52129, #14306, #13415, #5926 ) ) ;
#25417=CARTESIAN_POINT ( 'NONE',  ( 2.977408999572650039, 94.06250000204838102, -7.188101187500001821 ) ) ;
#25447=CARTESIAN_POINT ( 'NONE',  ( 5.082755093536326818, 109.7187500020483810, 5.082755093536325042 ) ) ;
#25454=CARTESIAN_POINT ( 'NONE',  ( 8.000000000000001776, 92.84375000409677625, 3.313708498984759387 ) ) ;
#25474=CARTESIAN_POINT ( 'NONE',  ( -7.188101187500000044, 13.59374999795161187, -8.802885111219163269E-16 ) ) ;
#25483=EDGE_CURVE ( 'NONE', #65546, #49924, #3123, .T. ) ;
#25484=CARTESIAN_POINT ( 'NONE',  ( 9.797174393178825657E-16, 125.0000000000000000, -8.000000000000000000 ) ) ;
#25493=CARTESIAN_POINT ( 'NONE',  ( -1.469576158976823947E-15, 23.62500000000000355, 8.000000000000000000 ) ) ;
#25495=ORIENTED_EDGE ( 'NONE', *, *, #17332, .T. ) ;
#25504=CARTESIAN_POINT ( 'NONE',  ( -5.082755093536326818, 5.906249997951610986, 5.082755093536325042 ) ) ;
#25507=CARTESIAN_POINT ( 'NONE',  ( 5.082755093536325042, 117.9687500020483810, -5.082755093536325930 ) ) ;
#25519=VERTEX_POINT ( 'NONE', #59458 ) ;
#25521=CARTESIAN_POINT ( 'NONE',  ( 1.469576158976823947E-15, 99.87499999999998579, 8.000000000000000000 ) ) ;
#25533=CARTESIAN_POINT ( 'NONE',  ( -7.188101187500000044, 27.09374999795161898, -8.802885111219163269E-16 ) ) ;
#25535=CARTESIAN_POINT ( 'NONE',  ( -7.188101187500000044, 90.03125000204838102, 0.000000000000000000 ) ) ;
#25545=CARTESIAN_POINT ( 'NONE',  ( -5.656854249492379694, 9.374999995903223748, -5.656854249492380582 ) ) ;
#25558=CARTESIAN_POINT ( 'NONE',  ( -7.188101187499999156, 93.12500000204836681, 2.977408999572654924 ) ) ;
#25566=CARTESIAN_POINT ( 'NONE',  ( 7.188101187500000044, 0.6562499979516100979, 0.000000000000000000 ) ) ;
#25568=CARTESIAN_POINT ( 'NONE',  ( -1.469576158976823947E-15, 14.43749999590322375, 8.000000000000000000 ) ) ;
#25583=CARTESIAN_POINT ( 'NONE',  ( 8.000000000000000000, 97.53125000409676204, -3.313708498984762496 ) ) ;
#25593=CARTESIAN_POINT ( 'NONE',  ( 2.977408999572650039, 99.68750000204838102, -7.188101187500001821 ) ) ;
#25594=CARTESIAN_POINT ( 'NONE',  ( -4.898587196589412829E-16, 91.81250000409677625, -8.000000000000000000 ) ) ;
#25596=ORIENTED_EDGE ( 'NONE', *, *, #8272, .T. ) ;
#25598=EDGE_CURVE ( 'NONE', #67076, #28600, #46515, .T. ) ;
#25602=EDGE_CURVE ( 'NONE', #42073, #35953, #16103, .T. ) ;
#25614=CARTESIAN_POINT ( 'NONE',  ( -3.313708498984760720, 3.281249995903220640, -8.000000000000000000 ) ) ;
#25616=CARTESIAN_POINT ( 'NONE',  ( 2.977408999572650927, 11.62499999795161365, -7.188101187500001821 ) ) ;
#25618=FACE_OUTER_BOUND ( 'NONE', #12620, .T. ) ;
#25619=CARTESIAN_POINT ( 'NONE',  ( -5.082755093536325930, 112.3437500020483810, -5.082755093536325930 ) ) ;
#25638=CARTESIAN_POINT ( 'NONE',  ( 5.082755093536325042, 107.0937500020483810, -5.082755093536325930 ) ) ;
#25644=CARTESIAN_POINT ( 'NONE',  ( -5.082755093536325930, 110.8437500020483810, -5.082755093536325930 ) ) ;
#25645=ORIENTED_EDGE ( 'NONE', *, *, #13232, .F. ) ;
#25649=ORIENTED_EDGE ( 'NONE', *, *, #4462, .F. ) ;
#25655=CARTESIAN_POINT ( 'NONE',  ( -5.082755093536326818, 1.781249997951610098, 5.082755093536325042 ) ) ;
#25669=CARTESIAN_POINT ( 'NONE',  ( -5.082755093536326818, 27.28124999795161543, 5.082755093536325042 ) ) ;
#25670=CARTESIAN_POINT ( 'NONE',  ( 8.000000000000001776, 113.8437500040967763, 3.313708498984759387 ) ) ;
#25684=CARTESIAN_POINT ( 'NONE',  ( 8.000000000000000000, 1.312499995903220196, 0.000000000000000000 ) ) ;
#25695=CARTESIAN_POINT ( 'NONE',  ( -8.000000000000000000, 111.4062500000000142, -3.313708498984761608 ) ) ;
#25699=CARTESIAN_POINT ( 'NONE',  ( -3.313708498984760720, 22.78124999590322375, -8.000000000000000000 ) ) ;
#25710=CARTESIAN_POINT ( 'NONE',  ( 3.594044162775203333, 89.15552387383502264, -6.225081946264263699 ) ) ;
#25713=FACE_OUTER_BOUND ( 'NONE', #48786, .T. ) ;
#25714=CARTESIAN_POINT ( 'NONE',  ( -1.469576158976823947E-15, 14.43749999590322375, 8.000000000000000000 ) ) ;
#25727=CARTESIAN_POINT ( 'NONE',  ( -2.977408999572651815, 89.93750000204840944, 7.188101187500000933 ) ) ;
#25746=CARTESIAN_POINT ( 'NONE',  ( 4.898587196589412829E-16, 22.68749999590322375, -8.000000000000000000 ) ) ;
#25753=CARTESIAN_POINT ( 'NONE',  ( 0.000000000000000000, 125.0000000000000000, 0.000000000000000000 ) ) ;
#25757=CARTESIAN_POINT ( 'NONE',  ( 5.082755093536325930, 23.15624999795161543, -5.082755093536325930 ) ) ;
#25759=CARTESIAN_POINT ( 'NONE',  ( -4.898587196589412829E-16, 117.3125000040967763, -8.000000000000000000 ) ) ;
#25760=CARTESIAN_POINT ( 'NONE',  ( 4.401442555609581635E-16, 14.71874999795161187, -7.188101187500000044 ) ) ;
#25765=DIRECTION ( 'NONE',  ( 0.000000000000000000, 0.000000000000000000, 1.000000000000000000 ) ) ;
#25771=CARTESIAN_POINT ( 'NONE',  ( 2.977408999572650039, 113.1875000020483810, -7.188101187500001821 ) ) ;
#25775=( BOUNDED_CURVE ( )  B_SPLINE_CURVE ( 2, ( #29537, #52548, #12177, #12547, #52921, #47607, #35941, #23872, #24965 ),
 .UNSPECIFIED., .F., .F. ) 
 B_SPLINE_CURVE_WITH_KNOTS ( ( 3, 2, 2, 2, 3 ),
 ( 0.3750000000000000000, 0.3819444444444444198, 0.3888888888888888951, 0.3958333333333333148, 0.4027777777777777901 ),
 .UNSPECIFIED. ) 
 CURVE ( )  GEOMETRIC_REPRESENTATION_ITEM ( )  RATIONAL_B_SPLINE_CURVE ( ( 1.000000000000000000, 0.9238795325112867385, 1.000000000000000000, 0.9238795325112867385, 1.000000000000000000, 0.9238795325112867385, 1.000000000000000000, 0.9238795325112867385, 1.000000000000000000 ) ) 
 REPRESENTATION_ITEM ( '' )  );
#25776=CARTESIAN_POINT ( 'NONE',  ( -7.188101187500002709, 25.31249999795161543, 2.977408999572649151 ) ) ;
#25777=ORIENTED_EDGE ( 'NONE', *, *, #57260, .T. ) ;
#25783=VECTOR ( 'NONE', #23672, 1000.000000000000000 ) ;
#25784=CARTESIAN_POINT ( 'NONE',  ( -7.188101187499999156, 93.12500000204836681, 2.977408999572654924 ) ) ;
#25789=EDGE_CURVE ( 'NONE', #47572, #9713, #41671, .T. ) ;
#25816=CARTESIAN_POINT ( 'NONE',  ( 2.977408999572654480, 106.6250000020483952, 7.188101187499999156 ) ) ;
#25821=CARTESIAN_POINT ( 'NONE',  ( -8.000000000000000000, 26.15625000000000711, -3.313708498984762496 ) ) ;
#25841=CARTESIAN_POINT ( 'NONE',  ( 4.401442555609581635E-16, 20.71874999795161543, -7.188101187500000044 ) ) ;
#25847=DIRECTION ( 'NONE',  ( 0.000000000000000000, 0.000000000000000000, 1.000000000000000000 ) ) ;
#25850=CARTESIAN_POINT ( 'NONE',  ( 2.977408999572651815, 3.187499997951610098, 7.188101187500000933 ) ) ;
#25857=FACE_OUTER_BOUND ( 'NONE', #44853, .T. ) ;
#25866=VERTEX_POINT ( 'NONE', #51849 ) ;
#25867=CARTESIAN_POINT ( 'NONE',  ( 2.977408999572652260, 3.187499997951610098, 7.188101187500000044 ) ) ;
#25872=CARTESIAN_POINT ( 'NONE',  ( 1.320432766682874540E-15, 112.9062500020483952, 7.188101187500000044 ) ) ;
#25873=PLANE ( 'NONE',  #32406 ) ;
#25885=CARTESIAN_POINT ( 'NONE',  ( 8.000000000000000000, 95.84374999999998579, -3.313708498984762496 ) ) ;
#25887=DIRECTION ( 'NONE',  ( -0.000000000000000000, 1.000000000000000000, -0.000000000000000000 ) ) ;
#25903=CARTESIAN_POINT ( 'NONE',  ( 5.082755093536325042, 92.46875000204838102, -5.082755093536325930 ) ) ;
#25919=CARTESIAN_POINT ( 'NONE',  ( -8.000000000000000000, 102.5000000000000000, 0.000000000000000000 ) ) ;
#25921=CARTESIAN_POINT ( 'NONE',  ( 5.656854249492381470, 121.2500000040967905, 5.656854249492379694 ) ) ;
#25928=CARTESIAN_POINT ( 'NONE',  ( 2.977408999572654480, 90.50000000204840944, 7.188101187499999156 ) ) ;
#25938=CARTESIAN_POINT ( 'NONE',  ( 4.898587196589412829E-16, 15.18749999590322197, -8.000000000000000000 ) ) ;
#25941=CARTESIAN_POINT ( 'NONE',  ( 8.000000000000000000, 2.906249995903220640, -3.313708498984761164 ) ) ;
#25948=ORIENTED_EDGE ( 'NONE', *, *, #32142, .F. ) ;
#25949=CARTESIAN_POINT ( 'NONE',  ( -7.999999999999998224, 99.78125000409679046, 3.313708498984766493 ) ) ;
#25950=CARTESIAN_POINT ( 'NONE',  ( 7.594050593750000466, 1.078124996927415147, 0.000000000000000000 ) ) ;
#25955=EDGE_CURVE ( 'NONE', #17336, #26713, #33539, .T. ) ;
#25958=CARTESIAN_POINT ( 'NONE',  ( -7.188101187499999156, 94.25000000204838102, 2.977408999572654924 ) ) ;
#25977=CARTESIAN_POINT ( 'NONE',  ( 3.313708498984762496, 2.531249995903220640, 7.999999999999998224 ) ) ;
#25979=CARTESIAN_POINT ( 'NONE',  ( -2.977408999572650039, 13.31249999795161187, -7.188101187500001821 ) ) ;
#25982=CARTESIAN_POINT ( 'NONE',  ( -5.082755093536324154, 111.2187500020483810, 5.082755093536326818 ) ) ;
#25985=FACE_OUTER_BOUND ( 'NONE', #39365, .T. ) ;
#25989=( BOUNDED_CURVE ( )  B_SPLINE_CURVE ( 2, ( #28081, #5454, #22041, #68081, #63527, #51462, #68814, #17127, #11850 ),
 .UNSPECIFIED., .F., .F. ) 
 B_SPLINE_CURVE_WITH_KNOTS ( ( 3, 2, 2, 2, 3 ),
 ( 0.1527777777777777901, 0.1597222222222222099, 0.1666666666666666574, 0.1736111111111111049, 0.1805555555555555525 ),
 .UNSPECIFIED. ) 
 CURVE ( )  GEOMETRIC_REPRESENTATION_ITEM ( )  RATIONAL_B_SPLINE_CURVE ( ( 1.000000000000000000, 0.9238795325112867385, 1.000000000000000000, 0.9238795325112867385, 1.000000000000000000, 0.9238795325112867385, 1.000000000000000000, 0.9238795325112867385, 1.000000000000000000 ) ) 
 REPRESENTATION_ITEM ( '' )  );
#26001=CARTESIAN_POINT ( 'NONE',  ( -2.977408999572652260, 101.9375000020483810, 7.188101187500000044 ) ) ;
#26009=CARTESIAN_POINT ( 'NONE',  ( 7.188101187500000044, 108.7812500020483810, -8.802885111219163269E-16 ) ) ;
#26010=ORIENTED_EDGE ( 'NONE', *, *, #39714, .F. ) ;
#26021=CARTESIAN_POINT ( 'NONE',  ( 5.082755093536325930, 2.531249997951610542, -5.082755093536325930 ) ) ;
#26030=CYLINDRICAL_SURFACE ( 'NONE', #29275, 8.000000000000000000 ) ;
#26038=CARTESIAN_POINT ( 'NONE',  ( 2.977408999572651815, 7.687499997951611874, 7.188101187500000933 ) ) ;
#26039=CARTESIAN_POINT ( 'NONE',  ( -5.656854249492380582, 117.5000000040967905, -5.656854249492380582 ) ) ;
#26049=EDGE_CURVE ( 'NONE', #663, #10294, #69671, .T. ) ;
#26051=( LENGTH_UNIT ( ) NAMED_UNIT ( * ) SI_UNIT ( .MILLI., .METRE. ) );
#26065=CARTESIAN_POINT ( 'NONE',  ( -8.000000000000000000, 111.5000000000000000, 0.000000000000000000 ) ) ;
#26072=CARTESIAN_POINT ( 'NONE',  ( 5.656854249492378806, 19.12499999590322020, 5.656854249492381470 ) ) ;
#26081=ADVANCED_FACE ( 'NONE', ( #58630 ), #41996, .T. ) ;
#26087=CARTESIAN_POINT ( 'NONE',  ( -8.000000000000000000, 107.0937500040967905, -3.313708498984761164 ) ) ;
#26088=CARTESIAN_POINT ( 'NONE',  ( 0.000000000000000000, 125.0000000000000000, 11.00000000000000000 ) ) ;
#26095=CARTESIAN_POINT ( 'NONE',  ( -2.977408999572650927, 119.3750000020483810, -7.188101187500000933 ) ) ;
#26102=CARTESIAN_POINT ( 'NONE',  ( -7.188101187500001821, 94.06250000204838102, -2.977408999572650483 ) ) ;
#26116=EDGE_LOOP ( 'NONE', ( #30409, #30763, #63733, #32500 ) ) ;
#26117=( BOUNDED_CURVE ( )  B_SPLINE_CURVE ( 2, ( #30004, #1349, #40956, #63582, #51521, #53018, #63209, #34943, #69626 ),
 .UNSPECIFIED., .F., .T. ) 
 B_SPLINE_CURVE_WITH_KNOTS ( ( 3, 2, 2, 2, 3 ),
 ( 0.9270833333333335924, 0.9322916666666667407, 0.9375000000000000000, 0.9427083333333333703, 0.9479166666666665186 ),
 .UNSPECIFIED. ) 
 CURVE ( )  GEOMETRIC_REPRESENTATION_ITEM ( )  RATIONAL_B_SPLINE_CURVE ( ( 0.9999999999999967804, 0.9238795325112899581, 1.000000000000000000, 0.9238795325112867385, 1.000000000000000000, 0.9238795325112867385, 1.000000000000000000, 0.9238795325112884038, 0.9999999999999983347 ) ) 
 REPRESENTATION_ITEM ( '' )  );
#26128=VERTEX_POINT ( 'NONE', #68277 ) ;
#26130=CARTESIAN_POINT ( 'NONE',  ( 7.188101187500001821, 18.56249999795161187, -2.977408999572650483 ) ) ;
#26132=CARTESIAN_POINT ( 'NONE',  ( 2.977408999572654480, 96.12500000204838102, 7.188101187499999156 ) ) ;
#26134=CARTESIAN_POINT ( 'NONE',  ( -7.188101187500002709, 18.18749999795161187, 2.977408999572649151 ) ) ;
#26136=( BOUNDED_CURVE ( )  B_SPLINE_CURVE ( 2, ( #41249, #23144, #17859, #40877, #63882, #63135, #6550, #52565, #62752 ),
 .UNSPECIFIED., .F., .F. ) 
 B_SPLINE_CURVE_WITH_KNOTS ( ( 3, 2, 2, 2, 3 ),
 ( 0.1979166666666667962, 0.2031250000000001388, 0.2083333333333334814, 0.2135416666666667962, 0.2187500000000001388 ),
 .UNSPECIFIED. ) 
 CURVE ( )  GEOMETRIC_REPRESENTATION_ITEM ( )  RATIONAL_B_SPLINE_CURVE ( ( 0.9999999999999980016, 0.9238795325112887369, 1.000000000000000000, 0.9238795325112867385, 1.000000000000000000, 0.9238795325112867385, 1.000000000000000000, 0.9238795325112847401, 1.000000000000001998 ) ) 
 REPRESENTATION_ITEM ( '' )  );
#26141=EDGE_LOOP ( 'NONE', ( #37599, #26822, #37169, #39117, #43691, #15863 ) ) ;
#26147=CARTESIAN_POINT ( 'NONE',  ( -2.977408999572651815, 107.9375000020483810, 7.188101187500000933 ) ) ;
#26159=CARTESIAN_POINT ( 'NONE',  ( -2.977408999572651815, 93.31250000204838102, 7.188101187500000933 ) ) ;
#26162=FACE_OUTER_BOUND ( 'NONE', #50706, .T. ) ;
#26163=ORIENTED_EDGE ( 'NONE', *, *, #41790, .F. ) ;
#26164=CARTESIAN_POINT ( 'NONE',  ( 3.313708498984740736, 9.093749995903223748, -8.000000000000021316 ) ) ;
#26180=CARTESIAN_POINT ( 'NONE',  ( 8.000000000000000000, 109.4375000040967905, -9.797174393178825657E-16 ) ) ;
#26190=CARTESIAN_POINT ( 'NONE',  ( -4.401442555609581635E-16, 107.2812500020483810, -7.188101187500000044 ) ) ;
#26197=LINE ( 'NONE', #20543, #44824 ) ;
#26211=CARTESIAN_POINT ( 'NONE',  ( -5.656854249492378806, 110.1875000000000000, 5.656854249492381470 ) ) ;
#26212=CARTESIAN_POINT ( 'NONE',  ( 0.000000000000000000, 125.0000000000000000, 0.000000000000000000 ) ) ;
#26215=CARTESIAN_POINT ( 'NONE',  ( 7.188101187499999156, 18.74999999795161543, 2.977408999572654924 ) ) ;
#26223=CARTESIAN_POINT ( 'NONE',  ( 5.082755093536324154, 3.281249997951610098, 5.082755093536326818 ) ) ;
#26244=CARTESIAN_POINT ( 'NONE',  ( -5.082755093536325042, 11.53124999795161010, -5.082755093536325930 ) ) ;
#26249=CARTESIAN_POINT ( 'NONE',  ( -2.977408999572650927, 112.2500000020483952, -7.188101187500001821 ) ) ;
#26262=CARTESIAN_POINT ( 'NONE',  ( -4.898587196589412829E-16, 94.62499999999998579, -8.000000000000000000 ) ) ;
#26276=CARTESIAN_POINT ( 'NONE',  ( -5.082755093536325930, 89.84375000204839523, -5.082755093536325930 ) ) ;
#26286=CARTESIAN_POINT ( 'NONE',  ( -7.188101187500002709, 17.81249999795161543, 2.977408999572649151 ) ) ;
#26318=ORIENTED_EDGE ( 'NONE', *, *, #39713, .T. ) ;
#26326=CARTESIAN_POINT ( 'NONE',  ( -5.656854249492378806, 98.37500000409677625, 5.656854249492381470 ) ) ;
#26333=ORIENTED_EDGE ( 'NONE', *, *, #72345, .F. ) ;
#26335=CARTESIAN_POINT ( 'NONE',  ( 5.082755093536326818, 94.71875000204838102, 5.082755093536325042 ) ) ;
#26345=ORIENTED_EDGE ( 'NONE', *, *, #30618, .F. ) ;
#26356=CARTESIAN_POINT ( 'NONE',  ( 8.000000000000000000, 2.906249995903220640, -3.313708498984761608 ) ) ;
#26358=CARTESIAN_POINT ( 'NONE',  ( -1.320432766682874540E-15, 13.96874999795161187, 7.188101187500000044 ) ) ;
#26361=CARTESIAN_POINT ( 'NONE',  ( -2.977408999572650927, 107.7500000020483810, -7.188101187500000933 ) ) ;
#26378=CARTESIAN_POINT ( 'NONE',  ( 7.188101187500000044, 102.4062500020483810, -8.802885111219163269E-16 ) ) ;
#26384=CARTESIAN_POINT ( 'NONE',  ( -7.188101187500000044, 108.0312500020483810, 0.000000000000000000 ) ) ;
#26395=DIRECTION ( 'NONE',  ( -0.000000000000000000, 1.000000000000000000, -0.000000000000000000 ) ) ;
#26404=CARTESIAN_POINT ( 'NONE',  ( -8.000000000000000000, 122.1875000040967763, 0.000000000000000000 ) ) ;
#26413=CARTESIAN_POINT ( 'NONE',  ( -7.188101187500000044, 8.718749997951611874, -8.802885111219163269E-16 ) ) ;
#26414=CARTESIAN_POINT ( 'NONE',  ( -5.656854249492378806, 116.3750000040967905, 5.656854249492381470 ) ) ;
#26442=CARTESIAN_POINT ( 'NONE',  ( 8.000000000000000000, 112.3437500000000000, -3.313708498984762496 ) ) ;
#26448=CARTESIAN_POINT ( 'NONE',  ( 5.656854249492378806, 22.12499999590322375, 5.656854249492381470 ) ) ;
#26473=CARTESIAN_POINT ( 'NONE',  ( 7.188101187500000933, 116.0000000020483810, -2.977408999572651371 ) ) ;
#26478=CARTESIAN_POINT ( 'NONE',  ( -5.082755093536325930, 92.46875000204838102, -5.082755093536325930 ) ) ;
#26505=CARTESIAN_POINT ( 'NONE',  ( -2.977408999572654480, 23.99999999795161543, 7.188101187499999156 ) ) ;
#26507=DIRECTION ( 'NONE',  ( -0.000000000000000000, 1.000000000000000000, -0.000000000000000000 ) ) ;
#26508=CARTESIAN_POINT ( 'NONE',  ( 2.977408999572650927, 19.12499999795161187, -7.188101187500001821 ) ) ;
#26517=ORIENTED_EDGE ( 'NONE', *, *, #24956, .T. ) ;
#26527=CARTESIAN_POINT ( 'NONE',  ( -7.188101187500000933, 26.62499999795161543, -2.977408999572651371 ) ) ;
#26534=CARTESIAN_POINT ( 'NONE',  ( -7.188101187500001821, 91.43750000204838102, -2.977408999572650483 ) ) ;
#26538=ORIENTED_EDGE ( 'NONE', *, *, #32223, .T. ) ;
#26556=CARTESIAN_POINT ( 'NONE',  ( -8.000000000000001776, 17.34375000000000000, 3.313708498984759387 ) ) ;
#26560=CARTESIAN_POINT ( 'NONE',  ( 0.000000000000000000, 125.0000000000000000, 0.000000000000000000 ) ) ;
#26564=( BOUNDED_CURVE ( )  B_SPLINE_CURVE ( 2, ( #47714, #53766, #30746 ),
 .UNSPECIFIED., .F., .F. ) 
 B_SPLINE_CURVE_WITH_KNOTS ( ( 3, 3 ),
 ( 0.9687500000000000000, 0.9722122500602408124 ),
 .UNSPECIFIED. ) 
 CURVE ( )  GEOMETRIC_REPRESENTATION_ITEM ( )  RATIONAL_B_SPLINE_CURVE ( ( 1.000000000000000000, 0.9493987661155159907, 0.9660720762559202868 ) ) 
 REPRESENTATION_ITEM ( '' )  );
#26567=CARTESIAN_POINT ( 'NONE',  ( 2.977408999572650039, 108.6875000020483952, -7.188101187500001821 ) ) ;
#26577=EDGE_CURVE ( 'NONE', #16961, #64023, #65196, .T. ) ;
#26584=CARTESIAN_POINT ( 'NONE',  ( -8.000000000000000000, 93.50000000000000000, 0.000000000000000000 ) ) ;
#26593=CARTESIAN_POINT ( 'NONE',  ( -5.656854249492380582, 109.8125000000000000, -5.656854249492380582 ) ) ;
#26597=CARTESIAN_POINT ( 'NONE',  ( 2.977408999572652260, 18.56249999795161187, 7.188101187500000044 ) ) ;
#26602=CARTESIAN_POINT ( 'NONE',  ( -7.999999999999998224, 96.78125000409679046, 3.313708498984766049 ) ) ;
#26605=CARTESIAN_POINT ( 'NONE',  ( -7.188101187500000044, 2.718749997951610098, -8.802885111219163269E-16 ) ) ;
#26608=CARTESIAN_POINT ( 'NONE',  ( -3.313708498984760276, 16.78124999590322375, -8.000000000000000000 ) ) ;
#26615=DIRECTION ( 'NONE',  ( 0.000000000000000000, 0.000000000000000000, 1.000000000000000000 ) ) ;
#26623=CARTESIAN_POINT ( 'NONE',  ( -5.082755093536325042, 13.03124999795161187, -5.082755093536325930 ) ) ;
#26628=CARTESIAN_POINT ( 'NONE',  ( 2.977408999572654480, 110.0000000020483668, 7.188101187499999156 ) ) ;
#26642=FACE_OUTER_BOUND ( 'NONE', #58085, .T. ) ;
#26644=CARTESIAN_POINT ( 'NONE',  ( -7.999999999999998224, 93.59375000000000000, 3.313708498984766493 ) ) ;
#26653=CARTESIAN_POINT ( 'NONE',  ( 8.000000000000001776, 100.1562500000000000, 3.313708498984759387 ) ) ;
#26661=FACE_OUTER_BOUND ( 'NONE', #21662, .T. ) ;
#26669=CARTESIAN_POINT ( 'NONE',  ( 7.188101187499999156, 21.37499999795161543, 2.977408999572654924 ) ) ;
#26709=CARTESIAN_POINT ( 'NONE',  ( -3.313708498984760720, 13.96875000000000355, -8.000000000000000000 ) ) ;
#26711=CARTESIAN_POINT ( 'NONE',  ( 1.469576158976823947E-15, 89.56250000409677625, 8.000000000000000000 ) ) ;
#26713=VERTEX_POINT ( 'NONE', #61788 ) ;
#26721=CARTESIAN_POINT ( 'NONE',  ( -5.082755093536324154, 92.84375000204838102, 5.082755093536326818 ) ) ;
#26742=CARTESIAN_POINT ( 'NONE',  ( 8.000000000000000000, 10.40624999590322020, -3.313708498984761608 ) ) ;
#26744=EDGE_LOOP ( 'NONE', ( #42954, #42372, #56989, #62549 ) ) ;
#26746=CARTESIAN_POINT ( 'NONE',  ( -5.082755093536325042, 13.40624999795161187, -5.082755093536325930 ) ) ;
#26749=CARTESIAN_POINT ( 'NONE',  ( -3.313708498984762496, 105.7812500000000000, 7.999999999999998224 ) ) ;
#26750=CARTESIAN_POINT ( 'NONE',  ( 7.188101187500002709, 104.1875000020483810, 2.977408999572649151 ) ) ;
#26753=CARTESIAN_POINT ( 'NONE',  ( 0.000000000000000000, 125.0000000000000000, 0.000000000000000000 ) ) ;
#26769=DIRECTION ( 'NONE',  ( -0.000000000000000000, 1.000000000000000000, -0.000000000000000000 ) ) ;
#26770=CARTESIAN_POINT ( 'NONE',  ( -7.188101187500000933, 101.5625000020483952, -2.977408999572650483 ) ) ;
#26777=CARTESIAN_POINT ( 'NONE',  ( 5.082755093536326818, 101.0937500020483810, 5.082755093536325042 ) ) ;
#26778=CARTESIAN_POINT ( 'NONE',  ( -0.3459307087060433106, 0.4270199122593540952, -7.927019912259357426 ) ) ;
#26795=CARTESIAN_POINT ( 'NONE',  ( 3.313708498984802020, 21.09374999590322020, -7.999999999999958256 ) ) ;
#26803=CARTESIAN_POINT ( 'NONE',  ( -2.977408999572654480, 7.499999997951610986, 7.188101187499999156 ) ) ;
#26804=CARTESIAN_POINT ( 'NONE',  ( 3.313708498984765161, 107.6562500040968189, 7.999999999999998224 ) ) ;
#26822=ORIENTED_EDGE ( 'NONE', *, *, #39141, .F. ) ;
#26830=CARTESIAN_POINT ( 'NONE',  ( -7.999999999999998224, 114.5937499999999858, 3.313708498984766493 ) ) ;
#26836=CARTESIAN_POINT ( 'NONE',  ( -8.000000000000001776, 23.15624999590322730, 3.313708498984759387 ) ) ;
#26850=CARTESIAN_POINT ( 'NONE',  ( 9.797174393178825657E-16, 125.0000000000000000, -8.000000000000000000 ) ) ;
#26854=EDGE_CURVE ( 'NONE', #38454, #53341, #59526, .T. ) ;
#26857=CARTESIAN_POINT ( 'NONE',  ( -1.469576158976823947E-15, 7.125000000000000888, 8.000000000000000000 ) ) ;
#26860=CARTESIAN_POINT ( 'NONE',  ( 7.188101187500002709, 120.3125000020483810, 2.977408999572649151 ) ) ;
#26866=CARTESIAN_POINT ( 'NONE',  ( 7.188101187500001821, 122.3750000020483952, -2.977408999572651371 ) ) ;
#26870=ORIENTED_EDGE ( 'NONE', *, *, #39714, .T. ) ;
#26883=FACE_OUTER_BOUND ( 'NONE', #42352, .T. ) ;
#26890=CARTESIAN_POINT ( 'NONE',  ( -1.320432766682874540E-15, 22.59374999795161187, 7.188101187500000044 ) ) ;
#26893=CARTESIAN_POINT ( 'NONE',  ( -7.188101187500000044, 16.59374999795161543, -8.802885111219163269E-16 ) ) ;
#26897=AXIS2_PLACEMENT_3D ( 'NONE', #72681, #38350, #61358 ) ;
#26919=CARTESIAN_POINT ( 'NONE',  ( -5.082755093536325930, 94.34375000204838102, -5.082755093536325930 ) ) ;
#26922=ORIENTED_EDGE ( 'NONE', *, *, #28415, .F. ) ;
#26946=CARTESIAN_POINT ( 'NONE',  ( 1.320432766682874540E-15, 109.5312500020483810, 7.188101187500000044 ) ) ;
#26969=EDGE_CURVE ( 'NONE', #72916, #54565, #290, .T. ) ;
#26975=CARTESIAN_POINT ( 'NONE',  ( -5.082755093536326818, 21.28124999795161543, 5.082755093536325042 ) ) ;
#26983=CARTESIAN_POINT ( 'NONE',  ( -5.082755093536325042, 2.531249997951610542, -5.082755093536325930 ) ) ;
#26992=DIRECTION ( 'NONE',  ( -0.000000000000000000, 1.000000000000000000, -0.000000000000000000 ) ) ;
#26999=CARTESIAN_POINT ( 'NONE',  ( 3.313708498984761608, 6.281250000000000888, -8.000000000000000000 ) ) ;
#27001=CARTESIAN_POINT ( 'NONE',  ( 7.188101187500000933, 11.06249999795161187, -2.977408999572650483 ) ) ;
#27007=CARTESIAN_POINT ( 'NONE',  ( 5.082755093536325042, 111.9687500020483810, -5.082755093536325930 ) ) ;
#27010=EDGE_CURVE ( 'NONE', #68569, #62240, #484, .T. ) ;
#27022=EDGE_CURVE ( 'NONE', #73500, #60057, #48928, .T. ) ;
#27025=CARTESIAN_POINT ( 'NONE',  ( 3.313708498984760720, 91.53125000000000000, -8.000000000000000000 ) ) ;
#27048=CARTESIAN_POINT ( 'NONE',  ( 7.188101187500000044, 18.46874999795161187, 0.000000000000000000 ) ) ;
#27063=CARTESIAN_POINT ( 'NONE',  ( -8.000000000000000000, 21.46874999590322375, -3.313708498984762496 ) ) ;
#27084=CARTESIAN_POINT ( 'NONE',  ( -8.000000000000000000, 11.25000000000000178, -9.797174393178825657E-16 ) ) ;
#27086=CARTESIAN_POINT ( 'NONE',  ( -8.000000000000000000, 92.18750000409679046, 0.000000000000000000 ) ) ;
#27095=CARTESIAN_POINT ( 'NONE',  ( 2.977408999572650039, 95.18750000204838102, -7.188101187500001821 ) ) ;
#27118=CARTESIAN_POINT ( 'NONE',  ( -5.656854249492379694, 9.374999995903223748, -5.656854249492380582 ) ) ;
#27121=CARTESIAN_POINT ( 'NONE',  ( 7.188101187500000044, 18.84374999795161187, 0.000000000000000000 ) ) ;
#27123=CARTESIAN_POINT ( 'NONE',  ( 7.999999999999998224, 7.406250000000001776, 3.313708498984766049 ) ) ;
#27124=CARTESIAN_POINT ( 'NONE',  ( -2.977408999572650927, 101.7500000020483810, -7.188101187500000933 ) ) ;
#27132=CARTESIAN_POINT ( 'NONE',  ( 3.313708498984720308, 21.28125000000000711, -8.000000000000040856 ) ) ;
#27141=CARTESIAN_POINT ( 'NONE',  ( -7.188101187499999156, 98.75000000204838102, 2.977408999572654924 ) ) ;
#27147=CARTESIAN_POINT ( 'NONE',  ( 7.188101187500001821, 101.3750000020483952, -2.977408999572651371 ) ) ;
#27151=EDGE_LOOP ( 'NONE', ( #16499, #40256, #16759, #62666 ) ) ;
#27170=CARTESIAN_POINT ( 'NONE',  ( 2.977408999572651815, 9.187499997951610098, 7.188101187500000933 ) ) ;
#27171=CARTESIAN_POINT ( 'NONE',  ( -8.000000000000000000, 108.6875000040967905, 0.000000000000000000 ) ) ;
#27195=CARTESIAN_POINT ( 'NONE',  ( 9.797174393178825657E-16, 125.0000000000000000, -8.000000000000000000 ) ) ;
#27197=CARTESIAN_POINT ( 'NONE',  ( -8.000000000000000000, 105.5000000000000000, 0.000000000000000000 ) ) ;
#27203=CARTESIAN_POINT ( 'NONE',  ( -8.000000000000001776, 26.15624999590322730, 3.313708498984759387 ) ) ;
#27205=CARTESIAN_POINT ( 'NONE',  ( 7.188101187500000044, 119.2812500020483810, -8.802885111219163269E-16 ) ) ;
#27209=CARTESIAN_POINT ( 'NONE',  ( 0.000000000000000000, 125.0000000000000000, 8.000000000000000000 ) ) ;
#27226=CARTESIAN_POINT ( 'NONE',  ( -7.188101187500000044, 116.6562500020483810, 0.000000000000000000 ) ) ;
#27232=CARTESIAN_POINT ( 'NONE',  ( 7.188101187500002709, 120.6875000020483952, 2.977408999572649151 ) ) ;
#27235=DIRECTION ( 'NONE',  ( -0.000000000000000000, 1.000000000000000000, -0.000000000000000000 ) ) ;
#27258=CARTESIAN_POINT ( 'NONE',  ( -5.082755093536326818, 25.40624999795161543, 5.082755093536325042 ) ) ;
#27261=CARTESIAN_POINT ( 'NONE',  ( 7.188101187500000044, 18.84374999795161187, 0.000000000000000000 ) ) ;
#27267=ORIENTED_EDGE ( 'NONE', *, *, #36179, .T. ) ;
#27285=CARTESIAN_POINT ( 'NONE',  ( 5.082755093536326818, 90.59375000204839523, 5.082755093536325042 ) ) ;
#27309=CYLINDRICAL_SURFACE ( 'NONE', #1107, 8.000000000000000000 ) ;
#27314=CARTESIAN_POINT ( 'NONE',  ( -7.188101187499999156, 100.2500000020483952, 2.977408999572654924 ) ) ;
#27319=ORIENTED_EDGE ( 'NONE', *, *, #50549, .F. ) ;
#27321=CARTESIAN_POINT ( 'NONE',  ( 3.313708498984721640, 28.03124999590321664, 8.000000000000039080 ) ) ;
#27327=ORIENTED_EDGE ( 'NONE', *, *, #37312, .T. ) ;
#27340=CARTESIAN_POINT ( 'NONE',  ( -7.188101187500000044, 16.59374999795161543, -8.802885111219163269E-16 ) ) ;
#27345=CARTESIAN_POINT ( 'NONE',  ( -8.000000000000000000, 96.68750000409679046, 0.000000000000000000 ) ) ;
#27350=CARTESIAN_POINT ( 'NONE',  ( -2.977408999572650039, 5.437499997951610986, -7.188101187500001821 ) ) ;
#27361=ORIENTED_EDGE ( 'NONE', *, *, #42405, .F. ) ;
#27362=EDGE_CURVE ( 'NONE', #55690, #64356, #1132, .T. ) ;
#27366=CARTESIAN_POINT ( 'NONE',  ( 8.000000000000000000, 6.093750000000000888, -3.313708498984761164 ) ) ;
#27368=CARTESIAN_POINT ( 'NONE',  ( 4.401442555609581635E-16, 11.34374999795161010, -7.188101187500000044 ) ) ;
#27372=CARTESIAN_POINT ( 'NONE',  ( -7.188101187499999156, 112.6250000020483668, 2.977408999572654924 ) ) ;
#27389=CARTESIAN_POINT ( 'NONE',  ( 8.000000000000000000, 94.25000000000000000, -9.797174393178825657E-16 ) ) ;
#27395=EDGE_CURVE ( 'NONE', #27944, #67659, #1856, .T. ) ;
#27405=CARTESIAN_POINT ( 'NONE',  ( -2.977408999572651815, 122.9375000020483810, 7.188101187500000933 ) ) ;
#27409=CARTESIAN_POINT ( 'NONE',  ( -8.000000000000000000, 12.65625000000000178, -3.313708498984762496 ) ) ;
#27412=DIRECTION ( 'NONE',  ( -0.000000000000000000, 1.000000000000000000, -0.000000000000000000 ) ) ;
#27413=CARTESIAN_POINT ( 'NONE',  ( -2.977408999572650039, 21.93749999795161543, -7.188101187500001821 ) ) ;
#27418=CARTESIAN_POINT ( 'NONE',  ( 0.000000000000000000, 125.0000000000000000, 8.000000000000000000 ) ) ;
#27436=CARTESIAN_POINT ( 'NONE',  ( -8.000000000000000000, 1.968749995903220196, -3.313708498984762496 ) ) ;
#27437=CARTESIAN_POINT ( 'NONE',  ( -8.000000000000000000, 120.4062500000000000, -3.313708498984761164 ) ) ;
#27447=CARTESIAN_POINT ( 'NONE',  ( -8.000000000000001776, 9.843750000000000000, 3.313708498984759387 ) ) ;
#27449=CARTESIAN_POINT ( 'NONE',  ( -4.898587196589412829E-16, 91.81250000409677625, -8.000000000000000000 ) ) ;
#27452=VECTOR ( 'NONE', #36058, 1000.000000000000000 ) ;
#27459=DIRECTION ( 'NONE',  ( -0.000000000000000000, 1.000000000000000000, -0.000000000000000000 ) ) ;
#27462=CARTESIAN_POINT ( 'NONE',  ( -7.188101187499999156, 92.75000000204839523, 2.977408999572654924 ) ) ;
#27485=CARTESIAN_POINT ( 'NONE',  ( -5.656854249492381470, 6.749999995903220196, 5.656854249492379694 ) ) ;
#27489=CARTESIAN_POINT ( 'NONE',  ( 7.188101187500000044, 20.34374999795161543, 0.000000000000000000 ) ) ;
#27492=CARTESIAN_POINT ( 'NONE',  ( -7.188101187500000044, 102.0312500020483810, 0.000000000000000000 ) ) ;
#27512=CARTESIAN_POINT ( 'NONE',  ( 7.188101187500000933, 99.50000000204838102, -2.977408999572651371 ) ) ;
#27519=CARTESIAN_POINT ( 'NONE',  ( -2.977408999572650927, 100.2500000020483952, -7.188101187500001821 ) ) ;
#27535=EDGE_LOOP ( 'NONE', ( #24529, #51542, #48707, #56524, #14594, #51216, #60615, #11918, #33097, #66246, #59483, #12073, #58825, #45180, #27327, #28470, #59441, #50835, #42455, #28627, #16982, #8484, #55706, #5459, #29048, #52637, #7582, #9626, #27934, #64494, #72413, #35375, #68948, #59943, #61743, #40746, #39086, #45081, #11232, #40907, #59820 ) ) ;
#27544=CARTESIAN_POINT ( 'NONE',  ( -2.977408999572654480, 5.999999997951610098, 7.188101187499999156 ) ) ;
#27545=CARTESIAN_POINT ( 'NONE',  ( -7.999999999999998224, 108.7812500040967763, 3.313708498984766493 ) ) ;
#27548=VECTOR ( 'NONE', #12395, 1000.000000000000000 ) ;
#27557=CARTESIAN_POINT ( 'NONE',  ( 7.188101187500000044, 109.9062500020483810, -8.802885111219163269E-16 ) ) ;
#27574=CARTESIAN_POINT ( 'NONE',  ( 8.000000000000001776, 104.6562500000000000, 3.313708498984759387 ) ) ;
#27577=CARTESIAN_POINT ( 'NONE',  ( 8.000000000000000000, 19.59375000000000711, -3.313708498984761164 ) ) ;
#27579=CARTESIAN_POINT ( 'NONE',  ( 3.313708498984762496, 26.53124999590322375, 7.999999999999998224 ) ) ;
#27581=CARTESIAN_POINT ( 'NONE',  ( 2.977408999572654480, 123.5000000020483810, 7.188101187499999156 ) ) ;
#27588=CARTESIAN_POINT ( 'NONE',  ( 8.000000000000001776, 122.6562500000000000, 3.313708498984759387 ) ) ;
#27601=CARTESIAN_POINT ( 'NONE',  ( -4.401442555609581635E-16, 114.7812500020483952, -7.188101187500000044 ) ) ;
#27608=CARTESIAN_POINT ( 'NONE',  ( -7.188101187499999156, 121.6250000020483810, 2.977408999572654924 ) ) ;
#27618=CARTESIAN_POINT ( 'NONE',  ( -8.000000000000000000, 18.75000000000000355, -9.797174393178825657E-16 ) ) ;
#27632=EDGE_CURVE ( 'NONE', #3802, #55604, #43601, .T. ) ;
#27635=CARTESIAN_POINT ( 'NONE',  ( -3.313708498984765161, 2.531250000000000888, 7.999999999999998224 ) ) ;
#27638=CARTESIAN_POINT ( 'NONE',  ( -7.188101187500001821, 20.99999999795161898, -2.977408999572651371 ) ) ;
#27654=CARTESIAN_POINT ( 'NONE',  ( 5.082755093536324154, 27.28124999795161543, 5.082755093536326818 ) ) ;
#27664=CARTESIAN_POINT ( 'NONE',  ( -3.313708498984762052, 123.2187500000000000, -8.000000000000000000 ) ) ;
#27691=CARTESIAN_POINT ( 'NONE',  ( 7.188101187500002709, 102.3125000020483810, 2.977408999572649151 ) ) ;
#27697=ORIENTED_EDGE ( 'NONE', *, *, #13700, .F. ) ;
#27715=DIRECTION ( 'NONE',  ( 0.000000000000000000, 0.000000000000000000, 1.000000000000000000 ) ) ;
#27718=CARTESIAN_POINT ( 'NONE',  ( 7.188101187500000044, 21.84374999795161543, 0.000000000000000000 ) ) ;
#27727=CARTESIAN_POINT ( 'NONE',  ( 7.188101187500000044, 10.96874999795161187, 0.000000000000000000 ) ) ;
#27744=CARTESIAN_POINT ( 'NONE',  ( -5.082755093536326818, 8.906249997951610098, 5.082755093536325042 ) ) ;
#27748=CARTESIAN_POINT ( 'NONE',  ( -7.188101187500000044, 108.0312500020483810, 0.000000000000000000 ) ) ;
#27749=DIRECTION ( 'NONE',  ( 0.000000000000000000, 0.000000000000000000, -1.000000000000000000 ) ) ;
#27753=ORIENTED_EDGE ( 'NONE', *, *, #60386, .F. ) ;
#27764=FACE_OUTER_BOUND ( 'NONE', #28862, .T. ) ;
#27779=CARTESIAN_POINT ( 'NONE',  ( 7.188101187500002709, 118.8125000020483810, 2.977408999572649151 ) ) ;
#27786=ORIENTED_EDGE ( 'NONE', *, *, #44122, .F. ) ;
#27787=( BOUNDED_SURFACE ( )  B_SPLINE_SURFACE ( 1, 2, ( 
 ( #17578, #4786, #51535, #17202, #16076, #57212, #45137, #5161, #21742, #74175, #11551, #39482, #40221, #27405, #34210, #50420, #33468, #33103, #62114, #39110, #23240, #5901, #57591, #63224, #16446, #5526, #16820, #62478, #28527, #51919, #22479, #22113, #10808, #62849, #28155, #74552, #45500, #68518, #45878, #40596, #73805, #22864, #10438, #34585, #28901, #257, #39848, #10068, #4409, #67784, #68149, #56100, #44770, #11185, #33842, #73434, #56470, #27779, #46248, #69267, #50792, #56840, #51166, #68892, #25074, #629, #70384, #1729, #47721, #69640, #41706, #30387, #17954, #64720, #53406, #57971, #70742, #63597, #13016, #18325, #1364, #29283, #24709, #47358, #6277, #19060, #42062, #52293, #58699, #65070, #997, #40972, #11924, #18699, #34956, #23610, #63979, #12292, #36054, #30752, #13383, #36421, #53773, #52661, #29646, #46620, #59435, #23978, #19420, #59071, #7747, #35327, #7380, #58339, #2082, #30019, #6643, #48091, #53033, #71100, #46986, #70019, #41340, #64350, #12653, #35684, #7010, #24349, #72607, #66943, #8860, #36789, #37157, #65816, #9230, #60159, #8478, #49210, #13746, #71467, #54519, #65449, #72979, #59799, #3575, #49591, #19793, #20158, #37910, #37534, #72219, #14495, #66562, #43548, #25447, #15247, #26946, #20913, #43175, #9613, #61286, #3957, #54145, #20534, #55270, #26567, #48462, #14871, #32252, #42800, #60907, #43934, #8112, #38281, #42433, #32633, #71841, #54891, #31117, #55642, #26190, #2454, #49965, #14123, #31498, #60534, #2825, #25816, #48835, #66191, #31870, #3202, #38660, #21656, #44681, #45411, #63141, #74460, #5439, #11469, #10352, #62028, #67323, #34124, #33376, #51827, #74092, #62758, #67697, #16730, #73352, #34503, #62391, #15994, #57124, #10718, #28809, #68801, #15620, #51078, #33012, #73718, #50330, #57508, #68065, #51447, #45791, #33750, #61662, #39024, #56377, #11101, #4698, #27691, #28067, #9981, #50700, #22028, #44308, #21285, #56013, #28441, #22768, #45054, #16354, #39756, #39392, #22391, #56753, #68427, #17113, #40135, #5073, #5814, #4325, #27314, #12198, #29561, #52947, #18238, #47270, #64262, #35599, #35967, #30668, #63887, #64634, #52206, #30300, #53319, #18974, #58614, #173, #69179, #57878, #58254, #23149, #11837, #1280, #6555, #46162, #34872, #35236, #59351, #24624, #1643, #12931, #52572, #46535, #40509, #12570, #6920, #539, #29931, #7662, #47635, #17490, #58987, #23895, #24257, #909, #46904, #6185, #13298, #69928, #36336, #7292, #41253, #29194, #70657, #17864, #41978, #63513, #70296, #69553, #18611, #23521, #40881, #41622, #64989, #59716, #26102, #14033, #48748, #65365, #43087, #55184, #8392, #9146, #71019, #3117, #19336, #2366, #1999, #31032, #8024, #66860, #49503, #26478, #60823, #60073, #49122, #31406, #54057, #20447, #24989, #61201, #9532, #43464, #54433, #60444, #31786, #72522, #19705, #8774, #20071, #53688, #48006, #25361, #15168, #42718, #66104, #2741, #72134, #42348, #25727, #66478, #54806, #14414, #48378, #38198, #65731, #37070, #13664, #71381 ),
 ( #36704, #14786, #71757, #37446, #37826, #32163, #20830, #3490, #43847, #10270, #74375, #51364, #68717, #44230, #39316, #45334, #16646, #38578, #10639, #74007, #61578, #33668, #22309, #26866, #68351, #56295, #16273, #21574, #4611, #67241, #45704, #27608, #17028, #39679, #33297, #15537, #57043, #50248, #62678, #40054, #56673, #27232, #21944, #63057, #73270, #11015, #34048, #9897, #4989, #67613, #50618, #32927, #44973, #5355, #61942, #28357, #49880, #27990, #72895, #55933, #55557, #4244, #44600, #32547, #22686, #3870, #21203, #38941, #50995, #73637, #15910, #67978, #62313, #18891, #41897, #1191, #63798, #18154, #64180, #30212, #52125, #41169, #52488, #11381, #57419, #57793, #24542, #457, #826, #12116, #35514, #34416, #35154, #52859, #12484, #23814, #6101, #47550, #23436, #46451, #5725, #11752, #28724, #69469, #17402, #70574, #51740, #29106, #53232, #40425, #24173, #58527, #89, #6834, #58170, #34789, #1563, #18524, #35882, #29848, #23067, #17779, #46076, #69095, #47183, #63424, #40792, #70215, #46816, #41532, #64548, #6475, #29479, #69842, #12844, #58899, #7210, #25273, #49409, #14698, #20357, #54719, #48291, #36616, #30580, #2654, #25644, #42261, #19988, #72430, #43374, #36250, #13579, #71298, #20739, #37737, #66390, #3026, #19618, #59625, #53602, #48659, #71668, #65273, #42996, #64906, #60736, #59265, #26009, #13942, #66016, #53967, #36984, #1914, #3400, #59989, #26384, #49033, #42633, #47918, #9058, #7940, #72040, #13212, #14323, #30945, #54343, #7577, #2278, #31697, #32072, #70937, #37356, #65646, #8306, #24901, #60355, #55094, #31316, #19250, #8682, #67889, #61108, #67152, #66770, #21117, #72809, #56956, #39595, #16558, #50906, #50164, #16181, #21489, #49794, #10550, #15074, #51279, #74288, #33582, #44510, #50530, #21853, #62591, #9810, #73546, #10179, #43756, #38108, #15447, #5271, #32833, #33213, #67521, #39223, #9438, #15819, #56586, #44885, #56210, #38483, #28272, #55842, #4159, #32455, #44140, #55465, #27147, #61486, #3774, #26777, #73181, #10922, #38855, #4899, #62223, #61859, #27895, #4524, #27519, #33957, #73919, #68262, #22223, #45250, #17314, #7122, #62972, #23724, #51655, #41452, #46728, #63710, #740, #29397, #68633, #35796, #23351, #16942, #57705, #5640, #47093, #40334, #35435, #58811, #69753, #63337, #12034, #30130, #11662, #64092, #29756, #28640, #18066, #6012, #17689, #34328, #35068, #24085, #52032, #52771, #39966, #41082, #11296, #45992, #45619, #4460, #22986, #53145, #18439, #70132, #1109, #29015, #12401, #370, #69008, #58444, #57329, #22598, #34697, #6753, #46363, #52405, #64465, #12764, #69379, #40706, #58080, #6391, #47469, #47834, #14613, #65183, #42549, #2194, #25558, #1478, #25190, #42911, #31234, #13856, #70856, #37651, #13494, #36533, #31985, #1833, #18810, #59543, #7492, #60650, #8972, #19168, #43292, #30496, #14236, #48572, #41814, #71582, #48204, #24821, #66307, #8595, #25928, #8223, #54631, #53883, #24461, #20269, #70492, #13127, #54259, #37275, #60269, #53516 ) ),
 .UNSPECIFIED., .F., .F., .F. ) 
 B_SPLINE_SURFACE_WITH_KNOTS ( ( 2, 2 ),
 ( 3, 2, 2, 2, 2, 2, 2, 2, 2, 2, 2, 2, 2, 2, 2, 2, 2, 2, 2, 2, 2, 2, 2, 2, 2, 2, 2, 2, 2, 2, 2, 2, 2, 2, 2, 2, 2, 2, 2, 2, 2, 2, 2, 2, 2, 2, 2, 2, 2, 2, 2, 2, 2, 2, 2, 2, 2, 2, 2, 2, 2, 2, 2, 2, 2, 2, 2, 2, 2, 2, 2, 2, 2, 2, 2, 2, 2, 2, 2, 2, 2, 2, 2, 2, 2, 2, 2, 2, 2, 2, 2, 2, 2, 2, 2, 2, 2, 2, 2, 2, 2, 2, 2, 2, 2, 2, 2, 2, 2, 2, 2, 2, 2, 2, 2, 2, 2, 2, 2, 2, 2, 2, 2, 2, 2, 2, 2, 2, 2, 2, 2, 2, 2, 2, 2, 2, 2, 2, 2, 2, 2, 2, 2, 2, 2, 2, 2, 2, 2, 2, 2, 2, 2, 2, 2, 2, 2, 2, 2, 2, 2, 2, 2, 2, 2, 2, 2, 2, 2, 2, 2, 2, 2, 2, 2, 2, 2, 2, 2, 2, 2, 2, 2, 2, 2, 2, 2, 3 ),
 ( 0.000000000000000000, 1.000000000000000000 ),
 ( 0.000000000000000000, 0.005208333333333333044, 0.01041666666666666609, 0.01562500000000000000, 0.02083333333333333218, 0.02604166666666666782, 0.03125000000000000000, 0.03645833333333333565, 0.04166666666666666435, 0.04687500000000000000, 0.05208333333333333565, 0.05729166666666666435, 0.06250000000000000000, 0.06770833333333332871, 0.07291666666666667129, 0.07812500000000000000, 0.08333333333333332871, 0.08854166666666667129, 0.09375000000000000000, 0.09895833333333332871, 0.1041666666666666713, 0.1093750000000000000, 0.1145833333333333287, 0.1197916666666666713, 0.1250000000000000000, 0.1302083333333333426, 0.1354166666666666574, 0.1406250000000000000, 0.1458333333333333426, 0.1510416666666666574, 0.1562500000000000000, 0.1614583333333333426, 0.1666666666666666574, 0.1718750000000000000, 0.1770833333333333426, 0.1822916666666666574, 0.1875000000000000000, 0.1927083333333333426, 0.1979166666666666574, 0.2031250000000000000, 0.2083333333333333426, 0.2135416666666666574, 0.2187500000000000000, 0.2239583333333333426, 0.2291666666666666574, 0.2343750000000000000, 0.2395833333333333426, 0.2447916666666666574, 0.2500000000000000000, 0.2552083333333333148, 0.2604166666666666852, 0.2656250000000000000, 0.2708333333333333148, 0.2760416666666666852, 0.2812500000000000000, 0.2864583333333333148, 0.2916666666666666852, 0.2968750000000000000, 0.3020833333333333148, 0.3072916666666666852, 0.3125000000000000000, 0.3177083333333333148, 0.3229166666666666852, 0.3281250000000000000, 0.3333333333333333148, 0.3385416666666666852, 0.3437500000000000000, 0.3489583333333333148, 0.3541666666666666852, 0.3593750000000000000, 0.3645833333333333148, 0.3697916666666666852, 0.3750000000000000000, 0.3802083333333333148, 0.3854166666666666852, 0.3906250000000000000, 0.3958333333333333148, 0.4010416666666666852, 0.4062500000000000000, 0.4114583333333333148, 0.4166666666666666852, 0.4218750000000000000, 0.4270833333333333148, 0.4322916666666666852, 0.4375000000000000000, 0.4427083333333333148, 0.4479166666666666852, 0.4531250000000000000, 0.4583333333333333148, 0.4635416666666666852, 0.4687500000000000000, 0.4739583333333333148, 0.4791666666666666852, 0.4843750000000000000, 0.4895833333333333148, 0.4947916666666666852, 0.5000000000000000000, 0.5052083333333333703, 0.5104166666666666297, 0.5156250000000000000, 0.5208333333333333703, 0.5260416666666666297, 0.5312500000000000000, 0.5364583333333333703, 0.5416666666666666297, 0.5468750000000000000, 0.5520833333333333703, 0.5572916666666666297, 0.5625000000000000000, 0.5677083333333333703, 0.5729166666666666297, 0.5781250000000000000, 0.5833333333333333703, 0.5885416666666666297, 0.5937500000000000000, 0.5989583333333333703, 0.6041666666666666297, 0.6093750000000000000, 0.6145833333333333703, 0.6197916666666666297, 0.6250000000000000000, 0.6302083333333333703, 0.6354166666666666297, 0.6406250000000000000, 0.6458333333333333703, 0.6510416666666666297, 0.6562500000000000000, 0.6614583333333333703, 0.6666666666666666297, 0.6718750000000000000, 0.6770833333333333703, 0.6822916666666666297, 0.6875000000000000000, 0.6927083333333333703, 0.6979166666666666297, 0.7031250000000000000, 0.7083333333333333703, 0.7135416666666666297, 0.7187500000000000000, 0.7239583333333333703, 0.7291666666666666297, 0.7343750000000000000, 0.7395833333333333703, 0.7447916666666666297, 0.7500000000000000000, 0.7552083333333333703, 0.7604166666666666297, 0.7656250000000000000, 0.7708333333333333703, 0.7760416666666666297, 0.7812500000000000000, 0.7864583333333333703, 0.7916666666666666297, 0.7968750000000000000, 0.8020833333333333703, 0.8072916666666666297, 0.8125000000000000000, 0.8177083333333333703, 0.8229166666666666297, 0.8281250000000000000, 0.8333333333333333703, 0.8385416666666666297, 0.8437500000000000000, 0.8489583333333333703, 0.8541666666666666297, 0.8593750000000000000, 0.8645833333333333703, 0.8697916666666666297, 0.8750000000000000000, 0.8802083333333333703, 0.8854166666666666297, 0.8906250000000000000, 0.8958333333333333703, 0.9010416666666666297, 0.9062500000000000000, 0.9114583333333333703, 0.9166666666666666297, 0.9218750000000000000, 0.9270833333333333703, 0.9322916666666666297, 0.9375000000000000000, 0.9427083333333333703, 0.9479166666666666297, 0.9531250000000000000, 0.9583333333333333703, 0.9635416666666666297, 0.9687500000000000000, 0.9722122636433919718 ),
 .UNSPECIFIED. ) 
 GEOMETRIC_REPRESENTATION_ITEM ( )  RATIONAL_B_SPLINE_SURFACE ( (
 ( 1.000000000000000000, 0.9238795325112867385, 1.000000000000000000, 0.9238795325112867385, 1.000000000000000000, 0.9238795325112867385, 1.000000000000000000, 0.9238795325112867385, 1.000000000000000000, 0.9238795325112867385, 1.000000000000000000, 0.9238795325112867385, 1.000000000000000000, 0.9238795325112867385, 1.000000000000000000, 0.9238795325112867385, 1.000000000000000000, 0.9238795325112867385, 1.000000000000000000, 0.9238795325112867385, 1.000000000000000000, 0.9238795325112867385, 1.000000000000000000, 0.9238795325112867385, 1.000000000000000000, 0.9238795325112867385, 1.000000000000000000, 0.9238795325112867385, 1.000000000000000000, 0.9238795325112867385, 1.000000000000000000, 0.9238795325112867385, 1.000000000000000000, 0.9238795325112867385, 1.000000000000000000, 0.9238795325112867385, 1.000000000000000000, 0.9238795325112867385, 1.000000000000000000, 0.9238795325112867385, 1.000000000000000000, 0.9238795325112867385, 1.000000000000000000, 0.9238795325112867385, 1.000000000000000000, 0.9238795325112867385, 1.000000000000000000, 0.9238795325112867385, 1.000000000000000000, 0.9238795325112867385, 1.000000000000000000, 0.9238795325112867385, 1.000000000000000000, 0.9238795325112867385, 1.000000000000000000, 0.9238795325112867385, 1.000000000000000000, 0.9238795325112867385, 1.000000000000000000, 0.9238795325112867385, 1.000000000000000000, 0.9238795325112867385, 1.000000000000000000, 0.9238795325112867385, 1.000000000000000000, 0.9238795325112867385, 1.000000000000000000, 0.9238795325112867385, 1.000000000000000000, 0.9238795325112867385, 1.000000000000000000, 0.9238795325112867385, 1.000000000000000000, 0.9238795325112867385, 1.000000000000000000, 0.9238795325112867385, 1.000000000000000000, 0.9238795325112867385, 1.000000000000000000, 0.9238795325112867385, 1.000000000000000000, 0.9238795325112867385, 1.000000000000000000, 0.9238795325112867385, 1.000000000000000000, 0.9238795325112867385, 1.000000000000000000, 0.9238795325112867385, 1.000000000000000000, 0.9238795325112867385, 1.000000000000000000, 0.9238795325112867385, 1.000000000000000000, 0.9238795325112867385, 1.000000000000000000, 0.9238795325112867385, 1.000000000000000000, 0.9238795325112867385, 1.000000000000000000, 0.9238795325112867385, 1.000000000000000000, 0.9238795325112867385, 1.000000000000000000, 0.9238795325112867385, 1.000000000000000000, 0.9238795325112867385, 1.000000000000000000, 0.9238795325112867385, 1.000000000000000000, 0.9238795325112867385, 1.000000000000000000, 0.9238795325112867385, 1.000000000000000000, 0.9238795325112867385, 1.000000000000000000, 0.9238795325112867385, 1.000000000000000000, 0.9238795325112867385, 1.000000000000000000, 0.9238795325112867385, 1.000000000000000000, 0.9238795325112867385, 1.000000000000000000, 0.9238795325112867385, 1.000000000000000000, 0.9238795325112867385, 1.000000000000000000, 0.9238795325112867385, 1.000000000000000000, 0.9238795325112867385, 1.000000000000000000, 0.9238795325112867385, 1.000000000000000000, 0.9238795325112867385, 1.000000000000000000, 0.9238795325112867385, 1.000000000000000000, 0.9238795325112867385, 1.000000000000000000, 0.9238795325112867385, 1.000000000000000000, 0.9238795325112867385, 1.000000000000000000, 0.9238795325112867385, 1.000000000000000000, 0.9238795325112867385, 1.000000000000000000, 0.9238795325112867385, 1.000000000000000000, 0.9238795325112867385, 1.000000000000000000, 0.9238795325112867385, 1.000000000000000000, 0.9238795325112867385, 1.000000000000000000, 0.9238795325112867385, 1.000000000000000000, 0.9238795325112867385, 1.000000000000000000, 0.9238795325112867385, 1.000000000000000000, 0.9238795325112867385, 1.000000000000000000, 0.9238795325112867385, 1.000000000000000000, 0.9238795325112867385, 1.000000000000000000, 0.9238795325112867385, 1.000000000000000000, 0.9238795325112867385, 1.000000000000000000, 0.9238795325112867385, 1.000000000000000000, 0.9238795325112867385, 1.000000000000000000, 0.9238795325112867385, 1.000000000000000000, 0.9238795325112867385, 1.000000000000000000, 0.9238795325112867385, 1.000000000000000000, 0.9238795325112867385, 1.000000000000000000, 0.9238795325112867385, 1.000000000000000000, 0.9238795325112867385, 1.000000000000000000, 0.9238795325112867385, 1.000000000000000000, 0.9238795325112867385, 1.000000000000000000, 0.9238795325112867385, 1.000000000000000000, 0.9238795325112867385, 1.000000000000000000, 0.9238795325112867385, 1.000000000000000000, 0.9238795325112867385, 1.000000000000000000, 0.9238795325112867385, 1.000000000000000000, 0.9238795325112867385, 1.000000000000000000, 0.9238795325112867385, 1.000000000000000000, 0.9238795325112867385, 1.000000000000000000, 0.9238795325112867385, 1.000000000000000000, 0.9238795325112867385, 1.000000000000000000, 0.9238795325112867385, 1.000000000000000000, 0.9238795325112867385, 1.000000000000000000, 0.9238795325112867385, 1.000000000000000000, 0.9238795325112867385, 1.000000000000000000, 0.9238795325112867385, 1.000000000000000000, 0.9238795325112867385, 1.000000000000000000, 0.9238795325112867385, 1.000000000000000000, 0.9238795325112867385, 1.000000000000000000, 0.9238795325112867385, 1.000000000000000000, 0.9238795325112867385, 1.000000000000000000, 0.9238795325112867385, 1.000000000000000000, 0.9238795325112867385, 1.000000000000000000, 0.9238795325112867385, 1.000000000000000000, 0.9238795325112867385, 1.000000000000000000, 0.9238795325112867385, 1.000000000000000000, 0.9238795325112867385, 1.000000000000000000, 0.9238795325112867385, 1.000000000000000000, 0.9238795325112867385, 1.000000000000000000, 0.9238795325112867385, 1.000000000000000000, 0.9238795325112867385, 1.000000000000000000, 0.9238795325112867385, 1.000000000000000000, 0.9238795325112867385, 1.000000000000000000, 0.9238795325112867385, 1.000000000000000000, 0.9238795325112867385, 1.000000000000000000, 0.9238795325112867385, 1.000000000000000000, 0.9238795325112867385, 1.000000000000000000, 0.9238795325112867385, 1.000000000000000000, 0.9238795325112867385, 1.000000000000000000, 0.9238795325112867385, 1.000000000000000000, 0.9238795325112867385, 1.000000000000000000, 0.9238795325112867385, 1.000000000000000000, 0.9238795325112867385, 1.000000000000000000, 0.9238795325112867385, 1.000000000000000000, 0.9238795325112867385, 1.000000000000000000, 0.9238795325112867385, 1.000000000000000000, 0.9238795325112867385, 1.000000000000000000, 0.9238795325112867385, 1.000000000000000000, 0.9238795325112867385, 1.000000000000000000, 0.9238795325112867385, 1.000000000000000000, 0.9238795325112867385, 1.000000000000000000, 0.9238795325112867385, 1.000000000000000000, 0.9238795325112867385, 1.000000000000000000, 0.9238795325112867385, 1.000000000000000000, 0.9238795325112867385, 1.000000000000000000, 0.9238795325112867385, 1.000000000000000000, 0.9238795325112867385, 1.000000000000000000, 0.9238795325112867385, 1.000000000000000000, 0.9238795325112867385, 1.000000000000000000, 0.9238795325112867385, 1.000000000000000000, 0.9238795325112867385, 1.000000000000000000, 0.9238795325112867385, 1.000000000000000000, 0.9238795325112867385, 1.000000000000000000, 0.9238795325112867385, 1.000000000000000000, 0.9238795325112867385, 1.000000000000000000, 0.9238795325112867385, 1.000000000000000000, 0.9238795325112867385, 1.000000000000000000, 0.9238795325112867385, 1.000000000000000000, 0.9238795325112867385, 1.000000000000000000, 0.9238795325112867385, 1.000000000000000000, 0.9238795325112867385, 1.000000000000000000, 0.9238795325112867385, 1.000000000000000000, 0.9238795325112867385, 1.000000000000000000, 0.9238795325112867385, 1.000000000000000000, 0.9238795325112867385, 1.000000000000000000, 0.9238795325112867385, 1.000000000000000000, 0.9238795325112867385, 1.000000000000000000, 0.9238795325112867385, 1.000000000000000000, 0.9238795325112867385, 1.000000000000000000, 0.9238795325112867385, 1.000000000000000000, 0.9238795325112867385, 1.000000000000000000, 0.9238795325112867385, 1.000000000000000000, 0.9238795325112867385, 1.000000000000000000, 0.9238795325112867385, 1.000000000000000000, 0.9238795325112867385, 1.000000000000000000, 0.9238795325112867385, 1.000000000000000000, 0.9238795325112867385, 1.000000000000000000, 0.9238795325112867385, 1.000000000000000000, 0.9238795325112867385, 1.000000000000000000, 0.9238795325112867385, 1.000000000000000000, 0.9238795325112867385, 1.000000000000000000, 0.9238795325112867385, 1.000000000000000000, 0.9493985675959992765, 0.9660722070829144137),
 ( 1.000000000000000000, 0.9238795325112867385, 1.000000000000000000, 0.9238795325112867385, 1.000000000000000000, 0.9238795325112867385, 1.000000000000000000, 0.9238795325112867385, 1.000000000000000000, 0.9238795325112867385, 1.000000000000000000, 0.9238795325112867385, 1.000000000000000000, 0.9238795325112867385, 1.000000000000000000, 0.9238795325112867385, 1.000000000000000000, 0.9238795325112867385, 1.000000000000000000, 0.9238795325112867385, 1.000000000000000000, 0.9238795325112867385, 1.000000000000000000, 0.9238795325112867385, 1.000000000000000000, 0.9238795325112867385, 1.000000000000000000, 0.9238795325112867385, 1.000000000000000000, 0.9238795325112867385, 1.000000000000000000, 0.9238795325112867385, 1.000000000000000000, 0.9238795325112867385, 1.000000000000000000, 0.9238795325112867385, 1.000000000000000000, 0.9238795325112867385, 1.000000000000000000, 0.9238795325112867385, 1.000000000000000000, 0.9238795325112867385, 1.000000000000000000, 0.9238795325112867385, 1.000000000000000000, 0.9238795325112867385, 1.000000000000000000, 0.9238795325112867385, 1.000000000000000000, 0.9238795325112867385, 1.000000000000000000, 0.9238795325112867385, 1.000000000000000000, 0.9238795325112867385, 1.000000000000000000, 0.9238795325112867385, 1.000000000000000000, 0.9238795325112867385, 1.000000000000000000, 0.9238795325112867385, 1.000000000000000000, 0.9238795325112867385, 1.000000000000000000, 0.9238795325112867385, 1.000000000000000000, 0.9238795325112867385, 1.000000000000000000, 0.9238795325112867385, 1.000000000000000000, 0.9238795325112867385, 1.000000000000000000, 0.9238795325112867385, 1.000000000000000000, 0.9238795325112867385, 1.000000000000000000, 0.9238795325112867385, 1.000000000000000000, 0.9238795325112867385, 1.000000000000000000, 0.9238795325112867385, 1.000000000000000000, 0.9238795325112867385, 1.000000000000000000, 0.9238795325112867385, 1.000000000000000000, 0.9238795325112867385, 1.000000000000000000, 0.9238795325112867385, 1.000000000000000000, 0.9238795325112867385, 1.000000000000000000, 0.9238795325112867385, 1.000000000000000000, 0.9238795325112867385, 1.000000000000000000, 0.9238795325112867385, 1.000000000000000000, 0.9238795325112867385, 1.000000000000000000, 0.9238795325112867385, 1.000000000000000000, 0.9238795325112867385, 1.000000000000000000, 0.9238795325112867385, 1.000000000000000000, 0.9238795325112867385, 1.000000000000000000, 0.9238795325112867385, 1.000000000000000000, 0.9238795325112867385, 1.000000000000000000, 0.9238795325112867385, 1.000000000000000000, 0.9238795325112867385, 1.000000000000000000, 0.9238795325112867385, 1.000000000000000000, 0.9238795325112867385, 1.000000000000000000, 0.9238795325112867385, 1.000000000000000000, 0.9238795325112867385, 1.000000000000000000, 0.9238795325112867385, 1.000000000000000000, 0.9238795325112867385, 1.000000000000000000, 0.9238795325112867385, 1.000000000000000000, 0.9238795325112867385, 1.000000000000000000, 0.9238795325112867385, 1.000000000000000000, 0.9238795325112867385, 1.000000000000000000, 0.9238795325112867385, 1.000000000000000000, 0.9238795325112867385, 1.000000000000000000, 0.9238795325112867385, 1.000000000000000000, 0.9238795325112867385, 1.000000000000000000, 0.9238795325112867385, 1.000000000000000000, 0.9238795325112867385, 1.000000000000000000, 0.9238795325112867385, 1.000000000000000000, 0.9238795325112867385, 1.000000000000000000, 0.9238795325112867385, 1.000000000000000000, 0.9238795325112867385, 1.000000000000000000, 0.9238795325112867385, 1.000000000000000000, 0.9238795325112867385, 1.000000000000000000, 0.9238795325112867385, 1.000000000000000000, 0.9238795325112867385, 1.000000000000000000, 0.9238795325112867385, 1.000000000000000000, 0.9238795325112867385, 1.000000000000000000, 0.9238795325112867385, 1.000000000000000000, 0.9238795325112867385, 1.000000000000000000, 0.9238795325112867385, 1.000000000000000000, 0.9238795325112867385, 1.000000000000000000, 0.9238795325112867385, 1.000000000000000000, 0.9238795325112867385, 1.000000000000000000, 0.9238795325112867385, 1.000000000000000000, 0.9238795325112867385, 1.000000000000000000, 0.9238795325112867385, 1.000000000000000000, 0.9238795325112867385, 1.000000000000000000, 0.9238795325112867385, 1.000000000000000000, 0.9238795325112867385, 1.000000000000000000, 0.9238795325112867385, 1.000000000000000000, 0.9238795325112867385, 1.000000000000000000, 0.9238795325112867385, 1.000000000000000000, 0.9238795325112867385, 1.000000000000000000, 0.9238795325112867385, 1.000000000000000000, 0.9238795325112867385, 1.000000000000000000, 0.9238795325112867385, 1.000000000000000000, 0.9238795325112867385, 1.000000000000000000, 0.9238795325112867385, 1.000000000000000000, 0.9238795325112867385, 1.000000000000000000, 0.9238795325112867385, 1.000000000000000000, 0.9238795325112867385, 1.000000000000000000, 0.9238795325112867385, 1.000000000000000000, 0.9238795325112867385, 1.000000000000000000, 0.9238795325112867385, 1.000000000000000000, 0.9238795325112867385, 1.000000000000000000, 0.9238795325112867385, 1.000000000000000000, 0.9238795325112867385, 1.000000000000000000, 0.9238795325112867385, 1.000000000000000000, 0.9238795325112867385, 1.000000000000000000, 0.9238795325112867385, 1.000000000000000000, 0.9238795325112867385, 1.000000000000000000, 0.9238795325112867385, 1.000000000000000000, 0.9238795325112867385, 1.000000000000000000, 0.9238795325112867385, 1.000000000000000000, 0.9238795325112867385, 1.000000000000000000, 0.9238795325112867385, 1.000000000000000000, 0.9238795325112867385, 1.000000000000000000, 0.9238795325112867385, 1.000000000000000000, 0.9238795325112867385, 1.000000000000000000, 0.9238795325112867385, 1.000000000000000000, 0.9238795325112867385, 1.000000000000000000, 0.9238795325112867385, 1.000000000000000000, 0.9238795325112867385, 1.000000000000000000, 0.9238795325112867385, 1.000000000000000000, 0.9238795325112867385, 1.000000000000000000, 0.9238795325112867385, 1.000000000000000000, 0.9238795325112867385, 1.000000000000000000, 0.9238795325112867385, 1.000000000000000000, 0.9238795325112867385, 1.000000000000000000, 0.9238795325112867385, 1.000000000000000000, 0.9238795325112867385, 1.000000000000000000, 0.9238795325112867385, 1.000000000000000000, 0.9238795325112867385, 1.000000000000000000, 0.9238795325112867385, 1.000000000000000000, 0.9238795325112867385, 1.000000000000000000, 0.9238795325112867385, 1.000000000000000000, 0.9238795325112867385, 1.000000000000000000, 0.9238795325112867385, 1.000000000000000000, 0.9238795325112867385, 1.000000000000000000, 0.9238795325112867385, 1.000000000000000000, 0.9238795325112867385, 1.000000000000000000, 0.9238795325112867385, 1.000000000000000000, 0.9238795325112867385, 1.000000000000000000, 0.9238795325112867385, 1.000000000000000000, 0.9238795325112867385, 1.000000000000000000, 0.9238795325112867385, 1.000000000000000000, 0.9238795325112867385, 1.000000000000000000, 0.9238795325112867385, 1.000000000000000000, 0.9238795325112867385, 1.000000000000000000, 0.9238795325112867385, 1.000000000000000000, 0.9238795325112867385, 1.000000000000000000, 0.9238795325112867385, 1.000000000000000000, 0.9238795325112867385, 1.000000000000000000, 0.9238795325112867385, 1.000000000000000000, 0.9238795325112867385, 1.000000000000000000, 0.9238795325112867385, 1.000000000000000000, 0.9238795325112867385, 1.000000000000000000, 0.9238795325112867385, 1.000000000000000000, 0.9238795325112867385, 1.000000000000000000, 0.9238795325112867385, 1.000000000000000000, 0.9238795325112867385, 1.000000000000000000, 0.9238795325112867385, 1.000000000000000000, 0.9238795325112867385, 1.000000000000000000, 0.9238795325112867385, 1.000000000000000000, 0.9238795325112867385, 1.000000000000000000, 0.9238795325112867385, 1.000000000000000000, 0.9238795325112867385, 1.000000000000000000, 0.9238795325112867385, 1.000000000000000000, 0.9238795325112867385, 1.000000000000000000, 0.9238795325112867385, 1.000000000000000000, 0.9238795325112867385, 1.000000000000000000, 0.9238795325112867385, 1.000000000000000000, 0.9238795325112867385, 1.000000000000000000, 0.9238795325112867385, 1.000000000000000000, 0.9238795325112867385, 1.000000000000000000, 0.9238795325112867385, 1.000000000000000000, 0.9238795325112867385, 1.000000000000000000, 0.9238795325112867385, 1.000000000000000000, 0.9238795325112867385, 1.000000000000000000, 0.9238795325112867385, 1.000000000000000000, 0.9493985675959992765, 0.9660722070829144137) ) ) 
 REPRESENTATION_ITEM ( '' )  SURFACE ( )  );
#27789=CARTESIAN_POINT ( 'NONE',  ( -1.320432766682874540E-15, 18.09374999795161187, 7.188101187500000044 ) ) ;
#27818=CARTESIAN_POINT ( 'NONE',  ( 4.898587196589412829E-16, 19.68749999590322020, -8.000000000000000000 ) ) ;
#27830=CARTESIAN_POINT ( 'NONE',  ( 7.999999999999998224, 10.40625000000000178, 3.313708498984766493 ) ) ;
#27833=CARTESIAN_POINT ( 'NONE',  ( -3.313708498984762052, 94.90625000409677625, -8.000000000000000000 ) ) ;
#27863=CARTESIAN_POINT ( 'NONE',  ( -1.469576158976823947E-15, 2.437499995903220196, 8.000000000000000000 ) ) ;
#27865=CARTESIAN_POINT ( 'NONE',  ( 5.656854249492378806, 7.124999995903221084, 5.656854249492381470 ) ) ;
#27868=CARTESIAN_POINT ( 'NONE',  ( 2.977408999572650927, 17.62499999795161543, -7.188101187500001821 ) ) ;
#27870=CARTESIAN_POINT ( 'NONE',  ( -4.898587196589412829E-16, 105.1250000000000000, -8.000000000000000000 ) ) ;
#27871=CARTESIAN_POINT ( 'NONE',  ( 7.188101187500000044, 104.2812500020483810, -8.802885111219163269E-16 ) ) ;
#27873=FACE_OUTER_BOUND ( 'NONE', #26141, .T. ) ;
#27888=CARTESIAN_POINT ( 'NONE',  ( -2.977408999572652260, 94.43750000204838102, 7.188101187500000044 ) ) ;
#27895=CARTESIAN_POINT ( 'NONE',  ( -7.188101187500001821, 100.4375000020483668, -2.977408999572650483 ) ) ;
#27925=CARTESIAN_POINT ( 'NONE',  ( -5.082755093536326818, 13.40624999795161187, 5.082755093536325042 ) ) ;
#27926=CARTESIAN_POINT ( 'NONE',  ( 5.656854249492379694, 109.6250000040967763, -5.656854249492380582 ) ) ;
#27934=ORIENTED_EDGE ( 'NONE', *, *, #57094, .T. ) ;
#27936=CARTESIAN_POINT ( 'NONE',  ( 7.188101187500001821, 105.5000000020483810, -2.977408999572651371 ) ) ;
#27938=CARTESIAN_POINT ( 'NONE',  ( -5.656854249492380582, 123.3125000000000000, -5.656854249492380582 ) ) ;
#27942=DIRECTION ( 'NONE',  ( -0.000000000000000000, 1.000000000000000000, -0.000000000000000000 ) ) ;
#27944=VERTEX_POINT ( 'NONE', #50902 ) ;
#27954=CARTESIAN_POINT ( 'NONE',  ( -3.313708498984762496, 105.7812500000000000, 7.999999999999998224 ) ) ;
#27957=EDGE_CURVE ( 'NONE', #35571, #38454, #17646, .T. ) ;
#27959=CARTESIAN_POINT ( 'NONE',  ( -3.313708498984707429, 97.71875000000000000, -8.000000000000055067 ) ) ;
#27961=CARTESIAN_POINT ( 'NONE',  ( 5.656854249492378806, 26.62499999590322375, 5.656854249492381470 ) ) ;
#27963=CARTESIAN_POINT ( 'NONE',  ( -7.188101187500000044, 121.5312500020483810, 0.000000000000000000 ) ) ;
#27971=CARTESIAN_POINT ( 'NONE',  ( 5.656854249492379694, 122.9375000000000000, -5.656854249492380582 ) ) ;
#27975=CARTESIAN_POINT ( 'NONE',  ( -8.000000000000000000, 25.96874999590322375, -3.313708498984762496 ) ) ;
#27976=CARTESIAN_POINT ( 'NONE',  ( 1.469576158976823947E-15, 101.5625000040967763, 8.000000000000000000 ) ) ;
#27977=ORIENTED_EDGE ( 'NONE', *, *, #51059, .F. ) ;
#27984=CARTESIAN_POINT ( 'NONE',  ( 5.082755093536325042, 110.0937500020483810, -5.082755093536325930 ) ) ;
#27990=CARTESIAN_POINT ( 'NONE',  ( 7.188101187500002709, 119.1875000020483810, 2.977408999572649151 ) ) ;
#27993=ORIENTED_EDGE ( 'NONE', *, *, #35372, .T. ) ;
#27995=CARTESIAN_POINT ( 'NONE',  ( 3.313708498984706985, 108.0312500000000000, -8.000000000000055067 ) ) ;
#28000=CARTESIAN_POINT ( 'NONE',  ( 8.000000000000000000, 103.2500000000000000, -9.797174393178825657E-16 ) ) ;
#28003=VECTOR ( 'NONE', #4663, 1000.000000000000000 ) ;
#28012=CARTESIAN_POINT ( 'NONE',  ( 5.082755093536324154, 24.28124999795161543, 5.082755093536326818 ) ) ;
#28014=CARTESIAN_POINT ( 'NONE',  ( -5.082755093536326818, 24.28124999795161543, 5.082755093536325042 ) ) ;
#28021=( BOUNDED_CURVE ( )  B_SPLINE_CURVE ( 2, ( #50872, #11263, #28238, #68227, #16147, #12006, #40676, #34669, #45960 ),
 .UNSPECIFIED., .F., .F. ) 
 B_SPLINE_CURVE_WITH_KNOTS ( ( 3, 2, 2, 2, 3 ),
 ( 0.2812499999999997780, 0.2864583333333330928, 0.2916666666666665186, 0.2968749999999998335, 0.3020833333333331483 ),
 .UNSPECIFIED. ) 
 CURVE ( )  GEOMETRIC_REPRESENTATION_ITEM ( )  RATIONAL_B_SPLINE_CURVE ( ( 1.000000000000003331, 0.9238795325112835188, 1.000000000000000000, 0.9238795325112867385, 1.000000000000000000, 0.9238795325112867385, 1.000000000000000000, 0.9238795325112891810, 0.9999999999999975575 ) ) 
 REPRESENTATION_ITEM ( '' )  );
#28039=CARTESIAN_POINT ( 'NONE',  ( 3.313708498984765161, 122.4687500000000000, 7.999999999999998224 ) ) ;
#28055=DIRECTION ( 'NONE',  ( 0.000000000000000000, 0.000000000000000000, 1.000000000000000000 ) ) ;
#28067=CARTESIAN_POINT ( 'NONE',  ( 5.082755093536326818, 102.2187500020483810, 5.082755093536325042 ) ) ;
#28070=CARTESIAN_POINT ( 'NONE',  ( 7.513779688745833241, 0.2176969057608504621, -1.780879344281421472 ) ) ;
#28081=CARTESIAN_POINT ( 'NONE',  ( -1.469576158976823947E-15, 4.125000000000000888, 8.000000000000000000 ) ) ;
#28090=CARTESIAN_POINT ( 'NONE',  ( -5.082755093536325042, 25.40624999795161543, -5.082755093536325930 ) ) ;
#28098=CARTESIAN_POINT ( 'NONE',  ( -7.188101187500000044, 11.71874999795161010, -8.802885111219163269E-16 ) ) ;
#28101=CARTESIAN_POINT ( 'NONE',  ( 4.401442555609581635E-16, 7.218749997951610986, -7.188101187500000044 ) ) ;
#28117=EDGE_LOOP ( 'NONE', ( #22038, #71106, #2955, #27753 ) ) ;
#28118=CARTESIAN_POINT ( 'NONE',  ( 2.977408999572652260, 16.68749999795161543, 7.188101187500000044 ) ) ;
#28123=CARTESIAN_POINT ( 'NONE',  ( 7.188101187500001821, 104.3750000020483952, -2.977408999572651371 ) ) ;
#28128=EDGE_LOOP ( 'NONE', ( #39630, #24805, #5102, #6692, #34003, #52720 ) ) ;
#28129=( BOUNDED_CURVE ( )  B_SPLINE_CURVE ( 2, ( #15354, #9341, #54626, #2935, #19898, #21393, #25921, #37647, #49704 ),
 .UNSPECIFIED., .F., .F. ) 
 B_SPLINE_CURVE_WITH_KNOTS ( ( 3, 2, 2, 2, 3 ),
 ( 0.05208333333333337034, 0.05729166666666669905, 0.06250000000000004163, 0.06770833333333337034, 0.07291666666666671293 ),
 .UNSPECIFIED. ) 
 CURVE ( )  GEOMETRIC_REPRESENTATION_ITEM ( )  RATIONAL_B_SPLINE_CURVE ( ( 0.9999999999999994449, 0.9238795325112872936, 1.000000000000000000, 0.9238795325112867385, 1.000000000000000000, 0.9238795325112867385, 1.000000000000000000, 0.9238795325112861834, 1.000000000000000666 ) ) 
 REPRESENTATION_ITEM ( '' )  );
#28134=FACE_OUTER_BOUND ( 'NONE', #49580, .T. ) ;
#28145=DIRECTION ( 'NONE',  ( -0.000000000000000000, 1.000000000000000000, -0.000000000000000000 ) ) ;
#28155=CARTESIAN_POINT ( 'NONE',  ( -5.082755093536325930, 120.9687500020483952, -5.082755093536325930 ) ) ;
#28164=CARTESIAN_POINT ( 'NONE',  ( 2.977408999572650927, 26.24999999795161898, -7.188101187500001821 ) ) ;
#28168=VERTEX_POINT ( 'NONE', #40330 ) ;
#28169=CARTESIAN_POINT ( 'NONE',  ( 9.797174393178825657E-16, 125.0000000000000000, -8.000000000000000000 ) ) ;
#28185=CARTESIAN_POINT ( 'NONE',  ( 7.188101187500000044, 3.843749997951610542, 0.000000000000000000 ) ) ;
#28189=ORIENTED_EDGE ( 'NONE', *, *, #29148, .T. ) ;
#28192=CARTESIAN_POINT ( 'NONE',  ( -5.656854249492380582, 120.3125000000000000, -5.656854249492380582 ) ) ;
#28202=CARTESIAN_POINT ( 'NONE',  ( 8.000000000000000000, 19.50000000000000355, 0.000000000000000000 ) ) ;
#28205=CARTESIAN_POINT ( 'NONE',  ( -3.313708498984762052, 90.40625000409676204, -8.000000000000000000 ) ) ;
#28217=CARTESIAN_POINT ( 'NONE',  ( 1.320432766682874540E-15, 123.4062500020483810, 7.188101187500000044 ) ) ;
#28238=CARTESIAN_POINT ( 'NONE',  ( -5.656854249492378806, 114.6875000000000000, 5.656854249492381470 ) ) ;
#28242=CARTESIAN_POINT ( 'NONE',  ( 5.656854249492378806, 8.624999995903221972, 5.656854249492381470 ) ) ;
#28245=CARTESIAN_POINT ( 'NONE',  ( -5.082755093536325042, 19.40624999795161543, -5.082755093536325930 ) ) ;
#28248=CARTESIAN_POINT ( 'NONE',  ( 7.188101187500002709, 101.1875000020483810, 2.977408999572649151 ) ) ;
#28258=FACE_OUTER_BOUND ( 'NONE', #9866, .T. ) ;
#28265=CARTESIAN_POINT ( 'NONE',  ( -5.082755093536324154, 95.84375000204838102, 5.082755093536326818 ) ) ;
#28272=CARTESIAN_POINT ( 'NONE',  ( -7.188101187500001821, 101.9375000020483810, -2.977408999572650483 ) ) ;
#28293=ORIENTED_EDGE ( 'NONE', *, *, #11345, .T. ) ;
#28297=CARTESIAN_POINT ( 'NONE',  ( 5.082755093536324154, 15.28124999795161187, 5.082755093536326818 ) ) ;
#28298=CARTESIAN_POINT ( 'NONE',  ( 8.000000000000000000, 110.9375000040967905, -9.797174393178825657E-16 ) ) ;
#28305=CARTESIAN_POINT ( 'NONE',  ( 8.000000000000000000, 116.7499999999999858, -9.797174393178825657E-16 ) ) ;
#28306=CARTESIAN_POINT ( 'NONE',  ( -7.188101187499999156, 104.7500000020483810, 2.977408999572654924 ) ) ;
#28307=VECTOR ( 'NONE', #15348, 1000.000000000000000 ) ;
#28323=CARTESIAN_POINT ( 'NONE',  ( 5.656854249492379694, 107.9374999999999858, -5.656854249492380582 ) ) ;
#28330=CARTESIAN_POINT ( 'NONE',  ( -3.313708498984765161, 26.34374999590322375, 7.999999999999998224 ) ) ;
#28332=CARTESIAN_POINT ( 'NONE',  ( -5.082755093536325930, 119.8437500020483810, -5.082755093536325930 ) ) ;
#28350=CARTESIAN_POINT ( 'NONE',  ( -7.188101187499999156, 113.7500000020483810, 2.977408999572654924 ) ) ;
#28357=CARTESIAN_POINT ( 'NONE',  ( 7.188101187500001821, 119.3750000020483810, -2.977408999572651371 ) ) ;
#28359=CARTESIAN_POINT ( 'NONE',  ( 4.898587196589412829E-16, 16.87500000000000000, -8.000000000000000000 ) ) ;
#28368=CARTESIAN_POINT ( 'NONE',  ( 8.000000000000001776, 103.1562499999999858, 3.313708498984759387 ) ) ;
#28372=AXIS2_PLACEMENT_3D ( 'NONE', #66544, #48076, #8094 ) ;
#28381=CARTESIAN_POINT ( 'NONE',  ( 3.313708498984762052, 0.2812500000000000000, -8.000000000000000000 ) ) ;
#28384=CARTESIAN_POINT ( 'NONE',  ( -5.082755093536325042, 23.90624999795161543, -5.082755093536325930 ) ) ;
#28410=CARTESIAN_POINT ( 'NONE',  ( -8.000000000000000000, 122.0000000000000000, 0.000000000000000000 ) ) ;
#28412=AXIS2_PLACEMENT_3D ( 'NONE', #25753, #12955, #48774 ) ;
#28415=EDGE_CURVE ( 'NONE', #26128, #46167, #73615, .T. ) ;
#28420=CARTESIAN_POINT ( 'NONE',  ( 3.313708498984762496, 13.03124999590322197, 7.999999999999998224 ) ) ;
#28441=CARTESIAN_POINT ( 'NONE',  ( -7.188101187500001821, 101.5625000020483810, -2.977408999572650483 ) ) ;
#28444=CARTESIAN_POINT ( 'NONE',  ( 7.231266549477588512, 0.2382077480156526428, -2.766445194245858996 ) ) ;
#28447=ORIENTED_EDGE ( 'NONE', *, *, #60201, .F. ) ;
#28454=CARTESIAN_POINT ( 'NONE',  ( -8.000000000000001776, 6.656249995903221084, 3.313708498984759387 ) ) ;
#28466=CARTESIAN_POINT ( 'NONE',  ( 2.977408999572650927, 23.62499999795161543, -7.188101187500000933 ) ) ;
#28470=ORIENTED_EDGE ( 'NONE', *, *, #19444, .T. ) ;
#28471=DIRECTION ( 'NONE',  ( 0.000000000000000000, 0.000000000000000000, 1.000000000000000000 ) ) ;
#28475=CARTESIAN_POINT ( 'NONE',  ( -7.188101187500002709, 10.31249999795161010, 2.977408999572649151 ) ) ;
#28478=CARTESIAN_POINT ( 'NONE',  ( 5.082755093536324154, 8.156249997951611874, 5.082755093536326818 ) ) ;
#28494=CARTESIAN_POINT ( 'NONE',  ( 7.188101187500000044, 19.96874999795161543, 0.000000000000000000 ) ) ;
#28498=CARTESIAN_POINT ( 'NONE',  ( -5.082755093536325930, 103.3437500020483668, -5.082755093536325930 ) ) ;
#28527=CARTESIAN_POINT ( 'NONE',  ( 1.320432766682874540E-15, 121.5312500020483810, 7.188101187500000044 ) ) ;
#28536=CARTESIAN_POINT ( 'NONE',  ( 4.401442555609581635E-16, 24.84374999795161543, -7.188101187500000044 ) ) ;
#28550=CARTESIAN_POINT ( 'NONE',  ( -8.000000000000001776, 27.65624999590322730, 3.313708498984759387 ) ) ;
#28555=DIRECTION ( 'NONE',  ( -0.000000000000000000, 1.000000000000000000, -0.000000000000000000 ) ) ;
#28559=CARTESIAN_POINT ( 'NONE',  ( 5.082755093536324154, 3.656249997951610542, 5.082755093536326818 ) ) ;
#28576=CARTESIAN_POINT ( 'NONE',  ( -8.000000000000001776, 20.34375000000000355, 3.313708498984759387 ) ) ;
#28578=CARTESIAN_POINT ( 'NONE',  ( -7.188101187500000044, 121.1562500020483810, 0.000000000000000000 ) ) ;
#28600=VERTEX_POINT ( 'NONE', #34981 ) ;
#28615=CARTESIAN_POINT ( 'NONE',  ( 4.401442555609581635E-16, 17.71874999795161187, -7.188101187500000044 ) ) ;
#28617=CARTESIAN_POINT ( 'NONE',  ( -5.656854249492381470, 8.249999995903221972, 5.656854249492379694 ) ) ;
#28618=CARTESIAN_POINT ( 'NONE',  ( 7.188101187500000933, 95.37500000204839523, -2.977408999572651371 ) ) ;
#28619=CARTESIAN_POINT ( 'NONE',  ( 0.000000000000000000, 125.0000000000000000, 0.000000000000000000 ) ) ;
#28626=CARTESIAN_POINT ( 'NONE',  ( -5.656854249492380582, 119.0000000040967905, -5.656854249492380582 ) ) ;
#28627=ORIENTED_EDGE ( 'NONE', *, *, #8106, .T. ) ;
#28634=CARTESIAN_POINT ( 'NONE',  ( 5.082755093536325042, 92.09375000204838102, -5.082755093536325930 ) ) ;
#28640=CARTESIAN_POINT ( 'NONE',  ( -4.401442555609581635E-16, 97.15625000204839523, -7.188101187500000044 ) ) ;
#28645=VERTEX_POINT ( 'NONE', #70040 ) ;
#28661=CARTESIAN_POINT ( 'NONE',  ( -2.977408999572654480, 14.99999999795161187, 7.188101187499999156 ) ) ;
#28663=CARTESIAN_POINT ( 'NONE',  ( -8.000000000000000000, 102.5937500040967763, -3.313708498984761608 ) ) ;
#28673=CARTESIAN_POINT ( 'NONE',  ( -7.188101187500001821, 103.0625000020483810, -2.977408999572650483 ) ) ;
#28690=CARTESIAN_POINT ( 'NONE',  ( -8.000000000000000000, 103.9062500000000000, -3.313708498984761608 ) ) ;
#28691=VECTOR ( 'NONE', #21194, 999.9999999999998863 ) ;
#28696=CARTESIAN_POINT ( 'NONE',  ( -3.313708498984760720, 25.78124999590322375, -8.000000000000000000 ) ) ;
#28698=CARTESIAN_POINT ( 'NONE',  ( -5.082755093536324154, 121.7187500020483952, 5.082755093536326818 ) ) ;
#28705=CARTESIAN_POINT ( 'NONE',  ( 3.313708498984815343, 100.7187500040967763, -7.999999999999944933 ) ) ;
#28712=EDGE_CURVE ( 'NONE', #50841, #66964, #63472, .T. ) ;
#28719=CARTESIAN_POINT ( 'NONE',  ( 2.977408999572650039, 110.1875000020483810, -7.188101187500000933 ) ) ;
#28724=CARTESIAN_POINT ( 'NONE',  ( 5.082755093536325042, 114.9687500020483810, -5.082755093536325930 ) ) ;
#28728=ORIENTED_EDGE ( 'NONE', *, *, #3917, .T. ) ;
#28742=DIRECTION ( 'NONE',  ( 0.000000000000000000, 0.000000000000000000, 1.000000000000000000 ) ) ;
#28750=CARTESIAN_POINT ( 'NONE',  ( -2.977408999572650039, 26.43749999795162253, -7.188101187500001821 ) ) ;
#28754=CARTESIAN_POINT ( 'NONE',  ( -5.082755093536326818, 25.78124999795161543, 5.082755093536325042 ) ) ;
#28761=ORIENTED_EDGE ( 'NONE', *, *, #71459, .F. ) ;
#28766=EDGE_CURVE ( 'NONE', #65516, #45475, #46082, .T. ) ;
#28769=VERTEX_POINT ( 'NONE', #1388 ) ;
#28778=CARTESIAN_POINT ( 'NONE',  ( 5.656854249492379694, 121.4375000000000000, -5.656854249492380582 ) ) ;
#28782=( BOUNDED_CURVE ( )  B_SPLINE_CURVE ( 2, ( #45211, #32792, #68222, #3358, #49369, #72386, #20699, #3734, #49753 ),
 .UNSPECIFIED., .F., .F. ) 
 B_SPLINE_CURVE_WITH_KNOTS ( ( 3, 2, 2, 2, 3 ),
 ( 0.4895833333333333148, 0.4947916666666666852, 0.5000000000000000000, 0.5052083333333333703, 0.5104166666666666297 ),
 .UNSPECIFIED. ) 
 CURVE ( )  GEOMETRIC_REPRESENTATION_ITEM ( )  RATIONAL_B_SPLINE_CURVE ( ( 1.000000000000000000, 0.9238795325112867385, 1.000000000000000000, 0.9238795325112867385, 1.000000000000000000, 0.9238795325112867385, 1.000000000000000000, 0.9238795325112867385, 1.000000000000000000 ) ) 
 REPRESENTATION_ITEM ( '' )  );
#28809=CARTESIAN_POINT ( 'NONE',  ( 7.188101187500000044, 103.9062500020483810, -8.802885111219163269E-16 ) ) ;
#28822=CARTESIAN_POINT ( 'NONE',  ( -5.656854249492379694, 6.374999995903221084, -5.656854249492380582 ) ) ;
#28824=CARTESIAN_POINT ( 'NONE',  ( 0.000000000000000000, 125.0000000000000000, 0.000000000000000000 ) ) ;
#28834=CARTESIAN_POINT ( 'NONE',  ( 7.188101187499999156, 24.74999999795161543, 2.977408999572654924 ) ) ;
#28842=CARTESIAN_POINT ( 'NONE',  ( -7.188101187500001821, 10.12499999795161187, -2.977408999572651371 ) ) ;
#28845=CARTESIAN_POINT ( 'NONE',  ( 5.082755093536325930, 4.031249997951610986, -5.082755093536325930 ) ) ;
#28862=EDGE_LOOP ( 'NONE', ( #40899, #52787, #19933, #14901 ) ) ;
#28863=EDGE_CURVE ( 'NONE', #39259, #61133, #35707, .T. ) ;
#28864=CARTESIAN_POINT ( 'NONE',  ( 2.977408999572650927, 14.24999999795161187, -7.188101187500000933 ) ) ;
#28868=CARTESIAN_POINT ( 'NONE',  ( 7.188101187500000044, 105.7812500020483810, -8.802885111219163269E-16 ) ) ;
#28871=CARTESIAN_POINT ( 'NONE',  ( -7.999999999999998224, 111.7812500040967763, 3.313708498984766049 ) ) ;
#28895=ADVANCED_FACE ( 'NONE', ( #55289 ), #20556, .T. ) ;
#28901=CARTESIAN_POINT ( 'NONE',  ( 1.320432766682874540E-15, 120.0312500020483810, 7.188101187500000044 ) ) ;
#28912=CARTESIAN_POINT ( 'NONE',  ( -7.188101187500002709, 23.81249999795161543, 2.977408999572649151 ) ) ;
#28934=CARTESIAN_POINT ( 'NONE',  ( -5.082755093536326818, 4.781249997951610986, 5.082755093536325042 ) ) ;
#28949=CARTESIAN_POINT ( 'NONE',  ( -1.469576158976823947E-15, 17.62500000000000000, 8.000000000000000000 ) ) ;
#28951=CARTESIAN_POINT ( 'NONE',  ( -4.401442555609581635E-16, 120.7812500020483810, -7.188101187500000044 ) ) ;
#28963=CARTESIAN_POINT ( 'NONE',  ( -5.082755093536324154, 121.7187500020483952, 5.082755093536326818 ) ) ;
#28969=ORIENTED_EDGE ( 'NONE', *, *, #18760, .T. ) ;
#28989=CARTESIAN_POINT ( 'NONE',  ( 5.082755093536325930, 22.03124999795161543, -5.082755093536325930 ) ) ;
#28992=CARTESIAN_POINT ( 'NONE',  ( 7.188101187500000933, 96.87500000204838102, -2.977408999572651371 ) ) ;
#29007=CARTESIAN_POINT ( 'NONE',  ( 0.000000000000000000, 125.0000000000000000, 0.000000000000000000 ) ) ;
#29008=CARTESIAN_POINT ( 'NONE',  ( -2.977408999572652260, 95.93750000204839523, 7.188101187500000044 ) ) ;
#29015=CARTESIAN_POINT ( 'NONE',  ( 7.188101187500000044, 95.28125000204836681, -8.802885111219163269E-16 ) ) ;
#29040=CARTESIAN_POINT ( 'NONE',  ( -7.188101187500002709, 14.81249999795161543, 2.977408999572649151 ) ) ;
#29041=CARTESIAN_POINT ( 'NONE',  ( -4.898587196589412829E-16, 106.8125000040967763, -8.000000000000000000 ) ) ;
#29048=ORIENTED_EDGE ( 'NONE', *, *, #62975, .T. ) ;
#29049=DIRECTION ( 'NONE',  ( -0.000000000000000000, 1.000000000000000000, -0.000000000000000000 ) ) ;
#29050=CARTESIAN_POINT ( 'NONE',  ( 7.188101187500002709, 106.8125000020484094, 2.977408999572649151 ) ) ;
#29070=CARTESIAN_POINT ( 'NONE',  ( 8.000000000000000000, 101.7500000000000000, -9.797174393178825657E-16 ) ) ;
#29076=CARTESIAN_POINT ( 'NONE',  ( -1.320432766682874540E-15, 6.468749997951610098, 7.188101187500000044 ) ) ;
#29079=CARTESIAN_POINT ( 'NONE',  ( -2.977408999572652260, 115.8125000020483952, 7.188101187500000044 ) ) ;
#29101=CARTESIAN_POINT ( 'NONE',  ( 2.977408999572650039, 108.6875000020483810, -7.188101187500000933 ) ) ;
#29106=CARTESIAN_POINT ( 'NONE',  ( 2.977408999572654480, 114.5000000020483810, 7.188101187499999156 ) ) ;
#29117=AXIS2_PLACEMENT_3D ( 'NONE', #26753, #43733, #42973 ) ;
#29118=CARTESIAN_POINT ( 'NONE',  ( -5.656854249492379694, 18.56250000000000355, -5.656854249492380582 ) ) ;
#29121=VERTEX_POINT ( 'NONE', #43196 ) ;
#29127=ORIENTED_EDGE ( 'NONE', *, *, #63112, .F. ) ;
#29132=CARTESIAN_POINT ( 'NONE',  ( 8.000000000000000000, 4.593750000000000888, -3.313708498984761608 ) ) ;
#29133=CARTESIAN_POINT ( 'NONE',  ( -4.898587196589412829E-16, 109.8125000040967905, -8.000000000000000000 ) ) ;
#29135=CARTESIAN_POINT ( 'NONE',  ( 7.188101187500001821, 26.43749999795162253, -2.977408999572650483 ) ) ;
#29136=CARTESIAN_POINT ( 'NONE',  ( 8.000000000000000000, 121.5312500040968047, -3.313708498984762496 ) ) ;
#29148=EDGE_CURVE ( 'NONE', #50014, #48435, #32661, .T. ) ;
#29162=CARTESIAN_POINT ( 'NONE',  ( -8.000000000000000000, 115.9999999999999858, 0.000000000000000000 ) ) ;
#29186=EDGE_CURVE ( 'NONE', #55947, #31825, #14327, .T. ) ;
#29188=CYLINDRICAL_SURFACE ( 'NONE', #50274, 8.000000000000000000 ) ;
#29194=CARTESIAN_POINT ( 'NONE',  ( -4.401442555609581635E-16, 95.28125000204836681, -7.188101187500000044 ) ) ;
#29217=CARTESIAN_POINT ( 'NONE',  ( -7.188101187500002709, 22.68749999795161187, 2.977408999572649151 ) ) ;
#29225=CARTESIAN_POINT ( 'NONE',  ( -2.977408999572650039, 8.437499997951611874, -7.188101187500001821 ) ) ;
#29228=CARTESIAN_POINT ( 'NONE',  ( -5.082755093536325042, 8.906249997951611874, -5.082755093536325930 ) ) ;
#29242=CARTESIAN_POINT ( 'NONE',  ( 2.977408999572654480, 115.6250000020483810, 7.188101187499999156 ) ) ;
#29246=CARTESIAN_POINT ( 'NONE',  ( -2.977408999572650039, 17.43749999795161187, -7.188101187500000933 ) ) ;
#29251=CARTESIAN_POINT ( 'NONE',  ( -7.188101187499999156, 102.1250000020483810, 2.977408999572654924 ) ) ;
#29254=CARTESIAN_POINT ( 'NONE',  ( -5.656854249492380582, 95.00000000409677625, -5.656854249492380582 ) ) ;
#29262=CYLINDRICAL_SURFACE ( 'NONE', #73687, 8.000000000000000000 ) ;
#29265=DIRECTION ( 'NONE',  ( 0.000000000000000000, 0.000000000000000000, 1.000000000000000000 ) ) ;
#29273=CARTESIAN_POINT ( 'NONE',  ( 0.000000000000000000, 125.0000000000000000, 8.000000000000000000 ) ) ;
#29275=AXIS2_PLACEMENT_3D ( 'NONE', #9077, #60374, #38126 ) ;
#29276=CARTESIAN_POINT ( 'NONE',  ( 5.656854249492380582, 10.68750000000000178, -5.656854249492380582 ) ) ;
#29283=CARTESIAN_POINT ( 'NONE',  ( -7.188101187500001821, 116.5625000020483810, -2.977408999572650483 ) ) ;
#29292=CARTESIAN_POINT ( 'NONE',  ( 7.188101187500001821, 24.56249999795161543, -2.977408999572650483 ) ) ;
#29297=CARTESIAN_POINT ( 'NONE',  ( 5.656854249492378806, 25.31250000000000355, 5.656854249492381470 ) ) ;
#29314=CARTESIAN_POINT ( 'NONE',  ( -5.082755093536325042, 5.906249997951610986, -5.082755093536325930 ) ) ;
#29330=CARTESIAN_POINT ( 'NONE',  ( 8.000000000000000000, 18.00000000000000355, 0.000000000000000000 ) ) ;
#29333=CARTESIAN_POINT ( 'NONE',  ( -7.188101187500001821, 124.0625000020483810, -2.977408999572650483 ) ) ;
#29334=( NAMED_UNIT ( * ) SI_UNIT ( $, .STERADIAN. ) SOLID_ANGLE_UNIT ( ) );
#29339=( BOUNDED_CURVE ( )  B_SPLINE_CURVE ( 2, ( #62939, #16148, #11264, #34295, #67489, #5611, #62190, #56552, #33549 ),
 .UNSPECIFIED., .F., .F. ) 
 B_SPLINE_CURVE_WITH_KNOTS ( ( 3, 2, 2, 2, 3 ),
 ( 0.6354166666666667407, 0.6406250000000001110, 0.6458333333333334814, 0.6510416666666666297, 0.6562500000000000000 ),
 .UNSPECIFIED. ) 
 CURVE ( )  GEOMETRIC_REPRESENTATION_ITEM ( )  RATIONAL_B_SPLINE_CURVE ( ( 0.9999999999999983347, 0.9238795325112884038, 1.000000000000000000, 0.9238795325112867385, 1.000000000000000000, 0.9238795325112867385, 1.000000000000000000, 0.9238795325112867385, 1.000000000000000000 ) ) 
 REPRESENTATION_ITEM ( '' )  );
#29343=CARTESIAN_POINT ( 'NONE',  ( 3.313708498984679895, 114.0312500000000000, -8.000000000000081712 ) ) ;
#29346=CARTESIAN_POINT ( 'NONE',  ( -7.188101187499999156, 123.1250000020484094, 2.977408999572654924 ) ) ;
#29353=ADVANCED_FACE ( 'NONE', ( #53759 ), #64707, .T. ) ;
#29373=CARTESIAN_POINT ( 'NONE',  ( -7.188101187500000044, 25.59374999795161543, -8.802885111219163269E-16 ) ) ;
#29375=CARTESIAN_POINT ( 'NONE',  ( -5.082755093536324154, 99.21875000204838102, 5.082755093536326818 ) ) ;
#29377=CARTESIAN_POINT ( 'NONE',  ( 1.469576158976823947E-15, 106.0625000040967763, 8.000000000000000000 ) ) ;
#29392=CARTESIAN_POINT ( 'NONE',  ( 5.082755093536325042, 90.59375000204838102, -5.082755093536325930 ) ) ;
#29397=CARTESIAN_POINT ( 'NONE',  ( -5.082755093536325930, 98.84375000204838102, -5.082755093536325930 ) ) ;
#29408=DIRECTION ( 'NONE',  ( -0.000000000000000000, 1.000000000000000000, -0.000000000000000000 ) ) ;
#29415=CARTESIAN_POINT ( 'NONE',  ( 4.898587196589412829E-16, 3.187499995903220640, -8.000000000000000000 ) ) ;
#29417=CARTESIAN_POINT ( 'NONE',  ( -5.656854249492378806, 102.8750000040967763, 5.656854249492381470 ) ) ;
#29418=EDGE_CURVE ( 'NONE', #25275, #62362, #40355, .T. ) ;
#29427=CARTESIAN_POINT ( 'NONE',  ( -5.082755093536324154, 104.8437500020483810, 5.082755093536326818 ) ) ;
#29429=CARTESIAN_POINT ( 'NONE',  ( -7.999999999999998224, 123.5937500000000000, 3.313708498984766049 ) ) ;
#29439=CYLINDRICAL_SURFACE ( 'NONE', #41080, 8.000000000000000000 ) ;
#29443=CARTESIAN_POINT ( 'NONE',  ( -8.000000000000000000, 99.40625000000000000, -3.313708498984761608 ) ) ;
#29449=CARTESIAN_POINT ( 'NONE',  ( -5.082755093536325042, 5.906249997951610986, -5.082755093536325930 ) ) ;
#29453=CARTESIAN_POINT ( 'NONE',  ( 2.977408999572654480, 116.0000000020483810, 7.188101187499999156 ) ) ;
#29473=CARTESIAN_POINT ( 'NONE',  ( 2.977408999572654480, 109.6250000020483952, 7.188101187499999156 ) ) ;
#29477=( BOUNDED_CURVE ( )  B_SPLINE_CURVE ( 2, ( #19189, #42190, #65204, #13511, #21046, #71231, #9744, #43690, #20671 ),
 .UNSPECIFIED., .F., .F. ) 
 B_SPLINE_CURVE_WITH_KNOTS ( ( 3, 2, 2, 2, 3 ),
 ( 0.6527777777777777901, 0.6597222222222222099, 0.6666666666666665186, 0.6736111111111110494, 0.6805555555555554692 ),
 .UNSPECIFIED. ) 
 CURVE ( )  GEOMETRIC_REPRESENTATION_ITEM ( )  RATIONAL_B_SPLINE_CURVE ( ( 1.000000000000000000, 0.9238795325112867385, 1.000000000000000000, 0.9238795325112867385, 1.000000000000000000, 0.9238795325112867385, 1.000000000000000000, 0.9238795325112879597, 0.9999999999999987788 ) ) 
 REPRESENTATION_ITEM ( '' )  );
#29479=CARTESIAN_POINT ( 'NONE',  ( -4.401442555609581635E-16, 112.1562500020483952, -7.188101187500000044 ) ) ;
#29491=CARTESIAN_POINT ( 'NONE',  ( 5.656854249492380582, 15.18750000000000355, -5.656854249492380582 ) ) ;
#29505=CARTESIAN_POINT ( 'NONE',  ( -8.000000000000001776, 8.343750000000001776, 3.313708498984759387 ) ) ;
#29507=CARTESIAN_POINT ( 'NONE',  ( 7.188101187500000044, 26.34374999795161543, 0.000000000000000000 ) ) ;
#29522=ORIENTED_EDGE ( 'NONE', *, *, #33498, .F. ) ;
#29530=CARTESIAN_POINT ( 'NONE',  ( 3.313708498984760720, 117.0312500000000000, -8.000000000000000000 ) ) ;
#29535=CARTESIAN_POINT ( 'NONE',  ( -1.469576158976823947E-15, 15.93749999590322197, 8.000000000000000000 ) ) ;
#29537=CARTESIAN_POINT ( 'NONE',  ( -1.469576158976823947E-15, 11.43749999590322197, 8.000000000000000000 ) ) ;
#29561=CARTESIAN_POINT ( 'NONE',  ( -7.188101187500001821, 100.0625000020483952, -2.977408999572650483 ) ) ;
#29575=FACE_OUTER_BOUND ( 'NONE', #40098, .T. ) ;
#29579=ORIENTED_EDGE ( 'NONE', *, *, #19333, .T. ) ;
#29592=EDGE_CURVE ( 'NONE', #39207, #1937, #55779, .T. ) ;
#29593=CARTESIAN_POINT ( 'NONE',  ( -2.977408999572650039, 14.43749999795161365, -7.188101187500001821 ) ) ;
#29596=CARTESIAN_POINT ( 'NONE',  ( -7.188101187500000044, 6.093749997951610986, -8.802885111219163269E-16 ) ) ;
#29608=CARTESIAN_POINT ( 'NONE',  ( -4.401442555609581635E-16, 119.2812500020483810, -7.188101187500000044 ) ) ;
#29614=CARTESIAN_POINT ( 'NONE',  ( 2.977408999572650927, 17.24999999795162253, -7.188101187500000933 ) ) ;
#29619=CARTESIAN_POINT ( 'NONE',  ( 7.188101187500001821, 101.3750000020483952, -2.977408999572651371 ) ) ;
#29633=CARTESIAN_POINT ( 'NONE',  ( 1.469576158976823947E-15, 119.3750000000000000, 8.000000000000000000 ) ) ;
#29641=ORIENTED_EDGE ( 'NONE', *, *, #23954, .T. ) ;
#29646=CARTESIAN_POINT ( 'NONE',  ( 7.188101187500000044, 114.4062500020483810, -8.802885111219163269E-16 ) ) ;
#29654=CARTESIAN_POINT ( 'NONE',  ( 5.082755093536325930, 23.15624999795161543, -5.082755093536325930 ) ) ;
#29660=CARTESIAN_POINT ( 'NONE',  ( 8.000000000000000000, 25.59375000000000711, -3.313708498984761164 ) ) ;
#29673=AXIS2_PLACEMENT_3D ( 'NONE', #8649, #44475, #3363 ) ;
#29677=CARTESIAN_POINT ( 'NONE',  ( 2.977408999572652260, 8.062499997951611874, 7.188101187500000044 ) ) ;
#29688=VERTEX_POINT ( 'NONE', #38647 ) ;
#29696=CARTESIAN_POINT ( 'NONE',  ( 3.313708498984762052, 16.78125000000000355, -8.000000000000000000 ) ) ;
#29698=CARTESIAN_POINT ( 'NONE',  ( -7.188101187499999156, 119.7500000020483810, 2.977408999572654924 ) ) ;
#29705=CARTESIAN_POINT ( 'NONE',  ( 5.082755093536325930, 0.6562499979516100979, -5.082755093536325930 ) ) ;
#29707=DIRECTION ( 'NONE',  ( -0.000000000000000000, 1.000000000000000000, -0.000000000000000000 ) ) ;
#29710=CARTESIAN_POINT ( 'NONE',  ( 7.188101187500001821, 117.8750000020483810, -2.977408999572651371 ) ) ;
#29723=DIRECTION ( 'NONE',  ( -0.000000000000000000, 1.000000000000000000, 0.000000000000000000 ) ) ;
#29734=CARTESIAN_POINT ( 'NONE',  ( -7.188101187500001821, 25.49999999795161898, -2.977408999572651371 ) ) ;
#29736=CARTESIAN_POINT ( 'NONE',  ( -5.082755093536325930, 98.84375000204838102, -5.082755093536325930 ) ) ;
#29751=CARTESIAN_POINT ( 'NONE',  ( 8.000000000000001776, 103.3437500040967763, 3.313708498984759387 ) ) ;
#29756=CARTESIAN_POINT ( 'NONE',  ( -2.977408999572650927, 97.25000000204839523, -7.188101187500001821 ) ) ;
#29775=EDGE_CURVE ( 'NONE', #31077, #25259, #35087, .T. ) ;
#29782=CARTESIAN_POINT ( 'NONE',  ( -7.999999999999998224, 102.7812500040967905, 3.313708498984766493 ) ) ;
#29784=EDGE_CURVE ( 'NONE', #31074, #67076, #42751, .T. ) ;
#29794=CARTESIAN_POINT ( 'NONE',  ( -7.188101187500001821, 97.06250000204838102, -2.977408999572650483 ) ) ;
#29800=VERTEX_POINT ( 'NONE', #6075 ) ;
#29812=CARTESIAN_POINT ( 'NONE',  ( 3.313708498984760720, 102.0312499999999858, -8.000000000000000000 ) ) ;
#29817=CARTESIAN_POINT ( 'NONE',  ( 5.082755093536325930, 2.531249997951610542, -5.082755093536325930 ) ) ;
#29820=CARTESIAN_POINT ( 'NONE',  ( 1.320432766682874540E-15, 118.9062500020483810, 7.188101187500000044 ) ) ;
#29824=CARTESIAN_POINT ( 'NONE',  ( -5.656854249492381470, 3.937500000000000888, 5.656854249492379694 ) ) ;
#29833=ORIENTED_EDGE ( 'NONE', *, *, #7216, .F. ) ;
#29841=CARTESIAN_POINT ( 'NONE',  ( 5.082755093536326818, 108.2187500020483810, 5.082755093536325042 ) ) ;
#29848=CARTESIAN_POINT ( 'NONE',  ( 7.188101187500001821, 113.3750000020483810, -2.977408999572651371 ) ) ;
#29851=EDGE_LOOP ( 'NONE', ( #46438, #5908, #15740, #11418 ) ) ;
#29860=CARTESIAN_POINT ( 'NONE',  ( 8.000000000000000000, 15.09375000000000711, -3.313708498984761164 ) ) ;
#29863=ORIENTED_EDGE ( 'NONE', *, *, #58835, .F. ) ;
#29872=CARTESIAN_POINT ( 'NONE',  ( -3.313708498984760720, 4.968750000000000888, -8.000000000000000000 ) ) ;
#29874=CARTESIAN_POINT ( 'NONE',  ( 7.188101187500000044, 3.468749997951610542, 0.000000000000000000 ) ) ;
#29875=CARTESIAN_POINT ( 'NONE',  ( 3.313708498984765161, 119.6562500040968047, 7.999999999999998224 ) ) ;
#29878=CARTESIAN_POINT ( 'NONE',  ( 4.898587196589412829E-16, 6.375000000000000888, -8.000000000000000000 ) ) ;
#29891=VERTEX_POINT ( 'NONE', #48637 ) ;
#29899=CARTESIAN_POINT ( 'NONE',  ( -3.313708498984762052, 117.2187500000000000, -8.000000000000000000 ) ) ;
#29902=ORIENTED_EDGE ( 'NONE', *, *, #23555, .T. ) ;
#29905=CARTESIAN_POINT ( 'NONE',  ( 3.313708498984762052, 13.59374999590322375, -8.000000000000000000 ) ) ;
#29925=CARTESIAN_POINT ( 'NONE',  ( 7.188101187500000044, 123.4062500020483810, -8.802885111219163269E-16 ) ) ;
#29929=AXIS2_PLACEMENT_3D ( 'NONE', #42239, #30193, #53210 ) ;
#29931=CARTESIAN_POINT ( 'NONE',  ( 2.977408999572650039, 96.68750000204836681, -7.188101187500001821 ) ) ;
#29951=CARTESIAN_POINT ( 'NONE',  ( 0.000000000000000000, 125.0000000000000000, 0.000000000000000000 ) ) ;
#29954=CARTESIAN_POINT ( 'NONE',  ( 1.469576158976823947E-15, 113.3750000000000000, 8.000000000000000000 ) ) ;
#29957=EDGE_LOOP ( 'NONE', ( #9845, #45492, #28447, #68674 ) ) ;
#29961=CARTESIAN_POINT ( 'NONE',  ( -2.977408999572654480, 17.99999999795161898, 7.188101187499999156 ) ) ;
#29964=CARTESIAN_POINT ( 'NONE',  ( -2.977408999572650039, 10.31249999795161010, -7.188101187500001821 ) ) ;
#29975=CARTESIAN_POINT ( 'NONE',  ( -2.977408999572650927, 117.8750000020483810, -7.188101187500001821 ) ) ;
#29979=CARTESIAN_POINT ( 'NONE',  ( 7.188101187499999156, 25.87499999795161543, 2.977408999572654924 ) ) ;
#29982=CARTESIAN_POINT ( 'NONE',  ( 7.999999999999998224, 13.40625000000000178, 3.313708498984766049 ) ) ;
#29986=CARTESIAN_POINT ( 'NONE',  ( 7.188101187500001821, 98.37500000204840944, -2.977408999572651371 ) ) ;
#29996=CARTESIAN_POINT ( 'NONE',  ( -8.000000000000000000, 14.15625000000000178, -3.313708498984762496 ) ) ;
#30004=CARTESIAN_POINT ( 'NONE',  ( -4.898587196589412829E-16, 91.62499999999998579, -8.000000000000000000 ) ) ;
#30010=CARTESIAN_POINT ( 'NONE',  ( 8.000000000000000000, 110.8437500000000000, -3.313708498984762496 ) ) ;
#30019=CARTESIAN_POINT ( 'NONE',  ( -2.977408999572650927, 113.3750000020483810, -7.188101187500001821 ) ) ;
#30023=CARTESIAN_POINT ( 'NONE',  ( -5.656854249492381470, 24.74999999590322375, 5.656854249492379694 ) ) ;
#30042=VERTEX_POINT ( 'NONE', #12655 ) ;
#30049=CARTESIAN_POINT ( 'NONE',  ( 2.977408999572650927, 13.12499999795161187, -7.188101187500000933 ) ) ;
#30055=CYLINDRICAL_SURFACE ( 'NONE', #39071, 8.000000000000000000 ) ;
#30066=CARTESIAN_POINT ( 'NONE',  ( -5.656854249492379694, 21.56250000000000355, -5.656854249492380582 ) ) ;
#30073=ORIENTED_EDGE ( 'NONE', *, *, #59311, .F. ) ;
#30074=CARTESIAN_POINT ( 'NONE',  ( -7.188101187500000933, 7.124999997951611874, -2.977408999572651371 ) ) ;
#30077=CARTESIAN_POINT ( 'NONE',  ( 7.188101187500000044, 120.7812500020483810, -8.802885111219163269E-16 ) ) ;
#30087=ORIENTED_EDGE ( 'NONE', *, *, #73944, .T. ) ;
#30088=CARTESIAN_POINT ( 'NONE',  ( 5.656854249492381470, 104.7500000040967905, 5.656854249492379694 ) ) ;
#30094=CARTESIAN_POINT ( 'NONE',  ( -8.000000000000000000, 2.250000000000000444, -9.797174393178825657E-16 ) ) ;
#30095=( BOUNDED_CURVE ( )  B_SPLINE_CURVE ( 2, ( #15807, #50151, #62958, #34314, #50516, #44128, #67138, #51266, #44871 ),
 .UNSPECIFIED., .F., .F. ) 
 B_SPLINE_CURVE_WITH_KNOTS ( ( 3, 2, 2, 2, 3 ),
 ( 0.7916666666666667407, 0.7986111111111111605, 0.8055555555555555802, 0.8124999999999998890, 0.8194444444444443088 ),
 .UNSPECIFIED. ) 
 CURVE ( )  GEOMETRIC_REPRESENTATION_ITEM ( )  RATIONAL_B_SPLINE_CURVE ( ( 0.9999999999999987788, 0.9238795325112879597, 1.000000000000000000, 0.9238795325112867385, 1.000000000000000000, 0.9238795325112867385, 1.000000000000000000, 0.9238795325112879597, 0.9999999999999987788 ) ) 
 REPRESENTATION_ITEM ( '' )  );
#30105=CARTESIAN_POINT ( 'NONE',  ( 2.977408999572651815, 23.06249999795161187, 7.188101187500000933 ) ) ;
#30107=CARTESIAN_POINT ( 'NONE',  ( 2.977408999572650039, 95.56250000204838102, -7.188101187500000933 ) ) ;
#30128=( BOUNDED_CURVE ( )  B_SPLINE_CURVE ( 2, ( #888, #28420, #23873, #68043, #16334, #39372, #62368, #10698, #33731 ),
 .UNSPECIFIED., .F., .F. ) 
 B_SPLINE_CURVE_WITH_KNOTS ( ( 3, 2, 2, 2, 3 ),
 ( 0.4305555555555555802, 0.4375000000000000000, 0.4444444444444444753, 0.4513888888888889506, 0.4583333333333334259 ),
 .UNSPECIFIED. ) 
 CURVE ( )  GEOMETRIC_REPRESENTATION_ITEM ( )  RATIONAL_B_SPLINE_CURVE ( ( 1.000000000000000000, 0.9238795325112867385, 1.000000000000000000, 0.9238795325112867385, 1.000000000000000000, 0.9238795325112867385, 1.000000000000000000, 0.9238795325112855172, 1.000000000000001110 ) ) 
 REPRESENTATION_ITEM ( '' )  );
#30130=CARTESIAN_POINT ( 'NONE',  ( -7.188101187500000044, 97.53125000204838102, 0.000000000000000000 ) ) ;
#30139=CARTESIAN_POINT ( 'NONE',  ( 0.000000000000000000, 125.0000000000000000, 8.000000000000000000 ) ) ;
#30151=CARTESIAN_POINT ( 'NONE',  ( 3.313708498984765161, 101.6562500040968047, 7.999999999999998224 ) ) ;
#30159=CARTESIAN_POINT ( 'NONE',  ( 7.188101187500000044, 97.90625000204838102, -8.802885111219163269E-16 ) ) ;
#30184=CARTESIAN_POINT ( 'NONE',  ( 4.401442555609581635E-16, 7.218749997951610986, -7.188101187500000044 ) ) ;
#30187=CARTESIAN_POINT ( 'NONE',  ( 1.320432766682874540E-15, 117.4062500020483810, 7.188101187500000044 ) ) ;
#30193=DIRECTION ( 'NONE',  ( -0.000000000000000000, 1.000000000000000000, -0.000000000000000000 ) ) ;
#30206=CARTESIAN_POINT ( 'NONE',  ( -4.401442555609581635E-16, 102.7812500020483810, -7.188101187500000044 ) ) ;
#30212=CARTESIAN_POINT ( 'NONE',  ( -7.188101187499999156, 117.1250000020483952, 2.977408999572654924 ) ) ;
#30221=CARTESIAN_POINT ( 'NONE',  ( -3.313708498984815343, 108.2187499999999858, -7.999999999999944933 ) ) ;
#30234=( BOUNDED_CURVE ( )  B_SPLINE_CURVE ( 2, ( #44371, #34183, #35298, #51140, #57185, #6251, #29254, #46225, #5876 ),
 .UNSPECIFIED., .F., .F. ) 
 B_SPLINE_CURVE_WITH_KNOTS ( ( 3, 2, 2, 2, 3 ),
 ( 0.7812500000000001110, 0.7864583333333334814, 0.7916666666666667407, 0.7968750000000001110, 0.8020833333333334814 ),
 .UNSPECIFIED. ) 
 CURVE ( )  GEOMETRIC_REPRESENTATION_ITEM ( )  RATIONAL_B_SPLINE_CURVE ( ( 0.9999999999999983347, 0.9238795325112884038, 1.000000000000000000, 0.9238795325112867385, 1.000000000000000000, 0.9238795325112867385, 1.000000000000000000, 0.9238795325112850731, 1.000000000000001554 ) ) 
 REPRESENTATION_ITEM ( '' )  );
#30236=ORIENTED_EDGE ( 'NONE', *, *, #10370, .T. ) ;
#30238=CARTESIAN_POINT ( 'NONE',  ( 8.000000000000000000, 6.000000000000000888, 0.000000000000000000 ) ) ;
#30240=CARTESIAN_POINT ( 'NONE',  ( -7.188101187500001821, 1.124999997951610098, -2.977408999572651371 ) ) ;
#30241=CARTESIAN_POINT ( 'NONE',  ( -5.656854249492380582, 123.5000000040967905, -5.656854249492380582 ) ) ;
#30243=CYLINDRICAL_SURFACE ( 'NONE', #10180, 8.000000000000000000 ) ;
#30254=CYLINDRICAL_SURFACE ( 'NONE', #23750, 8.000000000000000000 ) ;
#30270=CARTESIAN_POINT ( 'NONE',  ( -3.313708498984762496, 119.2812499999999858, 7.999999999999998224 ) ) ;
#30274=CARTESIAN_POINT ( 'NONE',  ( -8.000000000000000000, 17.06249999590322375, -9.797174393178825657E-16 ) ) ;
#30295=CARTESIAN_POINT ( 'NONE',  ( -5.082755093536325930, 123.9687500020483952, -5.082755093536325930 ) ) ;
#30300=CARTESIAN_POINT ( 'NONE',  ( 1.320432766682874540E-15, 99.03125000204838102, 7.188101187500000044 ) ) ;
#30320=CARTESIAN_POINT ( 'NONE',  ( 7.188101187500000044, 27.84374999795161543, 0.000000000000000000 ) ) ;
#30327=CARTESIAN_POINT ( 'NONE',  ( 5.082755093536325930, 14.15624999795161187, -5.082755093536325930 ) ) ;
#30331=CARTESIAN_POINT ( 'NONE',  ( -7.188101187500001821, 13.49999999795161187, -2.977408999572651371 ) ) ;
#30344=CARTESIAN_POINT ( 'NONE',  ( 7.188101187500000044, 115.9062500020483810, -8.802885111219163269E-16 ) ) ;
#30349=CARTESIAN_POINT ( 'NONE',  ( 7.188101187499999156, 21.37499999795161543, 2.977408999572654924 ) ) ;
#30355=CARTESIAN_POINT ( 'NONE',  ( 7.188101187500001821, 99.87500000204838102, -2.977408999572651371 ) ) ;
#30357=CARTESIAN_POINT ( 'NONE',  ( -3.313708498984708317, 89.46875000409679046, 8.000000000000053291 ) ) ;
#30368=CARTESIAN_POINT ( 'NONE',  ( 4.898587196589412829E-16, 24.18749999590322375, -8.000000000000000000 ) ) ;
#30371=FACE_OUTER_BOUND ( 'NONE', #2527, .T. ) ;
#30381=CARTESIAN_POINT ( 'NONE',  ( 0.000000000000000000, 125.0000000000000000, 8.000000000000000000 ) ) ;
#30387=CARTESIAN_POINT ( 'NONE',  ( 7.188101187500001821, 117.5000000020483810, -2.977408999572651371 ) ) ;
#30392=CARTESIAN_POINT ( 'NONE',  ( -3.313708498984719864, 25.96875000000000355, -8.000000000000040856 ) ) ;
#30397=CIRCLE ( 'NONE', #66511, 8.000000000000000000 ) ;
#30409=ORIENTED_EDGE ( 'NONE', *, *, #35372, .F. ) ;
#30415=CARTESIAN_POINT ( 'NONE',  ( 5.082755093536325930, 10.03124999795161187, -5.082755093536325930 ) ) ;
#30424=CARTESIAN_POINT ( 'NONE',  ( -4.898587196589412829E-16, 97.81250000409677625, -8.000000000000000000 ) ) ;
#30433=CARTESIAN_POINT ( 'NONE',  ( 8.000000000000000000, 25.50000000000000355, 0.000000000000000000 ) ) ;
#30443=ORIENTED_EDGE ( 'NONE', *, *, #69176, .F. ) ;
#30445=CARTESIAN_POINT ( 'NONE',  ( -7.188101187500002709, 7.312499997951610986, 2.977408999572649151 ) ) ;
#30449=CARTESIAN_POINT ( 'NONE',  ( 7.188101187500002709, 120.6875000020483952, 2.977408999572649151 ) ) ;
#30473=CARTESIAN_POINT ( 'NONE',  ( -7.188101187500001821, 22.49999999795161543, -2.977408999572651371 ) ) ;
#30475=CARTESIAN_POINT ( 'NONE',  ( 1.320432766682874540E-15, 93.40625000204838102, 7.188101187500000044 ) ) ;
#30496=CARTESIAN_POINT ( 'NONE',  ( -5.082755093536325930, 91.34375000204838102, -5.082755093536325930 ) ) ;
#30519=CARTESIAN_POINT ( 'NONE',  ( -3.313708498984762052, 100.9062500040967905, -8.000000000000000000 ) ) ;
#30520=ADVANCED_FACE ( 'NONE', ( #22770 ), #5075, .T. ) ;
#30529=CARTESIAN_POINT ( 'NONE',  ( 1.320432766682874540E-15, 100.5312500020483810, 7.188101187500000044 ) ) ;
#30532=CARTESIAN_POINT ( 'NONE',  ( -3.313708498984599515, 91.90625000409679046, -8.000000000000163425 ) ) ;
#30555=CARTESIAN_POINT ( 'NONE',  ( 2.977408999572650927, 2.624999997951610986, -7.188101187500001821 ) ) ;
#30557=DIRECTION ( 'NONE',  ( 0.000000000000000000, 0.000000000000000000, 1.000000000000000000 ) ) ;
#30558=CARTESIAN_POINT ( 'NONE',  ( 5.082755093536326818, 114.5937500020483810, 5.082755093536325042 ) ) ;
#30575=CARTESIAN_POINT ( 'NONE',  ( 2.977408999572654480, 106.6250000020483810, 7.188101187499999156 ) ) ;
#30580=CARTESIAN_POINT ( 'NONE',  ( -7.188101187500000044, 111.0312500020483810, 0.000000000000000000 ) ) ;
#30583=( BOUNDED_CURVE ( )  B_SPLINE_CURVE ( 2, ( #40631, #11584, #18732, #11962, #24385, #74587, #34993, #34619, #22901 ),
 .UNSPECIFIED., .F., .F. ) 
 B_SPLINE_CURVE_WITH_KNOTS ( ( 3, 2, 2, 2, 3 ),
 ( 0.01041666666666667303, 0.01562500000000001041, 0.02083333333333334605, 0.02604166666666668517, 0.03125000000000002082 ),
 .UNSPECIFIED. ) 
 CURVE ( )  GEOMETRIC_REPRESENTATION_ITEM ( )  RATIONAL_B_SPLINE_CURVE ( ( 0.9999999999999998890, 0.9238795325112868495, 1.000000000000000000, 0.9238795325112867385, 1.000000000000000000, 0.9238795325112867385, 1.000000000000000000, 0.9238795325112864054, 1.000000000000000222 ) ) 
 REPRESENTATION_ITEM ( '' )  );
#30585=ORIENTED_EDGE ( 'NONE', *, *, #18477, .F. ) ;
#30604=VECTOR ( 'NONE', #21320, 1000.000000000000000 ) ;
#30605=CARTESIAN_POINT ( 'NONE',  ( 8.000000000000000000, 7.500000000000001776, 0.000000000000000000 ) ) ;
#30608=CARTESIAN_POINT ( 'NONE',  ( 2.977408999572651815, 4.687499997951610986, 7.188101187500000933 ) ) ;
#30609=CARTESIAN_POINT ( 'NONE',  ( 1.469576158976823947E-15, 122.5625000040967763, 8.000000000000000000 ) ) ;
#30611=CARTESIAN_POINT ( 'NONE',  ( 0.000000000000000000, 125.0000000000000000, 8.000000000000000000 ) ) ;
#30618=EDGE_CURVE ( 'NONE', #31653, #10862, #24991, .T. ) ;
#30628=CARTESIAN_POINT ( 'NONE',  ( 8.000000000000001776, 95.84375000409679046, 3.313708498984759387 ) ) ;
#30635=CARTESIAN_POINT ( 'NONE',  ( 8.000000000000000000, 116.8437500000000000, -3.313708498984762496 ) ) ;
#30640=CARTESIAN_POINT ( 'NONE',  ( 7.999999999999998224, 16.21874999590322020, 3.313708498984766493 ) ) ;
#30663=CARTESIAN_POINT ( 'NONE',  ( -2.977408999572650927, 120.8750000020483810, -7.188101187500000933 ) ) ;
#30664=CARTESIAN_POINT ( 'NONE',  ( 5.656854249492379694, 119.9375000000000000, -5.656854249492380582 ) ) ;
#30668=CARTESIAN_POINT ( 'NONE',  ( 7.188101187500000044, 99.40625000204838102, -8.802885111219163269E-16 ) ) ;
#30674=( BOUNDED_CURVE ( )  B_SPLINE_CURVE ( 2, ( #43559, #14880, #37920, #67333, #45063, #32644, #16365, #60917, #9240 ),
 .UNSPECIFIED., .F., .F. ) 
 B_SPLINE_CURVE_WITH_KNOTS ( ( 3, 2, 2, 2, 3 ),
 ( 0.6979166666666667407, 0.7031250000000001110, 0.7083333333333334814, 0.7135416666666667407, 0.7187500000000001110 ),
 .UNSPECIFIED. ) 
 CURVE ( )  GEOMETRIC_REPRESENTATION_ITEM ( )  RATIONAL_B_SPLINE_CURVE ( ( 0.9999999999999983347, 0.9238795325112884038, 1.000000000000000000, 0.9238795325112867385, 1.000000000000000000, 0.9238795325112867385, 1.000000000000000000, 0.9238795325112850731, 1.000000000000001554 ) ) 
 REPRESENTATION_ITEM ( '' )  );
#30678=CYLINDRICAL_SURFACE ( 'NONE', #23660, 8.000000000000000000 ) ;
#30696=CARTESIAN_POINT ( 'NONE',  ( -1.320432766682874540E-15, 13.59374999795161187, 7.188101187500000044 ) ) ;
#30699=CARTESIAN_POINT ( 'NONE',  ( 2.977408999572650927, 10.12499999795161187, -7.188101187500001821 ) ) ;
#30711=CARTESIAN_POINT ( 'NONE',  ( 7.188101187500000044, 117.4062500020483810, -8.802885111219163269E-16 ) ) ;
#30715=CARTESIAN_POINT ( 'NONE',  ( 4.401442555609581635E-16, 24.84374999795161543, -7.188101187500000044 ) ) ;
#30721=CARTESIAN_POINT ( 'NONE',  ( 5.082755093536325042, 101.4687500020483810, -5.082755093536325930 ) ) ;
#30729=CARTESIAN_POINT ( 'NONE',  ( -5.656854249492381470, 14.43750000000000178, 5.656854249492379694 ) ) ;
#30746=CARTESIAN_POINT ( 'NONE',  ( 3.999985685286083115, 88.68677412680156635, -6.928211494859723985 ) ) ;
#30750=CARTESIAN_POINT ( 'NONE',  ( -6.159719417591432489, 124.7163422235197885, -4.786194028158367253 ) ) ;
#30752=CARTESIAN_POINT ( 'NONE',  ( -2.977408999572650927, 114.8750000020483810, -7.188101187500001821 ) ) ;
#30760=CARTESIAN_POINT ( 'NONE',  ( 3.313708498984819339, 108.9687500000000000, 7.999999999999943157 ) ) ;
#30763=ORIENTED_EDGE ( 'NONE', *, *, #63112, .T. ) ;
#30767=PLANE ( 'NONE',  #4046 ) ;
#30774=( BOUNDED_CURVE ( )  B_SPLINE_CURVE ( 2, ( #33669, #11753, #5726, #16274, #73638, #57044, #58171, #11382, #34790 ),
 .UNSPECIFIED., .F., .F. ) 
 B_SPLINE_CURVE_WITH_KNOTS ( ( 3, 2, 2, 2, 3 ),
 ( 0.4583333333333334259, 0.4652777777777779011, 0.4722222222222222654, 0.4791666666666667407, 0.4861111111111111605 ),
 .UNSPECIFIED. ) 
 CURVE ( )  GEOMETRIC_REPRESENTATION_ITEM ( )  RATIONAL_B_SPLINE_CURVE ( ( 0.9999999999999987788, 0.9238795325112879597, 1.000000000000000000, 0.9238795325112867385, 1.000000000000000000, 0.9238795325112867385, 1.000000000000000000, 0.9238795325112861834, 1.000000000000000666 ) ) 
 REPRESENTATION_ITEM ( '' )  );
#30780=CARTESIAN_POINT ( 'NONE',  ( 2.977408999572650927, 10.12499999795161187, -7.188101187500000933 ) ) ;
#30790=CARTESIAN_POINT ( 'NONE',  ( 1.469576158976823947E-15, 123.8750000000000000, 8.000000000000000000 ) ) ;
#30797=CARTESIAN_POINT ( 'NONE',  ( -3.313708498984765161, 23.53125000000000355, 7.999999999999998224 ) ) ;
#30807=CARTESIAN_POINT ( 'NONE',  ( 4.401442555609581635E-16, 2.343749997951610098, -7.188101187500000044 ) ) ;
#30809=CARTESIAN_POINT ( 'NONE',  ( -4.401442555609581635E-16, 119.6562500020483810, -7.188101187500000044 ) ) ;
#30818=CARTESIAN_POINT ( 'NONE',  ( 3.313708498984761608, 3.281250000000001332, -8.000000000000000000 ) ) ;
#30821=CARTESIAN_POINT ( 'NONE',  ( -1.469576158976823947E-15, 11.43749999590322197, 8.000000000000000000 ) ) ;
#30837=CARTESIAN_POINT ( 'NONE',  ( 7.188101187500000933, 92.37500000204838102, -2.977408999572651371 ) ) ;
#30849=CYLINDRICAL_SURFACE ( 'NONE', #14557, 8.000000000000000000 ) ;
#30852=VERTEX_POINT ( 'NONE', #55559 ) ;
#30860=ADVANCED_FACE ( 'NONE', ( #33299 ), #67615, .T. ) ;
#30884=( BOUNDED_CURVE ( )  B_SPLINE_CURVE ( 2, ( #17967, #62865, #29297, #5915, #69281, #29660, #70396, #272, #52307 ),
 .UNSPECIFIED., .F., .F. ) 
 B_SPLINE_CURVE_WITH_KNOTS ( ( 3, 2, 2, 2, 3 ),
 ( 0.9305555555555554692, 0.9374999999999998890, 0.9444444444444443088, 0.9513888888888887285, 0.9583333333333332593 ),
 .UNSPECIFIED. ) 
 CURVE ( )  GEOMETRIC_REPRESENTATION_ITEM ( )  RATIONAL_B_SPLINE_CURVE ( ( 1.000000000000001110, 0.9238795325112855172, 1.000000000000000000, 0.9238795325112867385, 1.000000000000000000, 0.9238795325112867385, 1.000000000000000000, 0.9238795325112879597, 0.9999999999999987788 ) ) 
 REPRESENTATION_ITEM ( '' )  );
#30886=CARTESIAN_POINT ( 'NONE',  ( 8.000000000000000000, 96.03125000409677625, -3.313708498984762496 ) ) ;
#30895=CARTESIAN_POINT ( 'NONE',  ( -7.188101187500000044, 100.1562500020483810, 0.000000000000000000 ) ) ;
#30897=CARTESIAN_POINT ( 'NONE',  ( 8.000000000000001776, 119.8437500040967620, 3.313708498984759387 ) ) ;
#30916=CARTESIAN_POINT ( 'NONE',  ( 7.188101187500001821, 11.43749999795161010, -2.977408999572650483 ) ) ;
#30919=CARTESIAN_POINT ( 'NONE',  ( -7.188101187500000933, 112.4375000020483810, -2.977408999572650483 ) ) ;
#30930=ORIENTED_EDGE ( 'NONE', *, *, #3515, .F. ) ;
#30938=DIRECTION ( 'NONE',  ( -0.8660254037844391517, 0.4999999999999990563, -0.000000000000000000 ) ) ;
#30940=CARTESIAN_POINT ( 'NONE',  ( -7.188101187499999156, 104.7500000020483810, 2.977408999572654924 ) ) ;
#30945=CARTESIAN_POINT ( 'NONE',  ( 7.188101187500002709, 107.1875000020483810, 2.977408999572649151 ) ) ;
#30948=ORIENTED_EDGE ( 'NONE', *, *, #69039, .T. ) ;
#30964=CARTESIAN_POINT ( 'NONE',  ( -1.469576158976823947E-15, 20.43749999590322375, 8.000000000000000000 ) ) ;
#30969=VERTEX_POINT ( 'NONE', #28359 ) ;
#30971=CARTESIAN_POINT ( 'NONE',  ( -8.000000000000000000, 9.750000000000001776, -9.797174393178825657E-16 ) ) ;
#30972=CARTESIAN_POINT ( 'NONE',  ( -8.000000000000000000, 106.9062500000000000, -3.313708498984761164 ) ) ;
#30973=CARTESIAN_POINT ( 'NONE',  ( 2.977408999572651815, 27.56249999795161187, 7.188101187500000933 ) ) ;
#30974=CARTESIAN_POINT ( 'NONE',  ( -8.000000000000000000, 116.1875000040967763, 0.000000000000000000 ) ) ;
#30999=CARTESIAN_POINT ( 'NONE',  ( -3.313708498984762052, 109.7187500000000000, -8.000000000000000000 ) ) ;
#31003=CARTESIAN_POINT ( 'NONE',  ( 8.000000000000000000, 13.31249999590322375, 0.000000000000000000 ) ) ;
#31016=CYLINDRICAL_SURFACE ( 'NONE', #62346, 8.000000000000000000 ) ;
#31032=CARTESIAN_POINT ( 'NONE',  ( -5.082755093536324154, 92.84375000204838102, 5.082755093536326818 ) ) ;
#31045=ORIENTED_EDGE ( 'NONE', *, *, #7668, .T. ) ;
#31056=CARTESIAN_POINT ( 'NONE',  ( 5.082755093536325930, 17.15624999795161543, -5.082755093536325930 ) ) ;
#31059=CARTESIAN_POINT ( 'NONE',  ( -1.320432766682874540E-15, 10.96874999795161187, 7.188101187500000044 ) ) ;
#31066=VERTEX_POINT ( 'NONE', #44026 ) ;
#31071=CARTESIAN_POINT ( 'NONE',  ( -4.401442555609581635E-16, 113.2812500020483952, -7.188101187500000044 ) ) ;
#31074=VERTEX_POINT ( 'NONE', #21372 ) ;
#31076=CARTESIAN_POINT ( 'NONE',  ( 5.082755093536324154, 21.28124999795161543, 5.082755093536326818 ) ) ;
#31077=VERTEX_POINT ( 'NONE', #55730 ) ;
#31082=CARTESIAN_POINT ( 'NONE',  ( -7.188101187500001821, 94.43750000204838102, -2.977408999572650483 ) ) ;
#31105=EDGE_LOOP ( 'NONE', ( #32851, #7076, #30443, #29833 ) ) ;
#31115=ADVANCED_FACE ( 'NONE', ( #26661 ), #14212, .T. ) ;
#31117=CARTESIAN_POINT ( 'NONE',  ( -5.082755093536325930, 107.4687500020483810, -5.082755093536325930 ) ) ;
#31124=DIRECTION ( 'NONE',  ( 0.000000000000000000, -1.000000000000000000, 0.000000000000000000 ) ) ;
#31144=CARTESIAN_POINT ( 'NONE',  ( 5.082755093536324154, 12.65624999795161187, 5.082755093536326818 ) ) ;
#31154=CARTESIAN_POINT ( 'NONE',  ( -5.656854249492378806, 93.87500000409677625, 5.656854249492381470 ) ) ;
#31158=B_SPLINE_CURVE_WITH_KNOTS ( 'NONE', 3,
 ( #67890, #26778, #61860, #33959, #56587, #22225, #21855, #50531, #44141, #67153 ),
 .UNSPECIFIED., .F., .F.,
 ( 4, 2, 2, 2, 4 ),
 ( 0.01226735695020646048, 0.01330218961086247764, 0.01433702227151849307, 0.01537185493217450849, 0.01640668759283052391 ),
 .UNSPECIFIED. ) ;
#31165=CARTESIAN_POINT ( 'NONE',  ( -8.000000000000000000, 23.25000000000000355, -9.797174393178825657E-16 ) ) ;
#31167=ORIENTED_EDGE ( 'NONE', *, *, #36266, .F. ) ;
#31176=CARTESIAN_POINT ( 'NONE',  ( 2.977408999572652260, 4.687499997951610986, 7.188101187500000044 ) ) ;
#31178=ADVANCED_FACE ( 'NONE', ( #9323 ), #27787, .T. ) ;
#31180=CARTESIAN_POINT ( 'NONE',  ( -2.977408999572651815, 115.8125000020484094, 7.188101187500000933 ) ) ;
#31186=VERTEX_POINT ( 'NONE', #19531 ) ;
#31191=EDGE_CURVE ( 'NONE', #54742, #65546, #43202, .T. ) ;
#31193=CARTESIAN_POINT ( 'NONE',  ( 7.999999999999998224, 23.90625000000000000, 3.313708498984766049 ) ) ;
#31194=CARTESIAN_POINT ( 'NONE',  ( -7.999999999999998224, 102.5937499999999858, 3.313708498984766493 ) ) ;
#31201=VERTEX_POINT ( 'NONE', #39411 ) ;
#31202=DIRECTION ( 'NONE',  ( -0.000000000000000000, 1.000000000000000000, -0.000000000000000000 ) ) ;
#31208=LINE ( 'NONE', #37624, #71338 ) ;
#31210=CARTESIAN_POINT ( 'NONE',  ( 5.082755093536326818, 90.59375000204839523, 5.082755093536325042 ) ) ;
#31234=CARTESIAN_POINT ( 'NONE',  ( -2.977408999572650927, 92.75000000204839523, -7.188101187500001821 ) ) ;
#31249=VERTEX_POINT ( 'NONE', #62045 ) ;
#31253=ORIENTED_EDGE ( 'NONE', *, *, #3024, .F. ) ;
#31254=CARTESIAN_POINT ( 'NONE',  ( -8.000000000000000000, 99.68750000409677625, 0.000000000000000000 ) ) ;
#31264=CARTESIAN_POINT ( 'NONE',  ( 5.082755093536326818, 100.7187500020483810, 5.082755093536325042 ) ) ;
#31265=EDGE_CURVE ( 'NONE', #30042, #19911, #50929, .T. ) ;
#31285=CARTESIAN_POINT ( 'NONE',  ( -8.000000000000000000, 4.968749995903220196, -3.313708498984762496 ) ) ;
#31287=CARTESIAN_POINT ( 'NONE',  ( 7.188101187499999156, 9.749999997951611874, 2.977408999572654924 ) ) ;
#31290=CARTESIAN_POINT ( 'NONE',  ( 2.977408999572650039, 110.5625000020483810, -7.188101187500000933 ) ) ;
#31310=CARTESIAN_POINT ( 'NONE',  ( 7.188101187500000933, 105.5000000020483810, -2.977408999572651371 ) ) ;
#31316=CARTESIAN_POINT ( 'NONE',  ( 5.082755093536325042, 105.9687500020483952, -5.082755093536325930 ) ) ;
#31333=CARTESIAN_POINT ( 'NONE',  ( 8.000000000000000000, 1.312499995903220196, 0.000000000000000000 ) ) ;
#31341=CARTESIAN_POINT ( 'NONE',  ( -5.082755093536325042, 4.031249997951610986, -5.082755093536325930 ) ) ;
#31342=CARTESIAN_POINT ( 'NONE',  ( -4.898587196589412829E-16, 117.3125000040967763, -8.000000000000000000 ) ) ;
#31348=LINE ( 'NONE', #30611, #16288 ) ;
#31373=AXIS2_PLACEMENT_3D ( 'NONE', #12213, #63903, #48018 ) ;
#31374=CARTESIAN_POINT ( 'NONE',  ( 5.656854249492381470, 110.5625000000000000, 5.656854249492379694 ) ) ;
#31376=EDGE_CURVE ( 'NONE', #43835, #6290, #74051, .T. ) ;
#31379=CARTESIAN_POINT ( 'NONE',  ( -8.000000000000001776, 18.65624999590322020, 3.313708498984759387 ) ) ;
#31398=LINE ( 'NONE', #49113, #28691 ) ;
#31406=CARTESIAN_POINT ( 'NONE',  ( 5.082755093536325042, 92.09375000204838102, -5.082755093536325930 ) ) ;
#31436=ADVANCED_FACE ( 'NONE', ( #74110 ), #51843, .T. ) ;
#31437=CARTESIAN_POINT ( 'NONE',  ( 7.188101187499999156, 19.87499999795161543, 2.977408999572654924 ) ) ;
#31440=CARTESIAN_POINT ( 'NONE',  ( 1.469576158976823947E-15, 118.0625000040967763, 8.000000000000000000 ) ) ;
#31441=CARTESIAN_POINT ( 'NONE',  ( -7.188101187500001821, 10.49999999795161010, -2.977408999572651371 ) ) ;
#31445=DIRECTION ( 'NONE',  ( -0.000000000000000000, 1.000000000000000000, -0.000000000000000000 ) ) ;
#31449=ADVANCED_FACE ( 'NONE', ( #23909 ), #57894, .T. ) ;
#31455=CARTESIAN_POINT ( 'NONE',  ( 7.188101187500000044, 112.9062500020483952, -8.802885111219163269E-16 ) ) ;
#31458=EDGE_LOOP ( 'NONE', ( #55232, #11667, #1682, #21969 ) ) ;
#31459=CARTESIAN_POINT ( 'NONE',  ( 5.082755093536325930, 21.65624999795161543, -5.082755093536325930 ) ) ;
#31467=CARTESIAN_POINT ( 'NONE',  ( -5.082755093536324154, 91.71875000204838102, 5.082755093536326818 ) ) ;
#31485=CARTESIAN_POINT ( 'NONE',  ( 1.469576158976823947E-15, 117.8750000000000000, 8.000000000000000000 ) ) ;
#31494=CARTESIAN_POINT ( 'NONE',  ( 1.469576158976823947E-15, 116.3750000000000000, 8.000000000000000000 ) ) ;
#31498=CARTESIAN_POINT ( 'NONE',  ( 7.188101187500000044, 106.9062500020483810, -8.802885111219163269E-16 ) ) ;
#31518=CARTESIAN_POINT ( 'NONE',  ( -4.898587196589412829E-16, 91.62499999999998579, -8.000000000000000000 ) ) ;
#31524=CARTESIAN_POINT ( 'NONE',  ( 7.188101187500000933, 14.43749999795161365, -2.977408999572650483 ) ) ;
#31534=CARTESIAN_POINT ( 'NONE',  ( -1.320432766682874540E-15, 6.093749997951610986, 7.188101187500000044 ) ) ;
#31542=CARTESIAN_POINT ( 'NONE',  ( 5.656854249492378806, 20.81250000000000355, 5.656854249492381470 ) ) ;
#31551=CARTESIAN_POINT ( 'NONE',  ( 7.188101187500000044, 3.468749997951610542, 0.000000000000000000 ) ) ;
#31555=CARTESIAN_POINT ( 'NONE',  ( -5.082755093536325930, 113.8437500020483810, -5.082755093536325930 ) ) ;
#31570=CARTESIAN_POINT ( 'NONE',  ( 3.313708498984760720, 96.03125000000000000, -8.000000000000000000 ) ) ;
#31587=CARTESIAN_POINT ( 'NONE',  ( 7.188101187500000044, 93.78125000204836681, -8.802885111219163269E-16 ) ) ;
#31600=ORIENTED_EDGE ( 'NONE', *, *, #73577, .T. ) ;
#31622=DIRECTION ( 'NONE',  ( -0.000000000000000000, 1.000000000000000000, -0.000000000000000000 ) ) ;
#31633=AXIS2_PLACEMENT_3D ( 'NONE', #33870, #16474, #73832 ) ;
#31634=CARTESIAN_POINT ( 'NONE',  ( 5.656854249492381470, 95.75000000409677625, 5.656854249492379694 ) ) ;
#31644=CARTESIAN_POINT ( 'NONE',  ( 1.320432766682874540E-15, 91.53125000204836681, 7.188101187500000044 ) ) ;
#31651=CARTESIAN_POINT ( 'NONE',  ( -8.000000000000000000, 101.1875000040967763, 0.000000000000000000 ) ) ;
#31653=VERTEX_POINT ( 'NONE', #66871 ) ;
#31668=CARTESIAN_POINT ( 'NONE',  ( 8.000000000000000000, 2.812499995903220640, 0.000000000000000000 ) ) ;
#31670=CARTESIAN_POINT ( 'NONE',  ( -5.082755093536326818, 12.28124999795161187, 5.082755093536325042 ) ) ;
#31673=CARTESIAN_POINT ( 'NONE',  ( 7.188101187500000044, 110.2812500020483810, -8.802885111219163269E-16 ) ) ;
#31691=CARTESIAN_POINT ( 'NONE',  ( 1.320432766682874540E-15, 100.5312500020483810, 7.188101187500000044 ) ) ;
#31697=CARTESIAN_POINT ( 'NONE',  ( -2.977408999572651815, 106.8125000020484094, 7.188101187500000933 ) ) ;
#31715=PLANE ( 'NONE',  #34135 ) ;
#31724=CARTESIAN_POINT ( 'NONE',  ( 7.188101187499999156, 6.374999997951610986, 2.977408999572654924 ) ) ;
#31725=CARTESIAN_POINT ( 'NONE',  ( -3.313708498984762052, 117.4062500040967905, -8.000000000000000000 ) ) ;
#31737=( NAMED_UNIT ( * ) PLANE_ANGLE_UNIT ( ) SI_UNIT ( $, .RADIAN. ) );
#31745=CARTESIAN_POINT ( 'NONE',  ( -1.469576158976823947E-15, 26.43749999590322375, 8.000000000000000000 ) ) ;
#31749=CARTESIAN_POINT ( 'NONE',  ( 8.000000000000000000, 104.8437500000000000, -3.313708498984762496 ) ) ;
#31751=CARTESIAN_POINT ( 'NONE',  ( -5.656854249492380582, 109.8125000000000000, -5.656854249492380582 ) ) ;
#31755=CARTESIAN_POINT ( 'NONE',  ( 7.999999999999998224, 19.21874999590322375, 3.313708498984766493 ) ) ;
#31779=CARTESIAN_POINT ( 'NONE',  ( -7.188101187499999156, 119.7500000020483810, 2.977408999572654924 ) ) ;
#31786=CARTESIAN_POINT ( 'NONE',  ( -7.188101187499999156, 91.25000000204838102, 2.977408999572654924 ) ) ;
#31797=VECTOR ( 'NONE', #13520, 1000.000000000000000 ) ;
#31815=CARTESIAN_POINT ( 'NONE',  ( -2.977408999572654480, 19.49999999795161898, 7.188101187499999156 ) ) ;
#31818=CARTESIAN_POINT ( 'NONE',  ( 4.401442555609581635E-16, 16.21874999795161543, -7.188101187500000044 ) ) ;
#31825=VERTEX_POINT ( 'NONE', #9545 ) ;
#31829=CARTESIAN_POINT ( 'NONE',  ( 7.188101187500001821, 110.0000000020483668, -2.977408999572651371 ) ) ;
#31836=DIRECTION ( 'NONE',  ( -0.000000000000000000, 1.000000000000000000, -0.000000000000000000 ) ) ;
#31840=CARTESIAN_POINT ( 'NONE',  ( 2.977408999572650039, 95.56250000204838102, -7.188101187500001821 ) ) ;
#31845=CARTESIAN_POINT ( 'NONE',  ( -1.469576158976823947E-15, 8.437499995903221972, 8.000000000000000000 ) ) ;
#31846=EDGE_CURVE ( 'NONE', #45576, #24477, #16304, .T. ) ;
#31867=( BOUNDED_CURVE ( )  B_SPLINE_CURVE ( 2, ( #59428, #7740, #42425, #65443, #36783, #34676, #28617, #8105, #5989 ),
 .UNSPECIFIED., .F., .F. ) 
 B_SPLINE_CURVE_WITH_KNOTS ( ( 3, 2, 2, 2, 3 ),
 ( 0.2361111111111111049, 0.2430555555555555802, 0.2500000000000000000, 0.2569444444444444753, 0.2638888888888889506 ),
 .UNSPECIFIED. ) 
 CURVE ( )  GEOMETRIC_REPRESENTATION_ITEM ( )  RATIONAL_B_SPLINE_CURVE ( ( 1.000000000000000000, 0.9238795325112867385, 1.000000000000000000, 0.9238795325112867385, 1.000000000000000000, 0.9238795325112867385, 1.000000000000000000, 0.9238795325112861834, 1.000000000000000666 ) ) 
 REPRESENTATION_ITEM ( '' )  );
#31870=CARTESIAN_POINT ( 'NONE',  ( -5.082755093536324154, 106.3437500020483810, 5.082755093536326818 ) ) ;
#31881=ORIENTED_EDGE ( 'NONE', *, *, #68591, .T. ) ;
#31886=PLANE ( 'NONE',  #34501 ) ;
#31898=CARTESIAN_POINT ( 'NONE',  ( 7.188101187500000044, 18.84374999795161187, 0.000000000000000000 ) ) ;
#31906=CARTESIAN_POINT ( 'NONE',  ( -5.656854249492380582, 98.00000000409677625, -5.656854249492380582 ) ) ;
#31907=CARTESIAN_POINT ( 'NONE',  ( -1.320432766682874540E-15, 4.593749997951610986, 7.188101187500000044 ) ) ;
#31925=CARTESIAN_POINT ( 'NONE',  ( -7.188101187500002709, 13.31249999795161187, 2.977408999572649151 ) ) ;
#31929=CARTESIAN_POINT ( 'NONE',  ( -5.082755093536324154, 112.7187500020483810, 5.082755093536326818 ) ) ;
#31943=CARTESIAN_POINT ( 'NONE',  ( 3.313708498984765161, 93.96874999999998579, 7.999999999999998224 ) ) ;
#31958=CARTESIAN_POINT ( 'NONE',  ( -4.401442555609581635E-16, 92.65625000204838102, -7.188101187500000044 ) ) ;
#31968=CARTESIAN_POINT ( 'NONE',  ( 2.977408999572650927, 17.24999999795162253, -7.188101187500001821 ) ) ;
#31985=CARTESIAN_POINT ( 'NONE',  ( 7.188101187500002709, 92.18750000204838102, 2.977408999572649151 ) ) ;
#31993=ORIENTED_EDGE ( 'NONE', *, *, #56605, .T. ) ;
#32010=CARTESIAN_POINT ( 'NONE',  ( -8.000000000000000000, 95.18750000409679046, 0.000000000000000000 ) ) ;
#32019=CARTESIAN_POINT ( 'NONE',  ( -4.401442555609581635E-16, 90.78125000204836681, -7.188101187500000044 ) ) ;
#32033=CARTESIAN_POINT ( 'NONE',  ( 0.000000000000000000, 125.0000000000000000, 8.000000000000000000 ) ) ;
#32040=CARTESIAN_POINT ( 'NONE',  ( 8.000000000000000000, 4.312499995903220196, 0.000000000000000000 ) ) ;
#32042=CARTESIAN_POINT ( 'NONE',  ( 2.977408999572651815, 9.562499997951608322, 7.188101187500000933 ) ) ;
#32045=CARTESIAN_POINT ( 'NONE',  ( -2.977408999572652260, 109.8125000020483952, 7.188101187500000044 ) ) ;
#32048=CARTESIAN_POINT ( 'NONE',  ( 9.797174393178825657E-16, 125.0000000000000000, -8.000000000000000000 ) ) ;
#32057=ORIENTED_EDGE ( 'NONE', *, *, #51227, .F. ) ;
#32065=CARTESIAN_POINT ( 'NONE',  ( -2.977408999572650927, 98.37500000204839523, -7.188101187500000933 ) ) ;
#32072=CARTESIAN_POINT ( 'NONE',  ( -5.082755093536324154, 106.7187500020483952, 5.082755093536326818 ) ) ;
#32085=CARTESIAN_POINT ( 'NONE',  ( 0.000000000000000000, 125.0000000000000000, 0.000000000000000000 ) ) ;
#32092=CARTESIAN_POINT ( 'NONE',  ( -5.656854249492378806, 122.3750000040967905, 5.656854249492381470 ) ) ;
#32100=CARTESIAN_POINT ( 'NONE',  ( 7.188101187500000044, 10.96874999795161187, 0.000000000000000000 ) ) ;
#32101=CARTESIAN_POINT ( 'NONE',  ( 5.656854249492381470, 118.2500000040967905, 5.656854249492379694 ) ) ;
#32106=FACE_OUTER_BOUND ( 'NONE', #69772, .T. ) ;
#32128=CARTESIAN_POINT ( 'NONE',  ( -8.000000000000000000, 112.9062500000000000, -3.313708498984761608 ) ) ;
#32135=CARTESIAN_POINT ( 'NONE',  ( 3.313708498984762052, 21.09374999590322375, -8.000000000000000000 ) ) ;
#32142=EDGE_CURVE ( 'NONE', #73206, #34267, #2491, .T. ) ;
#32148=CARTESIAN_POINT ( 'NONE',  ( -3.313708498984815343, 106.9062500040967763, -7.999999999999944933 ) ) ;
#32157=CARTESIAN_POINT ( 'NONE',  ( -4.401442555609581635E-16, 116.2812500020483810, -7.188101187500000044 ) ) ;
#32158=CARTESIAN_POINT ( 'NONE',  ( -4.898587196589412829E-16, 120.1250000000000000, -8.000000000000000000 ) ) ;
#32163=CARTESIAN_POINT ( 'NONE',  ( 2.977408999572650039, 124.0625000020483810, -7.188101187500001821 ) ) ;
#32191=CARTESIAN_POINT ( 'NONE',  ( -7.188101187500002709, 23.81249999795161543, 2.977408999572649151 ) ) ;
#32194=CARTESIAN_POINT ( 'NONE',  ( 7.188101187499999156, 20.24999999795161898, 2.977408999572654924 ) ) ;
#32201=VERTEX_POINT ( 'NONE', #59109 ) ;
#32207=CARTESIAN_POINT ( 'NONE',  ( -2.977408999572650927, 111.8750000020483668, -7.188101187500001821 ) ) ;
#32211=CARTESIAN_POINT ( 'NONE',  ( 4.401442555609581635E-16, 26.34374999795161543, -7.188101187500000044 ) ) ;
#32219=CARTESIAN_POINT ( 'NONE',  ( 7.188101187500002709, 93.68750000204838102, 2.977408999572649151 ) ) ;
#32222=CARTESIAN_POINT ( 'NONE',  ( 1.469576158976823947E-15, 111.8750000000000000, 8.000000000000000000 ) ) ;
#32223=EDGE_CURVE ( 'NONE', #64185, #39207, #3333, .T. ) ;
#32231=CARTESIAN_POINT ( 'NONE',  ( -4.898587196589412829E-16, 108.3125000040967905, -8.000000000000000000 ) ) ;
#32252=CARTESIAN_POINT ( 'NONE',  ( 7.188101187500000044, 108.4062500020483810, -8.802885111219163269E-16 ) ) ;
#32264=ORIENTED_EDGE ( 'NONE', *, *, #22173, .F. ) ;
#32267=CARTESIAN_POINT ( 'NONE',  ( -3.313708498984870410, 93.78125000000000000, 7.999999999999890754 ) ) ;
#32280=CARTESIAN_POINT ( 'NONE',  ( -7.188101187500002709, 21.18749999795161543, 2.977408999572649151 ) ) ;
#32287=CARTESIAN_POINT ( 'NONE',  ( 4.401442555609581635E-16, 2.343749997951610098, -7.188101187500000044 ) ) ;
#32290=CARTESIAN_POINT ( 'NONE',  ( -7.188101187500000044, 1.593749997951610098, -8.802885111219163269E-16 ) ) ;
#32304=CARTESIAN_POINT ( 'NONE',  ( 3.313708498984752726, 5.718750000000000000, 8.000000000000008882 ) ) ;
#32305=EDGE_LOOP ( 'NONE', ( #70871, #48173, #66972, #54946 ) ) ;
#32307=CARTESIAN_POINT ( 'NONE',  ( 4.401442555609581635E-16, 12.84374999795161187, -7.188101187500000044 ) ) ;
#32312=CARTESIAN_POINT ( 'NONE',  ( -5.082755093536324154, 111.2187500020483810, 5.082755093536326818 ) ) ;
#32328=CARTESIAN_POINT ( 'NONE',  ( 5.656854249492379694, 92.93749999999998579, -5.656854249492380582 ) ) ;
#32351=CARTESIAN_POINT ( 'NONE',  ( -7.188101187500000044, 19.21874999795161543, -8.802885111219163269E-16 ) ) ;
#32386=CARTESIAN_POINT ( 'NONE',  ( 8.000000000000000000, 12.09375000000000178, -3.313708498984761608 ) ) ;
#32389=CARTESIAN_POINT ( 'NONE',  ( 8.000000000000000000, 91.53125000409679046, -3.313708498984762496 ) ) ;
#32399=CARTESIAN_POINT ( 'NONE',  ( -5.082755093536324154, 89.84375000204839523, 5.082755093536326818 ) ) ;
#32406=AXIS2_PLACEMENT_3D ( 'NONE', #71905, #43237, #66252 ) ;
#32408=VERTEX_POINT ( 'NONE', #66600 ) ;
#32422=CARTESIAN_POINT ( 'NONE',  ( 7.999999999999998224, 8.718749995903221972, 3.313708498984766493 ) ) ;
#32423=EDGE_LOOP ( 'NONE', ( #40197, #44687, #54462, #3580 ) ) ;
#32425=CARTESIAN_POINT ( 'NONE',  ( 5.082755093536324154, 14.15624999795161187, 5.082755093536326818 ) ) ;
#32428=CARTESIAN_POINT ( 'NONE',  ( 7.188101187500000044, 107.2812500020483810, -8.802885111219163269E-16 ) ) ;
#32448=CARTESIAN_POINT ( 'NONE',  ( 2.977408999572654480, 97.62500000204836681, 7.188101187499999156 ) ) ;
#32455=CARTESIAN_POINT ( 'NONE',  ( -4.401442555609581635E-16, 101.6562500020483810, -7.188101187500000044 ) ) ;
#32464=FACE_OUTER_BOUND ( 'NONE', #46962, .T. ) ;
#32466=CARTESIAN_POINT ( 'NONE',  ( -5.082755093536326818, 3.281249997951610542, 5.082755093536325042 ) ) ;
#32471=ORIENTED_EDGE ( 'NONE', *, *, #25598, .F. ) ;
#32483=CARTESIAN_POINT ( 'NONE',  ( 5.082755093536325930, 11.15624999795161187, -5.082755093536325930 ) ) ;
#32484=CARTESIAN_POINT ( 'NONE',  ( 8.000000000000000000, 113.9375000040967763, -9.797174393178825657E-16 ) ) ;
#32500=ORIENTED_EDGE ( 'NONE', *, *, #13879, .F. ) ;
#32507=LINE ( 'NONE', #27195, #6067 ) ;
#32509=CARTESIAN_POINT ( 'NONE',  ( 1.469576158976823947E-15, 110.3750000000000000, 8.000000000000000000 ) ) ;
#32513=CARTESIAN_POINT ( 'NONE',  ( 3.313708498984721640, 19.21875000000000000, 8.000000000000039080 ) ) ;
#32514=EDGE_CURVE ( 'NONE', #26713, #65546, #48731, .T. ) ;
#32517=CARTESIAN_POINT ( 'NONE',  ( 8.000000000000000000, 20.90624999590322375, -3.313708498984761608 ) ) ;
#32519=LINE ( 'NONE', #59691, #39445 ) ;
#32534=AXIS2_PLACEMENT_3D ( 'NONE', #71452, #25059, #13005 ) ;
#32541=CARTESIAN_POINT ( 'NONE',  ( -2.977408999572652260, 118.4375000020483952, 7.188101187500000044 ) ) ;
#32546=EDGE_CURVE ( 'NONE', #28645, #43835, #11493, .T. ) ;
#32547=CARTESIAN_POINT ( 'NONE',  ( -7.188101187499999156, 118.6250000020483810, 2.977408999572654924 ) ) ;
#32573=CARTESIAN_POINT ( 'NONE',  ( 7.188101187500000044, 18.46874999795161187, 0.000000000000000000 ) ) ;
#32576=CARTESIAN_POINT ( 'NONE',  ( 5.082755093536324154, 15.65624999795161365, 5.082755093536326818 ) ) ;
#32602=CARTESIAN_POINT ( 'NONE',  ( 7.188101187500000044, 92.28125000204836681, -8.802885111219163269E-16 ) ) ;
#32607=CARTESIAN_POINT ( 'NONE',  ( -4.898587196589412829E-16, 94.62499999999998579, -8.000000000000000000 ) ) ;
#32627=CARTESIAN_POINT ( 'NONE',  ( 0.000000000000000000, 125.0000000000000000, 0.000000000000000000 ) ) ;
#32633=CARTESIAN_POINT ( 'NONE',  ( -7.188101187499999156, 107.7500000020483810, 2.977408999572654924 ) ) ;
#32644=CARTESIAN_POINT ( 'NONE',  ( -8.000000000000000000, 99.40625000000000000, -3.313708498984761164 ) ) ;
#32651=CARTESIAN_POINT ( 'NONE',  ( 0.000000000000000000, 125.0000000000000000, 8.000000000000000000 ) ) ;
#32660=CARTESIAN_POINT ( 'NONE',  ( 5.082755093536325930, 16.03124999795161543, -5.082755093536325930 ) ) ;
#32661=( BOUNDED_CURVE ( )  B_SPLINE_CURVE ( 2, ( #22411, #63905, #39774, #17130, #62777, #11486, #33771, #73737, #50722 ),
 .UNSPECIFIED., .F., .F. ) 
 B_SPLINE_CURVE_WITH_KNOTS ( ( 3, 2, 2, 2, 3 ),
 ( 0.6562500000000000000, 0.6614583333333333703, 0.6666666666666667407, 0.6718750000000001110, 0.6770833333333334814 ),
 .UNSPECIFIED. ) 
 CURVE ( )  GEOMETRIC_REPRESENTATION_ITEM ( )  RATIONAL_B_SPLINE_CURVE ( ( 1.000000000000000000, 0.9238795325112867385, 1.000000000000000000, 0.9238795325112867385, 1.000000000000000000, 0.9238795325112867385, 1.000000000000000000, 0.9238795325112850731, 1.000000000000001554 ) ) 
 REPRESENTATION_ITEM ( '' )  );
#32669=CARTESIAN_POINT ( 'NONE',  ( -7.188101187500001821, 4.124999997951610986, -2.977408999572651371 ) ) ;
#32678=EDGE_CURVE ( 'NONE', #20933, #19911, #48357, .T. ) ;
#32688=CARTESIAN_POINT ( 'NONE',  ( 2.977408999572650927, 9.749999997951610098, -7.188101187500000933 ) ) ;
#32692=CARTESIAN_POINT ( 'NONE',  ( -7.188101187500001821, 109.4375000020483810, -2.977408999572650483 ) ) ;
#32693=AXIS2_PLACEMENT_3D ( 'NONE', #41986, #7670, #63896 ) ;
#32702=CARTESIAN_POINT ( 'NONE',  ( 5.656854249492378806, 19.12499999590322020, 5.656854249492381470 ) ) ;
#32707=CARTESIAN_POINT ( 'NONE',  ( -4.898587196589412829E-16, 93.12499999999998579, -8.000000000000000000 ) ) ;
#32714=CARTESIAN_POINT ( 'NONE',  ( 8.000000000000000000, 118.4375000040967763, -9.797174393178825657E-16 ) ) ;
#32731=CARTESIAN_POINT ( 'NONE',  ( 7.188101187500001821, 20.06249999795161543, -2.977408999572650483 ) ) ;
#32766=CARTESIAN_POINT ( 'NONE',  ( 8.000000000000000000, 10.59375000000000178, -3.313708498984761608 ) ) ;
#32768=CARTESIAN_POINT ( 'NONE',  ( 1.469576158976823947E-15, 92.56250000409677625, 8.000000000000000000 ) ) ;
#32777=AXIS2_PLACEMENT_3D ( 'NONE', #52301, #10815, #51173 ) ;
#32780=CARTESIAN_POINT ( 'NONE',  ( -2.977408999572650927, 93.87500000204836681, -7.188101187500001821 ) ) ;
#32788=ORIENTED_EDGE ( 'NONE', *, *, #17317, .T. ) ;
#32792=CARTESIAN_POINT ( 'NONE',  ( -3.313708498984762496, 105.9687500040967620, 7.999999999999998224 ) ) ;
#32800=CARTESIAN_POINT ( 'NONE',  ( 3.313708498984762496, 7.031249995903221084, 7.999999999999998224 ) ) ;
#32804=CARTESIAN_POINT ( 'NONE',  ( -5.082755093536326818, 18.28124999795161187, 5.082755093536325042 ) ) ;
#32805=VECTOR ( 'NONE', #31836, 1000.000000000000000 ) ;
#32808=CARTESIAN_POINT ( 'NONE',  ( 2.977408999572654480, 102.5000000020483810, 7.188101187499999156 ) ) ;
#32815=CARTESIAN_POINT ( 'NONE',  ( 8.000000000000000000, 21.09375000000000355, -3.313708498984761164 ) ) ;
#32820=CARTESIAN_POINT ( 'NONE',  ( -3.313708498984719864, 19.78124999590321664, -8.000000000000040856 ) ) ;
#32826=CARTESIAN_POINT ( 'NONE',  ( -4.401442555609581635E-16, 101.2812500020483810, -7.188101187500000044 ) ) ;
#32833=CARTESIAN_POINT ( 'NONE',  ( 7.188101187500001821, 102.8750000020483810, -2.977408999572651371 ) ) ;
#32840=CARTESIAN_POINT ( 'NONE',  ( 7.999999999999998224, 16.40625000000000355, 3.313708498984766049 ) ) ;
#32851=ORIENTED_EDGE ( 'NONE', *, *, #53996, .T. ) ;
#32862=CARTESIAN_POINT ( 'NONE',  ( -2.977408999572654480, 8.999999997951610098, 7.188101187499999156 ) ) ;
#32864=CARTESIAN_POINT ( 'NONE',  ( 8.000000000000000000, 111.0312500040967763, -3.313708498984762496 ) ) ;
#32892=CARTESIAN_POINT ( 'NONE',  ( 8.000000000000000000, 103.3437500000000000, -3.313708498984762496 ) ) ;
#32898=CARTESIAN_POINT ( 'NONE',  ( -8.000000000000000000, 18.56249999590322020, -9.797174393178825657E-16 ) ) ;
#32900=CARTESIAN_POINT ( 'NONE',  ( -4.401442555609581635E-16, 122.6562500020483810, -7.188101187500000044 ) ) ;
#32912=CARTESIAN_POINT ( 'NONE',  ( -8.000000000000000000, 26.06249999590322375, -9.797174393178825657E-16 ) ) ;
#32922=CARTESIAN_POINT ( 'NONE',  ( 5.082755093536326818, 117.2187500020483810, 5.082755093536325042 ) ) ;
#32927=CARTESIAN_POINT ( 'NONE',  ( -2.977408999572650927, 119.7500000020483810, -7.188101187500001821 ) ) ;
#32931=EDGE_LOOP ( 'NONE', ( #55188, #63752, #23462, #30087 ) ) ;
#32951=AXIS2_PLACEMENT_3D ( 'NONE', #9560, #26507, #60854 ) ;
#32952=CARTESIAN_POINT ( 'NONE',  ( -3.313708498984760720, 1.968750000000000444, -8.000000000000000000 ) ) ;
#32955=CARTESIAN_POINT ( 'NONE',  ( -5.082755093536326818, 15.28124999795161187, 5.082755093536325042 ) ) ;
#32957=DIRECTION ( 'NONE',  ( -0.000000000000000000, 1.000000000000000000, -0.000000000000000000 ) ) ;
#32960=AXIS2_PLACEMENT_3D ( 'NONE', #46234, #52277, #29265 ) ;
#32961=CYLINDRICAL_SURFACE ( 'NONE', #12527, 8.000000000000000000 ) ;
#32974=VERTEX_POINT ( 'NONE', #26857 ) ;
#32983=CARTESIAN_POINT ( 'NONE',  ( -3.313708498984762496, 123.7812500000000000, 7.999999999999998224 ) ) ;
#32995=LINE ( 'NONE', #15233, #69314 ) ;
#33012=CARTESIAN_POINT ( 'NONE',  ( 1.320432766682874540E-15, 103.5312500020483810, 7.188101187500000044 ) ) ;
#33035=CARTESIAN_POINT ( 'NONE',  ( 1.469576158976823947E-15, 110.3750000000000000, 8.000000000000000000 ) ) ;
#33041=CARTESIAN_POINT ( 'NONE',  ( -5.082755093536326818, 18.28124999795161187, 5.082755093536325042 ) ) ;
#33045=CARTESIAN_POINT ( 'NONE',  ( 3.313708498984869077, 90.21875000409677625, -7.999999999999892530 ) ) ;
#33050=CARTESIAN_POINT ( 'NONE',  ( 7.188101187500001821, 3.562499997951610542, -2.977408999572650483 ) ) ;
#33053=CARTESIAN_POINT ( 'NONE',  ( -2.977408999572654480, 1.874999997951610098, 7.188101187499999156 ) ) ;
#33067=CARTESIAN_POINT ( 'NONE',  ( -7.999999999999998224, 104.0937500000000142, 3.313708498984766049 ) ) ;
#33070=CARTESIAN_POINT ( 'NONE',  ( 5.082755093536324154, 12.28124999795161187, 5.082755093536326818 ) ) ;
#33074=CARTESIAN_POINT ( 'NONE',  ( 7.188101187500001821, 110.3750000020484094, -2.977408999572651371 ) ) ;
#33090=CARTESIAN_POINT ( 'NONE',  ( -8.000000000000000000, 96.50000000000000000, 0.000000000000000000 ) ) ;
#33092=CARTESIAN_POINT ( 'NONE',  ( -4.898587196589412829E-16, 99.12499999999998579, -8.000000000000000000 ) ) ;
#33097=ORIENTED_EDGE ( 'NONE', *, *, #36266, .T. ) ;
#33098=DIRECTION ( 'NONE',  ( -0.000000000000000000, 1.000000000000000000, -0.000000000000000000 ) ) ;
#33099=EDGE_CURVE ( 'NONE', #2971, #3802, #31398, .T. ) ;
#33103=CARTESIAN_POINT ( 'NONE',  ( -7.188101187500001821, 122.5625000020483952, -2.977408999572650483 ) ) ;
#33110=VERTEX_POINT ( 'NONE', #20439 ) ;
#33114=CARTESIAN_POINT ( 'NONE',  ( -5.082755093536326818, 22.40624999795161187, 5.082755093536325042 ) ) ;
#33140=CARTESIAN_POINT ( 'NONE',  ( -3.313708498984762496, 1.781249995903220640, -8.000000000000000000 ) ) ;
#33151=CARTESIAN_POINT ( 'NONE',  ( 8.000000000000000000, 9.000000000000001776, 0.000000000000000000 ) ) ;
#33153=CARTESIAN_POINT ( 'NONE',  ( -4.898587196589412829E-16, 90.31250000409676204, -8.000000000000000000 ) ) ;
#33161=CARTESIAN_POINT ( 'NONE',  ( 2.977408999572654480, 90.12500000204836681, 7.188101187499999156 ) ) ;
#33184=CARTESIAN_POINT ( 'NONE',  ( -5.656854249492381470, 8.249999995903221972, 5.656854249492379694 ) ) ;
#33187=CARTESIAN_POINT ( 'NONE',  ( 7.188101187499999156, 20.24999999795161898, 2.977408999572654924 ) ) ;
#33189=CARTESIAN_POINT ( 'NONE',  ( 3.313708498984782036, 7.781250000000001776, -7.999999999999981348 ) ) ;
#33190=CARTESIAN_POINT ( 'NONE',  ( 1.320432766682874540E-15, 103.9062500020483810, 7.188101187500000044 ) ) ;
#33208=CARTESIAN_POINT ( 'NONE',  ( 7.188101187500002709, 97.81250000204840944, 2.977408999572649151 ) ) ;
#33213=CARTESIAN_POINT ( 'NONE',  ( 7.188101187500000044, 102.7812500020483810, -8.802885111219163269E-16 ) ) ;
#33221=CARTESIAN_POINT ( 'NONE',  ( 0.000000000000000000, 125.0000000000000000, 0.000000000000000000 ) ) ;
#33235=CARTESIAN_POINT ( 'NONE',  ( 2.977408999572651815, 6.187499997951610986, 7.188101187500000933 ) ) ;
#33237=CARTESIAN_POINT ( 'NONE',  ( 3.313708498984760720, 112.7187500040967763, -8.000000000000000000 ) ) ;
#33245=CARTESIAN_POINT ( 'NONE',  ( -4.898587196589412829E-16, 117.1250000000000000, -8.000000000000000000 ) ) ;
#33261=CARTESIAN_POINT ( 'NONE',  ( -7.999999999999998224, 107.0937500000000142, 3.313708498984766493 ) ) ;
#33267=CARTESIAN_POINT ( 'NONE',  ( -5.656854249492379694, 25.87499999590322375, -5.656854249492380582 ) ) ;
#33269=CARTESIAN_POINT ( 'NONE',  ( -7.188101187499999156, 121.6250000020483810, 2.977408999572654924 ) ) ;
#33276=CARTESIAN_POINT ( 'NONE',  ( -4.898587196589412829E-16, 123.1250000000000000, -8.000000000000000000 ) ) ;
#33291=CARTESIAN_POINT ( 'NONE',  ( -4.401442555609581635E-16, 119.2812500020483810, -7.188101187500000044 ) ) ;
#33297=CARTESIAN_POINT ( 'NONE',  ( -5.082755093536325930, 121.3437500020483952, -5.082755093536325930 ) ) ;
#33299=FACE_OUTER_BOUND ( 'NONE', #25035, .T. ) ;
#33315=CYLINDRICAL_SURFACE ( 'NONE', #70183, 8.000000000000000000 ) ;
#33321=CARTESIAN_POINT ( 'NONE',  ( -8.000000000000000000, 2.250000000000000444, -9.797174393178825657E-16 ) ) ;
#33324=CARTESIAN_POINT ( 'NONE',  ( -5.082755093536325042, 16.40624999795161543, -5.082755093536325930 ) ) ;
#33339=CARTESIAN_POINT ( 'NONE',  ( -5.082755093536326818, 26.90624999795161543, 5.082755093536325042 ) ) ;
#33347=CARTESIAN_POINT ( 'NONE',  ( 3.313708498984760720, 124.5312500000000142, -8.000000000000000000 ) ) ;
#33360=DIRECTION ( 'NONE',  ( -0.000000000000000000, 1.000000000000000000, -0.000000000000000000 ) ) ;
#33376=CARTESIAN_POINT ( 'NONE',  ( 1.320432766682874540E-15, 105.0312500020483810, 7.188101187500000044 ) ) ;
#33396=CARTESIAN_POINT ( 'NONE',  ( 1.469576158976823947E-15, 116.5625000040967763, 8.000000000000000000 ) ) ;
#33397=DIRECTION ( 'NONE',  ( 0.000000000000000000, 0.000000000000000000, 1.000000000000000000 ) ) ;
#33399=CARTESIAN_POINT ( 'NONE',  ( 8.000000000000000000, 106.4375000040967763, -9.797174393178825657E-16 ) ) ;
#33404=CARTESIAN_POINT ( 'NONE',  ( 4.401442555609581635E-16, 19.21874999795161543, -7.188101187500000044 ) ) ;
#33412=CARTESIAN_POINT ( 'NONE',  ( -2.977408999572654480, 10.49999999795161010, 7.188101187499999156 ) ) ;
#33421=CARTESIAN_POINT ( 'NONE',  ( 7.999999999999998224, 26.90625000000000355, 3.313708498984766493 ) ) ;
#33429=CARTESIAN_POINT ( 'NONE',  ( -1.469576158976823947E-15, 22.12500000000000355, 8.000000000000000000 ) ) ;
#33431=CARTESIAN_POINT ( 'NONE',  ( 2.977408999572650927, 8.249999997951611874, -7.188101187500000933 ) ) ;
#33436=CARTESIAN_POINT ( 'NONE',  ( 2.977408999572650039, 107.5625000020483810, -7.188101187500001821 ) ) ;
#33448=CARTESIAN_POINT ( 'NONE',  ( 7.188101187500000044, 0.8437499979516100979, 0.000000000000000000 ) ) ;
#33454=CARTESIAN_POINT ( 'NONE',  ( -5.656854249492378806, 90.68750000000000000, 5.656854249492381470 ) ) ;
#33461=ORIENTED_EDGE ( 'NONE', *, *, #23238, .T. ) ;
#33464=VECTOR ( 'NONE', #65350, 1000.000000000000000 ) ;
#33468=CARTESIAN_POINT ( 'NONE',  ( -7.188101187500000044, 122.6562500020483810, 0.000000000000000000 ) ) ;
#33477=CARTESIAN_POINT ( 'NONE',  ( -7.188101187500001821, 22.12499999795161187, -2.977408999572651371 ) ) ;
#33491=CARTESIAN_POINT ( 'NONE',  ( -5.656854249492379694, 21.37499999590322375, -5.656854249492380582 ) ) ;
#33498=EDGE_CURVE ( 'NONE', #24477, #60299, #70319, .T. ) ;
#33504=CARTESIAN_POINT ( 'NONE',  ( -4.898587196589412829E-16, 90.31250000409676204, -8.000000000000000000 ) ) ;
#33514=CARTESIAN_POINT ( 'NONE',  ( -3.313708498984765161, 13.03125000000000355, 7.999999999999998224 ) ) ;
#33518=CARTESIAN_POINT ( 'NONE',  ( 3.313708498984760720, 90.21875000409679046, -8.000000000000000000 ) ) ;
#33528=ORIENTED_EDGE ( 'NONE', *, *, #53779, .T. ) ;
#33530=CARTESIAN_POINT ( 'NONE',  ( -5.082755093536325930, 89.46875000204838102, -5.082755093536325930 ) ) ;
#33538=VERTEX_POINT ( 'NONE', #52413 ) ;
#33539=( BOUNDED_CURVE ( )  B_SPLINE_CURVE ( 2, ( #40900, #36719, #52963, #59730, #18990, #6938, #12219, #53704, #24277 ),
 .UNSPECIFIED., .F., .F. ) 
 B_SPLINE_CURVE_WITH_KNOTS ( ( 3, 2, 2, 2, 3 ),
 ( 0.3229166666666665186, 0.3281249999999998335, 0.3333333333333331483, 0.3385416666666665186, 0.3437499999999998335 ),
 .UNSPECIFIED. ) 
 CURVE ( )  GEOMETRIC_REPRESENTATION_ITEM ( )  RATIONAL_B_SPLINE_CURVE ( ( 1.000000000000002442, 0.9238795325112842960, 1.000000000000000000, 0.9238795325112867385, 1.000000000000000000, 0.9238795325112867385, 1.000000000000000000, 0.9238795325112891810, 0.9999999999999975575 ) ) 
 REPRESENTATION_ITEM ( '' )  );
#33543=DIRECTION ( 'NONE',  ( 0.000000000000000000, 0.000000000000000000, -1.000000000000000000 ) ) ;
#33549=CARTESIAN_POINT ( 'NONE',  ( 1.469576158976823947E-15, 101.3750000000000000, 8.000000000000000000 ) ) ;
#33551=CARTESIAN_POINT ( 'NONE',  ( -8.000000000000001776, 6.656249995903221084, 3.313708498984759387 ) ) ;
#33554=CARTESIAN_POINT ( 'NONE',  ( -5.082755093536326818, 19.78124999795161543, 5.082755093536325042 ) ) ;
#33557=CARTESIAN_POINT ( 'NONE',  ( -7.188101187499999156, 106.6250000020483810, 2.977408999572654924 ) ) ;
#33564=( BOUNDED_CURVE ( )  B_SPLINE_CURVE ( 2, ( #14472, #73329, #21633, #9590, #37511, #48812, #44658, #71817, #72194 ),
 .UNSPECIFIED., .F., .F. ) 
 B_SPLINE_CURVE_WITH_KNOTS ( ( 3, 2, 2, 2, 3 ),
 ( 0.4305555555555555247, 0.4374999999999999445, 0.4444444444444444198, 0.4513888888888888951, 0.4583333333333333148 ),
 .UNSPECIFIED. ) 
 CURVE ( )  GEOMETRIC_REPRESENTATION_ITEM ( )  RATIONAL_B_SPLINE_CURVE ( ( 1.000000000000000666, 0.9238795325112861834, 1.000000000000000000, 0.9238795325112867385, 1.000000000000000000, 0.9238795325112867385, 1.000000000000000000, 0.9238795325112867385, 1.000000000000000000 ) ) 
 REPRESENTATION_ITEM ( '' )  );
#33575=CARTESIAN_POINT ( 'NONE',  ( 7.188101187500000044, 93.40625000204838102, -8.802885111219163269E-16 ) ) ;
#33582=CARTESIAN_POINT ( 'NONE',  ( 2.977408999572654480, 104.0000000020483810, 7.188101187499999156 ) ) ;
#33590=CARTESIAN_POINT ( 'NONE',  ( 8.000000000000000000, 16.59375000000000355, -3.313708498984761164 ) ) ;
#33591=DIRECTION ( 'NONE',  ( -0.000000000000000000, 1.000000000000000000, -0.000000000000000000 ) ) ;
#33605=CARTESIAN_POINT ( 'NONE',  ( 5.082755093536325930, 12.65624999795161187, -5.082755093536325930 ) ) ;
#33606=CARTESIAN_POINT ( 'NONE',  ( -8.000000000000000000, 107.0937500040967905, -3.313708498984761608 ) ) ;
#33617=CARTESIAN_POINT ( 'NONE',  ( 3.313708498984887285, 116.4687500000000142, 7.999999999999878320 ) ) ;
#33618=CARTESIAN_POINT ( 'NONE',  ( -5.082755093536325930, 110.4687500020483810, -5.082755093536325930 ) ) ;
#33633=CARTESIAN_POINT ( 'NONE',  ( -3.313708498984762052, 103.7187500000000000, -8.000000000000000000 ) ) ;
#33638=CARTESIAN_POINT ( 'NONE',  ( -8.000000000000000000, 24.56249999590322375, -9.797174393178825657E-16 ) ) ;
#33640=CARTESIAN_POINT ( 'NONE',  ( -4.401442555609581635E-16, 124.1562500020483810, -7.188101187500000044 ) ) ;
#33661=CARTESIAN_POINT ( 'NONE',  ( -7.188101187500000933, 113.5625000020483810, -2.977408999572650483 ) ) ;
#33668=CARTESIAN_POINT ( 'NONE',  ( 2.977408999572650039, 122.5625000020483952, -7.188101187500001821 ) ) ;
#33669=CARTESIAN_POINT ( 'NONE',  ( 4.898587196589412829E-16, 13.68749999590322375, -8.000000000000000000 ) ) ;
#33679=CARTESIAN_POINT ( 'NONE',  ( -8.000000000000000000, 18.65625000000000355, -3.313708498984762496 ) ) ;
#33694=CARTESIAN_POINT ( 'NONE',  ( -1.469576158976823947E-15, 1.125000000000000222, 8.000000000000000000 ) ) ;
#33695=CARTESIAN_POINT ( 'NONE',  ( -5.656854249492378806, 110.3750000040967763, 5.656854249492381470 ) ) ;
#33697=CARTESIAN_POINT ( 'NONE',  ( 2.977408999572651815, 23.06249999795161187, 7.188101187500000933 ) ) ;
#33715=CARTESIAN_POINT ( 'NONE',  ( -3.313708498984762496, 104.4687500040967763, 7.999999999999998224 ) ) ;
#33723=CARTESIAN_POINT ( 'NONE',  ( -5.082755093536325930, 89.84375000204839523, -5.082755093536325930 ) ) ;
#33731=CARTESIAN_POINT ( 'NONE',  ( 4.898587196589412829E-16, 13.68749999590322375, -8.000000000000000000 ) ) ;
#33750=CARTESIAN_POINT ( 'NONE',  ( -2.977408999572650927, 102.8750000020483810, -7.188101187500001821 ) ) ;
#33753=CARTESIAN_POINT ( 'NONE',  ( 7.651181638696392895, 0.2025150128294917473, -1.024910111847489924 ) ) ;
#33756=( BOUNDED_CURVE ( )  B_SPLINE_CURVE ( 2, ( #16979, #46028, #17353, #40376, #63373, #408, #11698, #34739, #46402 ),
 .UNSPECIFIED., .F., .F. ) 
 B_SPLINE_CURVE_WITH_KNOTS ( ( 3, 2, 2, 2, 3 ),
 ( 0.5138888888888888395, 0.5208333333333333703, 0.5277777777777777901, 0.5347222222222222099, 0.5416666666666666297 ),
 .UNSPECIFIED. ) 
 CURVE ( )  GEOMETRIC_REPRESENTATION_ITEM ( )  RATIONAL_B_SPLINE_CURVE ( ( 1.000000000000000000, 0.9238795325112867385, 1.000000000000000000, 0.9238795325112867385, 1.000000000000000000, 0.9238795325112867385, 1.000000000000000000, 0.9238795325112867385, 1.000000000000000000 ) ) 
 REPRESENTATION_ITEM ( '' )  );
#33770=CARTESIAN_POINT ( 'NONE',  ( -3.313708498984842432, 112.9062500040967763, -7.999999999999920064 ) ) ;
#33771=CARTESIAN_POINT ( 'NONE',  ( -5.656854249492380582, 100.8125000000000000, -5.656854249492380582 ) ) ;
#33778=CARTESIAN_POINT ( 'NONE',  ( -7.188101187500000044, 24.09374999795161543, -8.802885111219163269E-16 ) ) ;
#33787=VECTOR ( 'NONE', #70659, 1000.000000000000000 ) ;
#33790=CARTESIAN_POINT ( 'NONE',  ( -2.977408999572650039, 6.937499997951610986, -7.188101187500001821 ) ) ;
#33793=CARTESIAN_POINT ( 'NONE',  ( -8.000000000000001776, 17.15624999590322375, 3.313708498984759387 ) ) ;
#33808=CARTESIAN_POINT ( 'NONE',  ( 2.977408999572652260, 18.18749999795161187, 7.188101187500000044 ) ) ;
#33812=CARTESIAN_POINT ( 'NONE',  ( -2.977408999572650927, 106.2500000020484094, -7.188101187500001821 ) ) ;
#33830=CARTESIAN_POINT ( 'NONE',  ( -4.898587196589412829E-16, 105.3125000040967763, -8.000000000000000000 ) ) ;
#33834=CARTESIAN_POINT ( 'NONE',  ( 5.656854249492381470, 118.2500000040967905, 5.656854249492379694 ) ) ;
#33837=LINE ( 'NONE', #44391, #3176 ) ;
#33842=CARTESIAN_POINT ( 'NONE',  ( 5.082755093536325042, 119.0937500020483810, -5.082755093536325930 ) ) ;
#33851=CARTESIAN_POINT ( 'NONE',  ( 2.977408999572651815, 25.68749999795162253, 7.188101187500000933 ) ) ;
#33861=CARTESIAN_POINT ( 'NONE',  ( 1.469576158976823947E-15, 117.8750000000000000, 8.000000000000000000 ) ) ;
#33869=CARTESIAN_POINT ( 'NONE',  ( 1.469576158976823947E-15, 117.8750000000000000, 8.000000000000000000 ) ) ;
#33870=CARTESIAN_POINT ( 'NONE',  ( 0.000000000000000000, 125.0000000000000000, 0.000000000000000000 ) ) ;
#33873=CARTESIAN_POINT ( 'NONE',  ( 7.188101187500000933, 6.937499997951610986, -2.977408999572650483 ) ) ;
#33876=ORIENTED_EDGE ( 'NONE', *, *, #29186, .F. ) ;
#33878=CARTESIAN_POINT ( 'NONE',  ( 3.313708498984828221, 115.7187500040967905, -7.999999999999932498 ) ) ;
#33888=CARTESIAN_POINT ( 'NONE',  ( -8.000000000000000000, 20.15625000000000355, -3.313708498984762496 ) ) ;
#33891=CARTESIAN_POINT ( 'NONE',  ( -7.999999999999998224, 93.78125000409679046, 3.313708498984766493 ) ) ;
#33905=CARTESIAN_POINT ( 'NONE',  ( -2.977408999572650927, 124.2500000020484094, -7.188101187500001821 ) ) ;
#33912=EDGE_CURVE ( 'NONE', #7386, #7343, #21605, .T. ) ;
#33927=CARTESIAN_POINT ( 'NONE',  ( -5.656854249492379694, 7.874999995903221972, -5.656854249492380582 ) ) ;
#33930=CARTESIAN_POINT ( 'NONE',  ( -5.082755093536326818, 16.78124999795161543, 5.082755093536325042 ) ) ;
#33932=DIRECTION ( 'NONE',  ( -0.000000000000000000, 1.000000000000000000, -0.000000000000000000 ) ) ;
#33933=CARTESIAN_POINT ( 'NONE',  ( 2.977408999572650039, 104.5625000020483810, -7.188101187500000933 ) ) ;
#33948=VECTOR ( 'NONE', #52215, 1000.000000000000000 ) ;
#33950=CARTESIAN_POINT ( 'NONE',  ( -5.082755093536325930, 93.96875000204838102, -5.082755093536325930 ) ) ;
#33957=CARTESIAN_POINT ( 'NONE',  ( -4.401442555609581635E-16, 100.1562500020483810, -7.188101187500000044 ) ) ;
#33959=CARTESIAN_POINT ( 'NONE',  ( -1.377103048673273156, 0.4464676475659328236, -7.833776318515849546 ) ) ;
#33968=CARTESIAN_POINT ( 'NONE',  ( 3.313708498984802020, 16.78125000000000000, -7.999999999999958256 ) ) ;
#33986=CARTESIAN_POINT ( 'NONE',  ( 4.401442555609581635E-16, 14.34374999795161187, -7.188101187500000044 ) ) ;
#33987=CARTESIAN_POINT ( 'NONE',  ( 5.656854249492381470, 112.2500000040967763, 5.656854249492379694 ) ) ;
#33995=VERTEX_POINT ( 'NONE', #33504 ) ;
#33997=CARTESIAN_POINT ( 'NONE',  ( -2.977408999572651815, 101.9375000020483810, 7.188101187500000933 ) ) ;
#34003=ORIENTED_EDGE ( 'NONE', *, *, #16454, .T. ) ;
#34006=CARTESIAN_POINT ( 'NONE',  ( 1.469576158976823947E-15, 91.06250000409676204, 8.000000000000000000 ) ) ;
#34011=DIRECTION ( 'NONE',  ( -0.000000000000000000, 1.000000000000000000, -0.000000000000000000 ) ) ;
#34013=CARTESIAN_POINT ( 'NONE',  ( 3.313708498984760720, 106.5312500000000142, -8.000000000000000000 ) ) ;
#34018=CARTESIAN_POINT ( 'NONE',  ( 7.999999999999998224, 25.21874999590322020, 3.313708498984766493 ) ) ;
#34020=CARTESIAN_POINT ( 'NONE',  ( -7.188101187500000044, 120.0312500020483810, 0.000000000000000000 ) ) ;
#34032=CARTESIAN_POINT ( 'NONE',  ( 3.313708498984765161, 101.6562500040967905, 7.999999999999998224 ) ) ;
#34041=CARTESIAN_POINT ( 'NONE',  ( 2.977408999572650039, 113.1875000020483810, -7.188101187500000933 ) ) ;
#34048=CARTESIAN_POINT ( 'NONE',  ( -5.082755093536324154, 120.2187500020483952, 5.082755093536326818 ) ) ;
#34049=CARTESIAN_POINT ( 'NONE',  ( -8.000000000000000000, 120.6875000040967763, 0.000000000000000000 ) ) ;
#34071=CARTESIAN_POINT ( 'NONE',  ( 7.188101187500000044, 24.46874999795161543, 0.000000000000000000 ) ) ;
#34074=CARTESIAN_POINT ( 'NONE',  ( 7.188101187499999156, 21.74999999795162253, 2.977408999572654924 ) ) ;
#34075=CARTESIAN_POINT ( 'NONE',  ( 0.000000000000000000, 54.99999999999999289, 0.000000000000000000 ) ) ;
#34096=CARTESIAN_POINT ( 'NONE',  ( 3.594034666126828981, 89.53052424436678791, -6.225087429138448591 ) ) ;
#34100=EDGE_CURVE ( 'NONE', #74424, #66034, #8615, .T. ) ;
#34112=CARTESIAN_POINT ( 'NONE',  ( 5.656854249492378806, 10.12499999590322020, 5.656854249492381470 ) ) ;
#34124=CARTESIAN_POINT ( 'NONE',  ( 2.977408999572654480, 105.1250000020483668, 7.188101187499999156 ) ) ;
#34135=AXIS2_PLACEMENT_3D ( 'NONE', #14717, #49809, #37002 ) ;
#34142=CARTESIAN_POINT ( 'NONE',  ( 5.656854249492381470, 116.7500000040967905, 5.656854249492379694 ) ) ;
#34149=CARTESIAN_POINT ( 'NONE',  ( -1.320432766682874540E-15, 22.96874999795161543, 7.188101187500000044 ) ) ;
#34153=FACE_OUTER_BOUND ( 'NONE', #31458, .T. ) ;
#34157=CARTESIAN_POINT ( 'NONE',  ( 7.188101187500001821, 6.562499997951610986, -2.977408999572650483 ) ) ;
#34160=CARTESIAN_POINT ( 'NONE',  ( -7.188101187500000044, 7.593749997951610986, -8.802885111219163269E-16 ) ) ;
#34167=VERTEX_POINT ( 'NONE', #34994 ) ;
#34175=CARTESIAN_POINT ( 'NONE',  ( -7.188101187500002709, 14.81249999795161365, 2.977408999572649151 ) ) ;
#34179=CARTESIAN_POINT ( 'NONE',  ( 7.188101187500002709, 108.6875000020483952, 2.977408999572649151 ) ) ;
#34183=CARTESIAN_POINT ( 'NONE',  ( -3.313708498984816231, 95.46875000409679046, 7.999999999999943157 ) ) ;
#34189=CYLINDRICAL_SURFACE ( 'NONE', #14641, 8.000000000000000000 ) ;
#34194=CARTESIAN_POINT ( 'NONE',  ( -8.000000000000000000, 90.50000000000000000, 0.000000000000000000 ) ) ;
#34204=CARTESIAN_POINT ( 'NONE',  ( -8.000000000000001776, 20.34375000000000355, 3.313708498984759387 ) ) ;
#34210=CARTESIAN_POINT ( 'NONE',  ( -5.082755093536324154, 122.8437500020483952, 5.082755093536326818 ) ) ;
#34220=CARTESIAN_POINT ( 'NONE',  ( 7.188101187499999156, 22.87499999795161187, 2.977408999572654924 ) ) ;
#34221=CARTESIAN_POINT ( 'NONE',  ( 0.000000000000000000, 124.5000000000000284, 0.000000000000000000 ) ) ;
#34242=CARTESIAN_POINT ( 'NONE',  ( 7.188101187500000044, 6.843749997951610986, 0.000000000000000000 ) ) ;
#34247=CARTESIAN_POINT ( 'NONE',  ( -1.469576158976823947E-15, 2.437499995903220196, 8.000000000000000000 ) ) ;
#34250=VECTOR ( 'NONE', #29707, 1000.000000000000000 ) ;
#34259=CARTESIAN_POINT ( 'NONE',  ( 7.999999999999998224, 14.90625000000000178, 3.313708498984766493 ) ) ;
#34262=CARTESIAN_POINT ( 'NONE',  ( 7.188101187500000044, 123.4062500020483810, -8.802885111219163269E-16 ) ) ;
#34267=VERTEX_POINT ( 'NONE', #46657 ) ;
#34273=CARTESIAN_POINT ( 'NONE',  ( 7.188101187500002709, 122.1875000020483668, 2.977408999572649151 ) ) ;
#34280=ORIENTED_EDGE ( 'NONE', *, *, #25302, .F. ) ;
#34295=CARTESIAN_POINT ( 'NONE',  ( 8.000000000000000000, 101.8437500000000000, -3.313708498984762496 ) ) ;
#34298=EDGE_CURVE ( 'NONE', #65440, #64185, #57332, .T. ) ;
#34300=CARTESIAN_POINT ( 'NONE',  ( 2.977408999572650927, 19.12499999795161187, -7.188101187500001821 ) ) ;
#34302=CARTESIAN_POINT ( 'NONE',  ( -4.898587196589412829E-16, 102.1250000000000000, -8.000000000000000000 ) ) ;
#34303=CARTESIAN_POINT ( 'NONE',  ( -7.188101187500000933, 106.4375000020483810, -2.977408999572650483 ) ) ;
#34311=ORIENTED_EDGE ( 'NONE', *, *, #51085, .F. ) ;
#34312=CARTESIAN_POINT ( 'NONE',  ( 0.000000000000000000, 0.5000000000000004441, 0.000000000000000000 ) ) ;
#34314=CARTESIAN_POINT ( 'NONE',  ( -8.000000000000000000, 22.96874999590322020, -3.313708498984762496 ) ) ;
#34319=CARTESIAN_POINT ( 'NONE',  ( 7.188101187500002709, 91.81250000204838102, 2.977408999572649151 ) ) ;
#34328=CARTESIAN_POINT ( 'NONE',  ( 7.188101187500000044, 96.78125000204838102, -8.802885111219163269E-16 ) ) ;
#34354=CARTESIAN_POINT ( 'NONE',  ( -5.082755093536326818, 16.40624999795161543, 5.082755093536325042 ) ) ;
#34355=CARTESIAN_POINT ( 'NONE',  ( 8.000000000000001776, 112.3437500040967905, 3.313708498984759387 ) ) ;
#34364=CARTESIAN_POINT ( 'NONE',  ( -5.082755093536324154, 103.3437500020483668, 5.082755093536326818 ) ) ;
#34382=CARTESIAN_POINT ( 'NONE',  ( 3.313708498984765161, 105.9687500000000142, 7.999999999999998224 ) ) ;
#34388=CARTESIAN_POINT ( 'NONE',  ( -8.000000000000000000, 24.46874999590322375, -3.313708498984762496 ) ) ;
#34390=CARTESIAN_POINT ( 'NONE',  ( 7.188101187500000933, 122.3750000020483952, -2.977408999572651371 ) ) ;
#34410=CARTESIAN_POINT ( 'NONE',  ( -4.401442555609581635E-16, 113.2812500020483952, -7.188101187500000044 ) ) ;
#34414=EDGE_CURVE ( 'NONE', #38802, #32408, #61530, .T. ) ;
#34416=CARTESIAN_POINT ( 'NONE',  ( 2.977408999572654480, 116.0000000020483810, 7.188101187499999156 ) ) ;
#34423=CARTESIAN_POINT ( 'NONE',  ( 8.000000000000000000, 107.7500000000000000, -9.797174393178825657E-16 ) ) ;
#34428=CARTESIAN_POINT ( 'NONE',  ( -8.000000000000001776, 18.84375000000000355, 3.313708498984759387 ) ) ;
#34439=( BOUNDED_CURVE ( )  B_SPLINE_CURVE ( 2, ( #31745, #20407, #7987, #54765, #43423, #47967, #19666, #24950, #3446 ),
 .UNSPECIFIED., .F., .F. ) 
 B_SPLINE_CURVE_WITH_KNOTS ( ( 3, 2, 2, 2, 3 ),
 ( 0.9305555555555554692, 0.9374999999999998890, 0.9444444444444443088, 0.9513888888888887285, 0.9583333333333332593 ),
 .UNSPECIFIED. ) 
 CURVE ( )  GEOMETRIC_REPRESENTATION_ITEM ( )  RATIONAL_B_SPLINE_CURVE ( ( 1.000000000000001110, 0.9238795325112855172, 1.000000000000000000, 0.9238795325112867385, 1.000000000000000000, 0.9238795325112867385, 1.000000000000000000, 0.9238795325112879597, 0.9999999999999987788 ) ) 
 REPRESENTATION_ITEM ( '' )  );
#34443=ORIENTED_EDGE ( 'NONE', *, *, #2738, .T. ) ;
#34444=CARTESIAN_POINT ( 'NONE',  ( -7.188101187500000044, 26.71874999795161543, -8.802885111219163269E-16 ) ) ;
#34447=CARTESIAN_POINT ( 'NONE',  ( -2.977408999572650039, 25.31249999795161543, -7.188101187500001821 ) ) ;
#34448=CARTESIAN_POINT ( 'NONE',  ( 0.000000000000000000, 125.0000000000000000, 8.000000000000000000 ) ) ;
#34453=EDGE_LOOP ( 'NONE', ( #67539, #20618 ) ) ;
#34459=DIRECTION ( 'NONE',  ( 1.000000000000000000, 0.000000000000000000, 0.000000000000000000 ) ) ;
#34472=CARTESIAN_POINT ( 'NONE',  ( -4.898587196589412829E-16, 121.6250000000000000, -8.000000000000000000 ) ) ;
#34478=CARTESIAN_POINT ( 'NONE',  ( -8.000000000000001776, 23.34375000000000355, 3.313708498984759387 ) ) ;
#34496=DIRECTION ( 'NONE',  ( -0.000000000000000000, 1.000000000000000000, -0.000000000000000000 ) ) ;
#34501=AXIS2_PLACEMENT_3D ( 'NONE', #67338, #3975, #20172 ) ;
#34503=CARTESIAN_POINT ( 'NONE',  ( -2.977408999572650927, 104.3750000020483952, -7.188101187500001821 ) ) ;
#34505=CARTESIAN_POINT ( 'NONE',  ( 0.000000000000000000, 125.0000000000000000, 0.000000000000000000 ) ) ;
#34527=CARTESIAN_POINT ( 'NONE',  ( -1.320432766682874540E-15, 21.46874999795161543, 7.188101187500000044 ) ) ;
#34534=CARTESIAN_POINT ( 'NONE',  ( 2.977408999572651815, 10.68749999795161187, 7.188101187500000933 ) ) ;
#34537=CARTESIAN_POINT ( 'NONE',  ( 7.188101187499999156, 8.249999997951611874, 2.977408999572654924 ) ) ;
#34546=EDGE_CURVE ( 'NONE', #42073, #38454, #13178, .T. ) ;
#34554=CARTESIAN_POINT ( 'NONE',  ( 7.188101187500000044, 15.46874999795161187, 0.000000000000000000 ) ) ;
#34558=CARTESIAN_POINT ( 'NONE',  ( -5.082755093536325930, 106.3437500020483810, -5.082755093536325930 ) ) ;
#34559=CARTESIAN_POINT ( 'NONE',  ( 0.000000000000000000, 0.000000000000000000, 0.000000000000000000 ) ) ;
#34585=CARTESIAN_POINT ( 'NONE',  ( 2.977408999572654480, 120.1250000020483952, 7.188101187499999156 ) ) ;
#34593=CARTESIAN_POINT ( 'NONE',  ( -7.188101187500002709, 26.81249999795161543, 2.977408999572649151 ) ) ;
#34615=CARTESIAN_POINT ( 'NONE',  ( -5.082755093536325042, 7.406249997951610986, -5.082755093536325930 ) ) ;
#34619=CARTESIAN_POINT ( 'NONE',  ( 3.313708498984755391, 122.6562500040968189, 8.000000000000008882 ) ) ;
#34632=CARTESIAN_POINT ( 'NONE',  ( -3.313708498984760720, 16.96875000000000000, -8.000000000000000000 ) ) ;
#34636=CARTESIAN_POINT ( 'NONE',  ( -4.401442555609581635E-16, 122.2812500020483810, -7.188101187500000044 ) ) ;
#34669=CARTESIAN_POINT ( 'NONE',  ( -3.313708498984842432, 114.2187500000000000, -7.999999999999920064 ) ) ;
#34674=CARTESIAN_POINT ( 'NONE',  ( 7.188101187500001821, 24.93749999795161543, -2.977408999572650483 ) ) ;
#34676=CARTESIAN_POINT ( 'NONE',  ( -8.000000000000001776, 8.156249995903221972, 3.313708498984759387 ) ) ;
#34677=CARTESIAN_POINT ( 'NONE',  ( -2.977408999572652260, 100.8125000020484094, 7.188101187500000044 ) ) ;
#34691=CARTESIAN_POINT ( 'NONE',  ( -2.977408999572650927, 93.87500000204838102, -7.188101187500000933 ) ) ;
#34694=CIRCLE ( 'NONE', #25043, 11.00000000000000000 ) ;
#34697=CARTESIAN_POINT ( 'NONE',  ( -7.188101187499999156, 94.62500000204838102, 2.977408999572654924 ) ) ;
#34710=CARTESIAN_POINT ( 'NONE',  ( -8.000000000000000000, 11.06249999590322020, -9.797174393178825657E-16 ) ) ;
#34723=EDGE_CURVE ( 'NONE', #4353, #33995, #72742, .T. ) ;
#34724=CARTESIAN_POINT ( 'NONE',  ( 2.977408999572651815, 13.68749999795161365, 7.188101187500000933 ) ) ;
#34725=CARTESIAN_POINT ( 'NONE',  ( -3.313708498984762496, 101.4687500040967763, 7.999999999999998224 ) ) ;
#34734=FACE_OUTER_BOUND ( 'NONE', #50306, .T. ) ;
#34735=CARTESIAN_POINT ( 'NONE',  ( -7.188101187499999156, 103.2500000020483810, 2.977408999572654924 ) ) ;
#34739=CARTESIAN_POINT ( 'NONE',  ( -3.313708498984765161, 15.84374999590322197, 7.999999999999998224 ) ) ;
#34753=CARTESIAN_POINT ( 'NONE',  ( -5.656854249492380582, 100.8125000000000000, -5.656854249492380582 ) ) ;
#34761=CARTESIAN_POINT ( 'NONE',  ( -5.656854249492379694, 27.37499999590322375, -5.656854249492380582 ) ) ;
#34764=CARTESIAN_POINT ( 'NONE',  ( 5.082755093536325042, 116.4687500020483810, -5.082755093536325930 ) ) ;
#34776=LINE ( 'NONE', #4598, #37542 ) ;
#34782=FACE_OUTER_BOUND ( 'NONE', #40073, .T. ) ;
#34784=CARTESIAN_POINT ( 'NONE',  ( -7.188101187500000933, 109.0625000020483810, -2.977408999572650483 ) ) ;
#34789=CARTESIAN_POINT ( 'NONE',  ( -2.977408999572650927, 113.7500000020483668, -7.188101187500001821 ) ) ;
#34790=CARTESIAN_POINT ( 'NONE',  ( -1.469576158976823947E-15, 14.43749999590322375, 8.000000000000000000 ) ) ;
#34813=CARTESIAN_POINT ( 'NONE',  ( 4.898587196589412829E-16, 7.875000000000001776, -8.000000000000000000 ) ) ;
#34817=CARTESIAN_POINT ( 'NONE',  ( 2.977408999572651815, 24.56249999795161543, 7.188101187500000933 ) ) ;
#34841=CARTESIAN_POINT ( 'NONE',  ( -8.000000000000000000, 118.9062500000000000, -3.313708498984761608 ) ) ;
#34851=CARTESIAN_POINT ( 'NONE',  ( 4.898587196589412829E-16, 6.187499995903221084, -8.000000000000000000 ) ) ;
#34872=CARTESIAN_POINT ( 'NONE',  ( 7.188101187500002709, 97.81250000204840944, 2.977408999572649151 ) ) ;
#34879=( BOUNDED_CURVE ( )  B_SPLINE_CURVE ( 2, ( #45315, #28705, #46059, #44954, #4594, #44582, #69078, #40409, #63406 ),
 .UNSPECIFIED., .F., .F. ) 
 B_SPLINE_CURVE_WITH_KNOTS ( ( 3, 2, 2, 2, 3 ),
 ( 0.6354166666666667407, 0.6406250000000001110, 0.6458333333333334814, 0.6510416666666666297, 0.6562500000000000000 ),
 .UNSPECIFIED. ) 
 CURVE ( )  GEOMETRIC_REPRESENTATION_ITEM ( )  RATIONAL_B_SPLINE_CURVE ( ( 0.9999999999999983347, 0.9238795325112884038, 1.000000000000000000, 0.9238795325112867385, 1.000000000000000000, 0.9238795325112867385, 1.000000000000000000, 0.9238795325112867385, 1.000000000000000000 ) ) 
 REPRESENTATION_ITEM ( '' )  );
#34885=CARTESIAN_POINT ( 'NONE',  ( 4.898587196589412829E-16, 6.187499995903221084, -8.000000000000000000 ) ) ;
#34896=CARTESIAN_POINT ( 'NONE',  ( -7.188101187500002709, 24.18749999795161543, 2.977408999572649151 ) ) ;
#34905=CARTESIAN_POINT ( 'NONE',  ( 4.401442555609581635E-16, 9.843749997951610098, -7.188101187500000044 ) ) ;
#34908=CARTESIAN_POINT ( 'NONE',  ( -2.977408999572654480, 7.874999997951610986, 7.188101187499999156 ) ) ;
#34911=EDGE_CURVE ( 'NONE', #60299, #50014, #29339, .T. ) ;
#34920=CARTESIAN_POINT ( 'NONE',  ( 5.082755093536326818, 115.7187500020483810, 5.082755093536325042 ) ) ;
#34923=VERTEX_POINT ( 'NONE', #27863 ) ;
#34924=CARTESIAN_POINT ( 'NONE',  ( 7.188101187500000933, 18.56249999795161187, -2.977408999572650483 ) ) ;
#34929=CARTESIAN_POINT ( 'NONE',  ( 5.082755093536326818, 107.0937500020483810, 5.082755093536325042 ) ) ;
#34932=CARTESIAN_POINT ( 'NONE',  ( -3.313708498984842432, 111.4062500040967763, -7.999999999999920064 ) ) ;
#34934=VERTEX_POINT ( 'NONE', #50873 ) ;
#34943=CARTESIAN_POINT ( 'NONE',  ( 3.313708498984819339, 90.96875000000000000, 7.999999999999943157 ) ) ;
#34956=CARTESIAN_POINT ( 'NONE',  ( -5.082755093536324154, 115.3437500020483810, 5.082755093536326818 ) ) ;
#34981=CARTESIAN_POINT ( 'NONE',  ( 3.999982273345623174, 89.99927424231840689, -6.928213464733948612 ) ) ;
#34988=CARTESIAN_POINT ( 'NONE',  ( 2.977408999572650927, 8.624999997951611874, -7.188101187500000933 ) ) ;
#34993=CARTESIAN_POINT ( 'NONE',  ( 5.656854249492381470, 122.7500000040967905, 5.656854249492379694 ) ) ;
#34994=CARTESIAN_POINT ( 'NONE',  ( -4.898587196589412829E-16, 94.81250000409677625, -8.000000000000000000 ) ) ;
#35007=CARTESIAN_POINT ( 'NONE',  ( 5.656854249492380582, 16.68750000000000355, -5.656854249492380582 ) ) ;
#35008=ORIENTED_EDGE ( 'NONE', *, *, #23238, .F. ) ;
#35009=CARTESIAN_POINT ( 'NONE',  ( -3.313708498984762052, 88.90625000409677625, -8.000000000000000000 ) ) ;
#35031=CARTESIAN_POINT ( 'NONE',  ( -4.898587196589412829E-16, 120.3125000040967763, -8.000000000000000000 ) ) ;
#35044=CARTESIAN_POINT ( 'NONE',  ( 7.188101187500000044, 24.84374999795161543, 0.000000000000000000 ) ) ;
#35046=CARTESIAN_POINT ( 'NONE',  ( 7.188101187500002709, 95.18750000204838102, 2.977408999572649151 ) ) ;
#35054=CARTESIAN_POINT ( 'NONE',  ( -3.313708498984796691, 119.4687500040968047, 7.999999999999965361 ) ) ;
#35055=ORIENTED_EDGE ( 'NONE', *, *, #14492, .F. ) ;
#35062=CARTESIAN_POINT ( 'NONE',  ( 5.082755093536326818, 93.21875000204838102, 5.082755093536325042 ) ) ;
#35068=CARTESIAN_POINT ( 'NONE',  ( 7.188101187500002709, 96.68750000204836681, 2.977408999572649151 ) ) ;
#35075=DIRECTION ( 'NONE',  ( -0.000000000000000000, 1.000000000000000000, -0.000000000000000000 ) ) ;
#35079=CARTESIAN_POINT ( 'NONE',  ( -8.000000000000000000, 10.96874999590322020, -3.313708498984762496 ) ) ;
#35082=CIRCLE ( 'NONE', #8542, 8.000000000000000000 ) ;
#35087=( BOUNDED_CURVE ( )  B_SPLINE_CURVE ( 2, ( #7185, #6811, #69074, #435, #41874, #23044, #29824, #57770, #1542 ),
 .UNSPECIFIED., .F., .F. ) 
 B_SPLINE_CURVE_WITH_KNOTS ( ( 3, 2, 2, 2, 3 ),
 ( 0.1250000000000000000, 0.1319444444444444475, 0.1388888888888888951, 0.1458333333333333426, 0.1527777777777777901 ),
 .UNSPECIFIED. ) 
 CURVE ( )  GEOMETRIC_REPRESENTATION_ITEM ( )  RATIONAL_B_SPLINE_CURVE ( ( 1.000000000000000000, 0.9238795325112867385, 1.000000000000000000, 0.9238795325112867385, 1.000000000000000000, 0.9238795325112867385, 1.000000000000000000, 0.9238795325112867385, 1.000000000000000000 ) ) 
 REPRESENTATION_ITEM ( '' )  );
#35088=CARTESIAN_POINT ( 'NONE',  ( -3.313708498984760276, 3.281249995903220640, -8.000000000000000000 ) ) ;
#35091=CARTESIAN_POINT ( 'NONE',  ( 3.313708498984760720, 102.2187500040967905, -8.000000000000000000 ) ) ;
#35101=CARTESIAN_POINT ( 'NONE',  ( 5.082755093536326818, 105.2187500020483952, 5.082755093536325042 ) ) ;
#35118=CARTESIAN_POINT ( 'NONE',  ( 8.000000000000001776, 100.1562500000000000, 3.313708498984759387 ) ) ;
#35124=CARTESIAN_POINT ( 'NONE',  ( 2.977408999572651815, 3.562499997951610542, 7.188101187500000933 ) ) ;
#35128=CARTESIAN_POINT ( 'NONE',  ( 7.188101187500000044, 117.7812500020483810, -8.802885111219163269E-16 ) ) ;
#35149=CARTESIAN_POINT ( 'NONE',  ( 7.188101187500002709, 112.8125000020483952, 2.977408999572649151 ) ) ;
#35154=CARTESIAN_POINT ( 'NONE',  ( 1.320432766682874540E-15, 115.9062500020483810, 7.188101187500000044 ) ) ;
#35155=CARTESIAN_POINT ( 'NONE',  ( 1.469576158976823947E-15, 121.0625000040967763, 8.000000000000000000 ) ) ;
#35160=CARTESIAN_POINT ( 'NONE',  ( 3.313708498984765161, 107.4687500000000000, 7.999999999999998224 ) ) ;
#35179=CARTESIAN_POINT ( 'NONE',  ( -1.469576158976823947E-15, 4.125000000000000888, 8.000000000000000000 ) ) ;
#35180=CARTESIAN_POINT ( 'NONE',  ( -5.656854249492380582, 106.8125000000000000, -5.656854249492380582 ) ) ;
#35181=CARTESIAN_POINT ( 'NONE',  ( 5.082755093536324154, 24.65624999795161543, 5.082755093536326818 ) ) ;
#35182=CARTESIAN_POINT ( 'NONE',  ( -8.000000000000000000, 122.1875000040967763, 0.000000000000000000 ) ) ;
#35185=FACE_OUTER_BOUND ( 'NONE', #70663, .T. ) ;
#35207=CARTESIAN_POINT ( 'NONE',  ( 3.313708498984760720, 115.5312500000000142, -8.000000000000000000 ) ) ;
#35213=CARTESIAN_POINT ( 'NONE',  ( -8.000000000000000000, 14.06249999590322375, -9.797174393178825657E-16 ) ) ;
#35236=CARTESIAN_POINT ( 'NONE',  ( 5.082755093536326818, 97.71875000204838102, 5.082755093536325042 ) ) ;
#35239=CARTESIAN_POINT ( 'NONE',  ( 4.850062511589654031E-16, 0.4207531754730554074, -7.920753175473053354 ) ) ;
#35260=CARTESIAN_POINT ( 'NONE',  ( 4.898587196589412829E-16, 9.187499995903221972, -8.000000000000000000 ) ) ;
#35268=EDGE_CURVE ( 'NONE', #64829, #61351, #60990, .T. ) ;
#35270=CARTESIAN_POINT ( 'NONE',  ( -7.188101187500002709, 17.81249999795161543, 2.977408999572649151 ) ) ;
#35273=CARTESIAN_POINT ( 'NONE',  ( -5.082755093536326818, 4.781249997951610986, 5.082755093536325042 ) ) ;
#35281=UNCERTAINTY_MEASURE_WITH_UNIT (LENGTH_MEASURE( 1.000000000000000082E-05 ), #55498, 'distance_accuracy_value', 'NONE');
#35286=CARTESIAN_POINT ( 'NONE',  ( -4.401442555609581635E-16, 116.2812500020483810, -7.188101187500000044 ) ) ;
#35289=VERTEX_POINT ( 'NONE', #59877 ) ;
#35290=CARTESIAN_POINT ( 'NONE',  ( -7.188101187500000933, 19.12499999795161898, -2.977408999572651371 ) ) ;
#35294=CARTESIAN_POINT ( 'NONE',  ( 5.082755093536326818, 101.0937500020483810, 5.082755093536325042 ) ) ;
#35298=CARTESIAN_POINT ( 'NONE',  ( -5.656854249492378806, 95.37500000409677625, 5.656854249492381470 ) ) ;
#35302=CARTESIAN_POINT ( 'NONE',  ( 1.469576158976823947E-15, 107.5625000040967905, 8.000000000000000000 ) ) ;
#35327=CARTESIAN_POINT ( 'NONE',  ( -7.188101187499999156, 113.7500000020483668, 2.977408999572654924 ) ) ;
#35335=CARTESIAN_POINT ( 'NONE',  ( -2.977408999572654480, 23.99999999795161543, 7.188101187499999156 ) ) ;
#35356=CARTESIAN_POINT ( 'NONE',  ( -7.188101187500000933, 8.999999997951611874, -2.977408999572651371 ) ) ;
#35366=CARTESIAN_POINT ( 'NONE',  ( -8.000000000000000000, 93.68750000409679046, 0.000000000000000000 ) ) ;
#35372=EDGE_CURVE ( 'NONE', #48435, #59499, #67453, .T. ) ;
#35374=CARTESIAN_POINT ( 'NONE',  ( 5.656854249492380582, 15.18750000000000355, -5.656854249492380582 ) ) ;
#35375=ORIENTED_EDGE ( 'NONE', *, *, #68008, .T. ) ;
#35377=CARTESIAN_POINT ( 'NONE',  ( -7.188101187500000044, 119.6562500020483810, 0.000000000000000000 ) ) ;
#35380=CARTESIAN_POINT ( 'NONE',  ( -8.000000000000000000, 8.250000000000001776, -9.797174393178825657E-16 ) ) ;
#35383=CARTESIAN_POINT ( 'NONE',  ( 3.313708498984846429, 113.4687500000000000, 7.999999999999918288 ) ) ;
#35384=LINE ( 'NONE', #6701, #34250 ) ;
#35385=CARTESIAN_POINT ( 'NONE',  ( 1.320432766682874540E-15, 120.4062500020483810, 7.188101187500000044 ) ) ;
#35405=( BOUNDED_CURVE ( )  B_SPLINE_CURVE ( 2, ( #44496, #32820, #73907, #15432, #38470, #61846, #45238, #61473, #55829 ),
 .UNSPECIFIED., .F., .T. ) 
 B_SPLINE_CURVE_WITH_KNOTS ( ( 3, 2, 2, 2, 3 ),
 ( 0.6805555555555554692, 0.6874999999999998890, 0.6944444444444443088, 0.7013888888888887285, 0.7083333333333332593 ),
 .UNSPECIFIED. ) 
 CURVE ( )  GEOMETRIC_REPRESENTATION_ITEM ( )  RATIONAL_B_SPLINE_CURVE ( ( 1.000000000000001110, 0.9238795325112855172, 1.000000000000000000, 0.9238795325112867385, 1.000000000000000000, 0.9238795325112867385, 1.000000000000000000, 0.9238795325112879597, 0.9999999999999987788 ) ) 
 REPRESENTATION_ITEM ( '' )  );
#35412=CARTESIAN_POINT ( 'NONE',  ( 5.082755093536324154, 23.15624999795161543, 5.082755093536326818 ) ) ;
#35414=CARTESIAN_POINT ( 'NONE',  ( 7.188101187500000933, 98.37500000204839523, -2.977408999572651371 ) ) ;
#35420=EDGE_CURVE ( 'NONE', #10908, #71473, #42141, .T. ) ;
#35424=CARTESIAN_POINT ( 'NONE',  ( -7.594050593750000466, 124.7656250010242047, 0.000000000000000000 ) ) ;
#35435=CARTESIAN_POINT ( 'NONE',  ( 2.977408999572654480, 98.00000000204838102, 7.188101187499999156 ) ) ;
#35442=CYLINDRICAL_SURFACE ( 'NONE', #36419, 8.000000000000000000 ) ;
#35454=CARTESIAN_POINT ( 'NONE',  ( -3.313708498984762052, 105.4062500040967763, -8.000000000000000000 ) ) ;
#35462=CARTESIAN_POINT ( 'NONE',  ( -8.000000000000000000, 24.65625000000000355, -3.313708498984762496 ) ) ;
#35463=CARTESIAN_POINT ( 'NONE',  ( -4.401442555609581635E-16, 104.2812500020483810, -7.188101187500000044 ) ) ;
#35464=EDGE_CURVE ( 'NONE', #34267, #69918, #44752, .T. ) ;
#35476=DIRECTION ( 'NONE',  ( 0.000000000000000000, 0.000000000000000000, 1.000000000000000000 ) ) ;
#35480=CARTESIAN_POINT ( 'NONE',  ( -8.000000000000000000, 98.00000000000000000, 0.000000000000000000 ) ) ;
#35485=CARTESIAN_POINT ( 'NONE',  ( 5.082755093536325930, 4.031249997951610986, -5.082755093536325930 ) ) ;
#35489=CARTESIAN_POINT ( 'NONE',  ( -4.401442555609581635E-16, 116.6562500020483810, -7.188101187500000044 ) ) ;
#35490=FACE_OUTER_BOUND ( 'NONE', #10573, .T. ) ;
#35509=CARTESIAN_POINT ( 'NONE',  ( 2.977408999572654480, 108.1250000020483810, 7.188101187499999156 ) ) ;
#35514=CARTESIAN_POINT ( 'NONE',  ( 5.082755093536326818, 116.0937500020483810, 5.082755093536325042 ) ) ;
#35523=CARTESIAN_POINT ( 'NONE',  ( 4.898587196589412829E-16, 18.18749999590322020, -8.000000000000000000 ) ) ;
#35527=EDGE_CURVE ( 'NONE', #4846, #54330, #33837, .T. ) ;
#35528=DIRECTION ( 'NONE',  ( -0.000000000000000000, 1.000000000000000000, -0.000000000000000000 ) ) ;
#35539=ORIENTED_EDGE ( 'NONE', *, *, #8071, .T. ) ;
#35540=CARTESIAN_POINT ( 'NONE',  ( -8.000000000000000000, 3.656250000000000888, -3.313708498984762496 ) ) ;
#35542=CARTESIAN_POINT ( 'NONE',  ( -7.188101187500002709, 2.812499997951610098, 2.977408999572649151 ) ) ;
#35544=CARTESIAN_POINT ( 'NONE',  ( 8.000000000000001776, 122.8437500040967763, 3.313708498984759387 ) ) ;
#35567=CARTESIAN_POINT ( 'NONE',  ( -5.656854249492378806, 117.6875000000000000, 5.656854249492381470 ) ) ;
#35571=VERTEX_POINT ( 'NONE', #991 ) ;
#35573=CARTESIAN_POINT ( 'NONE',  ( 3.313708498984762052, 16.59374999590322020, -8.000000000000000000 ) ) ;
#35598=STYLED_ITEM('',(#74706),#67548);
#35599=CARTESIAN_POINT ( 'NONE',  ( 5.082755093536325042, 99.59375000204838102, -5.082755093536325930 ) ) ;
#35602=CARTESIAN_POINT ( 'NONE',  ( 5.303777043537039049, 0.3075051904528932623, -5.735125114186721440 ) ) ;
#35604=ORIENTED_EDGE ( 'NONE', *, *, #27395, .T. ) ;
#35616=CARTESIAN_POINT ( 'NONE',  ( 5.656854249492378806, 17.62499999590322375, 5.656854249492381470 ) ) ;
#35627=EDGE_CURVE ( 'NONE', #10862, #73500, #9062, .T. ) ;
#35628=CARTESIAN_POINT ( 'NONE',  ( -7.188101187500002709, 13.31249999795161187, 2.977408999572649151 ) ) ;
#35631=CARTESIAN_POINT ( 'NONE',  ( 7.188101187500000044, 5.343749997951610098, 0.000000000000000000 ) ) ;
#35633=( BOUNDED_CURVE ( )  B_SPLINE_CURVE ( 2, ( #10682, #33715, #57467, #24124, #18476, #47503, #41852, #13165, #5035 ),
 .UNSPECIFIED., .F., .F. ) 
 B_SPLINE_CURVE_WITH_KNOTS ( ( 3, 2, 2, 2, 3 ),
 ( 0.5312500000000000000, 0.5364583333333333703, 0.5416666666666665186, 0.5468749999999998890, 0.5520833333333332593 ),
 .UNSPECIFIED. ) 
 CURVE ( )  GEOMETRIC_REPRESENTATION_ITEM ( )  RATIONAL_B_SPLINE_CURVE ( ( 1.000000000000000000, 0.9238795325112867385, 1.000000000000000000, 0.9238795325112867385, 1.000000000000000000, 0.9238795325112867385, 1.000000000000000000, 0.9238795325112884038, 0.9999999999999983347 ) ) 
 REPRESENTATION_ITEM ( '' )  );
#35636=DIRECTION ( 'NONE',  ( 0.000000000000000000, -1.000000000000000000, 0.000000000000000000 ) ) ;
#35645=CARTESIAN_POINT ( 'NONE',  ( 7.188101187500001821, 117.5000000020483810, -2.977408999572651371 ) ) ;
#35649=CARTESIAN_POINT ( 'NONE',  ( -7.188101187500000933, 23.62499999795161543, -2.977408999572651371 ) ) ;
#35652=CARTESIAN_POINT ( 'NONE',  ( -1.469576158976823947E-15, 13.12500000000000355, 8.000000000000000000 ) ) ;
#35654=CARTESIAN_POINT ( 'NONE',  ( 2.977408999572654480, 98.00000000204838102, 7.188101187499999156 ) ) ;
#35673=CARTESIAN_POINT ( 'NONE',  ( -8.000000000000000000, 117.5000000000000000, 0.000000000000000000 ) ) ;
#35677=ORIENTED_EDGE ( 'NONE', *, *, #16099, .F. ) ;
#35684=CARTESIAN_POINT ( 'NONE',  ( -2.977408999572651815, 112.4375000020483810, 7.188101187500000933 ) ) ;
#35689=CARTESIAN_POINT ( 'NONE',  ( -8.000000000000000000, 24.56249999590322375, -9.797174393178825657E-16 ) ) ;
#35691=CARTESIAN_POINT ( 'NONE',  ( 8.000000000000000000, 92.93750000409679046, -9.797174393178825657E-16 ) ) ;
#35704=VECTOR ( 'NONE', #45012, 1000.000000000000227 ) ;
#35707=LINE ( 'NONE', #65093, #40927 ) ;
#35715=CARTESIAN_POINT ( 'NONE',  ( 7.188101187500000044, 9.843749997951610098, 0.000000000000000000 ) ) ;
#35731=CARTESIAN_POINT ( 'NONE',  ( 3.313708498984762496, 20.71875000000000355, 7.999999999999998224 ) ) ;
#35744=CARTESIAN_POINT ( 'NONE',  ( -7.188101187500000044, 120.0312500020483810, 0.000000000000000000 ) ) ;
#35771=CARTESIAN_POINT ( 'NONE',  ( 7.188101187499999156, 26.24999999795161898, 2.977408999572654924 ) ) ;
#35774=CARTESIAN_POINT ( 'NONE',  ( -7.188101187499999156, 100.6250000020483810, 2.977408999572654924 ) ) ;
#35785=LINE ( 'NONE', #65548, #60347 ) ;
#35796=CARTESIAN_POINT ( 'NONE',  ( -4.401442555609581635E-16, 98.65625000204838102, -7.188101187500000044 ) ) ;
#35803=CARTESIAN_POINT ( 'NONE',  ( 8.000000000000000000, 0.5000000000000004441, 0.000000000000000000 ) ) ;
#35809=CARTESIAN_POINT ( 'NONE',  ( -1.469576158976823947E-15, 11.43749999590322197, 8.000000000000000000 ) ) ;
#35812=ORIENTED_EDGE ( 'NONE', *, *, #32223, .F. ) ;
#35819=CARTESIAN_POINT ( 'NONE',  ( -5.656854249492380582, 105.5000000040967905, -5.656854249492380582 ) ) ;
#35828=CARTESIAN_POINT ( 'NONE',  ( -5.082755093536325930, 101.4687500020483810, -5.082755093536325930 ) ) ;
#35830=CARTESIAN_POINT ( 'NONE',  ( -7.999999999999998224, 92.28125000409679046, 3.313708498984766049 ) ) ;
#35852=CARTESIAN_POINT ( 'NONE',  ( -2.977408999572654480, 7.874999997951610986, 7.188101187499999156 ) ) ;
#35855=CARTESIAN_POINT ( 'NONE',  ( -7.188101187500000044, 114.0312500020483952, 0.000000000000000000 ) ) ;
#35865=CARTESIAN_POINT ( 'NONE',  ( 5.656854249492379694, 112.4375000000000000, -5.656854249492380582 ) ) ;
#35876=CARTESIAN_POINT ( 'NONE',  ( -2.977408999572650927, 102.8750000020483810, -7.188101187500000933 ) ) ;
#35882=CARTESIAN_POINT ( 'NONE',  ( 5.082755093536325042, 113.4687500020483810, -5.082755093536325930 ) ) ;
#35886=ORIENTED_EDGE ( 'NONE', *, *, #5578, .F. ) ;
#35891=CARTESIAN_POINT ( 'NONE',  ( -8.000000000000000000, 108.4062500000000000, -3.313708498984761164 ) ) ;
#35908=CARTESIAN_POINT ( 'NONE',  ( -8.000000000000000000, 5.156250000000000888, -3.313708498984762496 ) ) ;
#35910=CARTESIAN_POINT ( 'NONE',  ( -2.977408999572654480, 2.999999997951610542, 7.188101187499999156 ) ) ;
#35911=CARTESIAN_POINT ( 'NONE',  ( -8.000000000000000000, 123.6875000040967905, 0.000000000000000000 ) ) ;
#35913=DIRECTION ( 'NONE',  ( -0.000000000000000000, 1.000000000000000000, -0.000000000000000000 ) ) ;
#35935=CARTESIAN_POINT ( 'NONE',  ( 5.656854249492381470, 121.0625000000000000, 5.656854249492379694 ) ) ;
#35939=CARTESIAN_POINT ( 'NONE',  ( -8.000000000000000000, 16.96874999590322730, -3.313708498984762496 ) ) ;
#35941=CARTESIAN_POINT ( 'NONE',  ( 5.656854249492380582, 11.99999999590322197, -5.656854249492380582 ) ) ;
#35951=CARTESIAN_POINT ( 'NONE',  ( -3.313708498984707429, 99.40625000409677625, -8.000000000000055067 ) ) ;
#35953=VERTEX_POINT ( 'NONE', #42077 ) ;
#35967=CARTESIAN_POINT ( 'NONE',  ( 7.188101187500001821, 99.50000000204838102, -2.977408999572651371 ) ) ;
#35970=CARTESIAN_POINT ( 'NONE',  ( 2.012362677162108593, 0.3822906927398848076, -7.638045755507497425 ) ) ;
#35985=EDGE_LOOP ( 'NONE', ( #8212, #5223, #62380, #38288 ) ) ;
#35998=CARTESIAN_POINT ( 'NONE',  ( 5.082755093536325930, 12.65624999795161187, -5.082755093536325930 ) ) ;
#36000=ADVANCED_FACE ( 'NONE', ( #8873 ), #31886, .F. ) ;
#36001=CARTESIAN_POINT ( 'NONE',  ( -2.977408999572654480, 12.37499999795161010, 7.188101187499999156 ) ) ;
#36013=CARTESIAN_POINT ( 'NONE',  ( 7.188101187500002709, 114.3125000020483952, 2.977408999572649151 ) ) ;
#36014=CARTESIAN_POINT ( 'NONE',  ( 9.797174393178825657E-16, 125.0000000000000000, -8.000000000000000000 ) ) ;
#36017=CARTESIAN_POINT ( 'NONE',  ( 5.082755093536325930, 26.15624999795161543, -5.082755093536325930 ) ) ;
#36024=CARTESIAN_POINT ( 'NONE',  ( -5.082755093536324154, 100.7187500020483810, 5.082755093536326818 ) ) ;
#36045=LINE ( 'NONE', #18690, #56293 ) ;
#36049=CYLINDRICAL_SURFACE ( 'NONE', #16661, 11.00000000000000000 ) ;
#36052=CARTESIAN_POINT ( 'NONE',  ( -7.232528283688802517, 124.7618676830046098, -2.762902653109465145 ) ) ;
#36054=CARTESIAN_POINT ( 'NONE',  ( -5.082755093536325930, 114.9687500020483810, -5.082755093536325930 ) ) ;
#36058=DIRECTION ( 'NONE',  ( -0.000000000000000000, 1.000000000000000000, -0.000000000000000000 ) ) ;
#36061=CARTESIAN_POINT ( 'NONE',  ( 4.898587196589412829E-16, 4.687499995903220196, -8.000000000000000000 ) ) ;
#36065=VERTEX_POINT ( 'NONE', #16010 ) ;
#36071=FACE_OUTER_BOUND ( 'NONE', #7722, .T. ) ;
#36075=( BOUNDED_CURVE ( )  B_SPLINE_CURVE ( 2, ( #62728, #41946, #65327, #47598, #25325, #70620, #37409, #54019, #36670 ),
 .UNSPECIFIED., .F., .F. ) 
 B_SPLINE_CURVE_WITH_KNOTS ( ( 3, 2, 2, 2, 3 ),
 ( 0.4027777777777777901, 0.4097222222222222099, 0.4166666666666666852, 0.4236111111111111049, 0.4305555555555555802 ),
 .UNSPECIFIED. ) 
 CURVE ( )  GEOMETRIC_REPRESENTATION_ITEM ( )  RATIONAL_B_SPLINE_CURVE ( ( 1.000000000000000000, 0.9238795325112867385, 1.000000000000000000, 0.9238795325112867385, 1.000000000000000000, 0.9238795325112867385, 1.000000000000000000, 0.9238795325112867385, 1.000000000000000000 ) ) 
 REPRESENTATION_ITEM ( '' )  );
#36082=CARTESIAN_POINT ( 'NONE',  ( -2.977408999572650039, 13.31249999795161187, -7.188101187500000933 ) ) ;
#36095=DIRECTION ( 'NONE',  ( -0.000000000000000000, 1.000000000000000000, -0.000000000000000000 ) ) ;
#36100=CARTESIAN_POINT ( 'NONE',  ( -5.656854249492381470, 26.43750000000000355, 5.656854249492379694 ) ) ;
#36109=CARTESIAN_POINT ( 'NONE',  ( 7.188101187500000044, 6.468749997951610986, 0.000000000000000000 ) ) ;
#36111=CARTESIAN_POINT ( 'NONE',  ( -5.082755093536325930, 115.3437500020483810, -5.082755093536325930 ) ) ;
#36138=CARTESIAN_POINT ( 'NONE',  ( -1.320432766682874540E-15, 25.96874999795161543, 7.188101187500000044 ) ) ;
#36157=CARTESIAN_POINT ( 'NONE',  ( 1.320432766682874540E-15, 90.03125000204838102, 7.188101187500000044 ) ) ;
#36169=CARTESIAN_POINT ( 'NONE',  ( -8.000000000000000000, 122.0000000000000000, 0.000000000000000000 ) ) ;
#36179=EDGE_CURVE ( 'NONE', #68569, #10908, #70448, .T. ) ;
#36188=CARTESIAN_POINT ( 'NONE',  ( -8.000000000000000000, 96.59375000409677625, -3.313708498984761608 ) ) ;
#36189=ADVANCED_FACE ( 'NONE', ( #10733 ), #69567, .T. ) ;
#36197=CARTESIAN_POINT ( 'NONE',  ( -4.401442555609581635E-16, 101.2812500020483810, -7.188101187500000044 ) ) ;
#36214=CARTESIAN_POINT ( 'NONE',  ( 0.000000000000000000, 125.0000000000000000, 8.000000000000000000 ) ) ;
#36220=CARTESIAN_POINT ( 'NONE',  ( 7.188101187500000044, 6.843749997951610986, 0.000000000000000000 ) ) ;
#36223=CARTESIAN_POINT ( 'NONE',  ( -7.188101187500000933, 113.9375000020483952, -2.977408999572650483 ) ) ;
#36244=CARTESIAN_POINT ( 'NONE',  ( 7.188101187500000044, 108.4062500020483810, -8.802885111219163269E-16 ) ) ;
#36250=CARTESIAN_POINT ( 'NONE',  ( 7.188101187500001821, 110.3750000020484094, -2.977408999572651371 ) ) ;
#36266=EDGE_CURVE ( 'NONE', #25259, #55947, #25989, .T. ) ;
#36274=CARTESIAN_POINT ( 'NONE',  ( 5.656854249492378806, 7.312500000000000888, 5.656854249492381470 ) ) ;
#36275=CARTESIAN_POINT ( 'NONE',  ( -8.000000000000001776, 11.34375000000000178, 3.313708498984759387 ) ) ;
#36276=CARTESIAN_POINT ( 'NONE',  ( -2.977408999572650039, 3.937499997951610986, -7.188101187500001821 ) ) ;
#36277=CARTESIAN_POINT ( 'NONE',  ( -7.999999999999998224, 122.2812500040967763, 3.313708498984766493 ) ) ;
#36278=( BOUNDED_CURVE ( )  B_SPLINE_CURVE ( 2, ( #12690, #53810, #31154, #54186, #35366, #58378, #1036, #64393, #42472 ),
 .UNSPECIFIED., .F., .F. ) 
 B_SPLINE_CURVE_WITH_KNOTS ( ( 3, 2, 2, 2, 3 ),
 ( 0.8229166666666667407, 0.8281250000000001110, 0.8333333333333334814, 0.8385416666666668517, 0.8437500000000002220 ),
 .UNSPECIFIED. ) 
 CURVE ( )  GEOMETRIC_REPRESENTATION_ITEM ( )  RATIONAL_B_SPLINE_CURVE ( ( 0.9999999999999983347, 0.9238795325112884038, 1.000000000000000000, 0.9238795325112867385, 1.000000000000000000, 0.9238795325112867385, 1.000000000000000000, 0.9238795325112835188, 1.000000000000003331 ) ) 
 REPRESENTATION_ITEM ( '' )  );
#36289=( BOUNDED_CURVE ( )  B_SPLINE_CURVE ( 2, ( #36528, #64086, #25185, #65178, #24079, #29751, #64459, #48198, #64819 ),
 .UNSPECIFIED., .F., .F. ) 
 B_SPLINE_CURVE_WITH_KNOTS ( ( 3, 2, 2, 2, 3 ),
 ( 0.5520833333333332593, 0.5572916666666665186, 0.5625000000000000000, 0.5677083333333333703, 0.5729166666666666297 ),
 .UNSPECIFIED. ) 
 CURVE ( )  GEOMETRIC_REPRESENTATION_ITEM ( )  RATIONAL_B_SPLINE_CURVE ( ( 1.000000000000001554, 0.9238795325112850731, 1.000000000000000000, 0.9238795325112867385, 1.000000000000000000, 0.9238795325112867385, 1.000000000000000000, 0.9238795325112867385, 1.000000000000000000 ) ) 
 REPRESENTATION_ITEM ( '' )  );
#36303=CARTESIAN_POINT ( 'NONE',  ( -7.999999999999998224, 117.5937499999999858, 3.313708498984766493 ) ) ;
#36308=CARTESIAN_POINT ( 'NONE',  ( 3.313708498984762496, 17.53124999590322375, 7.999999999999998224 ) ) ;
#36336=CARTESIAN_POINT ( 'NONE',  ( -7.188101187500001821, 95.56250000204838102, -2.977408999572650483 ) ) ;
#36355=CARTESIAN_POINT ( 'NONE',  ( -2.977408999572654480, 27.37499999795161543, 7.188101187499999156 ) ) ;
#36362=CARTESIAN_POINT ( 'NONE',  ( -5.082755093536326818, 16.40624999795161543, 5.082755093536325042 ) ) ;
#36365=CARTESIAN_POINT ( 'NONE',  ( 5.082755093536324154, 9.656249997951610098, 5.082755093536326818 ) ) ;
#36377=CARTESIAN_POINT ( 'NONE',  ( 7.188101187500000044, 118.9062500020483810, -8.802885111219163269E-16 ) ) ;
#36381=( BOUNDED_CURVE ( )  B_SPLINE_CURVE ( 2, ( #8018, #52564, #69923, #70291, #18605, #41248, #69547, #17858, #14780 ),
 .UNSPECIFIED., .F., .F. ) 
 B_SPLINE_CURVE_WITH_KNOTS ( ( 3, 2, 2, 2, 3 ),
 ( 0.09722222222222220989, 0.1041666666666666574, 0.1111111111111111049, 0.1180555555555555525, 0.1250000000000000000 ),
 .UNSPECIFIED. ) 
 CURVE ( )  GEOMETRIC_REPRESENTATION_ITEM ( )  RATIONAL_B_SPLINE_CURVE ( ( 1.000000000000000222, 0.9238795325112866275, 1.000000000000000000, 0.9238795325112867385, 1.000000000000000000, 0.9238795325112867385, 1.000000000000000000, 0.9238795325112867385, 1.000000000000000000 ) ) 
 REPRESENTATION_ITEM ( '' )  );
#36382=CARTESIAN_POINT ( 'NONE',  ( 5.082755093536324154, 22.78124999795161187, 5.082755093536326818 ) ) ;
#36388=CARTESIAN_POINT ( 'NONE',  ( -5.082755093536325930, 101.8437500020483810, -5.082755093536325930 ) ) ;
#36392=ADVANCED_FACE ( 'NONE', ( #29575 ), #30678, .T. ) ;
#36395=VECTOR ( 'NONE', #74143, 1000.000000000000000 ) ;
#36408=CARTESIAN_POINT ( 'NONE',  ( -3.313708498984693218, 117.2187499999999858, -8.000000000000065725 ) ) ;
#36418=CARTESIAN_POINT ( 'NONE',  ( -8.000000000000000000, 4.968749995903221084, -3.313708498984762496 ) ) ;
#36419=AXIS2_PLACEMENT_3D ( 'NONE', #58453, #52778, #6760 ) ;
#36421=CARTESIAN_POINT ( 'NONE',  ( 2.977408999572650039, 114.6875000020484094, -7.188101187500001821 ) ) ;
#36438=CARTESIAN_POINT ( 'NONE',  ( 1.469576158976823947E-15, 94.06250000409677625, 8.000000000000000000 ) ) ;
#36450=CARTESIAN_POINT ( 'NONE',  ( -7.188101187500000044, 12.09374999795161187, -8.802885111219163269E-16 ) ) ;
#36453=ORIENTED_EDGE ( 'NONE', *, *, #34298, .T. ) ;
#36465=CARTESIAN_POINT ( 'NONE',  ( -3.313708498984760720, 22.96875000000000355, -8.000000000000000000 ) ) ;
#36467=ORIENTED_EDGE ( 'NONE', *, *, #67432, .F. ) ;
#36476=CARTESIAN_POINT ( 'NONE',  ( -5.082755093536326818, 2.906249997951610098, 5.082755093536325042 ) ) ;
#36480=CARTESIAN_POINT ( 'NONE',  ( 7.188101187500002709, 116.1875000020483952, 2.977408999572649151 ) ) ;
#36510=CARTESIAN_POINT ( 'NONE',  ( -7.188101187500000933, 92.93750000204839523, -2.977408999572650483 ) ) ;
#36526=CARTESIAN_POINT ( 'NONE',  ( -5.656854249492380582, 102.3125000000000000, -5.656854249492380582 ) ) ;
#36527=CARTESIAN_POINT ( 'NONE',  ( 5.656854249492378806, 23.62499999590322020, 5.656854249492381470 ) ) ;
#36528=CARTESIAN_POINT ( 'NONE',  ( -4.898587196589412829E-16, 103.8125000040967763, -8.000000000000000000 ) ) ;
#36533=CARTESIAN_POINT ( 'NONE',  ( 7.188101187500000044, 92.28125000204836681, -8.802885111219163269E-16 ) ) ;
#36553=CARTESIAN_POINT ( 'NONE',  ( 3.313708498984760720, 97.71875000409676204, -8.000000000000000000 ) ) ;
#36562=CARTESIAN_POINT ( 'NONE',  ( 2.977408999572650039, 96.68750000204836681, -7.188101187500001821 ) ) ;
#36563=CARTESIAN_POINT ( 'NONE',  ( -8.000000000000000000, 92.18750000409679046, 0.000000000000000000 ) ) ;
#36570=ORIENTED_EDGE ( 'NONE', *, *, #32142, .T. ) ;
#36584=CARTESIAN_POINT ( 'NONE',  ( 3.313708498984762496, 5.531249995903220196, 7.999999999999998224 ) ) ;
#36586=CARTESIAN_POINT ( 'NONE',  ( -5.082755093536325042, 10.40624999795161187, -5.082755093536325930 ) ) ;
#36589=CARTESIAN_POINT ( 'NONE',  ( 7.188101187500000044, 111.7812500020483810, -8.802885111219163269E-16 ) ) ;
#36610=CARTESIAN_POINT ( 'NONE',  ( 5.082755093536326818, 105.2187500020483952, 5.082755093536325042 ) ) ;
#36616=CARTESIAN_POINT ( 'NONE',  ( -7.188101187499999156, 111.1250000020483810, 2.977408999572654924 ) ) ;
#36619=AXIS2_PLACEMENT_3D ( 'NONE', #66238, #26992, #26615 ) ;
#36620=VERTEX_POINT ( 'NONE', #38208 ) ;
#36629=CARTESIAN_POINT ( 'NONE',  ( 7.188101187500000044, 0.8437499979516100979, 0.000000000000000000 ) ) ;
#36643=CARTESIAN_POINT ( 'NONE',  ( -1.469576158976823947E-15, 13.12500000000000355, 8.000000000000000000 ) ) ;
#36644=CARTESIAN_POINT ( 'NONE',  ( -5.656854249492379694, 11.06250000000000178, -5.656854249492380582 ) ) ;
#36645=CARTESIAN_POINT ( 'NONE',  ( 7.188101187499999156, 4.874999997951610098, 2.977408999572654924 ) ) ;
#36646=CARTESIAN_POINT ( 'NONE',  ( 5.656854249492381470, 113.7500000040967763, 5.656854249492379694 ) ) ;
#36649=CARTESIAN_POINT ( 'NONE',  ( -1.469576158976823947E-15, 7.125000000000000888, 8.000000000000000000 ) ) ;
#36656=CARTESIAN_POINT ( 'NONE',  ( -8.000000000000000000, 15.65625000000000355, -3.313708498984762496 ) ) ;
#36670=CARTESIAN_POINT ( 'NONE',  ( -1.469576158976823947E-15, 12.93749999590322197, 8.000000000000000000 ) ) ;
#36672=CARTESIAN_POINT ( 'NONE',  ( 8.000000000000001776, 113.6562500000000000, 3.313708498984759387 ) ) ;
#36677=CARTESIAN_POINT ( 'NONE',  ( -8.000000000000000000, 12.46874999590322197, -3.313708498984762496 ) ) ;
#36690=CARTESIAN_POINT ( 'NONE',  ( -3.313708498984708317, 107.4687500040968047, 8.000000000000053291 ) ) ;
#36691=ORIENTED_EDGE ( 'NONE', *, *, #15091, .T. ) ;
#36704=CARTESIAN_POINT ( 'NONE',  ( -7.188101187500000044, 124.5312500020483810, 0.000000000000000000 ) ) ;
#36719=CARTESIAN_POINT ( 'NONE',  ( -3.313708498984681672, 113.2812500000000142, 8.000000000000078160 ) ) ;
#36732=CARTESIAN_POINT ( 'NONE',  ( 2.977408999572650927, 17.24999999795162253, -7.188101187500001821 ) ) ;
#36734=CARTESIAN_POINT ( 'NONE',  ( -4.850062511589670794E-16, 124.5792468245269475, -7.920753175473082663 ) ) ;
#36735=CARTESIAN_POINT ( 'NONE',  ( 7.188101187500000044, 9.843749997951610098, 0.000000000000000000 ) ) ;
#36743=VERTEX_POINT ( 'NONE', #55194 ) ;
#36748=CARTESIAN_POINT ( 'NONE',  ( 2.977408999572650039, 110.1875000020483810, -7.188101187500001821 ) ) ;
#36752=CARTESIAN_POINT ( 'NONE',  ( -7.188101187500000933, 25.12499999795161543, -2.977408999572651371 ) ) ;
#36759=CARTESIAN_POINT ( 'NONE',  ( -4.401442555609581635E-16, 100.1562500020483810, -7.188101187500000044 ) ) ;
#36783=CARTESIAN_POINT ( 'NONE',  ( -8.000000000000000000, 8.062499995903221972, -9.797174393178825657E-16 ) ) ;
#36787=CARTESIAN_POINT ( 'NONE',  ( -6.719196256674477397, 124.7364742007443965, -3.922907429097691967 ) ) ;
#36789=CARTESIAN_POINT ( 'NONE',  ( -2.977408999572650927, 111.8750000020483668, -7.188101187500001821 ) ) ;
#36812=CARTESIAN_POINT ( 'NONE',  ( 5.656854249492379694, 112.6250000040967763, -5.656854249492380582 ) ) ;
#36816=CARTESIAN_POINT ( 'NONE',  ( -2.977408999572654480, 10.87499999795161187, 7.188101187499999156 ) ) ;
#36837=CARTESIAN_POINT ( 'NONE',  ( -3.313708498984765161, 25.03125000000000355, 7.999999999999998224 ) ) ;
#36848=CARTESIAN_POINT ( 'NONE',  ( 7.188101187500000933, 6.562499997951610986, -2.977408999572650483 ) ) ;
#36850=CARTESIAN_POINT ( 'NONE',  ( 2.977408999572650039, 118.0625000020483952, -7.188101187500001821 ) ) ;
#36862=CARTESIAN_POINT ( 'NONE',  ( -8.000000000000000000, 102.5000000000000000, 0.000000000000000000 ) ) ;
#36877=CARTESIAN_POINT ( 'NONE',  ( -7.188101187499999156, 93.12500000204838102, 2.977408999572654924 ) ) ;
#36901=CARTESIAN_POINT ( 'NONE',  ( -3.313708498984654138, 113.4687500040968047, 8.000000000000106581 ) ) ;
#36922=CARTESIAN_POINT ( 'NONE',  ( 3.313708498984765161, 97.15625000409677625, 7.999999999999998224 ) ) ;
#36930=CARTESIAN_POINT ( 'NONE',  ( 2.977408999572650039, 101.1875000020483810, -7.188101187500001821 ) ) ;
#36935=ORIENTED_EDGE ( 'NONE', *, *, #31191, .F. ) ;
#36951=CARTESIAN_POINT ( 'NONE',  ( 3.313708498984762052, 3.093749995903220196, -8.000000000000000000 ) ) ;
#36953=CARTESIAN_POINT ( 'NONE',  ( 4.401442555609581635E-16, 10.21874999795161187, -7.188101187500000044 ) ) ;
#36956=CARTESIAN_POINT ( 'NONE',  ( -7.188101187500000044, 112.5312500020483952, 0.000000000000000000 ) ) ;
#36969=DIRECTION ( 'NONE',  ( 0.000000000000000000, 0.000000000000000000, 1.000000000000000000 ) ) ;
#36970=EDGE_CURVE ( 'NONE', #72478, #51619, #13576, .T. ) ;
#36977=DIRECTION ( 'NONE',  ( 0.000000000000000000, 0.000000000000000000, 1.000000000000000000 ) ) ;
#36978=CARTESIAN_POINT ( 'NONE',  ( 7.188101187500000933, 107.0000000020483810, -2.977408999572651371 ) ) ;
#36982=EDGE_CURVE ( 'NONE', #14878, #32201, #10279, .T. ) ;
#36984=CARTESIAN_POINT ( 'NONE',  ( 1.320432766682874540E-15, 108.4062500020483810, 7.188101187500000044 ) ) ;
#37002=DIRECTION ( 'NONE',  ( 0.000000000000000000, -0.000000000000000000, -1.000000000000000000 ) ) ;
#37009=CARTESIAN_POINT ( 'NONE',  ( 3.313708498984762496, 13.21875000000000178, 7.999999999999998224 ) ) ;
#37011=CARTESIAN_POINT ( 'NONE',  ( -5.082755093536325042, 5.531249997951610986, -5.082755093536325930 ) ) ;
#37012=EDGE_CURVE ( 'NONE', #45576, #35289, #65288, .T. ) ;
#37013=CARTESIAN_POINT ( 'NONE',  ( -8.000000000000000000, 116.0937500040968189, -3.313708498984761608 ) ) ;
#37015=CARTESIAN_POINT ( 'NONE',  ( 0.000000000000000000, 125.0000000000000000, 0.000000000000000000 ) ) ;
#37023=CARTESIAN_POINT ( 'NONE',  ( -8.000000000000001776, 15.84375000000000355, 3.313708498984759387 ) ) ;
#37037=CARTESIAN_POINT ( 'NONE',  ( -4.898587196589412829E-16, 114.1250000000000000, -8.000000000000000000 ) ) ;
#37042=CARTESIAN_POINT ( 'NONE',  ( -5.656854249492381470, 23.24999999590322020, 5.656854249492379694 ) ) ;
#37046=CARTESIAN_POINT ( 'NONE',  ( -3.313708498984640816, 114.9687500040968047, 8.000000000000119016 ) ) ;
#37055=DIRECTION ( 'NONE',  ( 0.000000000000000000, 0.000000000000000000, 1.000000000000000000 ) ) ;
#37056=CARTESIAN_POINT ( 'NONE',  ( 4.898587196589412829E-16, 9.375000000000001776, -8.000000000000000000 ) ) ;
#37065=CARTESIAN_POINT ( 'NONE',  ( -2.977408999572652260, 122.9375000020483810, 7.188101187500000044 ) ) ;
#37070=CARTESIAN_POINT ( 'NONE',  ( -4.401442555609581635E-16, 89.28125000204838102, -7.188101187500000044 ) ) ;
#37074=ORIENTED_EDGE ( 'NONE', *, *, #4932, .F. ) ;
#37099=CARTESIAN_POINT ( 'NONE',  ( -1.320432766682874540E-15, 21.09374999795161543, 7.188101187500000044 ) ) ;
#37102=CARTESIAN_POINT ( 'NONE',  ( -5.082755093536325042, 10.40624999795161187, -5.082755093536325930 ) ) ;
#37107=EDGE_CURVE ( 'NONE', #3972, #2312, #39160, .T. ) ;
#37108=CARTESIAN_POINT ( 'NONE',  ( 0.000000000000000000, 125.0000000000000000, 0.000000000000000000 ) ) ;
#37114=CARTESIAN_POINT ( 'NONE',  ( 5.082755093536325042, 108.5937500020483810, -5.082755093536325930 ) ) ;
#37119=CARTESIAN_POINT ( 'NONE',  ( -5.082755093536325042, 20.53124999795161543, -5.082755093536325930 ) ) ;
#37126=CARTESIAN_POINT ( 'NONE',  ( 7.188101187500000044, 95.28125000204836681, -8.802885111219163269E-16 ) ) ;
#37149=ADVANCED_FACE ( 'NONE', ( #60001 ), #67164, .T. ) ;
#37155=CARTESIAN_POINT ( 'NONE',  ( -7.455611905271029904, 124.7772109312973328, -2.029970500747677598 ) ) ;
#37157=CARTESIAN_POINT ( 'NONE',  ( -4.401442555609581635E-16, 111.7812500020483810, -7.188101187500000044 ) ) ;
#37169=ORIENTED_EDGE ( 'NONE', *, *, #64424, .T. ) ;
#37180=( BOUNDED_CURVE ( )  B_SPLINE_CURVE ( 2, ( #6047, #68298, #39635, #29429, #56993, #23388, #27938, #22261, #62633 ),
 .UNSPECIFIED., .F., .F. ) 
 B_SPLINE_CURVE_WITH_KNOTS ( ( 3, 2, 2, 2, 3 ),
 ( 0.03125000000000002082, 0.03645833333333335646, 0.04166666666666669211, 0.04687500000000002776, 0.05208333333333337034 ),
 .UNSPECIFIED. ) 
 CURVE ( )  GEOMETRIC_REPRESENTATION_ITEM ( )  RATIONAL_B_SPLINE_CURVE ( ( 0.9999999999999996669, 0.9238795325112870716, 1.000000000000000000, 0.9238795325112867385, 1.000000000000000000, 0.9238795325112867385, 1.000000000000000000, 0.9238795325112861834, 1.000000000000000444 ) ) 
 REPRESENTATION_ITEM ( '' )  );
#37186=CARTESIAN_POINT ( 'NONE',  ( 4.401442555609581635E-16, 11.71874999795161010, -7.188101187500000044 ) ) ;
#37195=CARTESIAN_POINT ( 'NONE',  ( -2.977408999572654480, 1.499999997951610542, 7.188101187499999156 ) ) ;
#37204=CARTESIAN_POINT ( 'NONE',  ( 3.313708498984762052, 21.28125000000000711, -8.000000000000000000 ) ) ;
#37215=CARTESIAN_POINT ( 'NONE',  ( 7.188101187500000933, 8.062499997951611874, -2.977408999572650483 ) ) ;
#37219=CARTESIAN_POINT ( 'NONE',  ( 2.977408999572650039, 112.0625000020483810, -7.188101187500001821 ) ) ;
#37231=ORIENTED_EDGE ( 'NONE', *, *, #53613, .T. ) ;
#37233=CARTESIAN_POINT ( 'NONE',  ( -5.656854249492378806, 102.6875000000000000, 5.656854249492381470 ) ) ;
#37249=CARTESIAN_POINT ( 'NONE',  ( 5.082755093536325042, 93.96875000204838102, -5.082755093536325930 ) ) ;
#37261=CARTESIAN_POINT ( 'NONE',  ( -3.313708498984786033, 9.843749995903220196, 7.999999999999979572 ) ) ;
#37275=CARTESIAN_POINT ( 'NONE',  ( -4.401442555609581635E-16, 89.65625000204838102, -7.188101187500000044 ) ) ;
#37288=CARTESIAN_POINT ( 'NONE',  ( 5.656854249492378806, 2.624999995903220196, 5.656854249492381470 ) ) ;
#37296=CARTESIAN_POINT ( 'NONE',  ( 1.469576158976823947E-15, 100.0625000040967763, 8.000000000000000000 ) ) ;
#37305=CARTESIAN_POINT ( 'NONE',  ( -7.188101187499999156, 98.75000000204838102, 2.977408999572654924 ) ) ;
#37312=EDGE_CURVE ( 'NONE', #66661, #7158, #46731, .T. ) ;
#37314=ORIENTED_EDGE ( 'NONE', *, *, #40052, .F. ) ;
#37330=CARTESIAN_POINT ( 'NONE',  ( 5.082755093536325930, 11.53124999795161187, -5.082755093536325930 ) ) ;
#37332=CARTESIAN_POINT ( 'NONE',  ( -7.188101187500000044, 124.1562500020483810, 0.000000000000000000 ) ) ;
#37333=CARTESIAN_POINT ( 'NONE',  ( 1.320432766682874540E-15, 112.9062500020483952, 7.188101187500000044 ) ) ;
#37350=CARTESIAN_POINT ( 'NONE',  ( 7.188101187500002709, 100.8125000020484094, 2.977408999572649151 ) ) ;
#37356=CARTESIAN_POINT ( 'NONE',  ( -7.188101187500000044, 106.5312500020483810, 0.000000000000000000 ) ) ;
#37381=CARTESIAN_POINT ( 'NONE',  ( -5.082755093536325042, 10.03124999795161187, -5.082755093536325930 ) ) ;
#37382=CARTESIAN_POINT ( 'NONE',  ( -8.000000000000000000, 113.1875000040967763, 0.000000000000000000 ) ) ;
#37393=CARTESIAN_POINT ( 'NONE',  ( 5.656854249492381470, 95.56250000000000000, 5.656854249492379694 ) ) ;
#37397=SHAPE_REPRESENTATION_RELATIONSHIP ( 'NONE' , 'NONE' ,  #66259, #50744 ) ;
#37409=CARTESIAN_POINT ( 'NONE',  ( -5.656854249492381470, 12.74999999590322197, 5.656854249492379694 ) ) ;
#37414=CARTESIAN_POINT ( 'NONE',  ( -5.656854249492378806, 113.1875000000000000, 5.656854249492381470 ) ) ;
#37419=CARTESIAN_POINT ( 'NONE',  ( 5.656854249492380582, 23.99999999590322375, -5.656854249492380582 ) ) ;
#37422=CARTESIAN_POINT ( 'NONE',  ( 3.313708498984794915, 121.5312500000000000, -7.999999999999967137 ) ) ;
#37440=CARTESIAN_POINT ( 'NONE',  ( 5.082755093536326818, 121.7187500020483952, 5.082755093536325042 ) ) ;
#37446=CARTESIAN_POINT ( 'NONE',  ( -2.977408999572650927, 124.2500000020484094, -7.188101187500001821 ) ) ;
#37459=CARTESIAN_POINT ( 'NONE',  ( 5.656854249492379694, 103.4374999999999858, -5.656854249492380582 ) ) ;
#37473=CARTESIAN_POINT ( 'NONE',  ( -5.082755093536325042, 23.53124999795161543, -5.082755093536325930 ) ) ;
#37477=CARTESIAN_POINT ( 'NONE',  ( -7.188101187500002709, 9.187499997951611874, 2.977408999572649151 ) ) ;
#37490=CARTESIAN_POINT ( 'NONE',  ( 2.977408999572650039, 108.6875000020483952, -7.188101187500001821 ) ) ;
#37491=CARTESIAN_POINT ( 'NONE',  ( 3.313708498984711426, 94.15625000409679046, 8.000000000000053291 ) ) ;
#37504=CARTESIAN_POINT ( 'NONE',  ( -2.977408999572650927, 97.25000000204839523, -7.188101187500001821 ) ) ;
#37511=CARTESIAN_POINT ( 'NONE',  ( 8.000000000000000000, 12.00000000000000178, 0.000000000000000000 ) ) ;
#37525=ORIENTED_EDGE ( 'NONE', *, *, #3489, .F. ) ;
#37534=CARTESIAN_POINT ( 'NONE',  ( 2.977408999572650039, 110.1875000020483810, -7.188101187500001821 ) ) ;
#37539=CARTESIAN_POINT ( 'NONE',  ( -5.656854249492379694, 26.06250000000000711, -5.656854249492380582 ) ) ;
#37542=VECTOR ( 'NONE', #23423, 1000.000000000000000 ) ;
#37543=CARTESIAN_POINT ( 'NONE',  ( 8.000000000000000000, 27.00000000000000355, 0.000000000000000000 ) ) ;
#37558=EDGE_CURVE ( 'NONE', #31201, #832, #63724, .T. ) ;
#37562=CARTESIAN_POINT ( 'NONE',  ( -2.977408999572654480, 16.87499999795161543, 7.188101187499999156 ) ) ;
#37571=CARTESIAN_POINT ( 'NONE',  ( -1.320432766682874540E-15, 1.593749997951610098, 7.188101187500000044 ) ) ;
#37589=CARTESIAN_POINT ( 'NONE',  ( 2.977408999572650927, 3.749999997951610542, -7.188101187500000933 ) ) ;
#37593=CARTESIAN_POINT ( 'NONE',  ( 2.977408999572650039, 115.0625000020483952, -7.188101187500001821 ) ) ;
#37599=ORIENTED_EDGE ( 'NONE', *, *, #2962, .F. ) ;
#37600=EDGE_CURVE ( 'NONE', #1389, #66596, #15864, .T. ) ;
#37607=CARTESIAN_POINT ( 'NONE',  ( 4.898587196589412829E-16, 24.37500000000000355, -8.000000000000000000 ) ) ;
#37608=CARTESIAN_POINT ( 'NONE',  ( -5.656854249492380582, 91.81249999999998579, -5.656854249492380582 ) ) ;
#37618=CARTESIAN_POINT ( 'NONE',  ( -4.898587196589412829E-16, 100.6249999999999858, -8.000000000000000000 ) ) ;
#37624=CARTESIAN_POINT ( 'NONE',  ( 9.797174393178825657E-16, 125.0000000000000000, -8.000000000000000000 ) ) ;
#37626=CARTESIAN_POINT ( 'NONE',  ( -7.188101187499999156, 90.12500000204836681, 2.977408999572654924 ) ) ;
#37631=CARTESIAN_POINT ( 'NONE',  ( -7.999999999999998224, 96.59374999999998579, 3.313708498984766049 ) ) ;
#37634=EDGE_CURVE ( 'NONE', #65516, #3567, #70143, .T. ) ;
#37637=CARTESIAN_POINT ( 'NONE',  ( 7.188101187500001821, 17.06249999795161543, -2.977408999572650483 ) ) ;
#37647=CARTESIAN_POINT ( 'NONE',  ( 3.313708498984744732, 121.1562500040967905, 8.000000000000019540 ) ) ;
#37651=CARTESIAN_POINT ( 'NONE',  ( 5.082755093536325042, 92.46875000204838102, -5.082755093536325930 ) ) ;
#37661=CARTESIAN_POINT ( 'NONE',  ( 3.313708498984782924, 14.53124999590322197, 7.999999999999979572 ) ) ;
#37675=CARTESIAN_POINT ( 'NONE',  ( -7.999999999999998224, 95.28125000409677625, 3.313708498984766493 ) ) ;
#37676=EDGE_CURVE ( 'NONE', #34923, #9455, #2878, .T. ) ;
#37684=CARTESIAN_POINT ( 'NONE',  ( 0.000000000000000000, 125.0000000000000000, 0.000000000000000000 ) ) ;
#37685=CARTESIAN_POINT ( 'NONE',  ( 2.977408999572654480, 94.62500000204838102, 7.188101187499999156 ) ) ;
#37706=CARTESIAN_POINT ( 'NONE',  ( 4.898587196589412829E-16, 3.187499995903220640, -8.000000000000000000 ) ) ;
#37708=CARTESIAN_POINT ( 'NONE',  ( -2.977408999572654480, 13.87499999795161365, 7.188101187499999156 ) ) ;
#37711=CARTESIAN_POINT ( 'NONE',  ( -5.082755093536324154, 112.7187500020483810, 5.082755093536326818 ) ) ;
#37721=ADVANCED_FACE ( 'NONE', ( #60662 ), #66319, .T. ) ;
#37725=CARTESIAN_POINT ( 'NONE',  ( 4.898587196589412829E-16, 10.68749999590322020, -8.000000000000000000 ) ) ;
#37731=CARTESIAN_POINT ( 'NONE',  ( -7.188101187499999156, 100.2500000020483810, 2.977408999572654924 ) ) ;
#37737=CARTESIAN_POINT ( 'NONE',  ( 2.977408999572654480, 110.0000000020483668, 7.188101187499999156 ) ) ;
#37748=CARTESIAN_POINT ( 'NONE',  ( -2.977408999572650039, 2.812499997951610542, -7.188101187500000933 ) ) ;
#37765=CARTESIAN_POINT ( 'NONE',  ( -7.188101187500002709, 5.812499997951610986, 2.977408999572649151 ) ) ;
#37766=CARTESIAN_POINT ( 'NONE',  ( -4.898587196589412829E-16, 118.8125000040967763, -8.000000000000000000 ) ) ;
#37784=ORIENTED_EDGE ( 'NONE', *, *, #13491, .F. ) ;
#37792=CARTESIAN_POINT ( 'NONE',  ( -4.898587196589412829E-16, 109.6250000000000000, -8.000000000000000000 ) ) ;
#37795=ORIENTED_EDGE ( 'NONE', *, *, #59637, .F. ) ;
#37797=CARTESIAN_POINT ( 'NONE',  ( 3.313708498984762052, 22.59374999590322375, -8.000000000000000000 ) ) ;
#37807=CARTESIAN_POINT ( 'NONE',  ( 3.594042629939374400, 89.53052393364181683, -6.225082831242716885 ) ) ;
#37821=CARTESIAN_POINT ( 'NONE',  ( -2.977408999572652260, 116.9375000020483952, 7.188101187500000044 ) ) ;
#37826=CARTESIAN_POINT ( 'NONE',  ( -4.401442555609581635E-16, 124.1562500020483810, -7.188101187500000044 ) ) ;
#37844=CARTESIAN_POINT ( 'NONE',  ( 8.000000000000000000, 22.31249999590322375, 0.000000000000000000 ) ) ;
#37853=EDGE_LOOP ( 'NONE', ( #21629, #72939, #31045, #53692 ) ) ;
#37855=CARTESIAN_POINT ( 'NONE',  ( 7.188101187500000044, 22.96874999795161543, 0.000000000000000000 ) ) ;
#37858=CARTESIAN_POINT ( 'NONE',  ( 7.188101187500001821, 18.93749999795161187, -2.977408999572650483 ) ) ;
#37869=CARTESIAN_POINT ( 'NONE',  ( 7.188101187500001821, 113.0000000020483668, -2.977408999572651371 ) ) ;
#37880=CARTESIAN_POINT ( 'NONE',  ( 1.320432766682874540E-15, 93.40625000204838102, 7.188101187500000044 ) ) ;
#37891=CARTESIAN_POINT ( 'NONE',  ( 8.000000000000000000, 107.9375000040967905, -9.797174393178825657E-16 ) ) ;
#37901=CARTESIAN_POINT ( 'NONE',  ( 4.898587196589412829E-16, 16.87500000000000000, -8.000000000000000000 ) ) ;
#37907=CARTESIAN_POINT ( 'NONE',  ( -5.656854249492380582, 115.8125000000000000, -5.656854249492380582 ) ) ;
#37910=CARTESIAN_POINT ( 'NONE',  ( -4.401442555609581635E-16, 110.2812500020483810, -7.188101187500000044 ) ) ;
#37920=CARTESIAN_POINT ( 'NONE',  ( -5.656854249492378806, 99.68750000000000000, 5.656854249492381470 ) ) ;
#37927=CARTESIAN_POINT ( 'NONE',  ( -8.000000000000000000, 94.90624999999998579, -3.313708498984761164 ) ) ;
#37935=CARTESIAN_POINT ( 'NONE',  ( -7.188101187500000933, 20.99999999795161898, -2.977408999572651371 ) ) ;
#37939=ORIENTED_EDGE ( 'NONE', *, *, #823, .F. ) ;
#37946=CARTESIAN_POINT ( 'NONE',  ( -7.188101187500002709, 5.812499997951610986, 2.977408999572649151 ) ) ;
#37955=( BOUNDED_CURVE ( )  B_SPLINE_CURVE ( 2, ( #13750, #30392, #37539, #25821, #42438, #59804, #70389, #70747, #71846 ),
 .UNSPECIFIED., .F., .F. ) 
 B_SPLINE_CURVE_WITH_KNOTS ( ( 3, 2, 2, 2, 3 ),
 ( 0.9583333333333332593, 0.9652777777777776791, 0.9722222222222220989, 0.9791666666666665186, 0.9861111111111110494 ),
 .UNSPECIFIED. ) 
 CURVE ( )  GEOMETRIC_REPRESENTATION_ITEM ( )  RATIONAL_B_SPLINE_CURVE ( ( 1.000000000000001110, 0.9238795325112855172, 1.000000000000000000, 0.9238795325112867385, 1.000000000000000000, 0.9238795325112867385, 1.000000000000000000, 0.9238795325112879597, 0.9999999999999987788 ) ) 
 REPRESENTATION_ITEM ( '' )  );
#37966=CARTESIAN_POINT ( 'NONE',  ( -5.082755093536325042, 10.03124999795161187, -5.082755093536325930 ) ) ;
#37970=CARTESIAN_POINT ( 'NONE',  ( 2.977408999572650039, 113.5625000020483668, -7.188101187500001821 ) ) ;
#37979=CARTESIAN_POINT ( 'NONE',  ( 3.313708498984762496, 19.03124999590322375, 7.999999999999998224 ) ) ;
#37984=CARTESIAN_POINT ( 'NONE',  ( -3.313708498984762496, 96.78125000000000000, 7.999999999999998224 ) ) ;
#37996=CARTESIAN_POINT ( 'NONE',  ( 2.977408999572650927, 26.62499999795161543, -7.188101187500001821 ) ) ;
#38007=CARTESIAN_POINT ( 'NONE',  ( 5.082755093536324154, 21.28124999795161543, 5.082755093536326818 ) ) ;
#38008=CARTESIAN_POINT ( 'NONE',  ( -8.000000000000000000, 108.5937500040967763, -3.313708498984761164 ) ) ;
#38024=CYLINDRICAL_SURFACE ( 'NONE', #31633, 8.000000000000000000 ) ;
#38038=ORIENTED_EDGE ( 'NONE', *, *, #21051, .F. ) ;
#38043=ORIENTED_EDGE ( 'NONE', *, *, #26854, .F. ) ;
#38044=CARTESIAN_POINT ( 'NONE',  ( -7.999999999999998224, 89.28125000409677625, 3.313708498984766493 ) ) ;
#38048=ORIENTED_EDGE ( 'NONE', *, *, #33099, .F. ) ;
#38056=CARTESIAN_POINT ( 'NONE',  ( 5.082755093536325042, 90.59375000204838102, -5.082755093536325930 ) ) ;
#38063=CARTESIAN_POINT ( 'NONE',  ( -8.000000000000000000, 101.0937500040968047, -3.313708498984761164 ) ) ;
#38079=CARTESIAN_POINT ( 'NONE',  ( 5.656854249492380582, 10.49999999590322020, -5.656854249492380582 ) ) ;
#38082=CARTESIAN_POINT ( 'NONE',  ( -2.977408999572654480, 10.87499999795161187, 7.188101187499999156 ) ) ;
#38084=CARTESIAN_POINT ( 'NONE',  ( 5.656854249492378806, 7.312500000000000888, 5.656854249492381470 ) ) ;
#38085=CARTESIAN_POINT ( 'NONE',  ( 5.082755093536326818, 111.5937500020483810, 5.082755093536325042 ) ) ;
#38101=CARTESIAN_POINT ( 'NONE',  ( 2.977408999572654480, 99.12500000204838102, 7.188101187499999156 ) ) ;
#38108=CARTESIAN_POINT ( 'NONE',  ( -4.401442555609581635E-16, 103.1562500020483810, -7.188101187500000044 ) ) ;
#38114=ORIENTED_EDGE ( 'NONE', *, *, #3024, .T. ) ;
#38126=DIRECTION ( 'NONE',  ( 0.000000000000000000, 0.000000000000000000, 1.000000000000000000 ) ) ;
#38134=CARTESIAN_POINT ( 'NONE',  ( -1.320432766682874540E-15, 10.59374999795161187, 7.188101187500000044 ) ) ;
#38135=CARTESIAN_POINT ( 'NONE',  ( -5.656854249492380582, 114.5000000040967763, -5.656854249492380582 ) ) ;
#38137=VECTOR ( 'NONE', #35528, 1000.000000000000000 ) ;
#38145=ORIENTED_EDGE ( 'NONE', *, *, #33099, .T. ) ;
#38162=CARTESIAN_POINT ( 'NONE',  ( -3.313708498984762496, 111.7812500000000000, 7.999999999999998224 ) ) ;
#38169=CARTESIAN_POINT ( 'NONE',  ( -5.656854249492381470, 21.74999999590322375, 5.656854249492379694 ) ) ;
#38175=CARTESIAN_POINT ( 'NONE',  ( -8.000000000000000000, 114.6875000040967763, 0.000000000000000000 ) ) ;
#38192=CARTESIAN_POINT ( 'NONE',  ( -7.188101187500000933, 119.5625000020483810, -2.977408999572650483 ) ) ;
#38198=CARTESIAN_POINT ( 'NONE',  ( -5.082755093536325930, 89.46875000204838102, -5.082755093536325930 ) ) ;
#38204=EDGE_CURVE ( 'NONE', #9455, #4200, #67582, .T. ) ;
#38208=CARTESIAN_POINT ( 'NONE',  ( 9.797174393178825657E-16, 75.00000000000000000, -8.000000000000000000 ) ) ;
#38217=CARTESIAN_POINT ( 'NONE',  ( -7.188101187500000044, 124.5312500020483810, 0.000000000000000000 ) ) ;
#38224=CARTESIAN_POINT ( 'NONE',  ( 7.188101187500000044, 21.46874999795161543, 0.000000000000000000 ) ) ;
#38227=CARTESIAN_POINT ( 'NONE',  ( 2.977408999572651815, 20.06249999795161543, 7.188101187500000933 ) ) ;
#38250=CARTESIAN_POINT ( 'NONE',  ( 7.188101187500000044, 96.78125000204838102, -8.802885111219163269E-16 ) ) ;
#38256=EDGE_CURVE ( 'NONE', #28600, #28645, #39613, .T. ) ;
#38257=CARTESIAN_POINT ( 'NONE',  ( 1.469576158976823947E-15, 115.0625000040967905, 8.000000000000000000 ) ) ;
#38273=ORIENTED_EDGE ( 'NONE', *, *, #53263, .F. ) ;
#38281=CARTESIAN_POINT ( 'NONE',  ( -2.977408999572651815, 107.9375000020483810, 7.188101187500000933 ) ) ;
#38288=ORIENTED_EDGE ( 'NONE', *, *, #51817, .F. ) ;
#38309=CARTESIAN_POINT ( 'NONE',  ( 5.082755093536324154, 20.15624999795161543, 5.082755093536326818 ) ) ;
#38313=CARTESIAN_POINT ( 'NONE',  ( 8.000000000000000000, 90.03125000409679046, -3.313708498984762496 ) ) ;
#38317=CARTESIAN_POINT ( 'NONE',  ( 7.188101187499999156, 1.874999997951610098, 2.977408999572654924 ) ) ;
#38319=LINE ( 'NONE', #49631, #50959 ) ;
#38320=CARTESIAN_POINT ( 'NONE',  ( -5.082755093536325042, 1.406249997951610098, -5.082755093536325930 ) ) ;
#38331=AXIS2_PLACEMENT_3D ( 'NONE', #14671, #54691, #30557 ) ;
#38335=CARTESIAN_POINT ( 'NONE',  ( 7.188101187500000933, 14.06249999795161365, -2.977408999572650483 ) ) ;
#38339=CARTESIAN_POINT ( 'NONE',  ( 2.977408999572654480, 111.5000000020483810, 7.188101187499999156 ) ) ;
#38350=DIRECTION ( 'NONE',  ( -0.000000000000000000, 1.000000000000000000, -0.000000000000000000 ) ) ;
#38352=CARTESIAN_POINT ( 'NONE',  ( 3.313708498984760720, 93.03124999999998579, -8.000000000000000000 ) ) ;
#38379=CARTESIAN_POINT ( 'NONE',  ( -5.082755093536326818, 20.90624999795161543, 5.082755093536325042 ) ) ;
#38380=CARTESIAN_POINT ( 'NONE',  ( -3.313708498984708317, 108.9687500040967905, 8.000000000000053291 ) ) ;
#38384=LINE ( 'NONE', #27418, #28307 ) ;
#38417=CARTESIAN_POINT ( 'NONE',  ( 3.313708498984762052, 9.281250000000001776, -8.000000000000000000 ) ) ;
#38418=ORIENTED_EDGE ( 'NONE', *, *, #48641, .T. ) ;
#38419=CARTESIAN_POINT ( 'NONE',  ( 5.656854249492379694, 91.62500000409677625, -5.656854249492380582 ) ) ;
#38427=EDGE_CURVE ( 'NONE', #38665, #72478, #29477, .T. ) ;
#38430=CARTESIAN_POINT ( 'NONE',  ( -4.401442555609581635E-16, 95.28125000204836681, -7.188101187500000044 ) ) ;
#38439=EDGE_LOOP ( 'NONE', ( #33461, #16007, #60771, #56891 ) ) ;
#38443=FACE_OUTER_BOUND ( 'NONE', #59583, .T. ) ;
#38453=CARTESIAN_POINT ( 'NONE',  ( -8.000000000000000000, 9.468749995903223748, -3.313708498984762496 ) ) ;
#38454=VERTEX_POINT ( 'NONE', #54278 ) ;
#38456=CARTESIAN_POINT ( 'NONE',  ( 7.188101187500000044, 17.34374999795161543, 0.000000000000000000 ) ) ;
#38459=CARTESIAN_POINT ( 'NONE',  ( -5.082755093536324154, 103.7187500020483810, 5.082755093536326818 ) ) ;
#38465=CARTESIAN_POINT ( 'NONE',  ( 8.000000000000000000, 21.00000000000000355, 0.000000000000000000 ) ) ;
#38470=CARTESIAN_POINT ( 'NONE',  ( -8.000000000000000000, 20.06249999590322375, -9.797174393178825657E-16 ) ) ;
#38476=CARTESIAN_POINT ( 'NONE',  ( 2.977408999572654480, 100.6250000020483810, 7.188101187499999156 ) ) ;
#38483=CARTESIAN_POINT ( 'NONE',  ( -7.188101187500000044, 102.0312500020483810, 0.000000000000000000 ) ) ;
#38501=( BOUNDED_CURVE ( )  B_SPLINE_CURVE ( 2, ( #63280, #29343, #22541, #57650, #52721, #51978, #41030, #35383, #69324 ),
 .UNSPECIFIED., .F., .F. ) 
 B_SPLINE_CURVE_WITH_KNOTS ( ( 3, 2, 2, 2, 3 ),
 ( 0.3020833333333331483, 0.3072916666666665186, 0.3124999999999998335, 0.3177083333333331483, 0.3229166666666665186 ),
 .UNSPECIFIED. ) 
 CURVE ( )  GEOMETRIC_REPRESENTATION_ITEM ( )  RATIONAL_B_SPLINE_CURVE ( ( 1.000000000000002442, 0.9238795325112842960, 1.000000000000000000, 0.9238795325112867385, 1.000000000000000000, 0.9238795325112867385, 1.000000000000000000, 0.9238795325112891810, 0.9999999999999975575 ) ) 
 REPRESENTATION_ITEM ( '' )  );
#38512=CARTESIAN_POINT ( 'NONE',  ( 7.188101187499999156, 7.874999997951610986, 2.977408999572654924 ) ) ;
#38513=CARTESIAN_POINT ( 'NONE',  ( 8.000000000000000000, 112.4375000040967905, -9.797174393178825657E-16 ) ) ;
#38539=CARTESIAN_POINT ( 'NONE',  ( 5.656854249492379694, 104.9374999999999858, -5.656854249492380582 ) ) ;
#38544=CARTESIAN_POINT ( 'NONE',  ( 1.469576158976823947E-15, 103.0625000040967763, 8.000000000000000000 ) ) ;
#38548=CARTESIAN_POINT ( 'NONE',  ( 7.999999999999998224, 22.21874999590322375, 3.313708498984766493 ) ) ;
#38550=CARTESIAN_POINT ( 'NONE',  ( 7.188101187500000933, 123.8750000020483952, -2.977408999572651371 ) ) ;
#38572=CARTESIAN_POINT ( 'NONE',  ( -4.401442555609581635E-16, 117.7812500020483810, -7.188101187500000044 ) ) ;
#38578=CARTESIAN_POINT ( 'NONE',  ( -7.188101187500001821, 122.9375000020483810, -2.977408999572650483 ) ) ;
#38601=CARTESIAN_POINT ( 'NONE',  ( -5.082755093536325042, 19.03124999795161543, -5.082755093536325930 ) ) ;
#38604=CARTESIAN_POINT ( 'NONE',  ( 7.188101187500000044, 15.84374999795161365, 0.000000000000000000 ) ) ;
#38608=FACE_OUTER_BOUND ( 'NONE', #43657, .T. ) ;
#38619=CARTESIAN_POINT ( 'NONE',  ( 8.000000000000001776, 94.34375000409677625, 3.313708498984759387 ) ) ;
#38623=CARTESIAN_POINT ( 'NONE',  ( 2.977408999572652260, 27.18749999795161898, 7.188101187500000044 ) ) ;
#38630=CARTESIAN_POINT ( 'NONE',  ( 7.188101187500001821, 96.87500000204836681, -2.977408999572651371 ) ) ;
#38634=VERTEX_POINT ( 'NONE', #73082 ) ;
#38647=CARTESIAN_POINT ( 'NONE',  ( -4.898587196589412829E-16, 108.1250000000000000, -8.000000000000000000 ) ) ;
#38650=CARTESIAN_POINT ( 'NONE',  ( -1.469576158976823947E-15, 17.62500000000000000, 8.000000000000000000 ) ) ;
#38660=CARTESIAN_POINT ( 'NONE',  ( -7.188101187500000044, 106.1562500020483810, 0.000000000000000000 ) ) ;
#38665=VERTEX_POINT ( 'NONE', #21390 ) ;
#38686=CARTESIAN_POINT ( 'NONE',  ( -7.188101187500000933, 17.99999999795161543, -2.977408999572651371 ) ) ;
#38695=CARTESIAN_POINT ( 'NONE',  ( -5.082755093536325042, 4.031249997951610986, -5.082755093536325930 ) ) ;
#38698=CARTESIAN_POINT ( 'NONE',  ( -7.188101187500001821, 1.499999997951610098, -2.977408999572651371 ) ) ;
#38709=EDGE_CURVE ( 'NONE', #2312, #38953, #23743, .T. ) ;
#38713=CARTESIAN_POINT ( 'NONE',  ( -8.000000000000000000, 104.0000000000000000, 0.000000000000000000 ) ) ;
#38716=CARTESIAN_POINT ( 'NONE',  ( -7.188101187500000044, 8.718749997951611874, -8.802885111219163269E-16 ) ) ;
#38720=CARTESIAN_POINT ( 'NONE',  ( 7.188101187500001821, 114.8750000020483810, -2.977408999572651371 ) ) ;
#38730=CARTESIAN_POINT ( 'NONE',  ( 5.656854249492379694, 106.4374999999999858, -5.656854249492380582 ) ) ;
#38737=CARTESIAN_POINT ( 'NONE',  ( 1.469576158976823947E-15, 93.87499999999998579, 8.000000000000000000 ) ) ;
#38744=DIRECTION ( 'NONE',  ( -0.000000000000000000, 1.000000000000000000, -0.000000000000000000 ) ) ;
#38745=VERTEX_POINT ( 'NONE', #7613 ) ;
#38758=CARTESIAN_POINT ( 'NONE',  ( 3.313708498984922812, 93.03124999999998579, -7.999999999999837463 ) ) ;
#38759=CARTESIAN_POINT ( 'NONE',  ( 5.082755093536324154, 19.78124999795161543, 5.082755093536326818 ) ) ;
#38764=EDGE_LOOP ( 'NONE', ( #51674, #55406 ) ) ;
#38779=VERTEX_POINT ( 'NONE', #41574 ) ;
#38791=CARTESIAN_POINT ( 'NONE',  ( -8.000000000000001776, 14.34375000000000355, 3.313708498984759387 ) ) ;
#38794=CARTESIAN_POINT ( 'NONE',  ( 5.656854249492379694, 94.62500000409677625, -5.656854249492380582 ) ) ;
#38802=VERTEX_POINT ( 'NONE', #12886 ) ;
#38804=CARTESIAN_POINT ( 'NONE',  ( 5.082755093536326818, 91.71875000204838102, 5.082755093536325042 ) ) ;
#38825=CARTESIAN_POINT ( 'NONE',  ( -3.313708498984765161, 6.843749995903221084, 7.999999999999998224 ) ) ;
#38828=CARTESIAN_POINT ( 'NONE',  ( -2.977408999572654480, 15.37499999795161187, 7.188101187499999156 ) ) ;
#38830=CYLINDRICAL_SURFACE ( 'NONE', #15415, 8.000000000000000000 ) ;
#38831=CARTESIAN_POINT ( 'NONE',  ( -7.188101187500000933, 104.9375000020483810, -2.977408999572650483 ) ) ;
#38848=CARTESIAN_POINT ( 'NONE',  ( -4.401442555609581635E-16, 96.78125000204838102, -7.188101187500000044 ) ) ;
#38855=CARTESIAN_POINT ( 'NONE',  ( -2.977408999572651815, 100.8125000020484094, 7.188101187500000933 ) ) ;
#38879=CARTESIAN_POINT ( 'NONE',  ( 7.188101187500001821, 8.062499997951611874, -2.977408999572650483 ) ) ;
#38880=CARTESIAN_POINT ( 'NONE',  ( 8.000000000000001776, 107.8437500040967620, 3.313708498984759387 ) ) ;
#38890=ADVANCED_FACE ( 'NONE', ( #13620 ), #30254, .T. ) ;
#38897=ORIENTED_EDGE ( 'NONE', *, *, #3343, .F. ) ;
#38906=CARTESIAN_POINT ( 'NONE',  ( 5.656854249492381470, 109.0624999999999858, 5.656854249492379694 ) ) ;
#38913=CARTESIAN_POINT ( 'NONE',  ( -8.000000000000001776, 27.65624999590323085, 3.313708498984759387 ) ) ;
#38915=CARTESIAN_POINT ( 'NONE',  ( -2.977408999572652260, 123.3125000020483810, 7.188101187500000044 ) ) ;
#38927=CARTESIAN_POINT ( 'NONE',  ( 4.898587196589412829E-16, 15.18749999590322197, -8.000000000000000000 ) ) ;
#38935=CARTESIAN_POINT ( 'NONE',  ( -2.977408999572652260, 115.4375000020483810, 7.188101187500000044 ) ) ;
#38941=CARTESIAN_POINT ( 'NONE',  ( -2.977408999572650927, 118.2500000020483952, -7.188101187500001821 ) ) ;
#38953=VERTEX_POINT ( 'NONE', #9479 ) ;
#38964=CARTESIAN_POINT ( 'NONE',  ( 5.082755093536324154, 25.78124999795161543, 5.082755093536326818 ) ) ;
#38966=CARTESIAN_POINT ( 'NONE',  ( -2.977408999572650039, 19.31249999795161543, -7.188101187500001821 ) ) ;
#38984=ORIENTED_EDGE ( 'NONE', *, *, #9313, .T. ) ;
#38986=CARTESIAN_POINT ( 'NONE',  ( 1.469576158976823947E-15, 95.56250000409677625, 8.000000000000000000 ) ) ;
#38993=CARTESIAN_POINT ( 'NONE',  ( 8.197002254987593162, 89.35092984469676480, -3.567578555610324997 ) ) ;
#38996=ORIENTED_EDGE ( 'NONE', *, *, #29418, .T. ) ;
#38997=CARTESIAN_POINT ( 'NONE',  ( 1.469576158976823947E-15, 93.87499999999998579, 8.000000000000000000 ) ) ;
#39002=DIRECTION ( 'NONE',  ( -0.000000000000000000, 1.000000000000000000, -0.000000000000000000 ) ) ;
#39016=VECTOR ( 'NONE', #27235, 1000.000000000000000 ) ;
#39024=CARTESIAN_POINT ( 'NONE',  ( 2.977408999572650039, 102.6875000020483810, -7.188101187500001821 ) ) ;
#39042=CARTESIAN_POINT ( 'NONE',  ( -4.898587196589412829E-16, 112.8125000040967905, -8.000000000000000000 ) ) ;
#39045=ORIENTED_EDGE ( 'NONE', *, *, #37012, .T. ) ;
#39050=CARTESIAN_POINT ( 'NONE',  ( -5.082755093536326818, 19.78124999795161543, 5.082755093536325042 ) ) ;
#39055=ORIENTED_EDGE ( 'NONE', *, *, #8471, .F. ) ;
#39060=CARTESIAN_POINT ( 'NONE',  ( 7.188101187500000044, 7.968749997951610986, 0.000000000000000000 ) ) ;
#39063=CARTESIAN_POINT ( 'NONE',  ( 7.188101187499999156, 2.249999997951610098, 2.977408999572654924 ) ) ;
#39071=AXIS2_PLACEMENT_3D ( 'NONE', #18734, #70779, #25847 ) ;
#39075=CARTESIAN_POINT ( 'NONE',  ( 5.656854249492378806, 5.812500000000000888, 5.656854249492381470 ) ) ;
#39077=CARTESIAN_POINT ( 'NONE',  ( 2.977408999572652260, 12.18749999795161365, 7.188101187500000044 ) ) ;
#39081=CARTESIAN_POINT ( 'NONE',  ( -5.082755093536324154, 106.7187500020483952, 5.082755093536326818 ) ) ;
#39086=ORIENTED_EDGE ( 'NONE', *, *, #71956, .T. ) ;
#39096=CARTESIAN_POINT ( 'NONE',  ( -1.469576158976823947E-15, 8.437499995903221972, 8.000000000000000000 ) ) ;
#39098=CARTESIAN_POINT ( 'NONE',  ( -4.898587196589412829E-16, 96.12499999999998579, -8.000000000000000000 ) ) ;
#39110=CARTESIAN_POINT ( 'NONE',  ( -2.977408999572650927, 122.3750000020483952, -7.188101187500001821 ) ) ;
#39117=ORIENTED_EDGE ( 'NONE', *, *, #48476, .T. ) ;
#39118=CARTESIAN_POINT ( 'NONE',  ( 0.000000000000000000, 125.0000000000000000, 0.000000000000000000 ) ) ;
#39119=CARTESIAN_POINT ( 'NONE',  ( 5.082755093536325930, 21.65624999795161543, -5.082755093536325930 ) ) ;
#39141=EDGE_CURVE ( 'NONE', #65034, #21298, #37180, .T. ) ;
#39153=( BOUNDED_CURVE ( )  B_SPLINE_CURVE ( 2, ( #29878, #53635, #65309, #13610, #24575, #53264, #19281, #858, #36649 ),
 .UNSPECIFIED., .F., .F. ) 
 B_SPLINE_CURVE_WITH_KNOTS ( ( 3, 2, 2, 2, 3 ),
 ( 0.2361111111111111049, 0.2430555555555555525, 0.2500000000000000000, 0.2569444444444444198, 0.2638888888888888951 ),
 .UNSPECIFIED. ) 
 CURVE ( )  GEOMETRIC_REPRESENTATION_ITEM ( )  RATIONAL_B_SPLINE_CURVE ( ( 1.000000000000000000, 0.9238795325112867385, 1.000000000000000000, 0.9238795325112867385, 1.000000000000000000, 0.9238795325112867385, 1.000000000000000000, 0.9238795325112867385, 1.000000000000000000 ) ) 
 REPRESENTATION_ITEM ( '' )  );
#39156=CARTESIAN_POINT ( 'NONE',  ( -5.656854249492381470, 9.937500000000001776, 5.656854249492379694 ) ) ;
#39158=CARTESIAN_POINT ( 'NONE',  ( 5.656854249492381470, 94.25000000409677625, 5.656854249492379694 ) ) ;
#39160=( BOUNDED_CURVE ( )  B_SPLINE_CURVE ( 2, ( #47930, #24185, #70947, #19262, #7953, #29860, #29491, #52872, #18167 ),
 .UNSPECIFIED., .F., .F. ) 
 B_SPLINE_CURVE_WITH_KNOTS ( ( 3, 2, 2, 2, 3 ),
 ( 0.5416666666666666297, 0.5486111111111111605, 0.5555555555555555802, 0.5625000000000000000, 0.5694444444444444198 ),
 .UNSPECIFIED. ) 
 CURVE ( )  GEOMETRIC_REPRESENTATION_ITEM ( )  RATIONAL_B_SPLINE_CURVE ( ( 1.000000000000000000, 0.9238795325112867385, 1.000000000000000000, 0.9238795325112867385, 1.000000000000000000, 0.9238795325112867385, 1.000000000000000000, 0.9238795325112867385, 1.000000000000000000 ) ) 
 REPRESENTATION_ITEM ( '' )  );
#39190=CARTESIAN_POINT ( 'NONE',  ( -8.000000000000000000, 11.06249999590322020, -9.797174393178825657E-16 ) ) ;
#39194=CARTESIAN_POINT ( 'NONE',  ( -2.977408999572654480, 18.37499999795161187, 7.188101187499999156 ) ) ;
#39198=CARTESIAN_POINT ( 'NONE',  ( 7.188101187500000044, 105.7812500020483810, -8.802885111219163269E-16 ) ) ;
#39207=VERTEX_POINT ( 'NONE', #22635 ) ;
#39210=EDGE_CURVE ( 'NONE', #7343, #21929, #33756, .T. ) ;
#39217=CARTESIAN_POINT ( 'NONE',  ( 2.977408999572650039, 90.68750000204838102, -7.188101187500000933 ) ) ;
#39223=CARTESIAN_POINT ( 'NONE',  ( 5.082755093536326818, 102.5937500020483810, 5.082755093536325042 ) ) ;
#39239=EDGE_CURVE ( 'NONE', #60077, #50120, #9919, .T. ) ;
#39248=CARTESIAN_POINT ( 'NONE',  ( -7.188101187500000044, 11.71874999795161010, -8.802885111219163269E-16 ) ) ;
#39249=VECTOR ( 'NONE', #42093, 1000.000000000000000 ) ;
#39250=CARTESIAN_POINT ( 'NONE',  ( -7.999999999999998224, 111.7812500040967763, 3.313708498984766493 ) ) ;
#39259=VERTEX_POINT ( 'NONE', #24850 ) ;
#39261=CARTESIAN_POINT ( 'NONE',  ( 1.320432766682874540E-15, 108.0312500020483810, 7.188101187500000044 ) ) ;
#39263=CARTESIAN_POINT ( 'NONE',  ( -7.188101187500000044, 124.5312500020483810, 0.000000000000000000 ) ) ;
#39267=ORIENTED_EDGE ( 'NONE', *, *, #68301, .T. ) ;
#39277=CARTESIAN_POINT ( 'NONE',  ( 5.656854249492381470, 107.5625000000000000, 5.656854249492379694 ) ) ;
#39282=CARTESIAN_POINT ( 'NONE',  ( 7.188101187499999156, 2.249999997951610098, 2.977408999572654924 ) ) ;
#39284=CARTESIAN_POINT ( 'NONE',  ( -7.188101187499999156, 123.1250000020484094, 2.977408999572654924 ) ) ;
#39288=LINE ( 'NONE', #27209, #57911 ) ;
#39297=CARTESIAN_POINT ( 'NONE',  ( -5.656854249492379694, 25.87499999590322375, -5.656854249492380582 ) ) ;
#39309=CARTESIAN_POINT ( 'NONE',  ( -7.188101187500000044, 112.1562500020483952, 0.000000000000000000 ) ) ;
#39316=CARTESIAN_POINT ( 'NONE',  ( -5.082755093536324154, 123.2187500020483952, 5.082755093536326818 ) ) ;
#39330=DIRECTION ( 'NONE',  ( 0.000000000000000000, 0.000000000000000000, 1.000000000000000000 ) ) ;
#39336=EDGE_LOOP ( 'NONE', ( #69558, #1194, #61443, #48056 ) ) ;
#39337=CARTESIAN_POINT ( 'NONE',  ( -1.320432766682874540E-15, 27.09374999795161543, 7.188101187500000044 ) ) ;
#39340=CARTESIAN_POINT ( 'NONE',  ( -5.082755093536326818, 22.78124999795161187, 5.082755093536325042 ) ) ;
#39361=EDGE_CURVE ( 'NONE', #53657, #2559, #3457, .T. ) ;
#39362=CARTESIAN_POINT ( 'NONE',  ( -8.000000000000000000, 124.9062499999999858, -3.313708498984761608 ) ) ;
#39365=EDGE_LOOP ( 'NONE', ( #50350, #21668, #48516, #23765 ) ) ;
#39367=AXIS2_PLACEMENT_3D ( 'NONE', #14251, #31622, #71969 ) ;
#39368=CARTESIAN_POINT ( 'NONE',  ( 8.000000000000000000, 94.34374999999998579, -3.313708498984762496 ) ) ;
#39372=CARTESIAN_POINT ( 'NONE',  ( 8.000000000000000000, 13.40624999590322375, -3.313708498984761164 ) ) ;
#39389=CARTESIAN_POINT ( 'NONE',  ( 0.000000000000000000, 54.99999999999999289, 0.000000000000000000 ) ) ;
#39392=CARTESIAN_POINT ( 'NONE',  ( 5.082755093536325042, 101.0937500020483810, -5.082755093536325930 ) ) ;
#39410=DIRECTION ( 'NONE',  ( 1.000000000000000000, 0.000000000000000000, -0.000000000000000000 ) ) ;
#39411=CARTESIAN_POINT ( 'NONE',  ( 0.000000000000000000, 0.000000000000000000, 7.499999999999992895 ) ) ;
#39416=CARTESIAN_POINT ( 'NONE',  ( -4.898587196589412829E-16, 106.8125000040967763, -8.000000000000000000 ) ) ;
#39420=CARTESIAN_POINT ( 'NONE',  ( -5.082755093536326818, 22.78124999795161187, 5.082755093536325042 ) ) ;
#39428=CARTESIAN_POINT ( 'NONE',  ( 7.188101187500001821, 8.062499997951611874, -2.977408999572650483 ) ) ;
#39442=ORIENTED_EDGE ( 'NONE', *, *, #45695, .F. ) ;
#39443=CARTESIAN_POINT ( 'NONE',  ( -7.188101187500000933, 16.12499999795161543, -2.977408999572651371 ) ) ;
#39445=VECTOR ( 'NONE', #48349, 1000.000000000000000 ) ;
#39448=CARTESIAN_POINT ( 'NONE',  ( -2.977408999572650927, 109.2500000020483952, -7.188101187500001821 ) ) ;
#39477=CARTESIAN_POINT ( 'NONE',  ( 4.898587196589412829E-16, 22.87500000000000355, -8.000000000000000000 ) ) ;
#39482=CARTESIAN_POINT ( 'NONE',  ( 2.977408999572654480, 123.1250000020484094, 7.188101187499999156 ) ) ;
#39493=CARTESIAN_POINT ( 'NONE',  ( 5.082755093536324154, 25.78124999795161543, 5.082755093536326818 ) ) ;
#39507=CARTESIAN_POINT ( 'NONE',  ( -3.313708498984719864, 27.28124999590322020, -8.000000000000040856 ) ) ;
#39515=CARTESIAN_POINT ( 'NONE',  ( 2.977408999572652260, 3.562499997951610542, 7.188101187500000044 ) ) ;
#39520=CARTESIAN_POINT ( 'NONE',  ( -8.000000000000000000, 2.062499995903220196, -9.797174393178825657E-16 ) ) ;
#39530=CARTESIAN_POINT ( 'NONE',  ( -3.313708498984760720, 19.96875000000000355, -8.000000000000000000 ) ) ;
#39533=CARTESIAN_POINT ( 'NONE',  ( -4.898587196589412829E-16, 94.81250000409677625, -8.000000000000000000 ) ) ;
#39566=CARTESIAN_POINT ( 'NONE',  ( -1.469576158976823947E-15, 11.43749999590322197, 8.000000000000000000 ) ) ;
#39570=CARTESIAN_POINT ( 'NONE',  ( -7.188101187500002709, 18.18749999795161187, 2.977408999572649151 ) ) ;
#39573=CARTESIAN_POINT ( 'NONE',  ( -5.082755093536325930, 101.8437500020483810, -5.082755093536325930 ) ) ;
#39581=LINE ( 'NONE', #12390, #18192 ) ;
#39588=CARTESIAN_POINT ( 'NONE',  ( -7.188101187500000044, 95.65625000204838102, 0.000000000000000000 ) ) ;
#39595=CARTESIAN_POINT ( 'NONE',  ( -7.188101187500000044, 105.0312500020483810, 0.000000000000000000 ) ) ;
#39613=( BOUNDED_CURVE ( )  B_SPLINE_CURVE ( 1, ( #64484, #53164 ),
 .UNSPECIFIED., .F., .F. ) 
 B_SPLINE_CURVE_WITH_KNOTS ( ( 2, 2 ),
 ( 0.000000000000000000, 1.000000000000000000 ),
 .UNSPECIFIED. ) 
 CURVE ( )  GEOMETRIC_REPRESENTATION_ITEM ( )  RATIONAL_B_SPLINE_CURVE ( ( 0.9660720450733824016, 0.9660720450733824016 ) ) 
 REPRESENTATION_ITEM ( '' )  );
#39620=CARTESIAN_POINT ( 'NONE',  ( -7.188101187500002709, 13.31249999795161187, 2.977408999572649151 ) ) ;
#39621=CARTESIAN_POINT ( 'NONE',  ( 1.469576158976823947E-15, 112.0625000040967905, 8.000000000000000000 ) ) ;
#39630=ORIENTED_EDGE ( 'NONE', *, *, #51227, .T. ) ;
#39632=CARTESIAN_POINT ( 'NONE',  ( 1.320432766682874540E-15, 103.5312500020483810, 7.188101187500000044 ) ) ;
#39633=ADVANCED_FACE ( 'NONE', ( #56440 ), #57184, .T. ) ;
#39635=CARTESIAN_POINT ( 'NONE',  ( -5.656854249492378806, 123.6875000000000000, 5.656854249492381470 ) ) ;
#39641=CARTESIAN_POINT ( 'NONE',  ( 8.000000000000000000, 91.43750000409679046, -9.797174393178825657E-16 ) ) ;
#39648=CARTESIAN_POINT ( 'NONE',  ( -5.656854249492380582, 105.3125000000000000, -5.656854249492380582 ) ) ;
#39653=CARTESIAN_POINT ( 'NONE',  ( 8.000000000000000000, 26.90624999590322730, -3.313708498984761608 ) ) ;
#39655=CARTESIAN_POINT ( 'NONE',  ( -5.082755093536324154, 120.2187500020483952, 5.082755093536326818 ) ) ;
#39674=CARTESIAN_POINT ( 'NONE',  ( -5.082755093536325930, 108.9687500020483810, -5.082755093536325930 ) ) ;
#39679=CARTESIAN_POINT ( 'NONE',  ( -7.188101187500001821, 121.4375000020483668, -2.977408999572650483 ) ) ;
#39702=CARTESIAN_POINT ( 'NONE',  ( 5.082755093536325930, 26.15624999795161543, -5.082755093536325930 ) ) ;
#39705=CARTESIAN_POINT ( 'NONE',  ( 4.401442555609581635E-16, 22.21874999795161543, -7.188101187500000044 ) ) ;
#39706=CARTESIAN_POINT ( 'NONE',  ( 0.000000000000000000, 125.0000000000000000, 0.000000000000000000 ) ) ;
#39712=ORIENTED_EDGE ( 'NONE', *, *, #27010, .T. ) ;
#39713=EDGE_CURVE ( 'NONE', #48764, #45738, #62824, .T. ) ;
#39714=EDGE_CURVE ( 'NONE', #49924, #35571, #49733, .T. ) ;
#39729=CARTESIAN_POINT ( 'NONE',  ( 8.000000000000000000, 121.3437500000000000, -3.313708498984762496 ) ) ;
#39737=CARTESIAN_POINT ( 'NONE',  ( -3.313708498984765161, 23.53125000000000355, 7.999999999999998224 ) ) ;
#39756=CARTESIAN_POINT ( 'NONE',  ( 2.977408999572650039, 101.1875000020483810, -7.188101187500001821 ) ) ;
#39768=CARTESIAN_POINT ( 'NONE',  ( -8.000000000000001776, 0.8437500000000000000, 3.313708498984759387 ) ) ;
#39774=CARTESIAN_POINT ( 'NONE',  ( -5.656854249492378806, 101.1875000000000000, 5.656854249492381470 ) ) ;
#39781=CARTESIAN_POINT ( 'NONE',  ( -7.188101187500000044, 22.59374999795161187, -8.802885111219163269E-16 ) ) ;
#39784=ORIENTED_EDGE ( 'NONE', *, *, #48591, .F. ) ;
#39785=CARTESIAN_POINT ( 'NONE',  ( 1.469576158976823947E-15, 97.06250000409677625, 8.000000000000000000 ) ) ;
#39791=CARTESIAN_POINT ( 'NONE',  ( 5.082755093536324154, 6.281249997951610986, 5.082755093536326818 ) ) ;
#39794=CARTESIAN_POINT ( 'NONE',  ( -1.320432766682874540E-15, 6.468749997951610098, 7.188101187500000044 ) ) ;
#39811=CARTESIAN_POINT ( 'NONE',  ( 5.082755093536325930, 18.65624999795161187, -5.082755093536325930 ) ) ;
#39815=CARTESIAN_POINT ( 'NONE',  ( 2.977408999572650039, 104.5625000020483668, -7.188101187500001821 ) ) ;
#39840=EDGE_CURVE ( 'NONE', #4108, #46386, #59003, .T. ) ;
#39848=CARTESIAN_POINT ( 'NONE',  ( -5.082755093536324154, 119.8437500020483810, 5.082755093536326818 ) ) ;
#39857=CARTESIAN_POINT ( 'NONE',  ( 7.188101187499999156, 27.37499999795161187, 2.977408999572654924 ) ) ;
#39879=CARTESIAN_POINT ( 'NONE',  ( -2.977408999572650039, 7.312499997951610986, -7.188101187500000933 ) ) ;
#39884=CARTESIAN_POINT ( 'NONE',  ( 8.000000000000000000, 115.4375000040967763, -9.797174393178825657E-16 ) ) ;
#39894=CARTESIAN_POINT ( 'NONE',  ( 8.000000000000000000, 16.50000000000000355, 0.000000000000000000 ) ) ;
#39897=CARTESIAN_POINT ( 'NONE',  ( -5.082755093536325930, 122.4687500020483952, -5.082755093536325930 ) ) ;
#39906=CARTESIAN_POINT ( 'NONE',  ( 7.188101187500000933, 0.5624999979516099868, -2.977408999572650483 ) ) ;
#39938=CARTESIAN_POINT ( 'NONE',  ( -2.977408999572654480, 16.87499999795161543, 7.188101187499999156 ) ) ;
#39941=CARTESIAN_POINT ( 'NONE',  ( -7.188101187500000044, 105.0312500020483810, 0.000000000000000000 ) ) ;
#39958=CIRCLE ( 'NONE', #65237, 8.000000000000000000 ) ;
#39960=CARTESIAN_POINT ( 'NONE',  ( 7.188101187500000933, 92.00000000204838102, -2.977408999572651371 ) ) ;
#39966=CARTESIAN_POINT ( 'NONE',  ( -2.977408999572651815, 96.31250000204838102, 7.188101187500000933 ) ) ;
#39993=CARTESIAN_POINT ( 'NONE',  ( 2.977408999572650927, 14.24999999795161010, -7.188101187500001821 ) ) ;
#39994=CARTESIAN_POINT ( 'NONE',  ( 1.469576158976823947E-15, 107.5625000040967905, 8.000000000000000000 ) ) ;
#40003=CARTESIAN_POINT ( 'NONE',  ( 1.320432766682874540E-15, 105.0312500020483810, 7.188101187500000044 ) ) ;
#40020=CARTESIAN_POINT ( 'NONE',  ( 8.000000000000001776, 106.1562499999999858, 3.313708498984759387 ) ) ;
#40024=CARTESIAN_POINT ( 'NONE',  ( -4.898587196589412829E-16, 102.3125000040967763, -8.000000000000000000 ) ) ;
#40026=CARTESIAN_POINT ( 'NONE',  ( 5.082755093536325930, 1.031249997951610098, -5.082755093536325930 ) ) ;
#40028=CARTESIAN_POINT ( 'NONE',  ( 2.977408999572650039, 119.5625000020483810, -7.188101187500000933 ) ) ;
#40030=CARTESIAN_POINT ( 'NONE',  ( 0.000000000000000000, 125.0000000000000000, 8.000000000000000000 ) ) ;
#40035=CARTESIAN_POINT ( 'NONE',  ( 5.656854249492381470, 122.5625000000000000, 5.656854249492379694 ) ) ;
#40047=CARTESIAN_POINT ( 'NONE',  ( -2.977408999572650927, 113.3750000020483810, -7.188101187500000933 ) ) ;
#40052=EDGE_CURVE ( 'NONE', #66964, #3547, #36045, .T. ) ;
#40054=CARTESIAN_POINT ( 'NONE',  ( 7.188101187500001821, 120.8750000020483810, -2.977408999572651371 ) ) ;
#40060=CARTESIAN_POINT ( 'NONE',  ( 8.000000000000000000, 107.8437500000000000, -3.313708498984762496 ) ) ;
#40073=EDGE_LOOP ( 'NONE', ( #44450, #24054, #50942, #39055 ) ) ;
#40075=EDGE_CURVE ( 'NONE', #50397, #42073, #10739, .T. ) ;
#40078=CARTESIAN_POINT ( 'NONE',  ( 4.401442555609581635E-16, 24.84374999795161543, -7.188101187500000044 ) ) ;
#40081=CARTESIAN_POINT ( 'NONE',  ( -2.977408999572650039, 23.81249999795161543, -7.188101187500001821 ) ) ;
#40098=EDGE_LOOP ( 'NONE', ( #21015, #57986, #49017, #16575 ) ) ;
#40104=CARTESIAN_POINT ( 'NONE',  ( -7.999999999999998224, 123.5937500000000000, 3.313708498984766493 ) ) ;
#40111=CARTESIAN_POINT ( 'NONE',  ( -1.469576158976823947E-15, 23.62500000000000355, 8.000000000000000000 ) ) ;
#40121=CARTESIAN_POINT ( 'NONE',  ( 7.999999999999998224, 10.21874999590321842, 3.313708498984766049 ) ) ;
#40135=CARTESIAN_POINT ( 'NONE',  ( 2.977408999572654480, 100.6250000020483810, 7.188101187499999156 ) ) ;
#40141=ORIENTED_EDGE ( 'NONE', *, *, #45885, .T. ) ;
#40154=CARTESIAN_POINT ( 'NONE',  ( 8.000000000000000000, 116.9375000040967763, -9.797174393178825657E-16 ) ) ;
#40161=CARTESIAN_POINT ( 'NONE',  ( 4.401442555609581635E-16, 22.21874999795161543, -7.188101187500000044 ) ) ;
#40166=CARTESIAN_POINT ( 'NONE',  ( 0.000000000000000000, 125.0000000000000000, 0.000000000000000000 ) ) ;
#40170=CARTESIAN_POINT ( 'NONE',  ( -1.320432766682874540E-15, 10.59374999795161187, 7.188101187500000044 ) ) ;
#40174=CARTESIAN_POINT ( 'NONE',  ( -2.977408999572650039, 4.312499997951610098, -7.188101187500001821 ) ) ;
#40187=CARTESIAN_POINT ( 'NONE',  ( -7.188101187500002709, 17.81249999795161187, 2.977408999572649151 ) ) ;
#40192=CARTESIAN_POINT ( 'NONE',  ( -7.188101187499999156, 108.1250000020483810, 2.977408999572654924 ) ) ;
#40197=ORIENTED_EDGE ( 'NONE', *, *, #63218, .F. ) ;
#40217=CARTESIAN_POINT ( 'NONE',  ( 9.797174393178825657E-16, 125.0000000000000000, -8.000000000000000000 ) ) ;
#40218=DIRECTION ( 'NONE',  ( 0.000000000000000000, 0.000000000000000000, 1.000000000000000000 ) ) ;
#40221=CARTESIAN_POINT ( 'NONE',  ( 1.320432766682874540E-15, 123.0312500020483810, 7.188101187500000044 ) ) ;
#40230=CARTESIAN_POINT ( 'NONE',  ( 5.082755093536325930, 24.65624999795161543, -5.082755093536325930 ) ) ;
#40249=CARTESIAN_POINT ( 'NONE',  ( -4.898587196589412829E-16, 115.6250000000000000, -8.000000000000000000 ) ) ;
#40253=CARTESIAN_POINT ( 'NONE',  ( -2.977408999572654480, 6.374999997951610098, 7.188101187499999156 ) ) ;
#40256=ORIENTED_EDGE ( 'NONE', *, *, #52512, .T. ) ;
#40270=CARTESIAN_POINT ( 'NONE',  ( -5.656854249492381470, 15.93750000000000355, 5.656854249492379694 ) ) ;
#40273=CARTESIAN_POINT ( 'NONE',  ( 2.977408999572654480, 123.1250000020484094, 7.188101187499999156 ) ) ;
#40276=CARTESIAN_POINT ( 'NONE',  ( -5.656854249492379694, 8.062500000000001776, -5.656854249492380582 ) ) ;
#40280=CARTESIAN_POINT ( 'NONE',  ( -2.977408999572654480, 1.499999997951610098, 7.188101187499999156 ) ) ;
#40283=CARTESIAN_POINT ( 'NONE',  ( 2.977408999572650039, 122.5625000020483952, -7.188101187500001821 ) ) ;
#40309=CARTESIAN_POINT ( 'NONE',  ( -2.977408999572654480, 24.37499999795161543, 7.188101187499999156 ) ) ;
#40312=CARTESIAN_POINT ( 'NONE',  ( -4.401442555609581635E-16, 100.1562500020483810, -7.188101187500000044 ) ) ;
#40321=DIRECTION ( 'NONE',  ( -0.000000000000000000, 1.000000000000000000, -0.000000000000000000 ) ) ;
#40327=CARTESIAN_POINT ( 'NONE',  ( -5.082755093536324154, 91.34375000204838102, 5.082755093536326818 ) ) ;
#40330=CARTESIAN_POINT ( 'NONE',  ( 9.797174393178825657E-16, 54.99999999999999289, -8.000000000000000000 ) ) ;
#40334=CARTESIAN_POINT ( 'NONE',  ( 5.082755093536326818, 98.09375000204838102, 5.082755093536325042 ) ) ;
#40355=( BOUNDED_CURVE ( )  B_SPLINE_CURVE ( 2, ( #31485, #42788, #18315, #48080, #35673, #41328, #24697, #36408, #64338 ),
 .UNSPECIFIED., .F., .F. ) 
 B_SPLINE_CURVE_WITH_KNOTS ( ( 3, 2, 2, 2, 3 ),
 ( 0.1979166666666667962, 0.2031250000000001388, 0.2083333333333334814, 0.2135416666666667962, 0.2187500000000001388 ),
 .UNSPECIFIED. ) 
 CURVE ( )  GEOMETRIC_REPRESENTATION_ITEM ( )  RATIONAL_B_SPLINE_CURVE ( ( 0.9999999999999980016, 0.9238795325112887369, 1.000000000000000000, 0.9238795325112867385, 1.000000000000000000, 0.9238795325112867385, 1.000000000000000000, 0.9238795325112847401, 1.000000000000001998 ) ) 
 REPRESENTATION_ITEM ( '' )  );
#40360=CARTESIAN_POINT ( 'NONE',  ( 2.977408999572650927, 12.74999999795161187, -7.188101187500001821 ) ) ;
#40361=CARTESIAN_POINT ( 'NONE',  ( 8.000000000000001776, 103.3437500040967763, 3.313708498984759387 ) ) ;
#40371=CYLINDRICAL_SURFACE ( 'NONE', #74037, 8.000000000000000000 ) ;
#40372=CARTESIAN_POINT ( 'NONE',  ( -2.977408999572651815, 104.9375000020483810, 7.188101187500000933 ) ) ;
#40376=CARTESIAN_POINT ( 'NONE',  ( -8.000000000000000000, 15.46874999590322197, -3.313708498984762496 ) ) ;
#40377=EDGE_LOOP ( 'NONE', ( #9104, #15648 ) ) ;
#40391=CARTESIAN_POINT ( 'NONE',  ( -7.999999999999998224, 101.0937500000000142, 3.313708498984766493 ) ) ;
#40395=CARTESIAN_POINT ( 'NONE',  ( 7.999999999999998224, 1.406250000000000000, 3.313708498984766049 ) ) ;
#40397=CARTESIAN_POINT ( 'NONE',  ( 7.188101187500001821, 0.9374999979516102089, -2.977408999572650483 ) ) ;
#40400=CARTESIAN_POINT ( 'NONE',  ( 2.977408999572654480, 119.0000000020483810, 7.188101187499999156 ) ) ;
#40404=CARTESIAN_POINT ( 'NONE',  ( -3.313708498984761608, 90.21874999999998579, -8.000000000000000000 ) ) ;
#40409=CARTESIAN_POINT ( 'NONE',  ( 3.313708498984765161, 100.1562500040967763, 7.999999999999998224 ) ) ;
#40419=CARTESIAN_POINT ( 'NONE',  ( 4.898587196589412829E-16, 7.687499995903221084, -8.000000000000000000 ) ) ;
#40420=CARTESIAN_POINT ( 'NONE',  ( 5.082755093536326818, 109.7187500020483810, 5.082755093536325042 ) ) ;
#40425=CARTESIAN_POINT ( 'NONE',  ( -2.977408999572651815, 114.3125000020483952, 7.188101187500000933 ) ) ;
#40429=ORIENTED_EDGE ( 'NONE', *, *, #58829, .F. ) ;
#40451=CARTESIAN_POINT ( 'NONE',  ( 4.898587196589412829E-16, 1.875000000000000444, -8.000000000000000000 ) ) ;
#40454=CARTESIAN_POINT ( 'NONE',  ( 5.082755093536324154, 26.15624999795161543, 5.082755093536326818 ) ) ;
#40455=CARTESIAN_POINT ( 'NONE',  ( 3.313708498984760720, 120.2187500040967763, -8.000000000000000000 ) ) ;
#40476=CARTESIAN_POINT ( 'NONE',  ( 5.656854249492381470, 116.5625000000000000, 5.656854249492379694 ) ) ;
#40485=CARTESIAN_POINT ( 'NONE',  ( 5.656854249492379694, 97.43750000000000000, -5.656854249492380582 ) ) ;
#40507=AXIS2_PLACEMENT_3D ( 'NONE', #28824, #5828, #45068 ) ;
#40509=CARTESIAN_POINT ( 'NONE',  ( -7.188101187500001821, 97.06250000204838102, -2.977408999572650483 ) ) ;
#40530=CARTESIAN_POINT ( 'NONE',  ( 7.188101187499999156, 23.24999999795161543, 2.977408999572654924 ) ) ;
#40538=CARTESIAN_POINT ( 'NONE',  ( -7.188101187500002709, 8.812499997951611874, 2.977408999572649151 ) ) ;
#40542=CARTESIAN_POINT ( 'NONE',  ( 7.188101187500001821, 8.437499997951611874, -2.977408999572650483 ) ) ;
#40557=CARTESIAN_POINT ( 'NONE',  ( -2.977408999572650927, 119.3750000020483810, -7.188101187500001821 ) ) ;
#40561=CARTESIAN_POINT ( 'NONE',  ( -5.082755093536326818, 17.90624999795161187, 5.082755093536325042 ) ) ;
#40564=CARTESIAN_POINT ( 'NONE',  ( 3.313708498984762496, 13.21875000000000355, 7.999999999999998224 ) ) ;
#40566=CARTESIAN_POINT ( 'NONE',  ( -4.401442555609581635E-16, 104.6562500020483810, -7.188101187500000044 ) ) ;
#40575=DIRECTION ( 'NONE',  ( -0.000000000000000000, 1.000000000000000000, -0.000000000000000000 ) ) ;
#40581=( BOUNDED_CURVE ( )  B_SPLINE_CURVE ( 2, ( #7192, #70558, #35865, #53214, #41881, #7560, #13194, #1897, #70922 ),
 .UNSPECIFIED., .F., .F. ) 
 B_SPLINE_CURVE_WITH_KNOTS ( ( 3, 2, 2, 2, 3 ),
 ( 0.3437499999999998335, 0.3489583333333331483, 0.3541666666666665186, 0.3593749999999998335, 0.3645833333333331483 ),
 .UNSPECIFIED. ) 
 CURVE ( )  GEOMETRIC_REPRESENTATION_ITEM ( )  RATIONAL_B_SPLINE_CURVE ( ( 1.000000000000002442, 0.9238795325112842960, 1.000000000000000000, 0.9238795325112867385, 1.000000000000000000, 0.9238795325112867385, 1.000000000000000000, 0.9238795325112891810, 0.9999999999999975575 ) ) 
 REPRESENTATION_ITEM ( '' )  );
#40596=CARTESIAN_POINT ( 'NONE',  ( 7.188101187500001821, 120.5000000020483810, -2.977408999572651371 ) ) ;
#40605=CARTESIAN_POINT ( 'NONE',  ( -1.320432766682874540E-15, 25.59374999795161543, 7.188101187500000044 ) ) ;
#40615=FACE_OUTER_BOUND ( 'NONE', #54823, .T. ) ;
#40627=CARTESIAN_POINT ( 'NONE',  ( -7.188101187500000933, 5.999999997951610986, -2.977408999572651371 ) ) ;
#40631=CARTESIAN_POINT ( 'NONE',  ( -4.898587196589412829E-16, 123.3125000040967905, -8.000000000000000000 ) ) ;
#40637=ORIENTED_EDGE ( 'NONE', *, *, #39141, .T. ) ;
#40643=CARTESIAN_POINT ( 'NONE',  ( -8.000000000000001776, 17.34375000000000000, 3.313708498984759387 ) ) ;
#40646=CARTESIAN_POINT ( 'NONE',  ( -5.082755093536324154, 121.3437500020483952, 5.082755093536326818 ) ) ;
#40652=CARTESIAN_POINT ( 'NONE',  ( 4.401442555609581635E-16, 0.8437499979516099868, -7.188101187500000044 ) ) ;
#40657=CARTESIAN_POINT ( 'NONE',  ( 7.188101187500001821, 122.3750000020483952, -2.977408999572651371 ) ) ;
#40676=CARTESIAN_POINT ( 'NONE',  ( -5.656854249492380582, 114.3125000000000000, -5.656854249492380582 ) ) ;
#40682=CARTESIAN_POINT ( 'NONE',  ( 5.082755093536325930, 25.03124999795161543, -5.082755093536325930 ) ) ;
#40685=CARTESIAN_POINT ( 'NONE',  ( -7.188101187500000044, 96.03125000204838102, 0.000000000000000000 ) ) ;
#40700=CARTESIAN_POINT ( 'NONE',  ( 5.082755093536325042, 93.59375000204838102, -5.082755093536325930 ) ) ;
#40706=CARTESIAN_POINT ( 'NONE',  ( 5.082755093536325042, 93.96875000204838102, -5.082755093536325930 ) ) ;
#40729=CARTESIAN_POINT ( 'NONE',  ( 3.313708498984765161, 104.6562500040968047, 7.999999999999998224 ) ) ;
#40736=ADVANCED_FACE ( 'NONE', ( #25713 ), #31016, .T. ) ;
#40738=CARTESIAN_POINT ( 'NONE',  ( 2.977408999572654480, 106.6250000020483952, 7.188101187499999156 ) ) ;
#40745=VERTEX_POINT ( 'NONE', #66088 ) ;
#40746=ORIENTED_EDGE ( 'NONE', *, *, #65509, .T. ) ;
#40755=CARTESIAN_POINT ( 'NONE',  ( -5.656854249492380582, 102.3125000000000000, -5.656854249492380582 ) ) ;
#40763=CARTESIAN_POINT ( 'NONE',  ( 2.977408999572651815, 5.062499997951609210, 7.188101187500000933 ) ) ;
#40766=CARTESIAN_POINT ( 'NONE',  ( -2.977408999572650927, 118.2500000020483952, -7.188101187500000933 ) ) ;
#40773=CARTESIAN_POINT ( 'NONE',  ( -1.469576158976823947E-15, 10.12500000000000178, 8.000000000000000000 ) ) ;
#40778=ORIENTED_EDGE ( 'NONE', *, *, #36970, .F. ) ;
#40786=CARTESIAN_POINT ( 'NONE',  ( -5.082755093536324154, 112.3437500020483810, 5.082755093536326818 ) ) ;
#40791=EDGE_CURVE ( 'NONE', #63531, #47572, #41138, .T. ) ;
#40792=CARTESIAN_POINT ( 'NONE',  ( -5.082755093536324154, 112.7187500020483810, 5.082755093536326818 ) ) ;
#40820=CARTESIAN_POINT ( 'NONE',  ( 3.313708498984762052, 4.781250000000000888, -8.000000000000000000 ) ) ;
#40823=CARTESIAN_POINT ( 'NONE',  ( -7.188101187500001821, 22.49999999795161543, -2.977408999572651371 ) ) ;
#40824=CARTESIAN_POINT ( 'NONE',  ( -4.898587196589412829E-16, 120.3125000040967763, -8.000000000000000000 ) ) ;
#40830=CARTESIAN_POINT ( 'NONE',  ( 9.797174393178825657E-16, 125.0000000000000000, -8.000000000000000000 ) ) ;
#40835=EDGE_CURVE ( 'NONE', #55027, #11019, #43448, .T. ) ;
#40843=CARTESIAN_POINT ( 'NONE',  ( 8.000000000000000000, 95.93750000409679046, -9.797174393178825657E-16 ) ) ;
#40848=CARTESIAN_POINT ( 'NONE',  ( -8.000000000000000000, 117.4062500000000000, -3.313708498984761608 ) ) ;
#40855=CARTESIAN_POINT ( 'NONE',  ( -5.656854249492379694, 15.37499999590322197, -5.656854249492380582 ) ) ;
#40858=CARTESIAN_POINT ( 'NONE',  ( 8.000000000000001776, 97.15625000000000000, 3.313708498984759387 ) ) ;
#40877=CARTESIAN_POINT ( 'NONE',  ( -7.999999999999998224, 116.2812500040967905, 3.313708498984766049 ) ) ;
#40881=CARTESIAN_POINT ( 'NONE',  ( -2.977408999572651815, 94.43750000204838102, 7.188101187500000933 ) ) ;
#40899=ORIENTED_EDGE ( 'NONE', *, *, #37676, .T. ) ;
#40900=CARTESIAN_POINT ( 'NONE',  ( 1.469576158976823947E-15, 113.3750000000000000, 8.000000000000000000 ) ) ;
#40904=CARTESIAN_POINT ( 'NONE',  ( 2.977408999572652260, 24.56249999795161543, 7.188101187500000044 ) ) ;
#40907=ORIENTED_EDGE ( 'NONE', *, *, #61021, .T. ) ;
#40912=CARTESIAN_POINT ( 'NONE',  ( 7.188101187500001821, 14.06249999795161365, -2.977408999572650483 ) ) ;
#40915=CARTESIAN_POINT ( 'NONE',  ( -5.082755093536326818, 6.281249997951610098, 5.082755093536325042 ) ) ;
#40927=VECTOR ( 'NONE', #42454, 999.9999999999998863 ) ;
#40931=CARTESIAN_POINT ( 'NONE',  ( 2.977408999572650039, 119.1875000020483810, -7.188101187500001821 ) ) ;
#40936=CARTESIAN_POINT ( 'NONE',  ( -2.977408999572654480, 14.99999999795161187, 7.188101187499999156 ) ) ;
#40941=CARTESIAN_POINT ( 'NONE',  ( -2.977408999572651815, 99.31250000204839523, 7.188101187500000933 ) ) ;
#40944=CARTESIAN_POINT ( 'NONE',  ( -8.000000000000000000, 89.09375000409676204, -3.313708498984761164 ) ) ;
#40955=FACE_OUTER_BOUND ( 'NONE', #20301, .T. ) ;
#40956=CARTESIAN_POINT ( 'NONE',  ( 5.656854249492379694, 91.43749999999998579, -5.656854249492380582 ) ) ;
#40972=CARTESIAN_POINT ( 'NONE',  ( 2.977408999572654480, 115.6250000020483810, 7.188101187499999156 ) ) ;
#40996=ORIENTED_EDGE ( 'NONE', *, *, #67930, .F. ) ;
#40997=EDGE_CURVE ( 'NONE', #61205, #28769, #17553, .T. ) ;
#41003=CARTESIAN_POINT ( 'NONE',  ( 5.082755093536325930, 7.031249997951610986, -5.082755093536325930 ) ) ;
#41021=CARTESIAN_POINT ( 'NONE',  ( 7.999999999999998224, 19.40625000000000000, 3.313708498984766493 ) ) ;
#41023=CARTESIAN_POINT ( 'NONE',  ( 2.977408999572654480, 120.1250000020483952, 7.188101187499999156 ) ) ;
#41030=CARTESIAN_POINT ( 'NONE',  ( 5.656854249492381470, 113.5625000000000000, 5.656854249492379694 ) ) ;
#41035=CARTESIAN_POINT ( 'NONE',  ( 7.188101187500002709, 119.1875000020483810, 2.977408999572649151 ) ) ;
#41046=CARTESIAN_POINT ( 'NONE',  ( 9.797174393178825657E-16, 125.0000000000000000, -8.000000000000000000 ) ) ;
#41050=CARTESIAN_POINT ( 'NONE',  ( -5.656854249492381470, 2.437500000000000444, 5.656854249492379694 ) ) ;
#41058=CARTESIAN_POINT ( 'NONE',  ( 5.082755093536324154, 21.65624999795161543, 5.082755093536326818 ) ) ;
#41060=CARTESIAN_POINT ( 'NONE',  ( 2.977408999572650039, 97.06250000204838102, -7.188101187500000933 ) ) ;
#41069=ORIENTED_EDGE ( 'NONE', *, *, #23954, .F. ) ;
#41075=LINE ( 'NONE', #18431, #27548 ) ;
#41079=CARTESIAN_POINT ( 'NONE',  ( 5.656854249492379694, 111.1250000040967763, -5.656854249492380582 ) ) ;
#41080=AXIS2_PLACEMENT_3D ( 'NONE', #57754, #23772, #35476 ) ;
#41082=CARTESIAN_POINT ( 'NONE',  ( -5.082755093536324154, 96.21875000204838102, 5.082755093536326818 ) ) ;
#41089=FACE_OUTER_BOUND ( 'NONE', #11039, .T. ) ;
#41091=CARTESIAN_POINT ( 'NONE',  ( 0.000000000000000000, 125.0000000000000000, 8.000000000000000000 ) ) ;
#41100=VECTOR ( 'NONE', #26395, 1000.000000000000000 ) ;
#41106=CARTESIAN_POINT ( 'NONE',  ( 8.000000000000000000, 103.5312500040967905, -3.313708498984762496 ) ) ;
#41116=CARTESIAN_POINT ( 'NONE',  ( -3.313708498984719864, 24.46875000000000355, -8.000000000000040856 ) ) ;
#41117=CARTESIAN_POINT ( 'NONE',  ( -7.188101187500000044, 106.1562500020483810, 0.000000000000000000 ) ) ;
#41118=( BOUNDED_CURVE ( )  B_SPLINE_CURVE ( 2, ( #66615, #32304, #39075, #49261, #55695, #27366, #21705, #26999, #50013 ),
 .UNSPECIFIED., .F., .F. ) 
 B_SPLINE_CURVE_WITH_KNOTS ( ( 3, 2, 2, 2, 3 ),
 ( 0.2083333333333333148, 0.2152777777777777624, 0.2222222222222221821, 0.2291666666666666574, 0.2361111111111111049 ),
 .UNSPECIFIED. ) 
 CURVE ( )  GEOMETRIC_REPRESENTATION_ITEM ( )  RATIONAL_B_SPLINE_CURVE ( ( 1.000000000000000222, 0.9238795325112864054, 1.000000000000000000, 0.9238795325112867385, 1.000000000000000000, 0.9238795325112867385, 1.000000000000000000, 0.9238795325112867385, 1.000000000000000000 ) ) 
 REPRESENTATION_ITEM ( '' )  );
#41133=CARTESIAN_POINT ( 'NONE',  ( -3.313708498984762496, 99.78124999999998579, 7.999999999999998224 ) ) ;
#41138=( BOUNDED_CURVE ( )  B_SPLINE_CURVE ( 2, ( #71365, #36690, #54418, #2351, #55544, #26087, #9517, #32148, #8759 ),
 .UNSPECIFIED., .F., .F. ) 
 B_SPLINE_CURVE_WITH_KNOTS ( ( 3, 2, 2, 2, 3 ),
 ( 0.4479166666666665741, 0.4531249999999998890, 0.4583333333333332038, 0.4635416666666665741, 0.4687499999999998890 ),
 .UNSPECIFIED. ) 
 CURVE ( )  GEOMETRIC_REPRESENTATION_ITEM ( )  RATIONAL_B_SPLINE_CURVE ( ( 1.000000000000001554, 0.9238795325112850731, 1.000000000000000000, 0.9238795325112867385, 1.000000000000000000, 0.9238795325112867385, 1.000000000000000000, 0.9238795325112884038, 0.9999999999999983347 ) ) 
 REPRESENTATION_ITEM ( '' )  );
#41140=CARTESIAN_POINT ( 'NONE',  ( 4.401442555609581635E-16, 2.718749997951610542, -7.188101187500000044 ) ) ;
#41144=CARTESIAN_POINT ( 'NONE',  ( 5.082755093536326818, 113.0937500020483810, 5.082755093536325042 ) ) ;
#41146=LINE ( 'NONE', #40030, #69121 ) ;
#41148=CARTESIAN_POINT ( 'NONE',  ( -5.656854249492380582, 90.31249999999998579, -5.656854249492380582 ) ) ;
#41154=CARTESIAN_POINT ( 'NONE',  ( 4.903509839973584583, 124.4676415472669788, -6.410198659011175693 ) ) ;
#41157=ORIENTED_EDGE ( 'NONE', *, *, #42267, .F. ) ;
#41164=CARTESIAN_POINT ( 'NONE',  ( -2.977408999572652260, 107.9375000020483810, 7.188101187500000044 ) ) ;
#41169=CARTESIAN_POINT ( 'NONE',  ( -7.188101187500001821, 116.9375000020483952, -2.977408999572650483 ) ) ;
#41195=CARTESIAN_POINT ( 'NONE',  ( 5.656854249492378806, 2.812500000000000444, 5.656854249492381470 ) ) ;
#41197=CARTESIAN_POINT ( 'NONE',  ( 7.188101187499999156, 1.874999997951610098, 2.977408999572654924 ) ) ;
#41201=VECTOR ( 'NONE', #62612, 1000.000000000000227 ) ;
#41222=CARTESIAN_POINT ( 'NONE',  ( 8.000000000000000000, 115.3437500000000000, -3.313708498984762496 ) ) ;
#41228=CARTESIAN_POINT ( 'NONE',  ( -3.313708498984765161, 12.84374999590322197, 7.999999999999998224 ) ) ;
#41248=CARTESIAN_POINT ( 'NONE',  ( 8.000000000000000000, 4.406249995903220196, -3.313708498984761164 ) ) ;
#41249=CARTESIAN_POINT ( 'NONE',  ( 1.469576158976823947E-15, 116.5625000040967763, 8.000000000000000000 ) ) ;
#41253=CARTESIAN_POINT ( 'NONE',  ( -2.977408999572650927, 95.37500000204839523, -7.188101187500001821 ) ) ;
#41284=CARTESIAN_POINT ( 'NONE',  ( 5.082755093536325930, 15.65624999795161365, -5.082755093536325930 ) ) ;
#41287=CARTESIAN_POINT ( 'NONE',  ( -5.082755093536325042, 4.406249997951610098, -5.082755093536325930 ) ) ;
#41289=AXIS2_PLACEMENT_3D ( 'NONE', #15973, #39002, #62006 ) ;
#41300=CARTESIAN_POINT ( 'NONE',  ( 7.188101187500002709, 118.8125000020483810, 2.977408999572649151 ) ) ;
#41306=CARTESIAN_POINT ( 'NONE',  ( -2.977408999572650039, 21.93749999795161187, -7.188101187500000933 ) ) ;
#41311=CARTESIAN_POINT ( 'NONE',  ( -4.401442555609581635E-16, 101.6562500020483810, -7.188101187500000044 ) ) ;
#41328=CARTESIAN_POINT ( 'NONE',  ( -8.000000000000000000, 117.4062500000000000, -3.313708498984761164 ) ) ;
#41332=VERTEX_POINT ( 'NONE', #53215 ) ;
#41337=FACE_OUTER_BOUND ( 'NONE', #51911, .T. ) ;
#41340=CARTESIAN_POINT ( 'NONE',  ( 5.082755093536326818, 112.7187500020483810, 5.082755093536325042 ) ) ;
#41345=CARTESIAN_POINT ( 'NONE',  ( -3.313708498984760276, 24.28124999590322375, -8.000000000000000000 ) ) ;
#41346=ORIENTED_EDGE ( 'NONE', *, *, #5832, .F. ) ;
#41372=CARTESIAN_POINT ( 'NONE',  ( 5.082755093536325930, 13.03124999795161187, -5.082755093536325930 ) ) ;
#41384=ORIENTED_EDGE ( 'NONE', *, *, #26577, .F. ) ;
#41389=CARTESIAN_POINT ( 'NONE',  ( 5.656854249492378806, 22.31250000000000355, 5.656854249492381470 ) ) ;
#41395=CARTESIAN_POINT ( 'NONE',  ( -4.898587196589412829E-16, 93.31250000409677625, -8.000000000000000000 ) ) ;
#41398=CARTESIAN_POINT ( 'NONE',  ( 7.188101187500000933, 2.062499997951610542, -2.977408999572650483 ) ) ;
#41401=CARTESIAN_POINT ( 'NONE',  ( -7.188101187499999156, 120.1250000020483952, 2.977408999572654924 ) ) ;
#41411=AXIS2_PLACEMENT_3D ( 'NONE', #45094, #62434, #57165 ) ;
#41428=CARTESIAN_POINT ( 'NONE',  ( -2.977408999572654480, 25.87499999795161543, 7.188101187499999156 ) ) ;
#41430=CARTESIAN_POINT ( 'NONE',  ( -2.977408999572652260, 99.31250000204838102, 7.188101187500000044 ) ) ;
#41442=VECTOR ( 'NONE', #66099, 1000.000000000000000 ) ;
#41452=CARTESIAN_POINT ( 'NONE',  ( -5.082755093536324154, 99.21875000204838102, 5.082755093536326818 ) ) ;
#41472=CARTESIAN_POINT ( 'NONE',  ( -5.656854249492380582, 102.5000000040967905, -5.656854249492380582 ) ) ;
#41479=ORIENTED_EDGE ( 'NONE', *, *, #24394, .F. ) ;
#41480=CARTESIAN_POINT ( 'NONE',  ( -5.656854249492379694, 24.56250000000000355, -5.656854249492380582 ) ) ;
#41481=CARTESIAN_POINT ( 'NONE',  ( -7.188101187500000044, 95.65625000204838102, 0.000000000000000000 ) ) ;
#41502=CARTESIAN_POINT ( 'NONE',  ( -2.977408999572650039, 7.312499997951610986, -7.188101187500001821 ) ) ;
#41506=CARTESIAN_POINT ( 'NONE',  ( 1.320432766682874540E-15, 114.4062500020483810, 7.188101187500000044 ) ) ;
#41527=CARTESIAN_POINT ( 'NONE',  ( 2.977408999572654480, 103.6250000020483810, 7.188101187499999156 ) ) ;
#41532=CARTESIAN_POINT ( 'NONE',  ( -7.188101187500001821, 112.4375000020483810, -2.977408999572650483 ) ) ;
#41538=CYLINDRICAL_SURFACE ( 'NONE', #69098, 8.000000000000000000 ) ;
#41557=CARTESIAN_POINT ( 'NONE',  ( 5.656854249492378806, 5.812500000000000888, 5.656854249492381470 ) ) ;
#41559=CARTESIAN_POINT ( 'NONE',  ( 7.188101187500000044, 1.968749997951610320, 0.000000000000000000 ) ) ;
#41561=CARTESIAN_POINT ( 'NONE',  ( -5.656854249492378806, 120.8750000040967905, 5.656854249492381470 ) ) ;
#41563=( BOUNDED_CURVE ( )  B_SPLINE_CURVE ( 2, ( #4373, #54945, #62441, #33067, #38713, #73769, #20963, #43987, #44361 ),
 .UNSPECIFIED., .F., .T. ) 
 B_SPLINE_CURVE_WITH_KNOTS ( ( 3, 2, 2, 2, 3 ),
 ( 0.5729166666666666297, 0.5781250000000000000, 0.5833333333333333703, 0.5885416666666666297, 0.5937500000000000000 ),
 .UNSPECIFIED. ) 
 CURVE ( )  GEOMETRIC_REPRESENTATION_ITEM ( )  RATIONAL_B_SPLINE_CURVE ( ( 1.000000000000000000, 0.9238795325112867385, 1.000000000000000000, 0.9238795325112867385, 1.000000000000000000, 0.9238795325112867385, 1.000000000000000000, 0.9238795325112867385, 1.000000000000000000 ) ) 
 REPRESENTATION_ITEM ( '' )  );
#41567=CARTESIAN_POINT ( 'NONE',  ( 0.000000000000000000, 125.0000000000000000, 0.000000000000000000 ) ) ;
#41574=CARTESIAN_POINT ( 'NONE',  ( 4.898587196589412829E-16, 22.68749999590322375, -8.000000000000000000 ) ) ;
#41589=CARTESIAN_POINT ( 'NONE',  ( -7.999999999999998224, 119.0937500000000000, 3.313708498984766493 ) ) ;
#41595=CARTESIAN_POINT ( 'NONE',  ( -8.000000000000000000, 13.96874999590322375, -3.313708498984762496 ) ) ;
#41622=CARTESIAN_POINT ( 'NONE',  ( -5.082755093536324154, 94.34375000204838102, 5.082755093536326818 ) ) ;
#41625=CARTESIAN_POINT ( 'NONE',  ( 4.725576163437660959, 0.3220367818099649226, -6.238486278272107555 ) ) ;
#41647=DIRECTION ( 'NONE',  ( 0.000000000000000000, -1.000000000000000000, 0.000000000000000000 ) ) ;
#41650=CARTESIAN_POINT ( 'NONE',  ( 7.188101187499999156, 12.37499999795161010, 2.977408999572654924 ) ) ;
#41652=CARTESIAN_POINT ( 'NONE',  ( -5.656854249492378806, 117.8750000040967905, 5.656854249492381470 ) ) ;
#41653=CARTESIAN_POINT ( 'NONE',  ( -5.082755093536326818, 13.78124999795161187, 5.082755093536325042 ) ) ;
#41666=CARTESIAN_POINT ( 'NONE',  ( -7.188101187499999156, 115.2500000020484094, 2.977408999572654924 ) ) ;
#41670=ORIENTED_EDGE ( 'NONE', *, *, #66956, .T. ) ;
#41671=( BOUNDED_CURVE ( )  B_SPLINE_CURVE ( 2, ( #39416, #16751, #62414, #11121, #33399, #56774, #73740, #67718, #21677 ),
 .UNSPECIFIED., .F., .F. ) 
 B_SPLINE_CURVE_WITH_KNOTS ( ( 3, 2, 2, 2, 3 ),
 ( 0.4687499999999998890, 0.4739583333333332593, 0.4791666666666666297, 0.4843750000000000000, 0.4895833333333333148 ),
 .UNSPECIFIED. ) 
 CURVE ( )  GEOMETRIC_REPRESENTATION_ITEM ( )  RATIONAL_B_SPLINE_CURVE ( ( 1.000000000000001554, 0.9238795325112850731, 1.000000000000000000, 0.9238795325112867385, 1.000000000000000000, 0.9238795325112867385, 1.000000000000000000, 0.9238795325112867385, 1.000000000000000000 ) ) 
 REPRESENTATION_ITEM ( '' )  );
#41672=CARTESIAN_POINT ( 'NONE',  ( -2.977408999572654480, 23.99999999795161543, 7.188101187499999156 ) ) ;
#41678=CARTESIAN_POINT ( 'NONE',  ( 2.977408999572650039, 101.5625000020483810, -7.188101187500001821 ) ) ;
#41685=CARTESIAN_POINT ( 'NONE',  ( -8.000000000000001776, 14.34375000000000178, 3.313708498984759387 ) ) ;
#41696=CARTESIAN_POINT ( 'NONE',  ( -4.898587196589412829E-16, 111.1250000000000000, -8.000000000000000000 ) ) ;
#41699=CARTESIAN_POINT ( 'NONE',  ( 7.999999999999998224, 10.40625000000000178, 3.313708498984766049 ) ) ;
#41706=CARTESIAN_POINT ( 'NONE',  ( 5.082755093536325042, 117.5937500020483810, -5.082755093536325930 ) ) ;
#41718=ORIENTED_EDGE ( 'NONE', *, *, #64424, .F. ) ;
#41723=DIRECTION ( 'NONE',  ( -0.000000000000000000, 1.000000000000000000, 0.000000000000000000 ) ) ;
#41736=CARTESIAN_POINT ( 'NONE',  ( 2.977408999572652260, 9.562499997951608322, 7.188101187500000044 ) ) ;
#41753=CARTESIAN_POINT ( 'NONE',  ( -5.656854249492379694, 26.06250000000000711, -5.656854249492380582 ) ) ;
#41763=CARTESIAN_POINT ( 'NONE',  ( -2.977408999572650039, 5.437499997951610986, -7.188101187500000933 ) ) ;
#41765=CARTESIAN_POINT ( 'NONE',  ( 2.977408999572654480, 119.0000000020483810, 7.188101187499999156 ) ) ;
#41778=PRODUCT_DEFINITION ( 'UNKNOWN', '', #23739, #45553 ) ;
#41790=EDGE_CURVE ( 'NONE', #60299, #44316, #46990, .T. ) ;
#41791=CARTESIAN_POINT ( 'NONE',  ( 5.082755093536325930, 20.53124999795161543, -5.082755093536325930 ) ) ;
#41793=CARTESIAN_POINT ( 'NONE',  ( -7.188101187500000044, 99.03125000204838102, 0.000000000000000000 ) ) ;
#41808=DIRECTION ( 'NONE',  ( -0.000000000000000000, 1.000000000000000000, -0.000000000000000000 ) ) ;
#41809=CARTESIAN_POINT ( 'NONE',  ( 5.082755093536326818, 90.21875000204838102, 5.082755093536325042 ) ) ;
#41814=CARTESIAN_POINT ( 'NONE',  ( 2.977408999572650039, 91.06250000204838102, -7.188101187500001821 ) ) ;
#41833=ORIENTED_EDGE ( 'NONE', *, *, #16454, .F. ) ;
#41834=CARTESIAN_POINT ( 'NONE',  ( -7.999999999999998224, 104.2812500040967763, 3.313708498984766493 ) ) ;
#41846=CARTESIAN_POINT ( 'NONE',  ( 5.082755093536326818, 97.71875000204838102, 5.082755093536325042 ) ) ;
#41852=CARTESIAN_POINT ( 'NONE',  ( -5.656854249492380582, 104.0000000040967905, -5.656854249492380582 ) ) ;
#41854=ORIENTED_EDGE ( 'NONE', *, *, #48591, .T. ) ;
#41867=CARTESIAN_POINT ( 'NONE',  ( 7.188101187500000044, 5.343749997951610098, 0.000000000000000000 ) ) ;
#41870=CARTESIAN_POINT ( 'NONE',  ( 7.188101187500000933, 114.8750000020483810, -2.977408999572651371 ) ) ;
#41874=CARTESIAN_POINT ( 'NONE',  ( -8.000000000000000000, 3.750000000000000888, -9.797174393178825657E-16 ) ) ;
#41876=LINE ( 'NONE', #3007, #44531 ) ;
#41881=CARTESIAN_POINT ( 'NONE',  ( 8.000000000000000000, 112.2500000000000000, -9.797174393178825657E-16 ) ) ;
#41889=CARTESIAN_POINT ( 'NONE',  ( 0.000000000000000000, 125.0000000000000000, 0.000000000000000000 ) ) ;
#41891=CARTESIAN_POINT ( 'NONE',  ( -7.188101187499999156, 103.2500000020483810, 2.977408999572654924 ) ) ;
#41897=CARTESIAN_POINT ( 'NONE',  ( 5.082755093536326818, 117.5937500020483810, 5.082755093536325042 ) ) ;
#41905=CARTESIAN_POINT ( 'NONE',  ( 1.469576158976823947E-15, 108.8750000000000000, 8.000000000000000000 ) ) ;
#41920=CARTESIAN_POINT ( 'NONE',  ( 3.313708498984762052, 3.281250000000001332, -8.000000000000000000 ) ) ;
#41922=CARTESIAN_POINT ( 'NONE',  ( 7.188101187499999156, 3.374999997951610098, 2.977408999572654924 ) ) ;
#41946=CARTESIAN_POINT ( 'NONE',  ( -3.313708498984760276, 12.28124999590322197, -8.000000000000000000 ) ) ;
#41948=CARTESIAN_POINT ( 'NONE',  ( 8.000000000000000000, 118.2500000000000000, -9.797174393178825657E-16 ) ) ;
#41952=CARTESIAN_POINT ( 'NONE',  ( 3.313708498984762496, 14.53124999590322375, 7.999999999999998224 ) ) ;
#41955=CARTESIAN_POINT ( 'NONE',  ( -4.898587196589412829E-16, 114.3125000040967905, -8.000000000000000000 ) ) ;
#41973=CARTESIAN_POINT ( 'NONE',  ( -5.082755093536325930, 120.9687500020483952, -5.082755093536325930 ) ) ;
#41975=VECTOR ( 'NONE', #30938, 1000.000000000000114 ) ;
#41978=CARTESIAN_POINT ( 'NONE',  ( 7.188101187500001821, 95.00000000204836681, -2.977408999572651371 ) ) ;
#41984=ORIENTED_EDGE ( 'NONE', *, *, #72397, .F. ) ;
#41986=CARTESIAN_POINT ( 'NONE',  ( 0.000000000000000000, 125.0000000000000000, 0.000000000000000000 ) ) ;
#41996=CYLINDRICAL_SURFACE ( 'NONE', #1099, 8.000000000000000000 ) ;
#42008=CARTESIAN_POINT ( 'NONE',  ( 7.188101187500000044, 15.46874999795161187, 0.000000000000000000 ) ) ;
#42010=CARTESIAN_POINT ( 'NONE',  ( 2.712922267096159246, 124.5269308481492487, -7.505356363335171643 ) ) ;
#42011=CARTESIAN_POINT ( 'NONE',  ( 5.082755093536324154, 11.15624999795161187, 5.082755093536326818 ) ) ;
#42024=CARTESIAN_POINT ( 'NONE',  ( 2.977408999572654480, 118.6250000020483810, 7.188101187499999156 ) ) ;
#42028=CARTESIAN_POINT ( 'NONE',  ( 2.977408999572650927, 23.24999999795161543, -7.188101187500000933 ) ) ;
#42035=CARTESIAN_POINT ( 'NONE',  ( -2.977408999572650927, 103.2500000020483810, -7.188101187500001821 ) ) ;
#42051=CARTESIAN_POINT ( 'NONE',  ( 3.313708498984711426, 97.15625000409679046, 8.000000000000053291 ) ) ;
#42053=CARTESIAN_POINT ( 'NONE',  ( 8.000000000000000000, 110.7500000000000000, -9.797174393178825657E-16 ) ) ;
#42060=CARTESIAN_POINT ( 'NONE',  ( -8.000000000000000000, 5.062499995903221084, -9.797174393178825657E-16 ) ) ;
#42062=CARTESIAN_POINT ( 'NONE',  ( 5.082755093536325042, 116.0937500020483810, -5.082755093536325930 ) ) ;
#42073=VERTEX_POINT ( 'NONE', #9617 ) ;
#42077=CARTESIAN_POINT ( 'NONE',  ( -4.898587196589412829E-16, 109.6250000000000000, -8.000000000000000000 ) ) ;
#42085=CARTESIAN_POINT ( 'NONE',  ( 3.313708498984761608, 22.78125000000000355, -8.000000000000000000 ) ) ;
#42089=CARTESIAN_POINT ( 'NONE',  ( 4.401442555609581635E-16, 10.21874999795161187, -7.188101187500000044 ) ) ;
#42093=DIRECTION ( 'NONE',  ( -0.000000000000000000, 1.000000000000000000, -0.000000000000000000 ) ) ;
#42094=CARTESIAN_POINT ( 'NONE',  ( 3.313708498984815343, 99.21875000409676204, -7.999999999999944933 ) ) ;
#42107=CARTESIAN_POINT ( 'NONE',  ( 3.313708498984762052, 24.28125000000000711, -8.000000000000000000 ) ) ;
#42118=CARTESIAN_POINT ( 'NONE',  ( -2.977408999572654480, 2.999999997951610542, 7.188101187499999156 ) ) ;
#42120=CARTESIAN_POINT ( 'NONE',  ( 1.320432766682874540E-15, 117.4062500020483810, 7.188101187500000044 ) ) ;
#42130=CARTESIAN_POINT ( 'NONE',  ( 5.656854249492380582, 3.187500000000000444, -5.656854249492380582 ) ) ;
#42133=CARTESIAN_POINT ( 'NONE',  ( 3.313708498984802020, 24.28125000000000000, -7.999999999999958256 ) ) ;
#42140=CARTESIAN_POINT ( 'NONE',  ( 1.347111479062088405E-15, 54.99999999999999289, -11.00000000000000000 ) ) ;
#42141=LINE ( 'NONE', #66646, #22441 ) ;
#42147=CARTESIAN_POINT ( 'NONE',  ( -2.977408999572650927, 94.25000000204838102, -7.188101187500000933 ) ) ;
#42165=CARTESIAN_POINT ( 'NONE',  ( -4.401442555609581635E-16, 89.28125000204838102, -7.188101187500000044 ) ) ;
#42190=CARTESIAN_POINT ( 'NONE',  ( 3.313708498984762496, 17.71875000000000355, 7.999999999999998224 ) ) ;
#42193=CARTESIAN_POINT ( 'NONE',  ( -7.999999999999998224, 96.78125000409679046, 3.313708498984766493 ) ) ;
#42203=CARTESIAN_POINT ( 'NONE',  ( 1.320432766682874540E-15, 99.03125000204838102, 7.188101187500000044 ) ) ;
#42227=CARTESIAN_POINT ( 'NONE',  ( -3.313708498984765161, 5.343749995903221084, 7.999999999999998224 ) ) ;
#42230=CARTESIAN_POINT ( 'NONE',  ( -2.977408999572654480, 4.874999997951610098, 7.188101187499999156 ) ) ;
#42233=CARTESIAN_POINT ( 'NONE',  ( -5.082755093536324154, 108.2187500020483810, 5.082755093536326818 ) ) ;
#42239=CARTESIAN_POINT ( 'NONE',  ( 0.000000000000000000, 125.0000000000000000, 0.000000000000000000 ) ) ;
#42255=CARTESIAN_POINT ( 'NONE',  ( -5.082755093536324154, 106.3437500020483810, 5.082755093536326818 ) ) ;
#42261=CARTESIAN_POINT ( 'NONE',  ( -2.977408999572650927, 110.7500000020483668, -7.188101187500001821 ) ) ;
#42267=EDGE_CURVE ( 'NONE', #60988, #54742, #3023, .T. ) ;
#42278=VERTEX_POINT ( 'NONE', #54779 ) ;
#42279=LINE ( 'NONE', #23829, #11233 ) ;
#42286=CARTESIAN_POINT ( 'NONE',  ( 3.313708498984762496, 4.218750000000000000, 7.999999999999998224 ) ) ;
#42287=CARTESIAN_POINT ( 'NONE',  ( 4.898587196589412829E-16, 10.87500000000000178, -8.000000000000000000 ) ) ;
#42288=CARTESIAN_POINT ( 'NONE',  ( -7.188101187500000044, 2.718749997951610098, -8.802885111219163269E-16 ) ) ;
#42289=CARTESIAN_POINT ( 'NONE',  ( 5.656854249492381470, 115.2500000040967905, 5.656854249492379694 ) ) ;
#42292=DIRECTION ( 'NONE',  ( 0.000000000000000000, 0.000000000000000000, 1.000000000000000000 ) ) ;
#42312=CARTESIAN_POINT ( 'NONE',  ( 5.656854249492379694, 104.9374999999999858, -5.656854249492380582 ) ) ;
#42314=CARTESIAN_POINT ( 'NONE',  ( 8.000000000000001776, 109.1562499999999858, 3.313708498984759387 ) ) ;
#42318=CARTESIAN_POINT ( 'NONE',  ( -5.656854249492379694, 16.87499999590322375, -5.656854249492380582 ) ) ;
#42329=CARTESIAN_POINT ( 'NONE',  ( 0.000000000000000000, 125.0000000000000000, 8.000000000000000000 ) ) ;
#42342=CARTESIAN_POINT ( 'NONE',  ( 2.977408999572650039, 123.6875000020483952, -7.188101187500000933 ) ) ;
#42343=CARTESIAN_POINT ( 'NONE',  ( 9.797174393178825657E-16, 125.0000000000000000, -8.000000000000000000 ) ) ;
#42348=CARTESIAN_POINT ( 'NONE',  ( 1.320432766682874540E-15, 90.03125000204838102, 7.188101187500000044 ) ) ;
#42352=EDGE_LOOP ( 'NONE', ( #42466, #10814, #65320, #58351 ) ) ;
#42361=VECTOR ( 'NONE', #56836, 1000.000000000000000 ) ;
#42365=VECTOR ( 'NONE', #5755, 1000.000000000000000 ) ;
#42372=ORIENTED_EDGE ( 'NONE', *, *, #55922, .T. ) ;
#42376=CARTESIAN_POINT ( 'NONE',  ( 7.188101187500000044, 16.96874999795161543, 0.000000000000000000 ) ) ;
#42379=CARTESIAN_POINT ( 'NONE',  ( 7.188101187500001821, 9.937499997951610098, -2.977408999572650483 ) ) ;
#42391=CARTESIAN_POINT ( 'NONE',  ( -5.082755093536324154, 107.8437500020483810, 5.082755093536326818 ) ) ;
#42395=CARTESIAN_POINT ( 'NONE',  ( 7.188101187500000044, 24.46874999795161543, 0.000000000000000000 ) ) ;
#42400=CARTESIAN_POINT ( 'NONE',  ( 7.188101187500000044, 102.7812500020483810, -8.802885111219163269E-16 ) ) ;
#42405=EDGE_CURVE ( 'NONE', #48764, #74424, #45990, .T. ) ;
#42407=CARTESIAN_POINT ( 'NONE',  ( -3.313708498984760276, 13.96875000000000355, -8.000000000000000000 ) ) ;
#42411=CARTESIAN_POINT ( 'NONE',  ( 5.656854249492381470, 107.7500000040967763, 5.656854249492379694 ) ) ;
#42417=CARTESIAN_POINT ( 'NONE',  ( -4.898587196589412829E-16, 106.6250000000000000, -8.000000000000000000 ) ) ;
#42418=CARTESIAN_POINT ( 'NONE',  ( 5.656854249492381470, 97.25000000409677625, 5.656854249492379694 ) ) ;
#42425=CARTESIAN_POINT ( 'NONE',  ( -5.656854249492379694, 7.874999995903221972, -5.656854249492380582 ) ) ;
#42430=CARTESIAN_POINT ( 'NONE',  ( -7.314694799365487832, 124.7669723012753167, -2.521986419001934099 ) ) ;
#42433=CARTESIAN_POINT ( 'NONE',  ( -5.082755093536324154, 107.8437500020483810, 5.082755093536326818 ) ) ;
#42438=CARTESIAN_POINT ( 'NONE',  ( -8.000000000000000000, 26.25000000000000711, -9.797174393178825657E-16 ) ) ;
#42449=DIRECTION ( 'NONE',  ( 0.000000000000000000, 0.000000000000000000, 1.000000000000000000 ) ) ;
#42450=CARTESIAN_POINT ( 'NONE',  ( -5.656854249492378806, 95.18750000000000000, 5.656854249492381470 ) ) ;
#42454=DIRECTION ( 'NONE',  ( 0.000000000000000000, -0.7071067811865425767, -0.7071067811865525687 ) ) ;
#42455=ORIENTED_EDGE ( 'NONE', *, *, #3521, .T. ) ;
#42462=CARTESIAN_POINT ( 'NONE',  ( 2.977408999572652260, 12.56249999795161365, 7.188101187500000044 ) ) ;
#42466=ORIENTED_EDGE ( 'NONE', *, *, #47817, .F. ) ;
#42472=CARTESIAN_POINT ( 'NONE',  ( -4.898587196589412829E-16, 93.31250000409677625, -8.000000000000000000 ) ) ;
#42480=CARTESIAN_POINT ( 'NONE',  ( 3.313708498984762496, 23.71875000000000355, 7.999999999999998224 ) ) ;
#42491=CARTESIAN_POINT ( 'NONE',  ( 7.188101187500000044, 4.968749997951610986, 0.000000000000000000 ) ) ;
#42495=CARTESIAN_POINT ( 'NONE',  ( 5.082755093536326818, 117.5937500020483810, 5.082755093536325042 ) ) ;
#42504=LINE ( 'NONE', #8179, #73113 ) ;
#42506=EDGE_LOOP ( 'NONE', ( #18444, #29863, #35539, #26870 ) ) ;
#42508=CARTESIAN_POINT ( 'NONE',  ( 5.656854249492379694, 97.43750000000000000, -5.656854249492380582 ) ) ;
#42518=CARTESIAN_POINT ( 'NONE',  ( 5.656854249492379694, 100.4375000000000000, -5.656854249492380582 ) ) ;
#42526=CARTESIAN_POINT ( 'NONE',  ( 2.977408999572650039, 94.06250000204838102, -7.188101187500000933 ) ) ;
#42541=CARTESIAN_POINT ( 'NONE',  ( -7.999999999999998224, 102.5937500000000000, 3.313708498984766049 ) ) ;
#42549=CARTESIAN_POINT ( 'NONE',  ( -2.977408999572651815, 93.31250000204838102, 7.188101187500000933 ) ) ;
#42555=EDGE_LOOP ( 'NONE', ( #64779, #68649, #46645, #7067 ) ) ;
#42567=VECTOR ( 'NONE', #14943, 1000.000000000000000 ) ;
#42570=CARTESIAN_POINT ( 'NONE',  ( 8.000000000000000000, 97.43750000409677625, -9.797174393178825657E-16 ) ) ;
#42580=CARTESIAN_POINT ( 'NONE',  ( 7.188101187500000044, 96.40625000204838102, -8.802885111219163269E-16 ) ) ;
#42603=CARTESIAN_POINT ( 'NONE',  ( -2.977408999572654480, 9.374999997951610098, 7.188101187499999156 ) ) ;
#42606=CARTESIAN_POINT ( 'NONE',  ( 7.188101187500002709, 108.6875000020483810, 2.977408999572649151 ) ) ;
#42624=CARTESIAN_POINT ( 'NONE',  ( -1.469576158976823947E-15, 24.93749999590322375, 8.000000000000000000 ) ) ;
#42625=CARTESIAN_POINT ( 'NONE',  ( 1.320432766682874540E-15, 105.0312500020483810, 7.188101187500000044 ) ) ;
#42633=CARTESIAN_POINT ( 'NONE',  ( -5.082755093536325930, 107.8437500020483810, -5.082755093536325930 ) ) ;
#42657=CARTESIAN_POINT ( 'NONE',  ( -3.313708498984765161, 11.53125000000000178, 7.999999999999998224 ) ) ;
#42659=CARTESIAN_POINT ( 'NONE',  ( -2.977408999572650039, 2.437499997951610542, -7.188101187500001821 ) ) ;
#42660=CARTESIAN_POINT ( 'NONE',  ( -3.313708498984762496, 116.4687500040967905, 7.999999999999998224 ) ) ;
#42684=CARTESIAN_POINT ( 'NONE',  ( -8.000000000000000000, 114.4062500000000142, -3.313708498984761608 ) ) ;
#42689=CARTESIAN_POINT ( 'NONE',  ( 8.000000000000000000, 22.31249999590322375, 0.000000000000000000 ) ) ;
#42712=CARTESIAN_POINT ( 'NONE',  ( 2.977408999572650039, 122.1875000020483810, -7.188101187500000933 ) ) ;
#42718=CARTESIAN_POINT ( 'NONE',  ( 7.188101187500000044, 90.40625000204838102, -8.802885111219163269E-16 ) ) ;
#42722=ORIENTED_EDGE ( 'NONE', *, *, #2140, .T. ) ;
#42745=CARTESIAN_POINT ( 'NONE',  ( 7.188101187500001821, 23.06249999795161187, -2.977408999572650483 ) ) ;
#42748=CARTESIAN_POINT ( 'NONE',  ( -7.188101187500000044, 13.59374999795161187, -8.802885111219163269E-16 ) ) ;
#42751=( BOUNDED_CURVE ( )  B_SPLINE_CURVE ( 2, ( #4685, #52836, #12094, #69816, #17380, #70192, #41148, #40404, #58874 ),
 .UNSPECIFIED., .F., .F. ) 
 B_SPLINE_CURVE_WITH_KNOTS ( ( 3, 2, 2, 2, 3 ),
 ( 0.9479166666666665186, 0.9531249999999998890, 0.9583333333333332593, 0.9635416666666666297, 0.9687500000000000000 ),
 .UNSPECIFIED. ) 
 CURVE ( )  GEOMETRIC_REPRESENTATION_ITEM ( )  RATIONAL_B_SPLINE_CURVE ( ( 1.000000000000001554, 0.9238795325112850731, 1.000000000000000000, 0.9238795325112867385, 1.000000000000000000, 0.9238795325112867385, 1.000000000000000000, 0.9238795325112867385, 1.000000000000000000 ) ) 
 REPRESENTATION_ITEM ( '' )  );
#42759=CARTESIAN_POINT ( 'NONE',  ( 7.188101187500002709, 112.8125000020483952, 2.977408999572649151 ) ) ;
#42764=CARTESIAN_POINT ( 'NONE',  ( 5.082755093536324154, 24.28124999795161543, 5.082755093536326818 ) ) ;
#42771=CARTESIAN_POINT ( 'NONE',  ( 5.082755093536325042, 96.96875000204838102, -5.082755093536325930 ) ) ;
#42788=CARTESIAN_POINT ( 'NONE',  ( -3.313708498984830442, 117.7812500000000000, 7.999999999999930722 ) ) ;
#42792=ORIENTED_EDGE ( 'NONE', *, *, #71684, .F. ) ;
#42796=CARTESIAN_POINT ( 'NONE',  ( -3.313708498984640816, 116.2812499999999858, 8.000000000000119016 ) ) ;
#42800=CARTESIAN_POINT ( 'NONE',  ( 7.188101187500002709, 108.3125000020483810, 2.977408999572649151 ) ) ;
#42825=CARTESIAN_POINT ( 'NONE',  ( -7.188101187500002709, 13.68749999795161187, 2.977408999572649151 ) ) ;
#42828=ORIENTED_EDGE ( 'NONE', *, *, #15670, .F. ) ;
#42833=CARTESIAN_POINT ( 'NONE',  ( 5.082755093536325930, 0.6562499979516100979, -5.082755093536325930 ) ) ;
#42836=FACE_OUTER_BOUND ( 'NONE', #74136, .T. ) ;
#42844=CARTESIAN_POINT ( 'NONE',  ( 8.000000000000000000, 25.59375000000000355, -3.313708498984761608 ) ) ;
#42854=CARTESIAN_POINT ( 'NONE',  ( -7.188101187500002709, 4.312499997951610986, 2.977408999572649151 ) ) ;
#42857=CARTESIAN_POINT ( 'NONE',  ( -2.977408999572651815, 109.8125000020483952, 7.188101187500000933 ) ) ;
#42862=( BOUNDED_CURVE ( )  B_SPLINE_CURVE ( 2, ( #1963, #24593, #42312, #31749, #1609, #2329, #13632, #59680, #14375 ),
 .UNSPECIFIED., .F., .F. ) 
 B_SPLINE_CURVE_WITH_KNOTS ( ( 3, 2, 2, 2, 3 ),
 ( 0.5520833333333332593, 0.5572916666666665186, 0.5625000000000000000, 0.5677083333333333703, 0.5729166666666666297 ),
 .UNSPECIFIED. ) 
 CURVE ( )  GEOMETRIC_REPRESENTATION_ITEM ( )  RATIONAL_B_SPLINE_CURVE ( ( 1.000000000000001554, 0.9238795325112850731, 1.000000000000000000, 0.9238795325112867385, 1.000000000000000000, 0.9238795325112867385, 1.000000000000000000, 0.9238795325112867385, 1.000000000000000000 ) ) 
 REPRESENTATION_ITEM ( '' )  );
#42871=CARTESIAN_POINT ( 'NONE',  ( -8.000000000000000000, 102.4062499999999858, -3.313708498984761608 ) ) ;
#42886=CARTESIAN_POINT ( 'NONE',  ( -4.401442555609581635E-16, 89.65625000204838102, -7.188101187500000044 ) ) ;
#42904=CARTESIAN_POINT ( 'NONE',  ( -4.898587196589412829E-16, 102.3125000040967763, -8.000000000000000000 ) ) ;
#42911=CARTESIAN_POINT ( 'NONE',  ( -5.082755093536325930, 92.84375000204838102, -5.082755093536325930 ) ) ;
#42931=ORIENTED_EDGE ( 'NONE', *, *, #69039, .F. ) ;
#42933=ADVANCED_FACE ( 'NONE', ( #35490 ), #70189, .T. ) ;
#42935=CARTESIAN_POINT ( 'NONE',  ( 8.000000000000001776, 97.34375000409679046, 3.313708498984759387 ) ) ;
#42943=CARTESIAN_POINT ( 'NONE',  ( 5.082755093536326818, 96.21875000204838102, 5.082755093536325042 ) ) ;
#42954=ORIENTED_EDGE ( 'NONE', *, *, #73059, .T. ) ;
#42965=FACE_OUTER_BOUND ( 'NONE', #55171, .T. ) ;
#42967=CARTESIAN_POINT ( 'NONE',  ( 5.082755093536324154, 9.656249997951610098, 5.082755093536326818 ) ) ;
#42969=CYLINDRICAL_SURFACE ( 'NONE', #38331, 8.000000000000000000 ) ;
#42970=CARTESIAN_POINT ( 'NONE',  ( 7.188101187500002709, 111.6875000020483810, 2.977408999572649151 ) ) ;
#42973=DIRECTION ( 'NONE',  ( 0.000000000000000000, 0.000000000000000000, 1.000000000000000000 ) ) ;
#42980=( BOUNDED_CURVE ( )  B_SPLINE_CURVE ( 2, ( #34885, #5826, #28822, #551, #68812, #28454, #13219, #57890, #74105 ),
 .UNSPECIFIED., .F., .F. ) 
 B_SPLINE_CURVE_WITH_KNOTS ( ( 3, 2, 2, 2, 3 ),
 ( 0.1805555555555555525, 0.1875000000000000000, 0.1944444444444444198, 0.2013888888888888673, 0.2083333333333333148 ),
 .UNSPECIFIED. ) 
 CURVE ( )  GEOMETRIC_REPRESENTATION_ITEM ( )  RATIONAL_B_SPLINE_CURVE ( ( 1.000000000000000000, 0.9238795325112867385, 1.000000000000000000, 0.9238795325112867385, 1.000000000000000000, 0.9238795325112867385, 1.000000000000000000, 0.9238795325112870716, 0.9999999999999996669 ) ) 
 REPRESENTATION_ITEM ( '' )  );
#42990=CARTESIAN_POINT ( 'NONE',  ( 7.999999999999998224, 25.21874999590322020, 3.313708498984766049 ) ) ;
#42991=CARTESIAN_POINT ( 'NONE',  ( -7.188101187500000044, 100.1562500020483810, 0.000000000000000000 ) ) ;
#42996=CARTESIAN_POINT ( 'NONE',  ( -4.401442555609581635E-16, 109.1562500020483810, -7.188101187500000044 ) ) ;
#43001=VERTEX_POINT ( 'NONE', #18498 ) ;
#43023=CARTESIAN_POINT ( 'NONE',  ( -1.320432766682874540E-15, 9.093749997951610098, 7.188101187500000044 ) ) ;
#43024=CARTESIAN_POINT ( 'NONE',  ( 8.000000000000000000, 115.5312500040968047, -3.313708498984762496 ) ) ;
#43053=CARTESIAN_POINT ( 'NONE',  ( -4.898587196589412829E-16, 112.6250000000000000, -8.000000000000000000 ) ) ;
#43057=CARTESIAN_POINT ( 'NONE',  ( -8.000000000000000000, 102.6875000040967763, 0.000000000000000000 ) ) ;
#43059=CARTESIAN_POINT ( 'NONE',  ( 8.000000000000000000, 23.81249999590322020, 0.000000000000000000 ) ) ;
#43062=CARTESIAN_POINT ( 'NONE',  ( 5.656854249492379694, 121.4375000000000000, -5.656854249492380582 ) ) ;
#43071=CARTESIAN_POINT ( 'NONE',  ( -5.656854249492380582, 99.50000000409679046, -5.656854249492380582 ) ) ;
#43072=CARTESIAN_POINT ( 'NONE',  ( 0.000000000000000000, 125.0000000000000000, 0.000000000000000000 ) ) ;
#43082=CARTESIAN_POINT ( 'NONE',  ( -4.401442555609581635E-16, 122.2812500020483810, -7.188101187500000044 ) ) ;
#43087=CARTESIAN_POINT ( 'NONE',  ( 2.977408999572650039, 93.68750000204838102, -7.188101187500001821 ) ) ;
#43104=CARTESIAN_POINT ( 'NONE',  ( 3.313708498984762496, 22.03124999590322375, 7.999999999999998224 ) ) ;
#43115=CARTESIAN_POINT ( 'NONE',  ( 5.082755093536324154, 21.28124999795161543, 5.082755093536326818 ) ) ;
#43118=CARTESIAN_POINT ( 'NONE',  ( -8.000000000000000000, 117.5937500040967905, -3.313708498984761164 ) ) ;
#43119=CARTESIAN_POINT ( 'NONE',  ( -7.188101187500000044, 10.59374999795161187, -8.802885111219163269E-16 ) ) ;
#43125=CARTESIAN_POINT ( 'NONE',  ( 3.898495371540924292, 89.88208674283050925, -6.752431955835072941 ) ) ;
#43133=CARTESIAN_POINT ( 'NONE',  ( -7.188101187499999156, 110.7500000020483668, 2.977408999572654924 ) ) ;
#43138=CARTESIAN_POINT ( 'NONE',  ( 2.977408999572650927, 26.24999999795161543, -7.188101187500000933 ) ) ;
#43145=CARTESIAN_POINT ( 'NONE',  ( -7.188101187499999156, 94.62500000204838102, 2.977408999572654924 ) ) ;
#43158=DIRECTION ( 'NONE',  ( 0.000000000000000000, -1.000000000000000000, 0.000000000000000000 ) ) ;
#43175=CARTESIAN_POINT ( 'NONE',  ( -5.082755093536324154, 109.3437500020483810, 5.082755093536326818 ) ) ;
#43196=CARTESIAN_POINT ( 'NONE',  ( 1.469576158976823947E-15, 119.3750000000000000, 8.000000000000000000 ) ) ;
#43201=CARTESIAN_POINT ( 'NONE',  ( -1.320432766682874540E-15, 15.46874999795161187, 7.188101187500000044 ) ) ;
#43202=( BOUNDED_CURVE ( )  B_SPLINE_CURVE ( 2, ( #65561, #36901, #59909, #2570, #65931, #2940, #45806, #33770, #39042 ),
 .UNSPECIFIED., .F., .F. ) 
 B_SPLINE_CURVE_WITH_KNOTS ( ( 3, 2, 2, 2, 3 ),
 ( 0.2812499999999997780, 0.2864583333333330928, 0.2916666666666665186, 0.2968749999999998335, 0.3020833333333331483 ),
 .UNSPECIFIED. ) 
 CURVE ( )  GEOMETRIC_REPRESENTATION_ITEM ( )  RATIONAL_B_SPLINE_CURVE ( ( 1.000000000000003331, 0.9238795325112835188, 1.000000000000000000, 0.9238795325112867385, 1.000000000000000000, 0.9238795325112867385, 1.000000000000000000, 0.9238795325112891810, 0.9999999999999975575 ) ) 
 REPRESENTATION_ITEM ( '' )  );
#43211=CARTESIAN_POINT ( 'NONE',  ( 5.082755093536325930, 2.156249997951610098, -5.082755093536325930 ) ) ;
#43232=CARTESIAN_POINT ( 'NONE',  ( 7.188101187499999156, 3.374999997951610098, 2.977408999572654924 ) ) ;
#43236=CARTESIAN_POINT ( 'NONE',  ( 5.082755093536325042, 110.4687500020483810, -5.082755093536325930 ) ) ;
#43237=DIRECTION ( 'NONE',  ( 0.000000000000000000, 0.000000000000000000, 1.000000000000000000 ) ) ;
#43245=CARTESIAN_POINT ( 'NONE',  ( 8.000000000000000000, 106.2500000000000000, -9.797174393178825657E-16 ) ) ;
#43250=CARTESIAN_POINT ( 'NONE',  ( 5.656854249492379694, 91.43749999999998579, -5.656854249492380582 ) ) ;
#43257=CARTESIAN_POINT ( 'NONE',  ( 7.188101187500000044, 27.65624999795161543, 0.000000000000000000 ) ) ;
#43263=LINE ( 'NONE', #3288, #64144 ) ;
#43265=CARTESIAN_POINT ( 'NONE',  ( -5.082755093536325930, 94.34375000204838102, -5.082755093536325930 ) ) ;
#43270=CARTESIAN_POINT ( 'NONE',  ( 1.469576158976823947E-15, 96.87499999999998579, 8.000000000000000000 ) ) ;
#43275=CARTESIAN_POINT ( 'NONE',  ( 4.401442555609581635E-16, 20.34374999795161543, -7.188101187500000044 ) ) ;
#43276=CARTESIAN_POINT ( 'NONE',  ( -8.000000000000000000, 108.6875000040967905, 0.000000000000000000 ) ) ;
#43292=CARTESIAN_POINT ( 'NONE',  ( -7.188101187500001821, 91.43750000204838102, -2.977408999572650483 ) ) ;
#43304=CARTESIAN_POINT ( 'NONE',  ( 8.000000000000000000, 2.812499995903220640, 0.000000000000000000 ) ) ;
#43312=CARTESIAN_POINT ( 'NONE',  ( -3.313708498984762496, 98.46875000409676204, 7.999999999999998224 ) ) ;
#43313=( BOUNDED_CURVE ( )  B_SPLINE_CURVE ( 2, ( #15029, #2231, #1868, #65600, #31651, #38063, #59941, #55045, #8257 ),
 .UNSPECIFIED., .F., .F. ) 
 B_SPLINE_CURVE_WITH_KNOTS ( ( 3, 2, 2, 2, 3 ),
 ( 0.6145833333333333703, 0.6197916666666666297, 0.6250000000000000000, 0.6302083333333334814, 0.6354166666666667407 ),
 .UNSPECIFIED. ) 
 CURVE ( )  GEOMETRIC_REPRESENTATION_ITEM ( )  RATIONAL_B_SPLINE_CURVE ( ( 1.000000000000000000, 0.9238795325112867385, 1.000000000000000000, 0.9238795325112867385, 1.000000000000000000, 0.9238795325112867385, 1.000000000000000000, 0.9238795325112850731, 1.000000000000001554 ) ) 
 REPRESENTATION_ITEM ( '' )  );
#43323=CARTESIAN_POINT ( 'NONE',  ( -5.082755093536325930, 90.96875000204838102, -5.082755093536325930 ) ) ;
#43339=CARTESIAN_POINT ( 'NONE',  ( 1.469576158976823947E-15, 91.06250000409676204, 8.000000000000000000 ) ) ;
#43342=CARTESIAN_POINT ( 'NONE',  ( -5.656854249492381470, 3.749999995903220640, 5.656854249492379694 ) ) ;
#43345=CARTESIAN_POINT ( 'NONE',  ( -2.977408999572650039, 10.31249999795161010, -7.188101187500001821 ) ) ;
#43348=CARTESIAN_POINT ( 'NONE',  ( -2.977408999572652260, 108.3125000020483810, 7.188101187500000044 ) ) ;
#43361=ADVANCED_FACE ( 'NONE', ( #4500 ), #44860, .T. ) ;
#43367=CARTESIAN_POINT ( 'NONE',  ( 1.320432766682874540E-15, 102.0312500020483810, 7.188101187500000044 ) ) ;
#43374=CARTESIAN_POINT ( 'NONE',  ( 5.082755093536325042, 110.4687500020483810, -5.082755093536325930 ) ) ;
#43393=FACE_BOUND ( 'NONE', #19620, .T. ) ;
#43394=CARTESIAN_POINT ( 'NONE',  ( 1.469576158976823947E-15, 122.5625000040967763, 8.000000000000000000 ) ) ;
#43401=CARTESIAN_POINT ( 'NONE',  ( -7.188101187500002709, 8.812499997951611874, 2.977408999572649151 ) ) ;
#43402=CARTESIAN_POINT ( 'NONE',  ( 8.000000000000000000, 115.4375000040967763, -9.797174393178825657E-16 ) ) ;
#43418=VERTEX_POINT ( 'NONE', #62201 ) ;
#43423=CARTESIAN_POINT ( 'NONE',  ( 8.000000000000000000, 26.81249999590322375, 0.000000000000000000 ) ) ;
#43430=CARTESIAN_POINT ( 'NONE',  ( 8.000000000000000000, 112.2500000000000000, -9.797174393178825657E-16 ) ) ;
#43435=CARTESIAN_POINT ( 'NONE',  ( -3.313708498984765161, 23.34374999590322020, 7.999999999999998224 ) ) ;
#43448=LINE ( 'NONE', #26850, #33464 ) ;
#43449=LINE ( 'NONE', #26088, #25400 ) ;
#43458=CARTESIAN_POINT ( 'NONE',  ( 2.977408999572650039, 117.6875000020484237, -7.188101187500000933 ) ) ;
#43459=LINE ( 'NONE', #3112, #41442 ) ;
#43464=CARTESIAN_POINT ( 'NONE',  ( 1.320432766682874540E-15, 91.53125000204836681, 7.188101187500000044 ) ) ;
#43490=CARTESIAN_POINT ( 'NONE',  ( 7.188101187500001821, 20.06249999795161543, -2.977408999572650483 ) ) ;
#43494=CARTESIAN_POINT ( 'NONE',  ( 5.082755093536325930, 16.03124999795161543, -5.082755093536325930 ) ) ;
#43497=CONICAL_SURFACE ( 'NONE', #10985, 8.000000000000000000, 0.7853981633974552734 ) ;
#43505=CARTESIAN_POINT ( 'NONE',  ( -5.082755093536324154, 109.3437500020483810, 5.082755093536326818 ) ) ;
#43506=CARTESIAN_POINT ( 'NONE',  ( 5.656854249492381470, 94.25000000409677625, 5.656854249492379694 ) ) ;
#43515=CARTESIAN_POINT ( 'NONE',  ( -2.977408999572651815, 96.31250000204838102, 7.188101187500000933 ) ) ;
#43527=CARTESIAN_POINT ( 'NONE',  ( 3.313708498984733186, 108.2187500040967763, -8.000000000000026645 ) ) ;
#43537=CARTESIAN_POINT ( 'NONE',  ( 3.313708498984819339, 109.1562500040967905, 7.999999999999943157 ) ) ;
#43548=CARTESIAN_POINT ( 'NONE',  ( 7.188101187500002709, 109.8125000020483952, 2.977408999572649151 ) ) ;
#43556=DIRECTION ( 'NONE',  ( -0.000000000000000000, 1.000000000000000000, -0.000000000000000000 ) ) ;
#43559=CARTESIAN_POINT ( 'NONE',  ( 1.469576158976823947E-15, 99.87499999999998579, 8.000000000000000000 ) ) ;
#43577=CARTESIAN_POINT ( 'NONE',  ( -5.082755093536326818, 16.78124999795161543, 5.082755093536325042 ) ) ;
#43586=FACE_OUTER_BOUND ( 'NONE', #27535, .T. ) ;
#43601=B_SPLINE_CURVE_WITH_KNOTS ( 'NONE', 3,
 ( #23524, #10721, #33753, #28070, #16733, #57127, #28444, #63890, #52575, #52950, #17867, #35602, #18614, #41625, #53322, #70660, #69556, #8679, #35970, #49029, #47273, #35239 ),
 .UNSPECIFIED., .F., .F.,
 ( 4, 2, 2, 2, 2, 2, 2, 2, 2, 2, 4 ),
 ( 0.000000000000000000, 0.001533419618775805826, 0.002300129428163708630, 0.003066839237551611651, 0.004600258856327418995, 0.006133678475103227640, 0.006900388284491131528, 0.007667098093879036284, 0.009200517712654843194, 0.01073393733143065097, 0.01226735695020646048 ),
 .UNSPECIFIED. ) ;
#43605=CARTESIAN_POINT ( 'NONE',  ( -2.977408999572654480, 8.999999997951610098, 7.188101187499999156 ) ) ;
#43610=CARTESIAN_POINT ( 'NONE',  ( 7.188101187500002709, 110.1875000020483810, 2.977408999572649151 ) ) ;
#43621=CARTESIAN_POINT ( 'NONE',  ( 3.313708498984760276, 106.5312500000000142, -8.000000000000000000 ) ) ;
#43627=CARTESIAN_POINT ( 'NONE',  ( 8.000000000000000000, 24.09375000000000355, -3.313708498984761164 ) ) ;
#43628=CARTESIAN_POINT ( 'NONE',  ( 8.000000000000000000, 92.75000000000000000, -9.797174393178825657E-16 ) ) ;
#43641=CARTESIAN_POINT ( 'NONE',  ( 2.977408999572651815, 27.56249999795161187, 7.188101187500000933 ) ) ;
#43643=CARTESIAN_POINT ( 'NONE',  ( -7.188101187499999156, 94.62500000204838102, 2.977408999572654924 ) ) ;
#43653=CARTESIAN_POINT ( 'NONE',  ( 5.082755093536324154, 16.78124999795161543, 5.082755093536326818 ) ) ;
#43657=EDGE_LOOP ( 'NONE', ( #58742, #43712, #51452, #46575 ) ) ;
#43667=CARTESIAN_POINT ( 'NONE',  ( 4.898587196589412829E-16, 21.18749999590322375, -8.000000000000000000 ) ) ;
#43677=ORIENTED_EDGE ( 'NONE', *, *, #18816, .T. ) ;
#43690=CARTESIAN_POINT ( 'NONE',  ( 3.313708498984802020, 18.28125000000000355, -7.999999999999958256 ) ) ;
#43691=ORIENTED_EDGE ( 'NONE', *, *, #74202, .T. ) ;
#43693=CARTESIAN_POINT ( 'NONE',  ( 5.656854249492381470, 98.75000000409677625, 5.656854249492379694 ) ) ;
#43703=CARTESIAN_POINT ( 'NONE',  ( -2.977408999572651815, 91.43750000204838102, 7.188101187500000933 ) ) ;
#43704=ADVANCED_FACE ( 'NONE', ( #50693 ), #14866, .T. ) ;
#43712=ORIENTED_EDGE ( 'NONE', *, *, #61207, .F. ) ;
#43714=ORIENTED_EDGE ( 'NONE', *, *, #39239, .F. ) ;
#43725=CARTESIAN_POINT ( 'NONE',  ( -8.000000000000000000, 2.062499995903220196, -9.797174393178825657E-16 ) ) ;
#43727=CARTESIAN_POINT ( 'NONE',  ( 7.188101187500001821, 12.93749999795161365, -2.977408999572650483 ) ) ;
#43730=CARTESIAN_POINT ( 'NONE',  ( 5.082755093536325042, 107.4687500020483952, -5.082755093536325930 ) ) ;
#43733=DIRECTION ( 'NONE',  ( -0.000000000000000000, 1.000000000000000000, -0.000000000000000000 ) ) ;
#43742=ORIENTED_EDGE ( 'NONE', *, *, #46821, .T. ) ;
#43750=CARTESIAN_POINT ( 'NONE',  ( -2.977408999572652260, 100.4375000020483810, 7.188101187500000044 ) ) ;
#43756=CARTESIAN_POINT ( 'NONE',  ( -2.977408999572650927, 103.2500000020483810, -7.188101187500001821 ) ) ;
#43757=VERTEX_POINT ( 'NONE', #49959 ) ;
#43765=DIRECTION ( 'NONE',  ( 0.000000000000000000, 0.000000000000000000, 1.000000000000000000 ) ) ;
#43767=CARTESIAN_POINT ( 'NONE',  ( -7.188101187500000933, 2.999999997951610542, -2.977408999572651371 ) ) ;
#43773=( BOUNDED_CURVE ( )  B_SPLINE_CURVE ( 2, ( #31845, #3548, #49564, #50307, #61636, #62002, #44657, #26164, #9954 ),
 .UNSPECIFIED., .F., .F. ) 
 B_SPLINE_CURVE_WITH_KNOTS ( ( 3, 2, 2, 2, 3 ),
 ( 0.2638888888888889506, 0.2708333333333333703, 0.2777777777777778456, 0.2847222222222222654, 0.2916666666666667407 ),
 .UNSPECIFIED. ) 
 CURVE ( )  GEOMETRIC_REPRESENTATION_ITEM ( )  RATIONAL_B_SPLINE_CURVE ( ( 0.9999999999999994449, 0.9238795325112872936, 1.000000000000000000, 0.9238795325112867385, 1.000000000000000000, 0.9238795325112867385, 1.000000000000000000, 0.9238795325112861834, 1.000000000000000666 ) ) 
 REPRESENTATION_ITEM ( '' )  );
#43774=CARTESIAN_POINT ( 'NONE',  ( 8.000000000000000000, 1.406249995903220196, -3.313708498984761164 ) ) ;
#43775=VECTOR ( 'NONE', #18160, 1000.000000000000000 ) ;
#43784=CARTESIAN_POINT ( 'NONE',  ( -5.082755093536326818, 7.406249997951610986, 5.082755093536325042 ) ) ;
#43785=CARTESIAN_POINT ( 'NONE',  ( -8.000000000000000000, 117.6875000040967763, 0.000000000000000000 ) ) ;
#43787=ADVANCED_FACE ( 'NONE', ( #45049 ), #27309, .T. ) ;
#43813=CARTESIAN_POINT ( 'NONE',  ( 8.000000000000000000, 113.8437500000000000, -3.313708498984762496 ) ) ;
#43819=CARTESIAN_POINT ( 'NONE',  ( 8.000000000000000000, 19.40624999590322375, -3.313708498984761608 ) ) ;
#43834=CARTESIAN_POINT ( 'NONE',  ( 5.656854249492379694, 102.1250000040967763, -5.656854249492380582 ) ) ;
#43835=VERTEX_POINT ( 'NONE', #21650 ) ;
#43842=CARTESIAN_POINT ( 'NONE',  ( -5.082755093536325930, 116.4687500020483810, -5.082755093536325930 ) ) ;
#43847=CARTESIAN_POINT ( 'NONE',  ( 7.188101187500000044, 123.7812500020483810, -8.802885111219163269E-16 ) ) ;
#43856=VECTOR ( 'NONE', #60440, 1000.000000000000000 ) ;
#43863=CARTESIAN_POINT ( 'NONE',  ( -1.469576158976823947E-15, 21.93749999590322375, 8.000000000000000000 ) ) ;
#43873=CARTESIAN_POINT ( 'NONE',  ( -5.082755093536325042, 22.03124999795161543, -5.082755093536325930 ) ) ;
#43876=CARTESIAN_POINT ( 'NONE',  ( 2.977408999572650927, 16.12499999795161187, -7.188101187500001821 ) ) ;
#43881=CYLINDRICAL_SURFACE ( 'NONE', #1679, 8.000000000000000000 ) ;
#43903=CARTESIAN_POINT ( 'NONE',  ( 5.082755093536326818, 96.59375000204838102, 5.082755093536325042 ) ) ;
#43907=DIRECTION ( 'NONE',  ( 0.000000000000000000, 0.000000000000000000, 1.000000000000000000 ) ) ;
#43909=CARTESIAN_POINT ( 'NONE',  ( 8.000000000000000000, 94.25000000000000000, -9.797174393178825657E-16 ) ) ;
#43934=CARTESIAN_POINT ( 'NONE',  ( 2.977408999572654480, 108.1250000020483810, 7.188101187499999156 ) ) ;
#43951=LINE ( 'NONE', #3591, #18462 ) ;
#43952=CARTESIAN_POINT ( 'NONE',  ( -3.313708498984653250, 94.71874999999998579, -8.000000000000108358 ) ) ;
#43960=CARTESIAN_POINT ( 'NONE',  ( 5.082755093536324154, 17.15624999795161543, 5.082755093536326818 ) ) ;
#43969=CARTESIAN_POINT ( 'NONE',  ( 7.188101187500000044, 0.4687499979516099868, 0.000000000000000000 ) ) ;
#43972=CARTESIAN_POINT ( 'NONE',  ( -5.656854249492379694, 16.87499999590322375, -5.656854249492380582 ) ) ;
#43987=CARTESIAN_POINT ( 'NONE',  ( -3.313708498984761608, 103.7187500000000000, -8.000000000000000000 ) ) ;
#43989=CARTESIAN_POINT ( 'NONE',  ( 4.401442555609581635E-16, 8.343749997951611874, -7.188101187500000044 ) ) ;
#43993=CARTESIAN_POINT ( 'NONE',  ( 2.977408999572654480, 113.0000000020483668, 7.188101187499999156 ) ) ;
#44001=EDGE_CURVE ( 'NONE', #19911, #67659, #26136, .T. ) ;
#44009=CARTESIAN_POINT ( 'NONE',  ( -3.313708498984762052, 91.71874999999998579, -8.000000000000000000 ) ) ;
#44023=ADVANCED_FACE ( 'NONE', ( #68796 ), #46900, .T. ) ;
#44026=CARTESIAN_POINT ( 'NONE',  ( 7.188101187500000044, 0.4687499979516099868, 0.000000000000000000 ) ) ;
#44034=CARTESIAN_POINT ( 'NONE',  ( 8.000000000000000000, 92.75000000000000000, -9.797174393178825657E-16 ) ) ;
#44035=CARTESIAN_POINT ( 'NONE',  ( 5.082755093536325930, 18.65624999795161187, -5.082755093536325930 ) ) ;
#44036=LINE ( 'NONE', #50430, #66382 ) ;
#44072=CARTESIAN_POINT ( 'NONE',  ( 5.656854249492380582, 12.18750000000000178, -5.656854249492380582 ) ) ;
#44074=CARTESIAN_POINT ( 'NONE',  ( 8.000000000000000000, 94.43750000409679046, -9.797174393178825657E-16 ) ) ;
#44085=CARTESIAN_POINT ( 'NONE',  ( -7.188101187500001821, 94.06250000204838102, -2.977408999572650483 ) ) ;
#44091=EDGE_CURVE ( 'NONE', #60077, #43835, #66700, .T. ) ;
#44093=VECTOR ( 'NONE', #24055, 1000.000000000000000 ) ;
#44106=CARTESIAN_POINT ( 'NONE',  ( -5.656854249492380582, 90.50000000409677625, -5.656854249492380582 ) ) ;
#44108=CARTESIAN_POINT ( 'NONE',  ( -8.000000000000000000, 6.562499995903221084, -9.797174393178825657E-16 ) ) ;
#44112=CARTESIAN_POINT ( 'NONE',  ( -5.082755093536325042, 8.906249997951611874, -5.082755093536325930 ) ) ;
#44114=CARTESIAN_POINT ( 'NONE',  ( -1.469576158976823947E-15, 7.125000000000000888, 8.000000000000000000 ) ) ;
#44115=CARTESIAN_POINT ( 'NONE',  ( -5.082755093536324154, 105.2187500020483952, 5.082755093536326818 ) ) ;
#44122=EDGE_CURVE ( 'NONE', #72985, #21405, #13143, .T. ) ;
#44128=CARTESIAN_POINT ( 'NONE',  ( -8.000000000000001776, 23.15624999590322375, 3.313708498984759387 ) ) ;
#44134=CARTESIAN_POINT ( 'NONE',  ( -7.188101187499999156, 101.7500000020483810, 2.977408999572654924 ) ) ;
#44140=CARTESIAN_POINT ( 'NONE',  ( 2.977408999572650039, 101.5625000020483810, -7.188101187500001821 ) ) ;
#44141=CARTESIAN_POINT ( 'NONE',  ( -3.674341569227068671, 0.4933058160190353925, -7.107250865053620359 ) ) ;
#44154=EDGE_CURVE ( 'NONE', #35289, #14040, #36289, .T. ) ;
#44161=ORIENTED_EDGE ( 'NONE', *, *, #2124, .T. ) ;
#44164=CARTESIAN_POINT ( 'NONE',  ( 5.082755093536324154, 6.281249997951610986, 5.082755093536326818 ) ) ;
#44165=CARTESIAN_POINT ( 'NONE',  ( -4.898587196589412829E-16, 112.8125000040967905, -8.000000000000000000 ) ) ;
#44179=DIRECTION ( 'NONE',  ( 0.000000000000000000, 0.000000000000000000, 1.000000000000000000 ) ) ;
#44191=CARTESIAN_POINT ( 'NONE',  ( -4.898587196589412829E-16, 106.6250000000000000, -8.000000000000000000 ) ) ;
#44198=CARTESIAN_POINT ( 'NONE',  ( 7.999999999999998224, 23.71874999590322375, 3.313708498984766493 ) ) ;
#44222=CARTESIAN_POINT ( 'NONE',  ( 7.188101187500002709, 118.8125000020483810, 2.977408999572649151 ) ) ;
#44230=CARTESIAN_POINT ( 'NONE',  ( -2.977408999572651815, 123.3125000020483810, 7.188101187500000933 ) ) ;
#44243=VERTEX_POINT ( 'NONE', #59903 ) ;
#44256=CARTESIAN_POINT ( 'NONE',  ( 2.977408999572651815, 21.18749999795161187, 7.188101187500000933 ) ) ;
#44259=CARTESIAN_POINT ( 'NONE',  ( 2.977408999572650927, 20.62499999795161543, -7.188101187500001821 ) ) ;
#44280=CARTESIAN_POINT ( 'NONE',  ( -7.188101187500000044, 93.03125000204836681, 0.000000000000000000 ) ) ;
#44298=CARTESIAN_POINT ( 'NONE',  ( 8.000000000000001776, 109.3437500040967763, 3.313708498984759387 ) ) ;
#44299=EDGE_LOOP ( 'NONE', ( #49200, #35604, #73864, #17918 ) ) ;
#44308=CARTESIAN_POINT ( 'NONE',  ( -5.082755093536324154, 101.8437500020483810, 5.082755093536326818 ) ) ;
#44316=VERTEX_POINT ( 'NONE', #42904 ) ;
#44336=CARTESIAN_POINT ( 'NONE',  ( -5.082755093536325042, 17.90624999795161187, -5.082755093536325930 ) ) ;
#44341=CARTESIAN_POINT ( 'NONE',  ( 5.656854249492381470, 89.75000000409677625, 5.656854249492379694 ) ) ;
#44345=CARTESIAN_POINT ( 'NONE',  ( -7.188101187500002709, 4.312499997951610986, 2.977408999572649151 ) ) ;
#44354=CARTESIAN_POINT ( 'NONE',  ( 3.313708498984762496, 26.71875000000000711, 7.999999999999998224 ) ) ;
#44361=CARTESIAN_POINT ( 'NONE',  ( -4.898587196589412829E-16, 103.6250000000000000, -8.000000000000000000 ) ) ;
#44363=CARTESIAN_POINT ( 'NONE',  ( -5.082755093536326818, 10.40624999795161187, 5.082755093536325042 ) ) ;
#44367=CARTESIAN_POINT ( 'NONE',  ( 7.188101187500001821, 111.8750000020483668, -2.977408999572651371 ) ) ;
#44371=CARTESIAN_POINT ( 'NONE',  ( 1.469576158976823947E-15, 95.56250000409677625, 8.000000000000000000 ) ) ;
#44376=CARTESIAN_POINT ( 'NONE',  ( 1.469576158976823947E-15, 105.8750000000000000, 8.000000000000000000 ) ) ;
#44382=CARTESIAN_POINT ( 'NONE',  ( 5.656854249492379694, 94.43750000000000000, -5.656854249492380582 ) ) ;
#44391=CARTESIAN_POINT ( 'NONE',  ( 9.797174393178825657E-16, 125.0000000000000000, -8.000000000000000000 ) ) ;
#44401=CARTESIAN_POINT ( 'NONE',  ( -5.656854249492381470, 12.93750000000000355, 5.656854249492379694 ) ) ;
#44405=CARTESIAN_POINT ( 'NONE',  ( -1.320432766682874540E-15, 21.09374999795161543, 7.188101187500000044 ) ) ;
#44409=ORIENTED_EDGE ( 'NONE', *, *, #47622, .F. ) ;
#44422=FACE_OUTER_BOUND ( 'NONE', #13707, .T. ) ;
#44433=VECTOR ( 'NONE', #27942, 1000.000000000000000 ) ;
#44443=CARTESIAN_POINT ( 'NONE',  ( -8.000000000000000000, 12.75000000000000178, -9.797174393178825657E-16 ) ) ;
#44444=ORIENTED_EDGE ( 'NONE', *, *, #13700, .T. ) ;
#44445=CARTESIAN_POINT ( 'NONE',  ( 5.656854249492381470, 92.75000000409677625, 5.656854249492379694 ) ) ;
#44450=ORIENTED_EDGE ( 'NONE', *, *, #53779, .F. ) ;
#44454=ORIENTED_EDGE ( 'NONE', *, *, #58117, .F. ) ;
#44456=CARTESIAN_POINT ( 'NONE',  ( -5.082755093536325930, 95.46875000204838102, -5.082755093536325930 ) ) ;
#44457=FACE_OUTER_BOUND ( 'NONE', #29851, .T. ) ;
#44459=CARTESIAN_POINT ( 'NONE',  ( 1.469576158976823947E-15, 91.06250000409676204, 8.000000000000000000 ) ) ;
#44475=DIRECTION ( 'NONE',  ( -0.000000000000000000, 1.000000000000000000, -0.000000000000000000 ) ) ;
#44478=CARTESIAN_POINT ( 'NONE',  ( -8.000000000000001776, 9.656249995903221972, 3.313708498984759387 ) ) ;
#44481=CARTESIAN_POINT ( 'NONE',  ( -7.188101187500002709, 19.68749999795161543, 2.977408999572649151 ) ) ;
#44483=CARTESIAN_POINT ( 'NONE',  ( 5.656854249492380582, 7.687500000000001776, -5.656854249492380582 ) ) ;
#44484=CARTESIAN_POINT ( 'NONE',  ( -5.082755093536324154, 106.7187500020483952, 5.082755093536326818 ) ) ;
#44496=CARTESIAN_POINT ( 'NONE',  ( 4.898587196589412829E-16, 19.68749999590322020, -8.000000000000000000 ) ) ;
#44502=CARTESIAN_POINT ( 'NONE',  ( -2.977408999572650927, 96.87500000204838102, -7.188101187500000933 ) ) ;
#44508=EDGE_CURVE ( 'NONE', #45738, #44243, #28129, .T. ) ;
#44510=CARTESIAN_POINT ( 'NONE',  ( 1.320432766682874540E-15, 103.9062500020483810, 7.188101187500000044 ) ) ;
#44516=CARTESIAN_POINT ( 'NONE',  ( -1.469576158976823947E-15, 16.12500000000000355, 8.000000000000000000 ) ) ;
#44520=CARTESIAN_POINT ( 'NONE',  ( 8.000000000000000000, 9.093750000000001776, -3.313708498984761164 ) ) ;
#44526=AXIS2_PLACEMENT_3D ( 'NONE', #51399, #21979, #57076 ) ;
#44531=VECTOR ( 'NONE', #19596, 1000.000000000000000 ) ;
#44536=CARTESIAN_POINT ( 'NONE',  ( -5.082755093536326818, 8.906249997951610098, 5.082755093536325042 ) ) ;
#44537=CARTESIAN_POINT ( 'NONE',  ( -5.656854249492380582, 108.5000000040967763, -5.656854249492380582 ) ) ;
#44548=CARTESIAN_POINT ( 'NONE',  ( 8.000000000000001776, 116.6562500000000000, 3.313708498984759387 ) ) ;
#44555=ORIENTED_EDGE ( 'NONE', *, *, #52160, .T. ) ;
#44564=CARTESIAN_POINT ( 'NONE',  ( 5.656854249492379694, 103.4374999999999858, -5.656854249492380582 ) ) ;
#44572=CARTESIAN_POINT ( 'NONE',  ( -2.977408999572650039, 1.312499997951610098, -7.188101187500001821 ) ) ;
#44574=CARTESIAN_POINT ( 'NONE',  ( 2.977408999572654480, 122.0000000020483810, 7.188101187499999156 ) ) ;
#44582=CARTESIAN_POINT ( 'NONE',  ( 8.000000000000001776, 100.3437500040967905, 3.313708498984759387 ) ) ;
#44587=CARTESIAN_POINT ( 'NONE',  ( 8.000000000000001776, 101.8437500040967905, 3.313708498984759387 ) ) ;
#44595=CARTESIAN_POINT ( 'NONE',  ( 5.082755093536325042, 116.0937500020483810, -5.082755093536325930 ) ) ;
#44600=CARTESIAN_POINT ( 'NONE',  ( -5.082755093536324154, 118.7187500020483810, 5.082755093536326818 ) ) ;
#44618=DIRECTION ( 'NONE',  ( 0.000000000000000000, 0.000000000000000000, 1.000000000000000000 ) ) ;
#44624=CARTESIAN_POINT ( 'NONE',  ( -8.000000000000001776, 2.343750000000000444, 3.313708498984759387 ) ) ;
#44627=CARTESIAN_POINT ( 'NONE',  ( -7.188101187500002709, 16.68749999795161543, 2.977408999572649151 ) ) ;
#44628=FACE_OUTER_BOUND ( 'NONE', #11520, .T. ) ;
#44650=CARTESIAN_POINT ( 'NONE',  ( -8.000000000000000000, 125.0000000000000000, 0.000000000000000000 ) ) ;
#44657=CARTESIAN_POINT ( 'NONE',  ( 5.656854249492380582, 8.999999995903221972, -5.656854249492380582 ) ) ;
#44658=CARTESIAN_POINT ( 'NONE',  ( 5.656854249492380582, 12.18750000000000178, -5.656854249492380582 ) ) ;
#44681=CARTESIAN_POINT ( 'NONE',  ( -5.082755093536325930, 105.9687500020483952, -5.082755093536325930 ) ) ;
#44687=ORIENTED_EDGE ( 'NONE', *, *, #24659, .T. ) ;
#44707=CARTESIAN_POINT ( 'NONE',  ( -7.188101187500002709, 19.68749999795161543, 2.977408999572649151 ) ) ;
#44711=CARTESIAN_POINT ( 'NONE',  ( -3.313708498984816231, 96.96875000409677625, 7.999999999999943157 ) ) ;
#44716=CARTESIAN_POINT ( 'NONE',  ( 7.188101187500000044, 9.468749997951610098, 0.000000000000000000 ) ) ;
#44719=CARTESIAN_POINT ( 'NONE',  ( 2.977408999572651815, 2.062499997951609654, 7.188101187500000933 ) ) ;
#44732=CARTESIAN_POINT ( 'NONE',  ( -8.000000000000000000, 21.65625000000000355, -3.313708498984762496 ) ) ;
#44733=ORIENTED_EDGE ( 'NONE', *, *, #15375, .T. ) ;
#44734=CARTESIAN_POINT ( 'NONE',  ( -2.977408999572650039, 8.437499997951611874, -7.188101187500000933 ) ) ;
#44740=CARTESIAN_POINT ( 'NONE',  ( -2.977408999572650927, 107.7500000020483810, -7.188101187500001821 ) ) ;
#44745=ORIENTED_EDGE ( 'NONE', *, *, #73889, .T. ) ;
#44752=( BOUNDED_CURVE ( )  B_SPLINE_CURVE ( 2, ( #50416, #55725, #22474, #15703, #10801, #34204, #22107, #5156, #56465 ),
 .UNSPECIFIED., .F., .F. ) 
 B_SPLINE_CURVE_WITH_KNOTS ( ( 3, 2, 2, 2, 3 ),
 ( 0.7361111111111110494, 0.7430555555555554692, 0.7500000000000000000, 0.7569444444444444198, 0.7638888888888888395 ),
 .UNSPECIFIED. ) 
 CURVE ( )  GEOMETRIC_REPRESENTATION_ITEM ( )  RATIONAL_B_SPLINE_CURVE ( ( 1.000000000000001110, 0.9238795325112855172, 1.000000000000000000, 0.9238795325112867385, 1.000000000000000000, 0.9238795325112867385, 1.000000000000000000, 0.9238795325112867385, 1.000000000000000000 ) ) 
 REPRESENTATION_ITEM ( '' )  );
#44756=CARTESIAN_POINT ( 'NONE',  ( 0.000000000000000000, 125.0000000000000000, 8.000000000000000000 ) ) ;
#44757=CARTESIAN_POINT ( 'NONE',  ( 5.656854249492381470, 92.56249999999998579, 5.656854249492379694 ) ) ;
#44759=CARTESIAN_POINT ( 'NONE',  ( 5.656854249492379694, 98.93750000000000000, -5.656854249492380582 ) ) ;
#44763=CARTESIAN_POINT ( 'NONE',  ( 1.469576158976823947E-15, 118.0625000040967763, 8.000000000000000000 ) ) ;
#44770=CARTESIAN_POINT ( 'NONE',  ( -4.401442555609581635E-16, 119.2812500020483810, -7.188101187500000044 ) ) ;
#44779=CARTESIAN_POINT ( 'NONE',  ( -2.977408999572654480, 22.49999999795161543, 7.188101187499999156 ) ) ;
#44803=CARTESIAN_POINT ( 'NONE',  ( 4.898587196589412829E-16, 1.687499995903220196, -8.000000000000000000 ) ) ;
#44814=CARTESIAN_POINT ( 'NONE',  ( 8.000000000000000000, 10.50000000000000178, 0.000000000000000000 ) ) ;
#44816=ADVANCED_FACE ( 'NONE', ( #40615 ), #7029, .T. ) ;
#44817=CARTESIAN_POINT ( 'NONE',  ( -3.313708498984762496, 90.96875000409676204, 7.999999999999998224 ) ) ;
#44824=VECTOR ( 'NONE', #43556, 1000.000000000000000 ) ;
#44829=CARTESIAN_POINT ( 'NONE',  ( -7.188101187500001821, 92.56250000204838102, -2.977408999572650483 ) ) ;
#44833=PRODUCT_CONTEXT ( 'NONE', #16814, 'mechanical' ) ;
#44852=CARTESIAN_POINT ( 'NONE',  ( 5.656854249492380582, 7.499999995903221084, -5.656854249492380582 ) ) ;
#44853=EDGE_LOOP ( 'NONE', ( #9042, #62503, #70924, #24715 ) ) ;
#44855=CARTESIAN_POINT ( 'NONE',  ( -7.188101187500000044, 19.59374999795161543, -8.802885111219163269E-16 ) ) ;
#44858=FACE_OUTER_BOUND ( 'NONE', #56798, .T. ) ;
#44859=CARTESIAN_POINT ( 'NONE',  ( -7.188101187500000044, 106.5312500020483810, 0.000000000000000000 ) ) ;
#44860=CYLINDRICAL_SURFACE ( 'NONE', #10667, 8.000000000000000000 ) ;
#44866=CARTESIAN_POINT ( 'NONE',  ( -1.469576158976823947E-15, 20.62500000000000355, 8.000000000000000000 ) ) ;
#44871=CARTESIAN_POINT ( 'NONE',  ( -1.469576158976823947E-15, 23.43749999590322020, 8.000000000000000000 ) ) ;
#44877=CARTESIAN_POINT ( 'NONE',  ( -5.082755093536325930, 95.46875000204838102, -5.082755093536325930 ) ) ;
#44881=( BOUNDED_CURVE ( )  B_SPLINE_CURVE ( 2, ( #61354, #43621, #38730, #2894, #43245, #66632, #21352, #55334, #44376 ),
 .UNSPECIFIED., .F., .F. ) 
 B_SPLINE_CURVE_WITH_KNOTS ( ( 3, 2, 2, 2, 3 ),
 ( 0.5104166666666666297, 0.5156250000000000000, 0.5208333333333333703, 0.5260416666666666297, 0.5312500000000000000 ),
 .UNSPECIFIED. ) 
 CURVE ( )  GEOMETRIC_REPRESENTATION_ITEM ( )  RATIONAL_B_SPLINE_CURVE ( ( 1.000000000000000000, 0.9238795325112867385, 1.000000000000000000, 0.9238795325112867385, 1.000000000000000000, 0.9238795325112867385, 1.000000000000000000, 0.9238795325112867385, 1.000000000000000000 ) ) 
 REPRESENTATION_ITEM ( '' )  );
#44885=CARTESIAN_POINT ( 'NONE',  ( -5.082755093536324154, 102.2187500020483810, 5.082755093536326818 ) ) ;
#44907=ORIENTED_EDGE ( 'NONE', *, *, #44001, .F. ) ;
#44911=CARTESIAN_POINT ( 'NONE',  ( -2.977408999572654480, 16.49999999795161543, 7.188101187499999156 ) ) ;
#44912=CARTESIAN_POINT ( 'NONE',  ( 8.000000000000000000, 108.0312500040967620, -3.313708498984762496 ) ) ;
#44920=CARTESIAN_POINT ( 'NONE',  ( 3.313708498984828221, 117.0312499999999858, -7.999999999999932498 ) ) ;
#44921=CARTESIAN_POINT ( 'NONE',  ( -7.188101187499999156, 109.2500000020483952, 2.977408999572654924 ) ) ;
#44938=CARTESIAN_POINT ( 'NONE',  ( 1.469576158976823947E-15, 108.8750000000000000, 8.000000000000000000 ) ) ;
#44944=CARTESIAN_POINT ( 'NONE',  ( -5.656854249492381470, 26.24999999590322375, 5.656854249492379694 ) ) ;
#44954=CARTESIAN_POINT ( 'NONE',  ( 8.000000000000000000, 100.5312500040967905, -3.313708498984762496 ) ) ;
#44958=CARTESIAN_POINT ( 'NONE',  ( -3.313708498984719864, 25.78124999590322020, -8.000000000000040856 ) ) ;
#44966=CARTESIAN_POINT ( 'NONE',  ( 3.313708498984752726, 7.031249995903221972, 8.000000000000008882 ) ) ;
#44967=CARTESIAN_POINT ( 'NONE',  ( 2.977408999572654480, 117.1250000020483810, 7.188101187499999156 ) ) ;
#44973=CARTESIAN_POINT ( 'NONE',  ( -4.401442555609581635E-16, 119.6562500020483810, -7.188101187500000044 ) ) ;
#44998=CARTESIAN_POINT ( 'NONE',  ( -5.656854249492379694, 0.5625000000000000000, -5.656854249492380582 ) ) ;
#45001=CARTESIAN_POINT ( 'NONE',  ( -7.188101187500000044, 18.09374999795161187, -8.802885111219163269E-16 ) ) ;
#45002=LINE ( 'NONE', #34448, #42365 ) ;
#45003=EDGE_CURVE ( 'NONE', #38745, #1872, #59432, .T. ) ;
#45012=DIRECTION ( 'NONE',  ( 0.8660254037844408170, 0.4999999999999962808, -0.000000000000000000 ) ) ;
#45013=EDGE_CURVE ( 'NONE', #25275, #3031, #20554, .T. ) ;
#45026=CARTESIAN_POINT ( 'NONE',  ( -4.898587196589412829E-16, 124.6250000000000000, -8.000000000000000000 ) ) ;
#45049=FACE_OUTER_BOUND ( 'NONE', #28128, .T. ) ;
#45054=CARTESIAN_POINT ( 'NONE',  ( -2.977408999572650927, 101.3750000020483952, -7.188101187500001821 ) ) ;
#45063=CARTESIAN_POINT ( 'NONE',  ( -8.000000000000000000, 99.49999999999998579, 0.000000000000000000 ) ) ;
#45068=DIRECTION ( 'NONE',  ( 0.000000000000000000, 0.000000000000000000, 1.000000000000000000 ) ) ;
#45078=CARTESIAN_POINT ( 'NONE',  ( -7.188101187500000933, 25.49999999795161187, -2.977408999572651371 ) ) ;
#45081=ORIENTED_EDGE ( 'NONE', *, *, #8471, .T. ) ;
#45085=CARTESIAN_POINT ( 'NONE',  ( 2.977408999572650927, 11.24999999795161187, -7.188101187500001821 ) ) ;
#45088=CARTESIAN_POINT ( 'NONE',  ( 4.401442555609581635E-16, 2.718749997951610542, -7.188101187500000044 ) ) ;
#45094=CARTESIAN_POINT ( 'NONE',  ( 0.000000000000000000, 125.0000000000000000, 0.000000000000000000 ) ) ;
#45102=CARTESIAN_POINT ( 'NONE',  ( -5.656854249492381470, 21.93750000000000355, 5.656854249492379694 ) ) ;
#45104=CARTESIAN_POINT ( 'NONE',  ( -7.188101187500000044, 11.71874999795161010, -8.802885111219163269E-16 ) ) ;
#45108=CARTESIAN_POINT ( 'NONE',  ( 2.977408999572654480, 107.0000000020483810, 7.188101187499999156 ) ) ;
#45124=CYLINDRICAL_SURFACE ( 'NONE', #53202, 8.000000000000000000 ) ;
#45130=CARTESIAN_POINT ( 'NONE',  ( 5.656854249492379694, 118.6250000040967905, -5.656854249492380582 ) ) ;
#45131=ORIENTED_EDGE ( 'NONE', *, *, #61420, .F. ) ;
#45133=CARTESIAN_POINT ( 'NONE',  ( 0.000000000000000000, 125.0000000000000000, 8.000000000000000000 ) ) ;
#45137=CARTESIAN_POINT ( 'NONE',  ( 5.082755093536325042, 123.5937500020483952, -5.082755093536325930 ) ) ;
#45142=CARTESIAN_POINT ( 'NONE',  ( 0.000000000000000000, 125.0000000000000000, 8.000000000000000000 ) ) ;
#45146=CARTESIAN_POINT ( 'NONE',  ( -7.188101187500001821, 25.12499999795161187, -2.977408999572651371 ) ) ;
#45151=ORIENTED_EDGE ( 'NONE', *, *, #60387, .T. ) ;
#45156=CARTESIAN_POINT ( 'NONE',  ( 8.000000000000000000, 118.3437500000000000, -3.313708498984762496 ) ) ;
#45170=CARTESIAN_POINT ( 'NONE',  ( 2.977408999572650927, 7.124999997951611874, -7.188101187500000933 ) ) ;
#45175=CARTESIAN_POINT ( 'NONE',  ( -3.313708498984720308, 120.2187499999999858, -8.000000000000040856 ) ) ;
#45180=ORIENTED_EDGE ( 'NONE', *, *, #71459, .T. ) ;
#45185=CARTESIAN_POINT ( 'NONE',  ( -8.000000000000001776, 18.84375000000000355, 3.313708498984759387 ) ) ;
#45186=VERTEX_POINT ( 'NONE', #5090 ) ;
#45187=CARTESIAN_POINT ( 'NONE',  ( -5.656854249492378806, 93.87500000409677625, 5.656854249492381470 ) ) ;
#45197=CARTESIAN_POINT ( 'NONE',  ( -5.082755093536325930, 121.3437500020483952, -5.082755093536325930 ) ) ;
#45207=( BOUNDED_CURVE ( )  B_SPLINE_CURVE ( 2, ( #61275, #20523, #55259, #50321, #26180, #44298, #67313, #43537, #15611 ),
 .UNSPECIFIED., .F., .F. ) 
 B_SPLINE_CURVE_WITH_KNOTS ( ( 3, 2, 2, 2, 3 ),
 ( 0.3854166666666665741, 0.3906249999999998890, 0.3958333333333332038, 0.4010416666666665741, 0.4062499999999998890 ),
 .UNSPECIFIED. ) 
 CURVE ( )  GEOMETRIC_REPRESENTATION_ITEM ( )  RATIONAL_B_SPLINE_CURVE ( ( 1.000000000000001554, 0.9238795325112850731, 1.000000000000000000, 0.9238795325112867385, 1.000000000000000000, 0.9238795325112867385, 1.000000000000000000, 0.9238795325112884038, 0.9999999999999983347 ) ) 
 REPRESENTATION_ITEM ( '' )  );
#45211=CARTESIAN_POINT ( 'NONE',  ( 1.469576158976823947E-15, 106.0625000040967763, 8.000000000000000000 ) ) ;
#45220=CARTESIAN_POINT ( 'NONE',  ( -8.000000000000001776, 11.15624999590322020, 3.313708498984759387 ) ) ;
#45223=EDGE_CURVE ( 'NONE', #10294, #1217, #53260, .T. ) ;
#45224=CARTESIAN_POINT ( 'NONE',  ( 5.082755093536325930, 17.53124999795161543, -5.082755093536325930 ) ) ;
#45225=( GEOMETRIC_REPRESENTATION_CONTEXT ( 3 ) GLOBAL_UNCERTAINTY_ASSIGNED_CONTEXT ( ( #35281 ) ) GLOBAL_UNIT_ASSIGNED_CONTEXT ( ( #55498, #68199, #29334 ) ) REPRESENTATION_CONTEXT ( 'NONE', 'WORKASPACE' ) );
#45228=CARTESIAN_POINT ( 'NONE',  ( 7.188101187500000044, 102.7812500020483810, -8.802885111219163269E-16 ) ) ;
#45238=CARTESIAN_POINT ( 'NONE',  ( -5.656854249492381470, 20.24999999590322375, 5.656854249492379694 ) ) ;
#45244=CARTESIAN_POINT ( 'NONE',  ( 7.188101187500002709, 96.31250000204838102, 2.977408999572649151 ) ) ;
#45250=CARTESIAN_POINT ( 'NONE',  ( 7.188101187500000044, 99.78125000204838102, -8.802885111219163269E-16 ) ) ;
#45260=CARTESIAN_POINT ( 'NONE',  ( -4.898587196589412829E-16, 103.6250000000000000, -8.000000000000000000 ) ) ;
#45276=CARTESIAN_POINT ( 'NONE',  ( -2.977408999572650039, 12.93749999795161365, -7.188101187500001821 ) ) ;
#45278=CARTESIAN_POINT ( 'NONE',  ( 3.313708498984765161, 109.1562500040967905, 7.999999999999998224 ) ) ;
#45286=CARTESIAN_POINT ( 'NONE',  ( 2.977408999572650039, 107.1875000020483810, -7.188101187500001821 ) ) ;
#45300=CARTESIAN_POINT ( 'NONE',  ( -4.898587196589412829E-16, 105.1250000000000000, -8.000000000000000000 ) ) ;
#45303=( BOUNDED_CURVE ( )  B_SPLINE_CURVE ( 2, ( #67942, #3831, #56258, #62274, #10602, #73232, #21538, #72097, #3450 ),
 .UNSPECIFIED., .F., .F. ) 
 B_SPLINE_CURVE_WITH_KNOTS ( ( 3, 2, 2, 2, 3 ),
 ( 0.3645833333333331483, 0.3697916666666665186, 0.3749999999999998890, 0.3802083333333332038, 0.3854166666666665741 ),
 .UNSPECIFIED. ) 
 CURVE ( )  GEOMETRIC_REPRESENTATION_ITEM ( )  RATIONAL_B_SPLINE_CURVE ( ( 1.000000000000002442, 0.9238795325112842960, 1.000000000000000000, 0.9238795325112867385, 1.000000000000000000, 0.9238795325112867385, 1.000000000000000000, 0.9238795325112884038, 0.9999999999999983347 ) ) 
 REPRESENTATION_ITEM ( '' )  );
#45304=CARTESIAN_POINT ( 'NONE',  ( -1.469576158976823947E-15, 1.125000000000000222, 8.000000000000000000 ) ) ;
#45306=CARTESIAN_POINT ( 'NONE',  ( -2.977408999572654480, 1.874999997951610098, 7.188101187499999156 ) ) ;
#45308=CARTESIAN_POINT ( 'NONE',  ( 2.977408999572650039, 124.0625000020483810, -7.188101187500000933 ) ) ;
#45315=CARTESIAN_POINT ( 'NONE',  ( -4.898587196589412829E-16, 100.8125000040967763, -8.000000000000000000 ) ) ;
#45329=CARTESIAN_POINT ( 'NONE',  ( 7.188101187500000933, 110.0000000020483810, -2.977408999572651371 ) ) ;
#45334=CARTESIAN_POINT ( 'NONE',  ( -7.188101187499999156, 123.1250000020484094, 2.977408999572654924 ) ) ;
#45359=CARTESIAN_POINT ( 'NONE',  ( -2.977408999572654480, 25.49999999795161898, 7.188101187499999156 ) ) ;
#45361=CARTESIAN_POINT ( 'NONE',  ( 7.188101187500000044, 21.84374999795161543, 0.000000000000000000 ) ) ;
#45373=EDGE_CURVE ( 'NONE', #54549, #29688, #19958, .T. ) ;
#45378=ORIENTED_EDGE ( 'NONE', *, *, #36179, .F. ) ;
#45384=CARTESIAN_POINT ( 'NONE',  ( -5.656854249492380582, 121.8125000000000000, -5.656854249492380582 ) ) ;
#45411=CARTESIAN_POINT ( 'NONE',  ( -2.977408999572650927, 105.8750000020483952, -7.188101187500001821 ) ) ;
#45440=CARTESIAN_POINT ( 'NONE',  ( -5.082755093536326818, 25.78124999795161543, 5.082755093536325042 ) ) ;
#45447=CARTESIAN_POINT ( 'NONE',  ( 5.082755093536324154, 10.78124999795161187, 5.082755093536326818 ) ) ;
#45450=CARTESIAN_POINT ( 'NONE',  ( 7.188101187500000044, 3.843749997951610542, 0.000000000000000000 ) ) ;
#45466=CARTESIAN_POINT ( 'NONE',  ( -5.082755093536326818, 16.40624999795161543, 5.082755093536325042 ) ) ;
#45470=CARTESIAN_POINT ( 'NONE',  ( 7.188101187500001821, 107.3750000020484094, -2.977408999572651371 ) ) ;
#45475=VERTEX_POINT ( 'NONE', #61494 ) ;
#45487=DIRECTION ( 'NONE',  ( 0.000000000000000000, 0.000000000000000000, 1.000000000000000000 ) ) ;
#45491=ADVANCED_FACE ( 'NONE', ( #32464 ), #9069, .T. ) ;
#45492=ORIENTED_EDGE ( 'NONE', *, *, #40835, .T. ) ;
#45500=CARTESIAN_POINT ( 'NONE',  ( -4.401442555609581635E-16, 120.7812500020483810, -7.188101187500000044 ) ) ;
#45510=CARTESIAN_POINT ( 'NONE',  ( -1.320432766682874540E-15, 27.09374999795161543, 7.188101187500000044 ) ) ;
#45516=DIRECTION ( 'NONE',  ( -0.000000000000000000, 1.000000000000000000, -0.000000000000000000 ) ) ;
#45532=CARTESIAN_POINT ( 'NONE',  ( 7.188101187500000933, 3.937499997951610986, -2.977408999572650483 ) ) ;
#45538=CARTESIAN_POINT ( 'NONE',  ( -3.313708498984765161, 2.343749995903220196, 7.999999999999998224 ) ) ;
#45550=CARTESIAN_POINT ( 'NONE',  ( 3.313708498984762052, 18.28125000000000711, -8.000000000000000000 ) ) ;
#45553=PRODUCT_DEFINITION_CONTEXT ( 'detailed design', #61683, 'design' ) ;
#45554=CARTESIAN_POINT ( 'NONE',  ( 8.000000000000001776, 92.84375000409677625, 3.313708498984759387 ) ) ;
#45561=ORIENTED_EDGE ( 'NONE', *, *, #52344, .F. ) ;
#45564=LINE ( 'NONE', #15390, #12560 ) ;
#45566=CARTESIAN_POINT ( 'NONE',  ( 2.977408999572654480, 122.0000000020483668, 7.188101187499999156 ) ) ;
#45570=CARTESIAN_POINT ( 'NONE',  ( -8.000000000000000000, 123.6875000040967905, 0.000000000000000000 ) ) ;
#45576=VERTEX_POINT ( 'NONE', #45260 ) ;
#45592=CARTESIAN_POINT ( 'NONE',  ( -5.082755093536325042, 17.90624999795161187, -5.082755093536325930 ) ) ;
#45595=CARTESIAN_POINT ( 'NONE',  ( 7.188101187500000933, 104.3750000020483952, -2.977408999572651371 ) ) ;
#45612=CARTESIAN_POINT ( 'NONE',  ( 2.977408999572650039, 95.18750000204838102, -7.188101187500000933 ) ) ;
#45619=CARTESIAN_POINT ( 'NONE',  ( -7.188101187500001821, 95.93750000204839523, -2.977408999572650483 ) ) ;
#45622=CARTESIAN_POINT ( 'NONE',  ( 1.469576158976823947E-15, 119.5625000040967763, 8.000000000000000000 ) ) ;
#45642=CARTESIAN_POINT ( 'NONE',  ( 4.401442555609581635E-16, 15.84374999795161365, -7.188101187500000044 ) ) ;
#45643=CARTESIAN_POINT ( 'NONE',  ( 3.313708498984760720, 108.2187500040968047, -8.000000000000000000 ) ) ;
#45653=CARTESIAN_POINT ( 'NONE',  ( 5.082755093536325042, 104.0937500020483810, -5.082755093536325930 ) ) ;
#45670=CARTESIAN_POINT ( 'NONE',  ( -3.313708498984762496, 104.2812499999999858, 7.999999999999998224 ) ) ;
#45675=CARTESIAN_POINT ( 'NONE',  ( 8.000000000000000000, 28.31249999590322375, 0.000000000000000000 ) ) ;
#45677=CARTESIAN_POINT ( 'NONE',  ( -4.401442555609581635E-16, 121.1562500020483810, -7.188101187500000044 ) ) ;
#45687=CARTESIAN_POINT ( 'NONE',  ( 3.979266480698044450, 124.5000000000001137, -6.940132439340980675 ) ) ;
#45688=CARTESIAN_POINT ( 'NONE',  ( -5.656854249492381470, 26.24999999590322375, 5.656854249492379694 ) ) ;
#45695=EDGE_CURVE ( 'NONE', #29121, #2559, #11306, .T. ) ;
#45698=CARTESIAN_POINT ( 'NONE',  ( -2.977408999572652260, 110.9375000020483810, 7.188101187500000044 ) ) ;
#45702=AXIS2_PLACEMENT_3D ( 'NONE', #46326, #29723, #58410 ) ;
#45704=CARTESIAN_POINT ( 'NONE',  ( -5.082755093536324154, 121.7187500020483952, 5.082755093536326818 ) ) ;
#45728=CARTESIAN_POINT ( 'NONE',  ( 7.999999999999998224, 1.406250000000000000, 3.313708498984766493 ) ) ;
#45731=CARTESIAN_POINT ( 'NONE',  ( 7.188101187499999156, 24.74999999795161543, 2.977408999572654924 ) ) ;
#45738=VERTEX_POINT ( 'NONE', #22234 ) ;
#45750=ORIENTED_EDGE ( 'NONE', *, *, #60386, .T. ) ;
#45758=AXIS2_PLACEMENT_3D ( 'NONE', #67342, #8878, #33397 ) ;
#45760=CARTESIAN_POINT ( 'NONE',  ( -7.188101187500001821, 89.93750000204840944, -2.977408999572650483 ) ) ;
#45768=CARTESIAN_POINT ( 'NONE',  ( 3.313708498984711426, 96.96875000000001421, 8.000000000000053291 ) ) ;
#45785=FACE_OUTER_BOUND ( 'NONE', #57479, .T. ) ;
#45791=CARTESIAN_POINT ( 'NONE',  ( -5.082755093536325930, 102.9687500020483810, -5.082755093536325930 ) ) ;
#45793=DIRECTION ( 'NONE',  ( 0.000000000000000000, 0.000000000000000000, 1.000000000000000000 ) ) ;
#45799=DIRECTION ( 'NONE',  ( -0.000000000000000000, 1.000000000000000000, -0.000000000000000000 ) ) ;
#45806=CARTESIAN_POINT ( 'NONE',  ( -5.656854249492380582, 113.0000000040967763, -5.656854249492380582 ) ) ;
#45814=CARTESIAN_POINT ( 'NONE',  ( -7.188101187500000933, 26.99999999795161898, -2.977408999572651371 ) ) ;
#45824=CARTESIAN_POINT ( 'NONE',  ( -1.320432766682874540E-15, 12.09374999795161187, 7.188101187500000044 ) ) ;
#45827=CARTESIAN_POINT ( 'NONE',  ( -2.977408999572654480, 3.374999997951610098, 7.188101187499999156 ) ) ;
#45841=CARTESIAN_POINT ( 'NONE',  ( -7.188101187500000044, 19.21874999795161543, -8.802885111219163269E-16 ) ) ;
#45845=CARTESIAN_POINT ( 'NONE',  ( -4.401442555609581635E-16, 107.6562500020483810, -7.188101187500000044 ) ) ;
#45846=DIRECTION ( 'NONE',  ( -0.000000000000000000, 1.000000000000000000, -0.000000000000000000 ) ) ;
#45862=DIRECTION ( 'NONE',  ( 0.000000000000000000, 0.000000000000000000, 1.000000000000000000 ) ) ;
#45878=CARTESIAN_POINT ( 'NONE',  ( 5.082755093536325042, 120.5937500020483952, -5.082755093536325930 ) ) ;
#45885=EDGE_CURVE ( 'NONE', #50014, #52808, #48582, .T. ) ;
#45887=CARTESIAN_POINT ( 'NONE',  ( 2.977408999572650927, 23.24999999795161187, -7.188101187500001821 ) ) ;
#45888=DIRECTION ( 'NONE',  ( 0.000000000000000000, 0.000000000000000000, 1.000000000000000000 ) ) ;
#45909=CARTESIAN_POINT ( 'NONE',  ( 7.188101187500000044, 5.343749997951610098, 0.000000000000000000 ) ) ;
#45913=CARTESIAN_POINT ( 'NONE',  ( 0.000000000000000000, 125.0000000000000000, 8.000000000000000000 ) ) ;
#45925=CARTESIAN_POINT ( 'NONE',  ( -1.469576158976823947E-15, 20.62500000000000355, 8.000000000000000000 ) ) ;
#45929=CARTESIAN_POINT ( 'NONE',  ( -5.082755093536325930, 120.9687500020483952, -5.082755093536325930 ) ) ;
#45959=AXIS2_PLACEMENT_3D ( 'NONE', #58797, #7108, #54617 ) ;
#45960=CARTESIAN_POINT ( 'NONE',  ( -4.898587196589412829E-16, 114.1250000000000000, -8.000000000000000000 ) ) ;
#45967=CARTESIAN_POINT ( 'NONE',  ( 7.188101187500000044, 15.84374999795161365, 0.000000000000000000 ) ) ;
#45970=CARTESIAN_POINT ( 'NONE',  ( -7.188101187500000933, 98.93750000204836681, -2.977408999572650483 ) ) ;
#45985=CARTESIAN_POINT ( 'NONE',  ( 7.188101187500000044, 91.90625000204838102, -8.802885111219163269E-16 ) ) ;
#45990=( BOUNDED_CURVE ( )  B_SPLINE_CURVE ( 2, ( #49854, #37422, #43062, #21549, #20044, #61918, #21176, #72872, #49096 ),
 .UNSPECIFIED., .F., .F. ) 
 B_SPLINE_CURVE_WITH_KNOTS ( ( 3, 2, 2, 2, 3 ),
 ( 0.09375000000000006939, 0.09895833333333339810, 0.1041666666666667407, 0.1093750000000000694, 0.1145833333333333981 ),
 .UNSPECIFIED. ) 
 CURVE ( )  GEOMETRIC_REPRESENTATION_ITEM ( )  RATIONAL_B_SPLINE_CURVE ( ( 0.9999999999999990008, 0.9238795325112877377, 1.000000000000000000, 0.9238795325112867385, 1.000000000000000000, 0.9238795325112867385, 1.000000000000000000, 0.9238795325112857393, 1.000000000000001110 ) ) 
 REPRESENTATION_ITEM ( '' )  );
#45992=CARTESIAN_POINT ( 'NONE',  ( -7.188101187500000044, 96.03125000204838102, 0.000000000000000000 ) ) ;
#46014=CARTESIAN_POINT ( 'NONE',  ( 5.082755093536325930, 14.15624999795161187, -5.082755093536325930 ) ) ;
#46015=CARTESIAN_POINT ( 'NONE',  ( -7.999999999999998224, 101.2812500040967763, 3.313708498984766493 ) ) ;
#46025=CARTESIAN_POINT ( 'NONE',  ( -1.469576158976823947E-15, 23.43749999590322020, 8.000000000000000000 ) ) ;
#46026=CARTESIAN_POINT ( 'NONE',  ( -4.401442555609581635E-16, 105.7812500020483810, -7.188101187500000044 ) ) ;
#46028=CARTESIAN_POINT ( 'NONE',  ( -3.313708498984760276, 15.28124999590322197, -8.000000000000000000 ) ) ;
#46043=CARTESIAN_POINT ( 'NONE',  ( 8.000000000000000000, 100.3437500000000000, -3.313708498984762496 ) ) ;
#46049=CARTESIAN_POINT ( 'NONE',  ( 4.401442555609581635E-16, 1.218749997951610098, -7.188101187500000044 ) ) ;
#46051=CARTESIAN_POINT ( 'NONE',  ( -7.188101187499999156, 115.6250000020483810, 2.977408999572654924 ) ) ;
#46059=CARTESIAN_POINT ( 'NONE',  ( 5.656854249492379694, 100.6250000040967905, -5.656854249492380582 ) ) ;
#46070=CARTESIAN_POINT ( 'NONE',  ( -2.977408999572650927, 111.8750000020483810, -7.188101187500000933 ) ) ;
#46076=CARTESIAN_POINT ( 'NONE',  ( 5.082755093536326818, 113.0937500020483810, 5.082755093536325042 ) ) ;
#46077=CARTESIAN_POINT ( 'NONE',  ( -8.000000000000000000, 120.5937500040967763, -3.313708498984761164 ) ) ;
#46082=( BOUNDED_CURVE ( )  B_SPLINE_CURVE ( 2, ( #5548, #22889, #59093, #48111, #59455, #48854, #64373, #64739, #31518 ),
 .UNSPECIFIED., .F., .F. ) 
 B_SPLINE_CURVE_WITH_KNOTS ( ( 3, 2, 2, 2, 3 ),
 ( 0.9062500000000002220, 0.9114583333333335924, 0.9166666666666668517, 0.9218750000000002220, 0.9270833333333335924 ),
 .UNSPECIFIED. ) 
 CURVE ( )  GEOMETRIC_REPRESENTATION_ITEM ( )  RATIONAL_B_SPLINE_CURVE ( ( 0.9999999999999967804, 0.9238795325112899581, 1.000000000000000000, 0.9238795325112867385, 1.000000000000000000, 0.9238795325112867385, 1.000000000000000000, 0.9238795325112835188, 1.000000000000003331 ) ) 
 REPRESENTATION_ITEM ( '' )  );
#46103=CARTESIAN_POINT ( 'NONE',  ( 5.656854249492378806, 1.312500000000000222, 5.656854249492381470 ) ) ;
#46106=CARTESIAN_POINT ( 'NONE',  ( -2.977408999572650039, 22.31249999795161543, -7.188101187500001821 ) ) ;
#46130=CARTESIAN_POINT ( 'NONE',  ( 2.977408999572650039, 91.06250000204838102, -7.188101187500001821 ) ) ;
#46162=CARTESIAN_POINT ( 'NONE',  ( 7.188101187500000044, 97.90625000204838102, -8.802885111219163269E-16 ) ) ;
#46167=VERTEX_POINT ( 'NONE', #15370 ) ;
#46185=CARTESIAN_POINT ( 'NONE',  ( 4.401442555609581635E-16, 26.71874999795161543, -7.188101187500000044 ) ) ;
#46195=CARTESIAN_POINT ( 'NONE',  ( -5.082755093536325042, 7.031249997951611874, -5.082755093536325930 ) ) ;
#46198=CARTESIAN_POINT ( 'NONE',  ( -5.082755093536326818, 7.781249997951610986, 5.082755093536325042 ) ) ;
#46216=CARTESIAN_POINT ( 'NONE',  ( 7.188101187500000044, 16.96874999795161543, 0.000000000000000000 ) ) ;
#46221=CARTESIAN_POINT ( 'NONE',  ( 5.082755093536326818, 105.5937500020483810, 5.082755093536325042 ) ) ;
#46225=CARTESIAN_POINT ( 'NONE',  ( -3.313708498984707429, 94.90625000409679046, -8.000000000000055067 ) ) ;
#46234=CARTESIAN_POINT ( 'NONE',  ( 0.000000000000000000, 125.0000000000000000, 0.000000000000000000 ) ) ;
#46248=CARTESIAN_POINT ( 'NONE',  ( 5.082755093536326818, 118.7187500020483810, 5.082755093536325042 ) ) ;
#46253=CARTESIAN_POINT ( 'NONE',  ( 9.797174393178825657E-16, 0.5000000000000004441, -8.000000000000000000 ) ) ;
#46257=CARTESIAN_POINT ( 'NONE',  ( 2.977408999572650927, 24.74999999795161543, -7.188101187500001821 ) ) ;
#46272=CARTESIAN_POINT ( 'NONE',  ( -1.469576158976823947E-15, 27.93749999590322375, 8.000000000000000000 ) ) ;
#46275=CARTESIAN_POINT ( 'NONE',  ( 8.000000000000000000, 115.2499999999999858, -9.797174393178825657E-16 ) ) ;
#46279=CARTESIAN_POINT ( 'NONE',  ( 2.977408999572652260, 5.062499997951610098, 7.188101187500000044 ) ) ;
#46295=CARTESIAN_POINT ( 'NONE',  ( 3.313708498984762052, 19.78125000000001066, -8.000000000000000000 ) ) ;
#46297=CARTESIAN_POINT ( 'NONE',  ( -4.401442555609581635E-16, 123.7812500020483810, -7.188101187500000044 ) ) ;
#46302=AXIS2_PLACEMENT_3D ( 'NONE', #37684, #72373, #49356 ) ;
#46310=CARTESIAN_POINT ( 'NONE',  ( 0.000000000000000000, 125.0000000000000000, 8.000000000000000000 ) ) ;
#46313=CARTESIAN_POINT ( 'NONE',  ( 7.188101187500000044, 123.7812500020483810, -8.802885111219163269E-16 ) ) ;
#46326=CARTESIAN_POINT ( 'NONE',  ( 0.000000000000000000, 125.0000000000000000, 8.000000000000000000 ) ) ;
#46337=CARTESIAN_POINT ( 'NONE',  ( -7.188101187500002709, 22.68749999795161543, 2.977408999572649151 ) ) ;
#46340=CARTESIAN_POINT ( 'NONE',  ( 2.977408999572654480, 101.0000000020483810, 7.188101187499999156 ) ) ;
#46356=CARTESIAN_POINT ( 'NONE',  ( 5.082755093536326818, 94.71875000204838102, 5.082755093536325042 ) ) ;
#46360=CARTESIAN_POINT ( 'NONE',  ( 3.313708498984846429, 110.6562500040967763, 7.999999999999918288 ) ) ;
#46363=CARTESIAN_POINT ( 'NONE',  ( -7.188101187500001821, 94.43750000204838102, -2.977408999572650483 ) ) ;
#46386=VERTEX_POINT ( 'NONE', #21636 ) ;
#46388=CARTESIAN_POINT ( 'NONE',  ( 3.313708498984765161, 106.1562500040967763, 7.999999999999998224 ) ) ;
#46396=ORIENTED_EDGE ( 'NONE', *, *, #21387, .T. ) ;
#46398=CARTESIAN_POINT ( 'NONE',  ( 1.320432766682874540E-15, 102.0312500020483810, 7.188101187500000044 ) ) ;
#46402=CARTESIAN_POINT ( 'NONE',  ( -1.469576158976823947E-15, 15.93749999590322197, 8.000000000000000000 ) ) ;
#46407=ADVANCED_FACE ( 'NONE', ( #56357 ), #73332, .T. ) ;
#46417=CARTESIAN_POINT ( 'NONE',  ( -4.898587196589412829E-16, 99.12499999999998579, -8.000000000000000000 ) ) ;
#46423=CARTESIAN_POINT ( 'NONE',  ( -7.188101187500002709, 3.187499997951610542, 2.977408999572649151 ) ) ;
#46426=CARTESIAN_POINT ( 'NONE',  ( 7.188101187500002709, 113.1875000020483810, 2.977408999572649151 ) ) ;
#46437=CARTESIAN_POINT ( 'NONE',  ( 0.000000000000000000, 125.0000000000000000, 0.000000000000000000 ) ) ;
#46438=ORIENTED_EDGE ( 'NONE', *, *, #16478, .F. ) ;
#46445=CARTESIAN_POINT ( 'NONE',  ( 7.188101187500000933, 113.0000000020483810, -2.977408999572651371 ) ) ;
#46451=CARTESIAN_POINT ( 'NONE',  ( -2.977408999572650927, 115.2500000020484094, -7.188101187500001821 ) ) ;
#46475=CARTESIAN_POINT ( 'NONE',  ( -5.656854249492381470, 8.437500000000000000, 5.656854249492379694 ) ) ;
#46478=CARTESIAN_POINT ( 'NONE',  ( -1.320432766682874540E-15, 24.46874999795161543, 7.188101187500000044 ) ) ;
#46479=CARTESIAN_POINT ( 'NONE',  ( 5.656854249492379694, 121.6250000040967905, -5.656854249492380582 ) ) ;
#46495=CARTESIAN_POINT ( 'NONE',  ( 5.656854249492379694, 96.12500000409677625, -5.656854249492380582 ) ) ;
#46500=CARTESIAN_POINT ( 'NONE',  ( 3.313708498984765161, 119.4687499999999858, 7.999999999999998224 ) ) ;
#46507=AXIS2_PLACEMENT_3D ( 'NONE', #56000, #9969, #28055 ) ;
#46508=CARTESIAN_POINT ( 'NONE',  ( 7.999999999999998224, 13.21874999590322375, 3.313708498984766493 ) ) ;
#46515=( BOUNDED_CURVE ( )  B_SPLINE_CURVE ( 2, ( #66965, #66588, #3596 ),
 .UNSPECIFIED., .F., .T. ) 
 B_SPLINE_CURVE_WITH_KNOTS ( ( 3, 3 ),
 ( 0.9687500000000000000, 0.9722122468226729319 ),
 .UNSPECIFIED. ) 
 CURVE ( )  GEOMETRIC_REPRESENTATION_ITEM ( )  RATIONAL_B_SPLINE_CURVE ( ( 1.000000000000000000, 0.9493988134329905959, 0.9660720450733824016 ) ) 
 REPRESENTATION_ITEM ( '' )  );
#46535=CARTESIAN_POINT ( 'NONE',  ( -7.188101187500000044, 97.15625000204839523, 0.000000000000000000 ) ) ;
#46537=DIRECTION ( 'NONE',  ( -0.000000000000000000, 1.000000000000000000, -0.000000000000000000 ) ) ;
#46557=CARTESIAN_POINT ( 'NONE',  ( 5.082755093536324154, 21.65624999795161543, 5.082755093536326818 ) ) ;
#46565=CARTESIAN_POINT ( 'NONE',  ( -7.188101187500001821, 17.62499999795161187, -2.977408999572651371 ) ) ;
#46568=CARTESIAN_POINT ( 'NONE',  ( -2.977408999572650039, 5.812499997951610098, -7.188101187500001821 ) ) ;
#46575=ORIENTED_EDGE ( 'NONE', *, *, #32546, .F. ) ;
#46580=CARTESIAN_POINT ( 'NONE',  ( 7.188101187500001821, 114.5000000020483810, -2.977408999572651371 ) ) ;
#46583=CARTESIAN_POINT ( 'NONE',  ( -5.082755093536325042, 16.03124999795161543, -5.082755093536325930 ) ) ;
#46589=CARTESIAN_POINT ( 'NONE',  ( 7.188101187500000044, 101.2812500020483810, -8.802885111219163269E-16 ) ) ;
#46592=CARTESIAN_POINT ( 'NONE',  ( -5.656854249492378806, 89.37500000409679046, 5.656854249492381470 ) ) ;
#46603=CARTESIAN_POINT ( 'NONE',  ( -1.469576158976823947E-15, 27.93749999590322375, 8.000000000000000000 ) ) ;
#46607=CARTESIAN_POINT ( 'NONE',  ( -8.000000000000001776, 5.343750000000000888, 3.313708498984759387 ) ) ;
#46615=CARTESIAN_POINT ( 'NONE',  ( -3.313708498984720308, 118.9062500040967905, -8.000000000000040856 ) ) ;
#46620=CARTESIAN_POINT ( 'NONE',  ( 7.188101187500002709, 114.3125000020483952, 2.977408999572649151 ) ) ;
#46629=CARTESIAN_POINT ( 'NONE',  ( -7.188101187500001821, 23.62499999795161543, -2.977408999572651371 ) ) ;
#46638=CARTESIAN_POINT ( 'NONE',  ( 0.000000000000000000, 125.0000000000000000, 0.000000000000000000 ) ) ;
#46641=EDGE_CURVE ( 'NONE', #47140, #67997, #21958, .T. ) ;
#46645=ORIENTED_EDGE ( 'NONE', *, *, #71684, .T. ) ;
#46652=CARTESIAN_POINT ( 'NONE',  ( -2.977408999572650039, 8.812499997951611874, -7.188101187500000933 ) ) ;
#46657=CARTESIAN_POINT ( 'NONE',  ( 4.898587196589412829E-16, 19.87500000000000355, -8.000000000000000000 ) ) ;
#46668=CARTESIAN_POINT ( 'NONE',  ( -3.313708498984765161, 19.03125000000000711, 7.999999999999998224 ) ) ;
#46671=CARTESIAN_POINT ( 'NONE',  ( -2.977408999572650927, 123.8750000020483810, -7.188101187500001821 ) ) ;
#46680=CARTESIAN_POINT ( 'NONE',  ( 1.320432766682874540E-15, 121.9062500020483810, 7.188101187500000044 ) ) ;
#46689=ORIENTED_EDGE ( 'NONE', *, *, #31846, .F. ) ;
#46697=EDGE_CURVE ( 'NONE', #70312, #36065, #60508, .T. ) ;
#46704=CARTESIAN_POINT ( 'NONE',  ( -5.082755093536325042, 22.40624999795161543, -5.082755093536325930 ) ) ;
#46706=CARTESIAN_POINT ( 'NONE',  ( -5.082755093536324154, 96.21875000204838102, 5.082755093536326818 ) ) ;
#46721=CARTESIAN_POINT ( 'NONE',  ( -7.188101187500000933, 89.56250000204838102, -2.977408999572650483 ) ) ;
#46726=CARTESIAN_POINT ( 'NONE',  ( 1.469576158976823947E-15, 110.5625000040967905, 8.000000000000000000 ) ) ;
#46728=CARTESIAN_POINT ( 'NONE',  ( -7.188101187499999156, 99.12500000204838102, 2.977408999572654924 ) ) ;
#46731=( BOUNDED_CURVE ( )  B_SPLINE_CURVE ( 2, ( #10936, #73193, #50175, #73558, #74303, #44520, #56222, #16955, #15832 ),
 .UNSPECIFIED., .F., .F. ) 
 B_SPLINE_CURVE_WITH_KNOTS ( ( 3, 2, 2, 2, 3 ),
 ( 0.3194444444444443643, 0.3263888888888888395, 0.3333333333333332593, 0.3402777777777777901, 0.3472222222222222099 ),
 .UNSPECIFIED. ) 
 CURVE ( )  GEOMETRIC_REPRESENTATION_ITEM ( )  RATIONAL_B_SPLINE_CURVE ( ( 1.000000000000000666, 0.9238795325112861834, 1.000000000000000000, 0.9238795325112867385, 1.000000000000000000, 0.9238795325112867385, 1.000000000000000000, 0.9238795325112867385, 1.000000000000000000 ) ) 
 REPRESENTATION_ITEM ( '' )  );
#46747=EDGE_CURVE ( 'NONE', #43757, #25866, #58114, .T. ) ;
#46753=CARTESIAN_POINT ( 'NONE',  ( -7.999999999999998224, 105.7812500040967905, 3.313708498984766493 ) ) ;
#46760=CARTESIAN_POINT ( 'NONE',  ( -5.656854249492381470, 24.93750000000000355, 5.656854249492379694 ) ) ;
#46761=CARTESIAN_POINT ( 'NONE',  ( -5.082755093536325930, 107.4687500020483810, -5.082755093536325930 ) ) ;
#46772=CARTESIAN_POINT ( 'NONE',  ( 8.000000000000000000, 3.000000000000000444, 0.000000000000000000 ) ) ;
#46779=CARTESIAN_POINT ( 'NONE',  ( 3.313708498984765161, 102.9687500000000142, 7.999999999999998224 ) ) ;
#46787=CARTESIAN_POINT ( 'NONE',  ( 5.082755093536324154, 6.656249997951610986, 5.082755093536326818 ) ) ;
#46790=CARTESIAN_POINT ( 'NONE',  ( 2.977408999572650039, 113.5625000020483810, -7.188101187500000933 ) ) ;
#46810=CARTESIAN_POINT ( 'NONE',  ( -7.188101187499999156, 110.7500000020483810, 2.977408999572654924 ) ) ;
#46816=CARTESIAN_POINT ( 'NONE',  ( -7.188101187500000044, 112.5312500020483952, 0.000000000000000000 ) ) ;
#46821=EDGE_CURVE ( 'NONE', #33538, #38802, #30128, .T. ) ;
#46844=CARTESIAN_POINT ( 'NONE',  ( -8.000000000000001776, 5.343750000000000888, 3.313708498984759387 ) ) ;
#46847=CARTESIAN_POINT ( 'NONE',  ( 2.977408999572650927, 22.12499999795161543, -7.188101187500001821 ) ) ;
#46848=CARTESIAN_POINT ( 'NONE',  ( 1.469576158976823947E-15, 121.0625000040967763, 8.000000000000000000 ) ) ;
#46874=CARTESIAN_POINT ( 'NONE',  ( 5.656854249492379694, 115.4375000000000000, -5.656854249492380582 ) ) ;
#46879=AXIS2_PLACEMENT_3D ( 'NONE', #6265, #984, #45487 ) ;
#46880=CARTESIAN_POINT ( 'NONE',  ( -8.000000000000000000, 12.56249999590322197, -9.797174393178825657E-16 ) ) ;
#46900=CYLINDRICAL_SURFACE ( 'NONE', #70155, 11.00000000000000000 ) ;
#46904=CARTESIAN_POINT ( 'NONE',  ( -2.977408999572651815, 95.93750000204839523, 7.188101187500000933 ) ) ;
#46921=ORIENTED_EDGE ( 'NONE', *, *, #3489, .T. ) ;
#46929=ORIENTED_EDGE ( 'NONE', *, *, #37600, .F. ) ;
#46933=CARTESIAN_POINT ( 'NONE',  ( -7.188101187500002709, 16.31249999795161543, 2.977408999572649151 ) ) ;
#46936=CARTESIAN_POINT ( 'NONE',  ( -2.977408999572650039, 8.812499997951611874, -7.188101187500001821 ) ) ;
#46948=CARTESIAN_POINT ( 'NONE',  ( 1.320432766682874540E-15, 118.5312500020483810, 7.188101187500000044 ) ) ;
#46953=ADVANCED_FACE ( 'NONE', ( #57573 ), #29262, .T. ) ;
#46954=CARTESIAN_POINT ( 'NONE',  ( -5.082755093536325042, 17.53124999795161187, -5.082755093536325930 ) ) ;
#46959=CARTESIAN_POINT ( 'NONE',  ( 1.320432766682874540E-15, 100.9062500020483810, 7.188101187500000044 ) ) ;
#46962=EDGE_LOOP ( 'NONE', ( #47651, #68248, #53545, #49640 ) ) ;
#46972=CARTESIAN_POINT ( 'NONE',  ( -8.000000000000000000, 118.9062500000000000, -3.313708498984761164 ) ) ;
#46986=CARTESIAN_POINT ( 'NONE',  ( 7.188101187500000044, 112.9062500020483952, -8.802885111219163269E-16 ) ) ;
#46990=LINE ( 'NONE', #59439, #27452 ) ;
#47004=DIRECTION ( 'NONE',  ( -0.000000000000000000, 1.000000000000000000, -0.000000000000000000 ) ) ;
#47012=CARTESIAN_POINT ( 'NONE',  ( 3.313708498984721640, 22.21875000000000355, 8.000000000000039080 ) ) ;
#47016=CARTESIAN_POINT ( 'NONE',  ( -7.188101187500000933, 14.99999999795161187, -2.977408999572651371 ) ) ;
#47033=CARTESIAN_POINT ( 'NONE',  ( -8.000000000000000000, 26.25000000000000711, -9.797174393178825657E-16 ) ) ;
#47036=CARTESIAN_POINT ( 'NONE',  ( 5.082755093536326818, 123.2187500020483952, 5.082755093536325042 ) ) ;
#47046=CARTESIAN_POINT ( 'NONE',  ( -2.977408999572650927, 119.7500000020483810, -7.188101187500001821 ) ) ;
#47055=EDGE_LOOP ( 'NONE', ( #26163, #29522, #9653, #25777 ) ) ;
#47056=CARTESIAN_POINT ( 'NONE',  ( 5.656854249492379694, 105.1250000040967763, -5.656854249492380582 ) ) ;
#47062=CARTESIAN_POINT ( 'NONE',  ( -8.000000000000001776, 2.343750000000000444, 3.313708498984759387 ) ) ;
#47071=CARTESIAN_POINT ( 'NONE',  ( -7.188101187500000044, 21.09374999795161543, -8.802885111219163269E-16 ) ) ;
#47073=CARTESIAN_POINT ( 'NONE',  ( 1.320432766682874540E-15, 100.9062500020483810, 7.188101187500000044 ) ) ;
#47093=CARTESIAN_POINT ( 'NONE',  ( 7.188101187500002709, 98.18750000204838102, 2.977408999572649151 ) ) ;
#47094=ADVANCED_FACE ( 'NONE', ( #28134 ), #34189, .T. ) ;
#47101=CARTESIAN_POINT ( 'NONE',  ( -5.656854249492380582, 121.8125000000000000, -5.656854249492380582 ) ) ;
#47109=VECTOR ( 'NONE', #14683, 1000.000000000000000 ) ;
#47116=AXIS2_PLACEMENT_3D ( 'NONE', #7737, #7370, #24700 ) ;
#47120=CARTESIAN_POINT ( 'NONE',  ( 5.656854249492381470, 101.7500000040967905, 5.656854249492379694 ) ) ;
#47127=LINE ( 'NONE', #70160, #31797 ) ;
#47130=CARTESIAN_POINT ( 'NONE',  ( -2.977408999572651815, 95.93750000204839523, 7.188101187500000933 ) ) ;
#47140=VERTEX_POINT ( 'NONE', #39477 ) ;
#47152=CARTESIAN_POINT ( 'NONE',  ( -5.082755093536325042, 7.406249997951610986, -5.082755093536325930 ) ) ;
#47156=CARTESIAN_POINT ( 'NONE',  ( -7.188101187500000933, 115.4375000020483810, -2.977408999572650483 ) ) ;
#47178=CARTESIAN_POINT ( 'NONE',  ( -2.977408999572652260, 106.4375000020483810, 7.188101187500000044 ) ) ;
#47183=CARTESIAN_POINT ( 'NONE',  ( 1.320432766682874540E-15, 112.9062500020483952, 7.188101187500000044 ) ) ;
#47192=CARTESIAN_POINT ( 'NONE',  ( -7.999999999999998224, 108.5937499999999858, 3.313708498984766049 ) ) ;
#47207=EDGE_LOOP ( 'NONE', ( #10651, #71588, #48315, #69845, #8074, #69758, #14602, #16667, #57514, #63947, #2756, #73924, #37074, #7332, #8329, #20238, #35812, #15113, #25209, #10163, #63237, #7812, #23847, #61419, #11737, #62534, #59674, #49349, #54904, #1751, #42828, #23026, #38043, #69334, #26010, #51042, #36935, #41157, #25645, #30930, #44907, #67196, #23305, #41346, #44409, #7893, #24105, #52350, #2922, #62875, #27786 ) ) ;
#47209=CARTESIAN_POINT ( 'NONE',  ( 5.656854249492380582, 4.687500000000000888, -5.656854249492380582 ) ) ;
#47210=CARTESIAN_POINT ( 'NONE',  ( -5.082755093536326818, 1.406249997951610320, 5.082755093536325042 ) ) ;
#47211=CARTESIAN_POINT ( 'NONE',  ( -3.313708498984762496, 119.4687500040967905, 7.999999999999998224 ) ) ;
#47220=ADVANCED_FACE ( 'NONE', ( #25985 ), #65623, .T. ) ;
#47232=CARTESIAN_POINT ( 'NONE',  ( 8.000000000000000000, 96.03125000409677625, -3.313708498984762496 ) ) ;
#47238=CARTESIAN_POINT ( 'NONE',  ( 8.000000000000000000, 119.7500000000000000, -9.797174393178825657E-16 ) ) ;
#47243=EDGE_CURVE ( 'NONE', #43757, #39207, #72020, .T. ) ;
#47244=CARTESIAN_POINT ( 'NONE',  ( 5.656854249492380582, 16.49999999590322375, -5.656854249492380582 ) ) ;
#47265=CARTESIAN_POINT ( 'NONE',  ( -2.977408999572652260, 121.4375000020483810, 7.188101187500000044 ) ) ;
#47270=CARTESIAN_POINT ( 'NONE',  ( -4.401442555609581635E-16, 99.78125000204838102, -7.188101187500000044 ) ) ;
#47273=CARTESIAN_POINT ( 'NONE',  ( 0.5126016559340066392, 0.4114670971541452560, -7.911467097154144312 ) ) ;
#47276=EDGE_LOOP ( 'NONE', ( #26517, #33528, #61614, #51208 ) ) ;
#47302=CARTESIAN_POINT ( 'NONE',  ( -5.082755093536326818, 13.40624999795161187, 5.082755093536325042 ) ) ;
#47304=CARTESIAN_POINT ( 'NONE',  ( 3.360070523759410399, 124.5134190293533010, -7.253681227061663073 ) ) ;
#47305=CARTESIAN_POINT ( 'NONE',  ( -7.188101187500001821, 11.99999999795161187, -2.977408999572651371 ) ) ;
#47313=ORIENTED_EDGE ( 'NONE', *, *, #71387, .T. ) ;
#47317=ADVANCED_FACE ( 'NONE', ( #41337 ), #5897, .T. ) ;
#47319=CARTESIAN_POINT ( 'NONE',  ( -5.082755093536324154, 116.8437500020483810, 5.082755093536326818 ) ) ;
#47323=CARTESIAN_POINT ( 'NONE',  ( -5.082755093536325042, 22.03124999795161543, -5.082755093536325930 ) ) ;
#47326=CARTESIAN_POINT ( 'NONE',  ( 5.656854249492380582, 13.68750000000000178, -5.656854249492380582 ) ) ;
#47329=CARTESIAN_POINT ( 'NONE',  ( 1.320432766682874540E-15, 102.4062500020483810, 7.188101187500000044 ) ) ;
#47343=CARTESIAN_POINT ( 'NONE',  ( -4.898587196589412829E-16, 118.6250000000000000, -8.000000000000000000 ) ) ;
#47347=CARTESIAN_POINT ( 'NONE',  ( 8.000000000000001776, 97.34375000409679046, 3.313708498984759387 ) ) ;
#47353=CARTESIAN_POINT ( 'NONE',  ( 3.313708498984762496, 10.21875000000000178, 7.999999999999998224 ) ) ;
#47358=CARTESIAN_POINT ( 'NONE',  ( -2.977408999572650927, 116.3750000020483810, -7.188101187500001821 ) ) ;
#47365=CARTESIAN_POINT ( 'NONE',  ( 5.656854249492379694, 93.12500000409677625, -5.656854249492380582 ) ) ;
#47375=DIRECTION ( 'NONE',  ( 0.000000000000000000, 0.000000000000000000, 1.000000000000000000 ) ) ;
#47388=CARTESIAN_POINT ( 'NONE',  ( 5.082755093536325930, 11.53124999795161187, -5.082755093536325930 ) ) ;
#47403=( BOUNDED_SURFACE ( )  B_SPLINE_SURFACE ( 1, 2, ( 
 ( #35911, #64208, #30241, #58197, #23467, #57825, #12512, #7601, #12146, #35544, #13243, #53631, #30609, #47577, #70600, #36277, #35182, #63830, #18917, #24200, #52519, #6130, #46479, #29136, #58558, #856, #52890, #6863, #46848, #52151, #41561, #487, #69499, #23841, #1941, #69126, #40824, #40455, #69870, #18183, #11779, #64934, #17431, #29875, #1221, #47211, #70245, #64577, #12874, #58930, #7237, #3056, #37766, #49441, #3425, #48689, #9088, #53993, #32101, #49060, #71695, #20013, #2304, #55121, #43785, #72069, #26039, #31725, #31342, #8332, #13970, #60384, #66800, #70962, #55492, #54373, #8710, #42660, #26414, #72460, #30974, #37013, #14726, #25301, #65303, #59655, #15103, #43024, #43402, #20388, #42289, #20767, #66047, #19647, #9466, #13608, #66417, #48320, #38135, #60765, #14354, #61136, #54747, #19279, #32484, #25670, #36646, #60014, #71326, #65672, #7972, #2683, #37382, #24930, #47944, #50188, #44165, #33237, #68288, #11322, #38513, #34355, #33987, #49818, #39621, #16585, #3807, #39250, #9837, #61514, #56235, #4929, #15846, #62621, #4550, #32864, #28298, #73573, #10207, #55868, #62998, #73210, #50935, #67179, #15475, #62249, #10951, #56982, #5296, #61885, #27926, #4185, #73947, #51305, #74317, #45278, #22249, #10576, #21883, #27545, #27171, #21515, #44537, #16968, #22624, #45643, #67549, #44912, #68658, #38880, #50559, #26804, #39994, #72835, #67918, #21141, #16211, #33606, #56615, #58466, #29041, #70154, #12421, #12057, #18091, #52059, #70511, #46388, #23749, #47488, #763, #46753, #12784, #57355, #35819, #35454, #64486, #18830, #69406, #69774, #58833, #57730, #23, #40729, #63361, #6036, #394, #41834, #64113, #11687, #18461, #6777, #17713, #51677, #52795, #41106, #23009, #40361, #63737, #5665, #23376, #6412, #29417, #29782, #1130, #28663, #41472, #24108, #7144, #35091, #24484, #1504, #64847, #69036, #47120, #30151, #53168, #34725, #13148, #46015, #58101, #17339, #52428, #30519, #2216, #65209, #65583, #65955, #48598, #1853, #48968, #19925, #37296, #60292, #66705, #25949, #31254, #20295, #48228, #13514, #47856, #54282, #49346, #25210, #2594, #3336, #43693, #20674, #14634, #43312, #26326, #71234, #53903, #60673, #14260, #19555, #70876, #36553, #19191, #25583, #42570, #42935, #71603, #36922, #24839, #8620, #59565, #42193, #13880, #36188, #59204, #7881, #53538, #59929, #8243, #30886, #66329, #8994, #31634, #54653, #2963, #72364, #71980, #37675, #32010, #55029, #7513, #27833, #39533, #68198, #38794, #73856, #44074, #22160, #39158, #61797, #10114, #67085, #45187, #33891, #62161, #16120, #21787, #21421, #73115, #4092, #50464, #56893, #61045, #45554, #44445, #73479, #32768, #16496, #62529, #21050, #27086, #4835, #15382, #10856, #27449, #5207, #38419, #32389, #67457, #61421, #9750, #55776, #74227, #44817, #50099, #50842, #10486, #55403, #49730, #28205, #33153, #33518, #56520, #3713, #51218, #56147, #15754, #22533, #26711, #15010, #4461, #38044, #9368, #67829, #72746, #35009, #16872, #24026, #51971 ),
 ( #6330, #29333, #18378, #46671, #46297, #18007, #11600, #74603, #34262, #23288, #47036, #40273, #69318, #52714, #70072, #68570, #58387, #64031, #39897, #57642, #34636, #1047, #52342, #5952, #22916, #68941, #51586, #63650, #309, #679, #40646, #17627, #28578, #23665, #45929, #17251, #28951, #62902, #11234, #11977, #63273, #58024, #69693, #41023, #57265, #5580, #12343, #29698, #35377, #6693, #58658, #40557, #29608, #40931, #69228, #13340, #36377, #41300, #11886, #42024, #46948, #59392, #70345, #63941, #7338, #24307, #23940, #29975, #12249, #7705, #58298, #35645, #30711, #12615, #6966, #24667, #17537, #47678, #47319, #1689, #53731, #6603, #588, #69601, #35286, #2043, #1324, #23569, #30344, #18657, #34920, #29242, #25030, #52992, #12976, #41666, #57931, #53363, #64310, #52622, #63559, #6238, #64677, #46580, #52254, #36013, #59031, #70699, #19018, #17915, #958, #69977, #18286, #65031, #71424, #19752, #31071, #25771, #71799, #37869, #31455, #42759, #13704, #2785, #60864, #56624, #8070, #4939, #4560, #19377, #9186, #32207, #48050, #8817, #54100, #2412, #48792, #49166, #60117, #55226, #20119, #25407, #73584, #43133, #54480, #48421, #33618, #65776, #20487, #36748, #59760, #31829, #27557, #50567, #21891, #66149, #72175, #14079, #43505, #44921, #67929, #14828, #66516, #54848, #14454, #37490, #37114, #8435, #60491, #62259, #16222, #3158, #39261, #26147, #42391, #10586, #71059, #65407, #46761, #69786, #32, #45286, #773, #5675, #18101, #29050, #74326, #40738, #57741, #57366, #63371, #22632, #41117, #16977, #69047, #64122, #46026, #17351, #58110, #27936, #6421, #6045, #35101, #12429, #40003, #40372, #29427, #28306, #68296, #11331, #52436, #12065, #35463, #63007, #45653, #23759, #52069, #68667, #62631, #5305, #39632, #11697, #34364, #34735, #406, #28673, #16593, #23386, #56990, #10962, #51687, #58476, #50944, #51315, #22257, #23019, #46398, #33997, #73956, #69415, #17722, #63747, #35828, #48237, #36197, #36930, #24848, #1514, #59576, #19565, #31264, #59937, #30529, #65594, #58843, #13891, #30895, #53547, #1862, #7155, #8250, #25593, #53912, #7889, #13524, #13160, #64855, #70520, #42203, #48609, #52804, #37305, #59213, #65219, #24494, #54292, #2604, #12796, #18838, #71245, #30159, #71614, #41846, #1139, #2225, #47866, #24117, #64496, #7524, #29794, #47497, #70886, #19201, #36562, #25223, #6784, #42580, #19935, #42943, #65964, #14269, #47130, #70163, #18470, #41481, #53177, #44456, #66338, #38430, #27095, #14644, #61433, #50111, #54664, #26335, #37685, #15022, #15393, #72757, #25958, #73127, #44085, #9759, #32780, #16129, #21433, #55413, #67470, #72374, #60685, #71990, #3722, #73491, #49357, #26721, #27462, #67837, #44829, #20303, #49741, #21798, #20685, #21061, #50476, #60301, #8631, #38804, #15767, #31644, #43703, #3345, #10124, #55787, #66718, #43323, #9005, #32019, #67096, #38056, #4103, #61806, #61056, #48977, #33161, #55039, #9380, #32399, #2973, #56156, #4472, #33530, #68579, #56904, #4848, #69327 ) ),
 .UNSPECIFIED., .F., .F., .F. ) 
 B_SPLINE_SURFACE_WITH_KNOTS ( ( 2, 2 ),
 ( 3, 2, 2, 2, 2, 2, 2, 2, 2, 2, 2, 2, 2, 2, 2, 2, 2, 2, 2, 2, 2, 2, 2, 2, 2, 2, 2, 2, 2, 2, 2, 2, 2, 2, 2, 2, 2, 2, 2, 2, 2, 2, 2, 2, 2, 2, 2, 2, 2, 2, 2, 2, 2, 2, 2, 2, 2, 2, 2, 2, 2, 2, 2, 2, 2, 2, 2, 2, 2, 2, 2, 2, 2, 2, 2, 2, 2, 2, 2, 2, 2, 2, 2, 2, 2, 2, 2, 2, 2, 2, 2, 2, 2, 2, 2, 2, 2, 2, 2, 2, 2, 2, 2, 2, 2, 2, 2, 2, 2, 2, 2, 2, 2, 2, 2, 2, 2, 2, 2, 2, 2, 2, 2, 2, 2, 2, 2, 2, 2, 2, 2, 2, 2, 2, 2, 2, 2, 2, 2, 2, 2, 2, 2, 2, 2, 2, 2, 2, 2, 2, 2, 2, 2, 2, 2, 2, 2, 2, 2, 2, 2, 2, 2, 2, 2, 2, 2, 2, 2, 2, 2, 2, 2, 2, 2, 2, 2, 2, 2, 2, 2, 2, 2, 2, 2, 2, 2, 3 ),
 ( 0.000000000000000000, 1.000000000000000000 ),
 ( 0.000000000000000000, 0.005208333333333333044, 0.01041666666666666609, 0.01562500000000000000, 0.02083333333333333218, 0.02604166666666666782, 0.03125000000000000000, 0.03645833333333333565, 0.04166666666666666435, 0.04687500000000000000, 0.05208333333333333565, 0.05729166666666666435, 0.06250000000000000000, 0.06770833333333332871, 0.07291666666666667129, 0.07812500000000000000, 0.08333333333333332871, 0.08854166666666667129, 0.09375000000000000000, 0.09895833333333332871, 0.1041666666666666713, 0.1093750000000000000, 0.1145833333333333287, 0.1197916666666666713, 0.1250000000000000000, 0.1302083333333333426, 0.1354166666666666574, 0.1406250000000000000, 0.1458333333333333426, 0.1510416666666666574, 0.1562500000000000000, 0.1614583333333333426, 0.1666666666666666574, 0.1718750000000000000, 0.1770833333333333426, 0.1822916666666666574, 0.1875000000000000000, 0.1927083333333333426, 0.1979166666666666574, 0.2031250000000000000, 0.2083333333333333426, 0.2135416666666666574, 0.2187500000000000000, 0.2239583333333333426, 0.2291666666666666574, 0.2343750000000000000, 0.2395833333333333426, 0.2447916666666666574, 0.2500000000000000000, 0.2552083333333333148, 0.2604166666666666852, 0.2656250000000000000, 0.2708333333333333148, 0.2760416666666666852, 0.2812500000000000000, 0.2864583333333333148, 0.2916666666666666852, 0.2968750000000000000, 0.3020833333333333148, 0.3072916666666666852, 0.3125000000000000000, 0.3177083333333333148, 0.3229166666666666852, 0.3281250000000000000, 0.3333333333333333148, 0.3385416666666666852, 0.3437500000000000000, 0.3489583333333333148, 0.3541666666666666852, 0.3593750000000000000, 0.3645833333333333148, 0.3697916666666666852, 0.3750000000000000000, 0.3802083333333333148, 0.3854166666666666852, 0.3906250000000000000, 0.3958333333333333148, 0.4010416666666666852, 0.4062500000000000000, 0.4114583333333333148, 0.4166666666666666852, 0.4218750000000000000, 0.4270833333333333148, 0.4322916666666666852, 0.4375000000000000000, 0.4427083333333333148, 0.4479166666666666852, 0.4531250000000000000, 0.4583333333333333148, 0.4635416666666666852, 0.4687500000000000000, 0.4739583333333333148, 0.4791666666666666852, 0.4843750000000000000, 0.4895833333333333148, 0.4947916666666666852, 0.5000000000000000000, 0.5052083333333333703, 0.5104166666666666297, 0.5156250000000000000, 0.5208333333333333703, 0.5260416666666666297, 0.5312500000000000000, 0.5364583333333333703, 0.5416666666666666297, 0.5468750000000000000, 0.5520833333333333703, 0.5572916666666666297, 0.5625000000000000000, 0.5677083333333333703, 0.5729166666666666297, 0.5781250000000000000, 0.5833333333333333703, 0.5885416666666666297, 0.5937500000000000000, 0.5989583333333333703, 0.6041666666666666297, 0.6093750000000000000, 0.6145833333333333703, 0.6197916666666666297, 0.6250000000000000000, 0.6302083333333333703, 0.6354166666666666297, 0.6406250000000000000, 0.6458333333333333703, 0.6510416666666666297, 0.6562500000000000000, 0.6614583333333333703, 0.6666666666666666297, 0.6718750000000000000, 0.6770833333333333703, 0.6822916666666666297, 0.6875000000000000000, 0.6927083333333333703, 0.6979166666666666297, 0.7031250000000000000, 0.7083333333333333703, 0.7135416666666666297, 0.7187500000000000000, 0.7239583333333333703, 0.7291666666666666297, 0.7343750000000000000, 0.7395833333333333703, 0.7447916666666666297, 0.7500000000000000000, 0.7552083333333333703, 0.7604166666666666297, 0.7656250000000000000, 0.7708333333333333703, 0.7760416666666666297, 0.7812500000000000000, 0.7864583333333333703, 0.7916666666666666297, 0.7968750000000000000, 0.8020833333333333703, 0.8072916666666666297, 0.8125000000000000000, 0.8177083333333333703, 0.8229166666666666297, 0.8281250000000000000, 0.8333333333333333703, 0.8385416666666666297, 0.8437500000000000000, 0.8489583333333333703, 0.8541666666666666297, 0.8593750000000000000, 0.8645833333333333703, 0.8697916666666666297, 0.8750000000000000000, 0.8802083333333333703, 0.8854166666666666297, 0.8906250000000000000, 0.8958333333333333703, 0.9010416666666666297, 0.9062500000000000000, 0.9114583333333333703, 0.9166666666666666297, 0.9218750000000000000, 0.9270833333333333703, 0.9322916666666666297, 0.9375000000000000000, 0.9427083333333333703, 0.9479166666666666297, 0.9531250000000000000, 0.9583333333333333703, 0.9635416666666666297, 0.9687500000000000000, 0.9722122500602408124 ),
 .UNSPECIFIED. ) 
 GEOMETRIC_REPRESENTATION_ITEM ( )  RATIONAL_B_SPLINE_SURFACE ( (
 ( 1.000000000000000000, 0.9238795325112867385, 1.000000000000000000, 0.9238795325112867385, 1.000000000000000000, 0.9238795325112867385, 1.000000000000000000, 0.9238795325112867385, 1.000000000000000000, 0.9238795325112867385, 1.000000000000000000, 0.9238795325112867385, 1.000000000000000000, 0.9238795325112867385, 1.000000000000000000, 0.9238795325112867385, 1.000000000000000000, 0.9238795325112867385, 1.000000000000000000, 0.9238795325112867385, 1.000000000000000000, 0.9238795325112867385, 1.000000000000000000, 0.9238795325112867385, 1.000000000000000000, 0.9238795325112867385, 1.000000000000000000, 0.9238795325112867385, 1.000000000000000000, 0.9238795325112867385, 1.000000000000000000, 0.9238795325112867385, 1.000000000000000000, 0.9238795325112867385, 1.000000000000000000, 0.9238795325112867385, 1.000000000000000000, 0.9238795325112867385, 1.000000000000000000, 0.9238795325112867385, 1.000000000000000000, 0.9238795325112867385, 1.000000000000000000, 0.9238795325112867385, 1.000000000000000000, 0.9238795325112867385, 1.000000000000000000, 0.9238795325112867385, 1.000000000000000000, 0.9238795325112867385, 1.000000000000000000, 0.9238795325112867385, 1.000000000000000000, 0.9238795325112867385, 1.000000000000000000, 0.9238795325112867385, 1.000000000000000000, 0.9238795325112867385, 1.000000000000000000, 0.9238795325112867385, 1.000000000000000000, 0.9238795325112867385, 1.000000000000000000, 0.9238795325112867385, 1.000000000000000000, 0.9238795325112867385, 1.000000000000000000, 0.9238795325112867385, 1.000000000000000000, 0.9238795325112867385, 1.000000000000000000, 0.9238795325112867385, 1.000000000000000000, 0.9238795325112867385, 1.000000000000000000, 0.9238795325112867385, 1.000000000000000000, 0.9238795325112867385, 1.000000000000000000, 0.9238795325112867385, 1.000000000000000000, 0.9238795325112867385, 1.000000000000000000, 0.9238795325112867385, 1.000000000000000000, 0.9238795325112867385, 1.000000000000000000, 0.9238795325112867385, 1.000000000000000000, 0.9238795325112867385, 1.000000000000000000, 0.9238795325112867385, 1.000000000000000000, 0.9238795325112867385, 1.000000000000000000, 0.9238795325112867385, 1.000000000000000000, 0.9238795325112867385, 1.000000000000000000, 0.9238795325112867385, 1.000000000000000000, 0.9238795325112867385, 1.000000000000000000, 0.9238795325112867385, 1.000000000000000000, 0.9238795325112867385, 1.000000000000000000, 0.9238795325112867385, 1.000000000000000000, 0.9238795325112867385, 1.000000000000000000, 0.9238795325112867385, 1.000000000000000000, 0.9238795325112867385, 1.000000000000000000, 0.9238795325112867385, 1.000000000000000000, 0.9238795325112867385, 1.000000000000000000, 0.9238795325112867385, 1.000000000000000000, 0.9238795325112867385, 1.000000000000000000, 0.9238795325112867385, 1.000000000000000000, 0.9238795325112867385, 1.000000000000000000, 0.9238795325112867385, 1.000000000000000000, 0.9238795325112867385, 1.000000000000000000, 0.9238795325112867385, 1.000000000000000000, 0.9238795325112867385, 1.000000000000000000, 0.9238795325112867385, 1.000000000000000000, 0.9238795325112867385, 1.000000000000000000, 0.9238795325112867385, 1.000000000000000000, 0.9238795325112867385, 1.000000000000000000, 0.9238795325112867385, 1.000000000000000000, 0.9238795325112867385, 1.000000000000000000, 0.9238795325112867385, 1.000000000000000000, 0.9238795325112867385, 1.000000000000000000, 0.9238795325112867385, 1.000000000000000000, 0.9238795325112867385, 1.000000000000000000, 0.9238795325112867385, 1.000000000000000000, 0.9238795325112867385, 1.000000000000000000, 0.9238795325112867385, 1.000000000000000000, 0.9238795325112867385, 1.000000000000000000, 0.9238795325112867385, 1.000000000000000000, 0.9238795325112867385, 1.000000000000000000, 0.9238795325112867385, 1.000000000000000000, 0.9238795325112867385, 1.000000000000000000, 0.9238795325112867385, 1.000000000000000000, 0.9238795325112867385, 1.000000000000000000, 0.9238795325112867385, 1.000000000000000000, 0.9238795325112867385, 1.000000000000000000, 0.9238795325112867385, 1.000000000000000000, 0.9238795325112867385, 1.000000000000000000, 0.9238795325112867385, 1.000000000000000000, 0.9238795325112867385, 1.000000000000000000, 0.9238795325112867385, 1.000000000000000000, 0.9238795325112867385, 1.000000000000000000, 0.9238795325112867385, 1.000000000000000000, 0.9238795325112867385, 1.000000000000000000, 0.9238795325112867385, 1.000000000000000000, 0.9238795325112867385, 1.000000000000000000, 0.9238795325112867385, 1.000000000000000000, 0.9238795325112867385, 1.000000000000000000, 0.9238795325112867385, 1.000000000000000000, 0.9238795325112867385, 1.000000000000000000, 0.9238795325112867385, 1.000000000000000000, 0.9238795325112867385, 1.000000000000000000, 0.9238795325112867385, 1.000000000000000000, 0.9238795325112867385, 1.000000000000000000, 0.9238795325112867385, 1.000000000000000000, 0.9238795325112867385, 1.000000000000000000, 0.9238795325112867385, 1.000000000000000000, 0.9238795325112867385, 1.000000000000000000, 0.9238795325112867385, 1.000000000000000000, 0.9238795325112867385, 1.000000000000000000, 0.9238795325112867385, 1.000000000000000000, 0.9238795325112867385, 1.000000000000000000, 0.9238795325112867385, 1.000000000000000000, 0.9238795325112867385, 1.000000000000000000, 0.9238795325112867385, 1.000000000000000000, 0.9238795325112867385, 1.000000000000000000, 0.9238795325112867385, 1.000000000000000000, 0.9238795325112867385, 1.000000000000000000, 0.9238795325112867385, 1.000000000000000000, 0.9238795325112867385, 1.000000000000000000, 0.9238795325112867385, 1.000000000000000000, 0.9238795325112867385, 1.000000000000000000, 0.9238795325112867385, 1.000000000000000000, 0.9238795325112867385, 1.000000000000000000, 0.9238795325112867385, 1.000000000000000000, 0.9238795325112867385, 1.000000000000000000, 0.9238795325112867385, 1.000000000000000000, 0.9238795325112867385, 1.000000000000000000, 0.9238795325112867385, 1.000000000000000000, 0.9238795325112867385, 1.000000000000000000, 0.9238795325112867385, 1.000000000000000000, 0.9238795325112867385, 1.000000000000000000, 0.9238795325112867385, 1.000000000000000000, 0.9238795325112867385, 1.000000000000000000, 0.9238795325112867385, 1.000000000000000000, 0.9238795325112867385, 1.000000000000000000, 0.9238795325112867385, 1.000000000000000000, 0.9238795325112867385, 1.000000000000000000, 0.9238795325112867385, 1.000000000000000000, 0.9238795325112867385, 1.000000000000000000, 0.9238795325112867385, 1.000000000000000000, 0.9238795325112867385, 1.000000000000000000, 0.9238795325112867385, 1.000000000000000000, 0.9238795325112867385, 1.000000000000000000, 0.9238795325112867385, 1.000000000000000000, 0.9238795325112867385, 1.000000000000000000, 0.9238795325112867385, 1.000000000000000000, 0.9238795325112867385, 1.000000000000000000, 0.9238795325112867385, 1.000000000000000000, 0.9238795325112867385, 1.000000000000000000, 0.9238795325112867385, 1.000000000000000000, 0.9238795325112867385, 1.000000000000000000, 0.9238795325112867385, 1.000000000000000000, 0.9238795325112867385, 1.000000000000000000, 0.9238795325112867385, 1.000000000000000000, 0.9238795325112867385, 1.000000000000000000, 0.9238795325112867385, 1.000000000000000000, 0.9238795325112867385, 1.000000000000000000, 0.9238795325112867385, 1.000000000000000000, 0.9238795325112867385, 1.000000000000000000, 0.9238795325112867385, 1.000000000000000000, 0.9238795325112867385, 1.000000000000000000, 0.9238795325112867385, 1.000000000000000000, 0.9238795325112867385, 1.000000000000000000, 0.9238795325112867385, 1.000000000000000000, 0.9238795325112867385, 1.000000000000000000, 0.9238795325112867385, 1.000000000000000000, 0.9238795325112867385, 1.000000000000000000, 0.9238795325112867385, 1.000000000000000000, 0.9238795325112867385, 1.000000000000000000, 0.9238795325112867385, 1.000000000000000000, 0.9238795325112867385, 1.000000000000000000, 0.9238795325112867385, 1.000000000000000000, 0.9238795325112867385, 1.000000000000000000, 0.9238795325112867385, 1.000000000000000000, 0.9238795325112867385, 1.000000000000000000, 0.9238795325112867385, 1.000000000000000000, 0.9238795325112867385, 1.000000000000000000, 0.9238795325112867385, 1.000000000000000000, 0.9238795325112867385, 1.000000000000000000, 0.9238795325112867385, 1.000000000000000000, 0.9238795325112867385, 1.000000000000000000, 0.9238795325112867385, 1.000000000000000000, 0.9493987661155159907, 0.9660720762559202868),
 ( 1.000000000000000000, 0.9238795325112867385, 1.000000000000000000, 0.9238795325112867385, 1.000000000000000000, 0.9238795325112867385, 1.000000000000000000, 0.9238795325112867385, 1.000000000000000000, 0.9238795325112867385, 1.000000000000000000, 0.9238795325112867385, 1.000000000000000000, 0.9238795325112867385, 1.000000000000000000, 0.9238795325112867385, 1.000000000000000000, 0.9238795325112867385, 1.000000000000000000, 0.9238795325112867385, 1.000000000000000000, 0.9238795325112867385, 1.000000000000000000, 0.9238795325112867385, 1.000000000000000000, 0.9238795325112867385, 1.000000000000000000, 0.9238795325112867385, 1.000000000000000000, 0.9238795325112867385, 1.000000000000000000, 0.9238795325112867385, 1.000000000000000000, 0.9238795325112867385, 1.000000000000000000, 0.9238795325112867385, 1.000000000000000000, 0.9238795325112867385, 1.000000000000000000, 0.9238795325112867385, 1.000000000000000000, 0.9238795325112867385, 1.000000000000000000, 0.9238795325112867385, 1.000000000000000000, 0.9238795325112867385, 1.000000000000000000, 0.9238795325112867385, 1.000000000000000000, 0.9238795325112867385, 1.000000000000000000, 0.9238795325112867385, 1.000000000000000000, 0.9238795325112867385, 1.000000000000000000, 0.9238795325112867385, 1.000000000000000000, 0.9238795325112867385, 1.000000000000000000, 0.9238795325112867385, 1.000000000000000000, 0.9238795325112867385, 1.000000000000000000, 0.9238795325112867385, 1.000000000000000000, 0.9238795325112867385, 1.000000000000000000, 0.9238795325112867385, 1.000000000000000000, 0.9238795325112867385, 1.000000000000000000, 0.9238795325112867385, 1.000000000000000000, 0.9238795325112867385, 1.000000000000000000, 0.9238795325112867385, 1.000000000000000000, 0.9238795325112867385, 1.000000000000000000, 0.9238795325112867385, 1.000000000000000000, 0.9238795325112867385, 1.000000000000000000, 0.9238795325112867385, 1.000000000000000000, 0.9238795325112867385, 1.000000000000000000, 0.9238795325112867385, 1.000000000000000000, 0.9238795325112867385, 1.000000000000000000, 0.9238795325112867385, 1.000000000000000000, 0.9238795325112867385, 1.000000000000000000, 0.9238795325112867385, 1.000000000000000000, 0.9238795325112867385, 1.000000000000000000, 0.9238795325112867385, 1.000000000000000000, 0.9238795325112867385, 1.000000000000000000, 0.9238795325112867385, 1.000000000000000000, 0.9238795325112867385, 1.000000000000000000, 0.9238795325112867385, 1.000000000000000000, 0.9238795325112867385, 1.000000000000000000, 0.9238795325112867385, 1.000000000000000000, 0.9238795325112867385, 1.000000000000000000, 0.9238795325112867385, 1.000000000000000000, 0.9238795325112867385, 1.000000000000000000, 0.9238795325112867385, 1.000000000000000000, 0.9238795325112867385, 1.000000000000000000, 0.9238795325112867385, 1.000000000000000000, 0.9238795325112867385, 1.000000000000000000, 0.9238795325112867385, 1.000000000000000000, 0.9238795325112867385, 1.000000000000000000, 0.9238795325112867385, 1.000000000000000000, 0.9238795325112867385, 1.000000000000000000, 0.9238795325112867385, 1.000000000000000000, 0.9238795325112867385, 1.000000000000000000, 0.9238795325112867385, 1.000000000000000000, 0.9238795325112867385, 1.000000000000000000, 0.9238795325112867385, 1.000000000000000000, 0.9238795325112867385, 1.000000000000000000, 0.9238795325112867385, 1.000000000000000000, 0.9238795325112867385, 1.000000000000000000, 0.9238795325112867385, 1.000000000000000000, 0.9238795325112867385, 1.000000000000000000, 0.9238795325112867385, 1.000000000000000000, 0.9238795325112867385, 1.000000000000000000, 0.9238795325112867385, 1.000000000000000000, 0.9238795325112867385, 1.000000000000000000, 0.9238795325112867385, 1.000000000000000000, 0.9238795325112867385, 1.000000000000000000, 0.9238795325112867385, 1.000000000000000000, 0.9238795325112867385, 1.000000000000000000, 0.9238795325112867385, 1.000000000000000000, 0.9238795325112867385, 1.000000000000000000, 0.9238795325112867385, 1.000000000000000000, 0.9238795325112867385, 1.000000000000000000, 0.9238795325112867385, 1.000000000000000000, 0.9238795325112867385, 1.000000000000000000, 0.9238795325112867385, 1.000000000000000000, 0.9238795325112867385, 1.000000000000000000, 0.9238795325112867385, 1.000000000000000000, 0.9238795325112867385, 1.000000000000000000, 0.9238795325112867385, 1.000000000000000000, 0.9238795325112867385, 1.000000000000000000, 0.9238795325112867385, 1.000000000000000000, 0.9238795325112867385, 1.000000000000000000, 0.9238795325112867385, 1.000000000000000000, 0.9238795325112867385, 1.000000000000000000, 0.9238795325112867385, 1.000000000000000000, 0.9238795325112867385, 1.000000000000000000, 0.9238795325112867385, 1.000000000000000000, 0.9238795325112867385, 1.000000000000000000, 0.9238795325112867385, 1.000000000000000000, 0.9238795325112867385, 1.000000000000000000, 0.9238795325112867385, 1.000000000000000000, 0.9238795325112867385, 1.000000000000000000, 0.9238795325112867385, 1.000000000000000000, 0.9238795325112867385, 1.000000000000000000, 0.9238795325112867385, 1.000000000000000000, 0.9238795325112867385, 1.000000000000000000, 0.9238795325112867385, 1.000000000000000000, 0.9238795325112867385, 1.000000000000000000, 0.9238795325112867385, 1.000000000000000000, 0.9238795325112867385, 1.000000000000000000, 0.9238795325112867385, 1.000000000000000000, 0.9238795325112867385, 1.000000000000000000, 0.9238795325112867385, 1.000000000000000000, 0.9238795325112867385, 1.000000000000000000, 0.9238795325112867385, 1.000000000000000000, 0.9238795325112867385, 1.000000000000000000, 0.9238795325112867385, 1.000000000000000000, 0.9238795325112867385, 1.000000000000000000, 0.9238795325112867385, 1.000000000000000000, 0.9238795325112867385, 1.000000000000000000, 0.9238795325112867385, 1.000000000000000000, 0.9238795325112867385, 1.000000000000000000, 0.9238795325112867385, 1.000000000000000000, 0.9238795325112867385, 1.000000000000000000, 0.9238795325112867385, 1.000000000000000000, 0.9238795325112867385, 1.000000000000000000, 0.9238795325112867385, 1.000000000000000000, 0.9238795325112867385, 1.000000000000000000, 0.9238795325112867385, 1.000000000000000000, 0.9238795325112867385, 1.000000000000000000, 0.9238795325112867385, 1.000000000000000000, 0.9238795325112867385, 1.000000000000000000, 0.9238795325112867385, 1.000000000000000000, 0.9238795325112867385, 1.000000000000000000, 0.9238795325112867385, 1.000000000000000000, 0.9238795325112867385, 1.000000000000000000, 0.9238795325112867385, 1.000000000000000000, 0.9238795325112867385, 1.000000000000000000, 0.9238795325112867385, 1.000000000000000000, 0.9238795325112867385, 1.000000000000000000, 0.9238795325112867385, 1.000000000000000000, 0.9238795325112867385, 1.000000000000000000, 0.9238795325112867385, 1.000000000000000000, 0.9238795325112867385, 1.000000000000000000, 0.9238795325112867385, 1.000000000000000000, 0.9238795325112867385, 1.000000000000000000, 0.9238795325112867385, 1.000000000000000000, 0.9238795325112867385, 1.000000000000000000, 0.9238795325112867385, 1.000000000000000000, 0.9238795325112867385, 1.000000000000000000, 0.9238795325112867385, 1.000000000000000000, 0.9238795325112867385, 1.000000000000000000, 0.9238795325112867385, 1.000000000000000000, 0.9238795325112867385, 1.000000000000000000, 0.9238795325112867385, 1.000000000000000000, 0.9238795325112867385, 1.000000000000000000, 0.9238795325112867385, 1.000000000000000000, 0.9238795325112867385, 1.000000000000000000, 0.9238795325112867385, 1.000000000000000000, 0.9238795325112867385, 1.000000000000000000, 0.9238795325112867385, 1.000000000000000000, 0.9238795325112867385, 1.000000000000000000, 0.9238795325112867385, 1.000000000000000000, 0.9238795325112867385, 1.000000000000000000, 0.9238795325112867385, 1.000000000000000000, 0.9238795325112867385, 1.000000000000000000, 0.9238795325112867385, 1.000000000000000000, 0.9238795325112867385, 1.000000000000000000, 0.9238795325112867385, 1.000000000000000000, 0.9238795325112867385, 1.000000000000000000, 0.9238795325112867385, 1.000000000000000000, 0.9238795325112867385, 1.000000000000000000, 0.9238795325112867385, 1.000000000000000000, 0.9238795325112867385, 1.000000000000000000, 0.9238795325112867385, 1.000000000000000000, 0.9238795325112867385, 1.000000000000000000, 0.9238795325112867385, 1.000000000000000000, 0.9238795325112867385, 1.000000000000000000, 0.9238795325112867385, 1.000000000000000000, 0.9493987661155159907, 0.9660720762559202868) ) ) 
 REPRESENTATION_ITEM ( '' )  SURFACE ( )  );
#47405=CARTESIAN_POINT ( 'NONE',  ( -8.000000000000001776, 21.84375000000000355, 3.313708498984759387 ) ) ;
#47414=CARTESIAN_POINT ( 'NONE',  ( -7.188101187500002709, 5.812499997951611874, 2.977408999572649151 ) ) ;
#47417=CARTESIAN_POINT ( 'NONE',  ( -4.401442555609581635E-16, 116.6562500020483810, -7.188101187500000044 ) ) ;
#47444=CARTESIAN_POINT ( 'NONE',  ( 7.188101187500001821, 21.93749999795161543, -2.977408999572650483 ) ) ;
#47446=CARTESIAN_POINT ( 'NONE',  ( 7.188101187500000044, 99.78125000204838102, -8.802885111219163269E-16 ) ) ;
#47469=CARTESIAN_POINT ( 'NONE',  ( 7.188101187500002709, 93.68750000204838102, 2.977408999572649151 ) ) ;
#47474=EDGE_LOOP ( 'NONE', ( #19236, #50573, #31881, #22640 ) ) ;
#47476=CARTESIAN_POINT ( 'NONE',  ( -8.000000000000000000, 121.9062500000000000, -3.313708498984761164 ) ) ;
#47488=CARTESIAN_POINT ( 'NONE',  ( -3.313708498984762496, 105.9687500040967620, 7.999999999999998224 ) ) ;
#47497=CARTESIAN_POINT ( 'NONE',  ( -5.082755093536325930, 96.96875000204838102, -5.082755093536325930 ) ) ;
#47503=CARTESIAN_POINT ( 'NONE',  ( -8.000000000000000000, 104.0937500040967905, -3.313708498984761164 ) ) ;
#47507=ORIENTED_EDGE ( 'NONE', *, *, #58117, .T. ) ;
#47519=CARTESIAN_POINT ( 'NONE',  ( 5.082755093536324154, 8.156249997951611874, 5.082755093536326818 ) ) ;
#47523=CARTESIAN_POINT ( 'NONE',  ( -5.082755093536325930, 115.3437500020483810, -5.082755093536325930 ) ) ;
#47545=CARTESIAN_POINT ( 'NONE',  ( 7.188101187500000044, 103.9062500020483810, -8.802885111219163269E-16 ) ) ;
#47550=CARTESIAN_POINT ( 'NONE',  ( -7.188101187500001821, 115.4375000020483810, -2.977408999572650483 ) ) ;
#47566=ORIENTED_EDGE ( 'NONE', *, *, #73059, .F. ) ;
#47572=VERTEX_POINT ( 'NONE', #61939 ) ;
#47574=CARTESIAN_POINT ( 'NONE',  ( 3.313708498984762496, 7.218750000000000888, 7.999999999999998224 ) ) ;
#47576=CARTESIAN_POINT ( 'NONE',  ( 7.188101187500001821, 0.5624999979516098758, -2.977408999572650483 ) ) ;
#47577=CARTESIAN_POINT ( 'NONE',  ( -3.313708498984762496, 122.4687500040967763, 7.999999999999998224 ) ) ;
#47591=ORIENTED_EDGE ( 'NONE', *, *, #11097, .T. ) ;
#47598=CARTESIAN_POINT ( 'NONE',  ( -8.000000000000000000, 12.46874999590322197, -3.313708498984762496 ) ) ;
#47601=CARTESIAN_POINT ( 'NONE',  ( 5.656854249492381470, 119.5625000000000000, 5.656854249492379694 ) ) ;
#47605=CARTESIAN_POINT ( 'NONE',  ( -8.000000000000001776, 17.15624999590322020, 3.313708498984759387 ) ) ;
#47607=CARTESIAN_POINT ( 'NONE',  ( 8.000000000000000000, 11.90624999590322375, -3.313708498984761164 ) ) ;
#47613=( BOUNDED_CURVE ( )  B_SPLINE_CURVE ( 2, ( #21377, #68153, #10812, #27409, #55360, #50425, #44401, #73439, #21747 ),
 .UNSPECIFIED., .F., .F. ) 
 B_SPLINE_CURVE_WITH_KNOTS ( ( 3, 2, 2, 2, 3 ),
 ( 0.4583333333333333148, 0.4652777777777777901, 0.4722222222222222099, 0.4791666666666666852, 0.4861111111111111049 ),
 .UNSPECIFIED. ) 
 CURVE ( )  GEOMETRIC_REPRESENTATION_ITEM ( )  RATIONAL_B_SPLINE_CURVE ( ( 1.000000000000000000, 0.9238795325112867385, 1.000000000000000000, 0.9238795325112867385, 1.000000000000000000, 0.9238795325112867385, 1.000000000000000000, 0.9238795325112867385, 1.000000000000000000 ) ) 
 REPRESENTATION_ITEM ( '' )  );
#47622=EDGE_CURVE ( 'NONE', #2559, #64356, #68230, .T. ) ;
#47629=CARTESIAN_POINT ( 'NONE',  ( -5.082755093536324154, 122.8437500020483952, 5.082755093536326818 ) ) ;
#47635=CARTESIAN_POINT ( 'NONE',  ( 7.188101187500001821, 96.50000000204838102, -2.977408999572651371 ) ) ;
#47651=ORIENTED_EDGE ( 'NONE', *, *, #71387, .F. ) ;
#47662=CARTESIAN_POINT ( 'NONE',  ( 2.977408999572651815, 15.18749999795161365, 7.188101187500000933 ) ) ;
#47665=CARTESIAN_POINT ( 'NONE',  ( 7.188101187499999156, 11.24999999795161187, 2.977408999572654924 ) ) ;
#47674=AXIS2_PLACEMENT_3D ( 'NONE', #40166, #22798, #28471 ) ;
#47678=CARTESIAN_POINT ( 'NONE',  ( -2.977408999572651815, 116.9375000020483952, 7.188101187500000933 ) ) ;
#47683=CARTESIAN_POINT ( 'NONE',  ( -1.320432766682874540E-15, 22.59374999795161187, 7.188101187500000044 ) ) ;
#47684=ORIENTED_EDGE ( 'NONE', *, *, #45003, .F. ) ;
#47688=CARTESIAN_POINT ( 'NONE',  ( 5.082755093536325042, 99.96875000204838102, -5.082755093536325930 ) ) ;
#47692=EDGE_LOOP ( 'NONE', ( #55290, #36570, #60540, #41 ) ) ;
#47708=CARTESIAN_POINT ( 'NONE',  ( 8.000000000000000000, 97.53125000409676204, -3.313708498984762496 ) ) ;
#47714=CARTESIAN_POINT ( 'NONE',  ( -4.898587196589412829E-16, 88.81250000409677625, -8.000000000000000000 ) ) ;
#47721=CARTESIAN_POINT ( 'NONE',  ( -4.401442555609581635E-16, 117.7812500020483810, -7.188101187500000044 ) ) ;
#47726=ORIENTED_EDGE ( 'NONE', *, *, #74600, .F. ) ;
#47744=CARTESIAN_POINT ( 'NONE',  ( -4.898587196589412829E-16, 112.8125000040967905, -8.000000000000000000 ) ) ;
#47748=CARTESIAN_POINT ( 'NONE',  ( -7.188101187500002709, 12.18749999795161365, 2.977408999572649151 ) ) ;
#47766=CARTESIAN_POINT ( 'NONE',  ( 4.898587196589412829E-16, 21.37500000000000355, -8.000000000000000000 ) ) ;
#47776=CARTESIAN_POINT ( 'NONE',  ( 2.977408999572652260, 7.687499997951611874, 7.188101187500000044 ) ) ;
#47779=CARTESIAN_POINT ( 'NONE',  ( 2.977408999572650039, 121.0625000020483668, -7.188101187500001821 ) ) ;
#47780=CARTESIAN_POINT ( 'NONE',  ( 1.469576158976823947E-15, 116.5625000040967763, 8.000000000000000000 ) ) ;
#47783=ADVANCED_FACE ( 'NONE', ( #71566 ), #1818, .T. ) ;
#47785=CYLINDRICAL_SURFACE ( 'NONE', #8451, 8.000000000000000000 ) ;
#47817=EDGE_CURVE ( 'NONE', #10908, #65516, #14665, .T. ) ;
#47834=CARTESIAN_POINT ( 'NONE',  ( 5.082755093536326818, 93.59375000204838102, 5.082755093536325042 ) ) ;
#47843=CARTESIAN_POINT ( 'NONE',  ( -5.656854249492378806, 122.1875000000000000, 5.656854249492381470 ) ) ;
#47856=CARTESIAN_POINT ( 'NONE',  ( -4.898587196589412829E-16, 99.31250000409677625, -8.000000000000000000 ) ) ;
#47860=CARTESIAN_POINT ( 'NONE',  ( 9.797174393178825657E-16, 125.0000000000000000, -8.000000000000000000 ) ) ;
#47866=CARTESIAN_POINT ( 'NONE',  ( -2.977408999572651815, 97.43750000204839523, 7.188101187500000933 ) ) ;
#47886=DIRECTION ( 'NONE',  ( -0.000000000000000000, 1.000000000000000000, -0.000000000000000000 ) ) ;
#47888=CARTESIAN_POINT ( 'NONE',  ( 5.656854249492380582, 4.499999995903220196, -5.656854249492380582 ) ) ;
#47890=CARTESIAN_POINT ( 'NONE',  ( -7.188101187500001821, 7.499999997951610986, -2.977408999572651371 ) ) ;
#47893=CARTESIAN_POINT ( 'NONE',  ( 5.082755093536326818, 107.0937500020483810, 5.082755093536325042 ) ) ;
#47901=CARTESIAN_POINT ( 'NONE',  ( 4.898587196589412829E-16, 9.375000000000001776, -8.000000000000000000 ) ) ;
#47913=CARTESIAN_POINT ( 'NONE',  ( 5.082755093536326818, 106.7187500020483952, 5.082755093536325042 ) ) ;
#47918=CARTESIAN_POINT ( 'NONE',  ( -2.977408999572650927, 107.7500000020483810, -7.188101187500001821 ) ) ;
#47930=CARTESIAN_POINT ( 'NONE',  ( -1.469576158976823947E-15, 14.62500000000000178, 8.000000000000000000 ) ) ;
#47941=CARTESIAN_POINT ( 'NONE',  ( 5.656854249492380582, 3.187500000000000444, -5.656854249492380582 ) ) ;
#47943=CARTESIAN_POINT ( 'NONE',  ( 7.188101187500000044, 4.968749997951610986, 0.000000000000000000 ) ) ;
#47944=CARTESIAN_POINT ( 'NONE',  ( -5.656854249492380582, 113.0000000040967763, -5.656854249492380582 ) ) ;
#47949=ADVANCED_FACE ( 'NONE', ( #15716 ), #21009, .T. ) ;
#47967=CARTESIAN_POINT ( 'NONE',  ( 8.000000000000000000, 26.90624999590322730, -3.313708498984761164 ) ) ;
#47973=CARTESIAN_POINT ( 'NONE',  ( 8.000000000000000000, 116.7499999999999858, -9.797174393178825657E-16 ) ) ;
#47978=CARTESIAN_POINT ( 'NONE',  ( -3.313708498984765161, 15.84374999590322197, 7.999999999999998224 ) ) ;
#47988=DIRECTION ( 'NONE',  ( -0.000000000000000000, 1.000000000000000000, -0.000000000000000000 ) ) ;
#48001=CARTESIAN_POINT ( 'NONE',  ( 8.000000000000000000, 119.7500000000000000, -9.797174393178825657E-16 ) ) ;
#48006=CARTESIAN_POINT ( 'NONE',  ( 2.977408999572650039, 90.68750000204838102, -7.188101187500001821 ) ) ;
#48018=DIRECTION ( 'NONE',  ( 0.000000000000000000, 0.000000000000000000, 1.000000000000000000 ) ) ;
#48034=CARTESIAN_POINT ( 'NONE',  ( -1.320432766682874540E-15, 16.59374999795161543, 7.188101187500000044 ) ) ;
#48037=CARTESIAN_POINT ( 'NONE',  ( -5.082755093536325042, 13.40624999795161187, -5.082755093536325930 ) ) ;
#48043=EDGE_LOOP ( 'NONE', ( #4477, #1958, #65199, #24216 ) ) ;
#48050=CARTESIAN_POINT ( 'NONE',  ( -4.401442555609581635E-16, 111.7812500020483810, -7.188101187500000044 ) ) ;
#48054=CARTESIAN_POINT ( 'NONE',  ( -2.977408999572654480, 22.49999999795161187, 7.188101187499999156 ) ) ;
#48056=ORIENTED_EDGE ( 'NONE', *, *, #19444, .F. ) ;
#48062=CARTESIAN_POINT ( 'NONE',  ( -7.188101187500000044, 99.03125000204838102, 0.000000000000000000 ) ) ;
#48076=DIRECTION ( 'NONE',  ( -0.000000000000000000, 1.000000000000000000, -0.000000000000000000 ) ) ;
#48080=CARTESIAN_POINT ( 'NONE',  ( -7.999999999999998224, 117.5937500000000000, 3.313708498984766049 ) ) ;
#48091=CARTESIAN_POINT ( 'NONE',  ( 2.977408999572650039, 113.1875000020483810, -7.188101187500001821 ) ) ;
#48102=ORIENTED_EDGE ( 'NONE', *, *, #53263, .T. ) ;
#48111=CARTESIAN_POINT ( 'NONE',  ( -7.999999999999998224, 92.09375000000000000, 3.313708498984766049 ) ) ;
#48112=ORIENTED_EDGE ( 'NONE', *, *, #8272, .F. ) ;
#48121=CARTESIAN_POINT ( 'NONE',  ( -5.082755093536325042, 13.40624999795161187, -5.082755093536325930 ) ) ;
#48130=CARTESIAN_POINT ( 'NONE',  ( -3.313708498984816231, 98.46875000409676204, 7.999999999999943157 ) ) ;
#48137=CARTESIAN_POINT ( 'NONE',  ( 4.898587196589412829E-16, 22.87500000000000355, -8.000000000000000000 ) ) ;
#48148=CARTESIAN_POINT ( 'NONE',  ( -5.082755093536326818, 4.406249997951610986, 5.082755093536325042 ) ) ;
#48150=CARTESIAN_POINT ( 'NONE',  ( -4.401442555609581635E-16, 121.1562500020483810, -7.188101187500000044 ) ) ;
#48156=( BOUNDED_CURVE ( )  B_SPLINE_CURVE ( 2, ( #64123, #64498, #13525, #25224, #65220, #7525, #2605, #54293, #18471 ),
 .UNSPECIFIED., .F., .F. ) 
 B_SPLINE_CURVE_WITH_KNOTS ( ( 3, 2, 2, 2, 3 ),
 ( 0.5416666666666666297, 0.5486111111111111605, 0.5555555555555555802, 0.5625000000000000000, 0.5694444444444444198 ),
 .UNSPECIFIED. ) 
 CURVE ( )  GEOMETRIC_REPRESENTATION_ITEM ( )  RATIONAL_B_SPLINE_CURVE ( ( 1.000000000000000000, 0.9238795325112867385, 1.000000000000000000, 0.9238795325112867385, 1.000000000000000000, 0.9238795325112867385, 1.000000000000000000, 0.9238795325112867385, 1.000000000000000000 ) ) 
 REPRESENTATION_ITEM ( '' )  );
#48166=CARTESIAN_POINT ( 'NONE',  ( -3.313708498984762052, 97.71874999999998579, -8.000000000000000000 ) ) ;
#48173=ORIENTED_EDGE ( 'NONE', *, *, #5242, .T. ) ;
#48182=CARTESIAN_POINT ( 'NONE',  ( -7.188101187500000044, 91.53125000204836681, 0.000000000000000000 ) ) ;
#48198=CARTESIAN_POINT ( 'NONE',  ( 3.313708498984765161, 103.1562500040967905, 7.999999999999998224 ) ) ;
#48204=CARTESIAN_POINT ( 'NONE',  ( 7.188101187500001821, 90.87500000204838102, -2.977408999572651371 ) ) ;
#48228=CARTESIAN_POINT ( 'NONE',  ( -5.656854249492380582, 99.50000000409679046, -5.656854249492380582 ) ) ;
#48237=CARTESIAN_POINT ( 'NONE',  ( -2.977408999572650927, 101.3750000020483952, -7.188101187500001821 ) ) ;
#48238=CARTESIAN_POINT ( 'NONE',  ( -8.000000000000000000, 92.09375000409679046, -3.313708498984761164 ) ) ;
#48258=CARTESIAN_POINT ( 'NONE',  ( 8.000000000000000000, 5.812499995903220196, 0.000000000000000000 ) ) ;
#48261=CARTESIAN_POINT ( 'NONE',  ( -7.188101187500001821, 10.49999999795161010, -2.977408999572651371 ) ) ;
#48264=CARTESIAN_POINT ( 'NONE',  ( -7.188101187500000933, 109.4375000020483810, -2.977408999572650483 ) ) ;
#48286=CARTESIAN_POINT ( 'NONE',  ( 7.188101187500000044, 106.9062500020483810, -8.802885111219163269E-16 ) ) ;
#48291=CARTESIAN_POINT ( 'NONE',  ( -5.082755093536324154, 111.2187500020483810, 5.082755093536326818 ) ) ;
#48307=ADVANCED_FACE ( 'NONE', ( #62487 ), #69275, .T. ) ;
#48308=CARTESIAN_POINT ( 'NONE',  ( 5.656854249492378806, 20.62499999590322375, 5.656854249492381470 ) ) ;
#48315=ORIENTED_EDGE ( 'NONE', *, *, #31376, .T. ) ;
#48317=CARTESIAN_POINT ( 'NONE',  ( 7.999999999999998224, 8.906250000000001776, 3.313708498984766493 ) ) ;
#48319=CARTESIAN_POINT ( 'NONE',  ( -5.082755093536326818, 4.406249997951610986, 5.082755093536325042 ) ) ;
#48320=CARTESIAN_POINT ( 'NONE',  ( -8.000000000000000000, 114.5937500040967763, -3.313708498984761608 ) ) ;
#48333=VERTEX_POINT ( 'NONE', #12660 ) ;
#48343=CARTESIAN_POINT ( 'NONE',  ( 1.469576158976823947E-15, 114.8750000000000000, 8.000000000000000000 ) ) ;
#48347=CARTESIAN_POINT ( 'NONE',  ( 7.999999999999998224, 20.71874999590322375, 3.313708498984766493 ) ) ;
#48349=DIRECTION ( 'NONE',  ( -0.000000000000000000, 1.000000000000000000, -0.000000000000000000 ) ) ;
#48357=LINE ( 'NONE', #42329, #63649 ) ;
#48363=( BOUNDED_CURVE ( )  B_SPLINE_CURVE ( 2, ( #65190, #24092, #47843, #70864, #36169, #47476, #47101, #53890, #59189 ),
 .UNSPECIFIED., .F., .F. ) 
 B_SPLINE_CURVE_WITH_KNOTS ( ( 3, 2, 2, 2, 3 ),
 ( 0.07291666666666671293, 0.07812500000000005551, 0.08333333333333338422, 0.08854166666666674068, 0.09375000000000006939 ),
 .UNSPECIFIED. ) 
 CURVE ( )  GEOMETRIC_REPRESENTATION_ITEM ( )  RATIONAL_B_SPLINE_CURVE ( ( 0.9999999999999994449, 0.9238795325112872936, 1.000000000000000000, 0.9238795325112867385, 1.000000000000000000, 0.9238795325112867385, 1.000000000000000000, 0.9238795325112857393, 1.000000000000001110 ) ) 
 REPRESENTATION_ITEM ( '' )  );
#48371=CARTESIAN_POINT ( 'NONE',  ( -2.977408999572650927, 122.3750000020483952, -7.188101187500000933 ) ) ;
#48375=EDGE_CURVE ( 'NONE', #71473, #3567, #56142, .T. ) ;
#48378=CARTESIAN_POINT ( 'NONE',  ( -7.188101187500001821, 89.56250000204838102, -2.977408999572650483 ) ) ;
#48406=CARTESIAN_POINT ( 'NONE',  ( -5.082755093536326818, 22.40624999795161187, 5.082755093536325042 ) ) ;
#48408=CARTESIAN_POINT ( 'NONE',  ( 3.979266480698044450, 124.5000000000001137, -6.940132439340980675 ) ) ;
#48409=CARTESIAN_POINT ( 'NONE',  ( -7.188101187500002709, 13.68749999795161365, 2.977408999572649151 ) ) ;
#48421=CARTESIAN_POINT ( 'NONE',  ( -7.188101187500001821, 110.5625000020483810, -2.977408999572650483 ) ) ;
#48425=CARTESIAN_POINT ( 'NONE',  ( 5.082755093536325930, 23.15624999795161543, -5.082755093536325930 ) ) ;
#48431=CARTESIAN_POINT ( 'NONE',  ( 7.188101187500001821, 92.37500000204839523, -2.977408999572651371 ) ) ;
#48435=VERTEX_POINT ( 'NONE', #70750 ) ;
#48459=CARTESIAN_POINT ( 'NONE',  ( -3.893442805679455887, 124.6581723871223488, -6.826363913033100417 ) ) ;
#48462=CARTESIAN_POINT ( 'NONE',  ( 5.082755093536325042, 108.5937500020483810, -5.082755093536325930 ) ) ;
#48469=CARTESIAN_POINT ( 'NONE',  ( 3.313708498984869077, 93.21875000409677625, -7.999999999999892530 ) ) ;
#48476=EDGE_CURVE ( 'NONE', #9708, #18825, #30397, .T. ) ;
#48487=CARTESIAN_POINT ( 'NONE',  ( 5.656854249492381470, 112.2500000040967763, 5.656854249492379694 ) ) ;
#48491=CARTESIAN_POINT ( 'NONE',  ( -2.977408999572654480, 9.374999997951610098, 7.188101187499999156 ) ) ;
#48508=CARTESIAN_POINT ( 'NONE',  ( -1.469576158976823947E-15, 25.12500000000000355, 8.000000000000000000 ) ) ;
#48510=VERTEX_POINT ( 'NONE', #36061 ) ;
#48516=ORIENTED_EDGE ( 'NONE', *, *, #66343, .T. ) ;
#48517=CARTESIAN_POINT ( 'NONE',  ( 5.082755093536325930, 3.656249997951610542, -5.082755093536325930 ) ) ;
#48520=CARTESIAN_POINT ( 'NONE',  ( 1.320432766682874540E-15, 115.9062500020483810, 7.188101187500000044 ) ) ;
#48533=CARTESIAN_POINT ( 'NONE',  ( 8.000000000000000000, 98.84374999999998579, -3.313708498984762496 ) ) ;
#48546=CARTESIAN_POINT ( 'NONE',  ( -2.977408999572654480, 27.37499999795161187, 7.188101187499999156 ) ) ;
#48548=CARTESIAN_POINT ( 'NONE',  ( -7.188101187500000933, 89.93750000204839523, -2.977408999572650483 ) ) ;
#48558=CARTESIAN_POINT ( 'NONE',  ( -8.000000000000000000, 9.468749995903223748, -3.313708498984762496 ) ) ;
#48572=CARTESIAN_POINT ( 'NONE',  ( -4.401442555609581635E-16, 91.15625000204838102, -7.188101187500000044 ) ) ;
#48581=CARTESIAN_POINT ( 'NONE',  ( 5.656854249492378806, 14.62499999590322020, 5.656854249492381470 ) ) ;
#48582=LINE ( 'NONE', #30139, #50925 ) ;
#48591=EDGE_CURVE ( 'NONE', #66964, #16528, #16660, .T. ) ;
#48598=CARTESIAN_POINT ( 'NONE',  ( 8.000000000000000000, 100.4375000040967763, -9.797174393178825657E-16 ) ) ;
#48609=CARTESIAN_POINT ( 'NONE',  ( -2.977408999572651815, 98.93750000204838102, 7.188101187500000933 ) ) ;
#48626=CARTESIAN_POINT ( 'NONE',  ( -3.313708498984870410, 90.96875000409676204, 7.999999999999890754 ) ) ;
#48628=CARTESIAN_POINT ( 'NONE',  ( 8.000000000000000000, 5.906249995903220196, -3.313708498984761608 ) ) ;
#48630=CARTESIAN_POINT ( 'NONE',  ( -7.188101187500000044, 10.59374999795161187, -8.802885111219163269E-16 ) ) ;
#48633=CARTESIAN_POINT ( 'NONE',  ( -7.188101187500000933, 110.9375000020483810, -2.977408999572650483 ) ) ;
#48637=CARTESIAN_POINT ( 'NONE',  ( 4.898587196589412829E-16, 21.37500000000000355, -8.000000000000000000 ) ) ;
#48641=EDGE_CURVE ( 'NONE', #23857, #29800, #26197, .T. ) ;
#48653=CARTESIAN_POINT ( 'NONE',  ( 2.977408999572650039, 105.6875000020483952, -7.188101187500000933 ) ) ;
#48659=CARTESIAN_POINT ( 'NONE',  ( -7.188101187500001821, 109.4375000020483810, -2.977408999572650483 ) ) ;
#48665=CARTESIAN_POINT ( 'NONE',  ( 4.898587196589412829E-16, 18.37500000000000355, -8.000000000000000000 ) ) ;
#48671=CARTESIAN_POINT ( 'NONE',  ( -7.188101187500000044, 1.593749997951610320, -8.802885111219163269E-16 ) ) ;
#48678=CARTESIAN_POINT ( 'NONE',  ( 5.656854249492380582, 1.499999995903219974, -5.656854249492380582 ) ) ;
#48688=CARTESIAN_POINT ( 'NONE',  ( -7.188101187500002709, 27.18749999795162609, 2.977408999572649151 ) ) ;
#48689=CARTESIAN_POINT ( 'NONE',  ( 8.000000000000000000, 118.5312500040968047, -3.313708498984762496 ) ) ;
#48702=DIRECTION ( 'NONE',  ( -0.000000000000000000, 1.000000000000000000, -0.000000000000000000 ) ) ;
#48705=( BOUNDED_CURVE ( )  B_SPLINE_CURVE ( 2, ( #31494, #42796, #72216, #54139, #14490, #66558, #37907, #65812, #49587 ),
 .UNSPECIFIED., .F., .F. ) 
 B_SPLINE_CURVE_WITH_KNOTS ( ( 3, 2, 2, 2, 3 ),
 ( 0.2395833333333330928, 0.2447916666666664076, 0.2499999999999997780, 0.2552083333333330928, 0.2604166666666664631 ),
 .UNSPECIFIED. ) 
 CURVE ( )  GEOMETRIC_REPRESENTATION_ITEM ( )  RATIONAL_B_SPLINE_CURVE ( ( 1.000000000000003553, 0.9238795325112830747, 1.000000000000000000, 0.9238795325112867385, 1.000000000000000000, 0.9238795325112867385, 1.000000000000000000, 0.9238795325112899581, 0.9999999999999967804 ) ) 
 REPRESENTATION_ITEM ( '' )  );
#48707=ORIENTED_EDGE ( 'NONE', *, *, #49121, .T. ) ;
#48715=CARTESIAN_POINT ( 'NONE',  ( -3.313708498984762052, 114.2187500000000000, -8.000000000000000000 ) ) ;
#48720=CARTESIAN_POINT ( 'NONE',  ( -3.313708498984765161, 20.34374999590322020, 7.999999999999998224 ) ) ;
#48731=LINE ( 'NONE', #14015, #64836 ) ;
#48733=CARTESIAN_POINT ( 'NONE',  ( -5.656854249492378806, 99.87500000409679046, 5.656854249492381470 ) ) ;
#48748=CARTESIAN_POINT ( 'NONE',  ( -2.977408999572650927, 93.87500000204836681, -7.188101187500001821 ) ) ;
#48764=VERTEX_POINT ( 'NONE', #63520 ) ;
#48774=DIRECTION ( 'NONE',  ( 0.000000000000000000, 0.000000000000000000, -1.000000000000000000 ) ) ;
#48778=CARTESIAN_POINT ( 'NONE',  ( 2.977408999572650927, 18.74999999795161898, -7.188101187500001821 ) ) ;
#48781=CARTESIAN_POINT ( 'NONE',  ( -5.082755093536325042, 14.90624999795161187, -5.082755093536325930 ) ) ;
#48784=CYLINDRICAL_SURFACE ( 'NONE', #53474, 8.000000000000000000 ) ;
#48786=EDGE_LOOP ( 'NONE', ( #22524, #66128, #57883, #9065 ) ) ;
#48792=CARTESIAN_POINT ( 'NONE',  ( 7.188101187500000044, 111.4062500020483810, -8.802885111219163269E-16 ) ) ;
#48796=CARTESIAN_POINT ( 'NONE',  ( 7.188101187500000044, 22.96874999795161543, 0.000000000000000000 ) ) ;
#48803=CARTESIAN_POINT ( 'NONE',  ( -7.188101187499999156, 91.62500000204838102, 2.977408999572654924 ) ) ;
#48809=( BOUNDED_CURVE ( )  B_SPLINE_CURVE ( 2, ( #33245, #44920, #5304, #61524, #28305, #44548, #67558, #33617, #67928 ),
 .UNSPECIFIED., .F., .F. ) 
 B_SPLINE_CURVE_WITH_KNOTS ( ( 3, 2, 2, 2, 3 ),
 ( 0.2187500000000001388, 0.2239583333333333703, 0.2291666666666666019, 0.2343749999999998335, 0.2395833333333330928 ),
 .UNSPECIFIED. ) 
 CURVE ( )  GEOMETRIC_REPRESENTATION_ITEM ( )  RATIONAL_B_SPLINE_CURVE ( ( 0.9999999999999980016, 0.9238795325112887369, 1.000000000000000000, 0.9238795325112867385, 1.000000000000000000, 0.9238795325112867385, 1.000000000000000000, 0.9238795325112904022, 0.9999999999999963363 ) ) 
 REPRESENTATION_ITEM ( '' )  );
#48812=CARTESIAN_POINT ( 'NONE',  ( 8.000000000000000000, 12.09375000000000178, -3.313708498984761164 ) ) ;
#48835=CARTESIAN_POINT ( 'NONE',  ( 1.320432766682874540E-15, 106.5312500020483810, 7.188101187500000044 ) ) ;
#48851=CARTESIAN_POINT ( 'NONE',  ( -4.898587196589412829E-16, 94.62499999999998579, -8.000000000000000000 ) ) ;
#48854=CARTESIAN_POINT ( 'NONE',  ( -8.000000000000000000, 91.90625000000000000, -3.313708498984761164 ) ) ;
#48856=CARTESIAN_POINT ( 'NONE',  ( -8.000000000000000000, 110.0000000000000000, 0.000000000000000000 ) ) ;
#48861=CARTESIAN_POINT ( 'NONE',  ( -2.977408999572650039, 20.81249999795161543, -7.188101187500000933 ) ) ;
#48870=CARTESIAN_POINT ( 'NONE',  ( 7.188101187499999156, 3.374999997951610098, 2.977408999572654924 ) ) ;
#48887=CARTESIAN_POINT ( 'NONE',  ( -2.977408999572654480, 5.999999997951610986, 7.188101187499999156 ) ) ;
#48892=CARTESIAN_POINT ( 'NONE',  ( -2.977408999572650927, 113.7500000020483668, -7.188101187500001821 ) ) ;
#48899=LINE ( 'NONE', #3269, #72698 ) ;
#48904=CARTESIAN_POINT ( 'NONE',  ( -5.656854249492378806, 95.18750000000000000, 5.656854249492381470 ) ) ;
#48912=CARTESIAN_POINT ( 'NONE',  ( 8.000000000000000000, 100.2499999999999858, -9.797174393178825657E-16 ) ) ;
#48920=CARTESIAN_POINT ( 'NONE',  ( 2.977408999572654480, 92.00000000204838102, 7.188101187499999156 ) ) ;
#48925=DIRECTION ( 'NONE',  ( -0.000000000000000000, 1.000000000000000000, -0.000000000000000000 ) ) ;
#48928=( BOUNDED_CURVE ( )  B_SPLINE_CURVE ( 2, ( #42287, #19277, #36644, #12143, #7235, #36275, #59291, #6500, #1585 ),
 .UNSPECIFIED., .F., .F. ) 
 B_SPLINE_CURVE_WITH_KNOTS ( ( 3, 2, 2, 2, 3 ),
 ( 0.4027777777777776791, 0.4097222222222220989, 0.4166666666666666297, 0.4236111111111110494, 0.4305555555555555247 ),
 .UNSPECIFIED. ) 
 CURVE ( )  GEOMETRIC_REPRESENTATION_ITEM ( )  RATIONAL_B_SPLINE_CURVE ( ( 1.000000000000001110, 0.9238795325112855172, 1.000000000000000000, 0.9238795325112867385, 1.000000000000000000, 0.9238795325112867385, 1.000000000000000000, 0.9238795325112872936, 0.9999999999999994449 ) ) 
 REPRESENTATION_ITEM ( '' )  );
#48958=CARTESIAN_POINT ( 'NONE',  ( 4.898587196589412829E-16, 3.187499995903220640, -8.000000000000000000 ) ) ;
#48968=CARTESIAN_POINT ( 'NONE',  ( 5.656854249492381470, 100.2500000040967905, 5.656854249492379694 ) ) ;
#48976=FACE_OUTER_BOUND ( 'NONE', #73186, .T. ) ;
#48977=CARTESIAN_POINT ( 'NONE',  ( 5.082755093536326818, 90.21875000204838102, 5.082755093536325042 ) ) ;
#49002=CARTESIAN_POINT ( 'NONE',  ( 7.999999999999998224, 2.718749995903220196, 3.313708498984766493 ) ) ;
#49004=CARTESIAN_POINT ( 'NONE',  ( -7.188101187500000044, 13.59374999795161187, -8.802885111219163269E-16 ) ) ;
#49007=CARTESIAN_POINT ( 'NONE',  ( 2.977408999572650039, 109.0625000020483810, -7.188101187500000933 ) ) ;
#49017=ORIENTED_EDGE ( 'NONE', *, *, #45695, .T. ) ;
#49026=CARTESIAN_POINT ( 'NONE',  ( 5.082755093536326818, 100.7187500020483810, 5.082755093536325042 ) ) ;
#49029=CARTESIAN_POINT ( 'NONE',  ( 1.017526493066789772, 0.4019176081028156267, -7.852628965127530059 ) ) ;
#49033=CARTESIAN_POINT ( 'NONE',  ( -7.188101187500001821, 107.9375000020483810, -2.977408999572650483 ) ) ;
#49034=ORIENTED_EDGE ( 'NONE', *, *, #28863, .F. ) ;
#49044=CARTESIAN_POINT ( 'NONE',  ( 4.401442555609581635E-16, 1.218749997951610098, -7.188101187500000044 ) ) ;
#49059=CARTESIAN_POINT ( 'NONE',  ( -5.082755093536326818, 10.40624999795161187, 5.082755093536325042 ) ) ;
#49060=CARTESIAN_POINT ( 'NONE',  ( 3.313708498984765161, 118.1562500040967763, 7.999999999999998224 ) ) ;
#49072=( NAMED_UNIT ( * ) SI_UNIT ( $, .STERADIAN. ) SOLID_ANGLE_UNIT ( ) );
#49086=CARTESIAN_POINT ( 'NONE',  ( 3.313708498984760720, 109.5312500000000142, -8.000000000000000000 ) ) ;
#49091=CARTESIAN_POINT ( 'NONE',  ( -1.469576158976823947E-15, 19.12500000000000355, 8.000000000000000000 ) ) ;
#49093=CARTESIAN_POINT ( 'NONE',  ( 5.656854249492378806, 20.62499999590322375, 5.656854249492381470 ) ) ;
#49096=CARTESIAN_POINT ( 'NONE',  ( 1.469576158976823947E-15, 120.8750000000000000, 8.000000000000000000 ) ) ;
#49113=CARTESIAN_POINT ( 'NONE',  ( 0.000000000000000000, -7.499999999999890754, 0.000000000000000000 ) ) ;
#49116=CARTESIAN_POINT ( 'NONE',  ( 2.977408999572650039, 119.1875000020483952, -7.188101187500000933 ) ) ;
#49121=EDGE_CURVE ( 'NONE', #55604, #3980, #31158, .T. ) ;
#49122=CARTESIAN_POINT ( 'NONE',  ( 2.977408999572650039, 92.18750000204838102, -7.188101187500001821 ) ) ;
#49134=AXIS2_PLACEMENT_3D ( 'NONE', #2648, #26769, #36977 ) ;
#49144=ORIENTED_EDGE ( 'NONE', *, *, #20488, .F. ) ;
#49147=ORIENTED_EDGE ( 'NONE', *, *, #32678, .F. ) ;
#49149=CARTESIAN_POINT ( 'NONE',  ( 5.082755093536325930, 18.65624999795161187, -5.082755093536325930 ) ) ;
#49153=CARTESIAN_POINT ( 'NONE',  ( -2.977408999572650039, 16.31249999795161543, -7.188101187500001821 ) ) ;
#49159=( BOUNDED_CURVE ( )  B_SPLINE_CURVE ( 2, ( #14010, #37046, #67217, #15143, #38175, #66840, #16250, #21919, #55536 ),
 .UNSPECIFIED., .F., .F. ) 
 B_SPLINE_CURVE_WITH_KNOTS ( ( 3, 2, 2, 2, 3 ),
 ( 0.2395833333333330928, 0.2447916666666664076, 0.2499999999999997780, 0.2552083333333330928, 0.2604166666666664631 ),
 .UNSPECIFIED. ) 
 CURVE ( )  GEOMETRIC_REPRESENTATION_ITEM ( )  RATIONAL_B_SPLINE_CURVE ( ( 1.000000000000003553, 0.9238795325112830747, 1.000000000000000000, 0.9238795325112867385, 1.000000000000000000, 0.9238795325112867385, 1.000000000000000000, 0.9238795325112899581, 0.9999999999999967804 ) ) 
 REPRESENTATION_ITEM ( '' )  );
#49166=CARTESIAN_POINT ( 'NONE',  ( 7.188101187500002709, 111.3125000020483810, 2.977408999572649151 ) ) ;
#49167=CARTESIAN_POINT ( 'NONE',  ( 1.469576158976823947E-15, 93.87499999999998579, 8.000000000000000000 ) ) ;
#49177=CARTESIAN_POINT ( 'NONE',  ( 2.977408999572654480, 95.00000000204836681, 7.188101187499999156 ) ) ;
#49199=CARTESIAN_POINT ( 'NONE',  ( -3.313708498984765161, 17.53125000000000711, 7.999999999999998224 ) ) ;
#49200=ORIENTED_EDGE ( 'NONE', *, *, #25172, .F. ) ;
#49210=CARTESIAN_POINT ( 'NONE',  ( 7.188101187500002709, 111.3125000020483810, 2.977408999572649151 ) ) ;
#49231=CARTESIAN_POINT ( 'NONE',  ( -3.313708498984789141, 109.7187499999999858, -7.999999999999974243 ) ) ;
#49235=CARTESIAN_POINT ( 'NONE',  ( 7.188101187500000044, 20.34374999795161543, 0.000000000000000000 ) ) ;
#49243=CARTESIAN_POINT ( 'NONE',  ( 2.977408999572651815, 4.687499997951610986, 7.188101187500000933 ) ) ;
#49261=CARTESIAN_POINT ( 'NONE',  ( 7.999999999999998224, 5.906250000000000888, 3.313708498984766049 ) ) ;
#49263=CARTESIAN_POINT ( 'NONE',  ( -2.977408999572654480, 13.49999999795161187, 7.188101187499999156 ) ) ;
#49267=CARTESIAN_POINT ( 'NONE',  ( 1.320432766682874540E-15, 111.4062500020483810, 7.188101187500000044 ) ) ;
#49277=CARTESIAN_POINT ( 'NONE',  ( 4.898587196589412829E-16, 19.68749999590322020, -8.000000000000000000 ) ) ;
#49281=CARTESIAN_POINT ( 'NONE',  ( 3.313708498984762496, 23.71875000000000355, 7.999999999999998224 ) ) ;
#49282=CARTESIAN_POINT ( 'NONE',  ( -7.999999999999998224, 96.59375000000000000, 3.313708498984766493 ) ) ;
#49297=CARTESIAN_POINT ( 'NONE',  ( -2.977408999572650927, 92.75000000204839523, -7.188101187500000933 ) ) ;
#49306=CARTESIAN_POINT ( 'NONE',  ( 5.656854249492381470, 92.56249999999998579, 5.656854249492379694 ) ) ;
#49307=CARTESIAN_POINT ( 'NONE',  ( -7.188101187500001821, 19.12499999795161187, -2.977408999572651371 ) ) ;
#49346=CARTESIAN_POINT ( 'NONE',  ( 5.656854249492379694, 99.12500000409677625, -5.656854249492380582 ) ) ;
#49349=ORIENTED_EDGE ( 'NONE', *, *, #25789, .F. ) ;
#49356=DIRECTION ( 'NONE',  ( 0.000000000000000000, 0.000000000000000000, 1.000000000000000000 ) ) ;
#49357=CARTESIAN_POINT ( 'NONE',  ( -2.977408999572651815, 92.93750000204839523, 7.188101187500000933 ) ) ;
#49369=CARTESIAN_POINT ( 'NONE',  ( -8.000000000000000000, 105.6875000040967763, 0.000000000000000000 ) ) ;
#49377=CARTESIAN_POINT ( 'NONE',  ( 3.313708498984762052, 4.593749995903220196, -8.000000000000000000 ) ) ;
#49380=CARTESIAN_POINT ( 'NONE',  ( 2.977408999572651815, 14.06249999795161365, 7.188101187500000933 ) ) ;
#49383=CARTESIAN_POINT ( 'NONE',  ( -2.977408999572650927, 110.7500000020483810, -7.188101187500000933 ) ) ;
#49401=CARTESIAN_POINT ( 'NONE',  ( 8.000000000000000000, 25.40624999590322730, -3.313708498984761164 ) ) ;
#49402=CARTESIAN_POINT ( 'NONE',  ( 7.188101187500000933, 101.0000000020483810, -2.977408999572651371 ) ) ;
#49409=CARTESIAN_POINT ( 'NONE',  ( 5.082755093536326818, 111.5937500020483810, 5.082755093536325042 ) ) ;
#49420=CARTESIAN_POINT ( 'NONE',  ( -2.977408999572650039, 1.312499997951610098, -7.188101187500000933 ) ) ;
#49439=CARTESIAN_POINT ( 'NONE',  ( -7.188101187500001821, 5.624999997951611874, -2.977408999572651371 ) ) ;
#49441=CARTESIAN_POINT ( 'NONE',  ( 3.313708498984760720, 118.7187500040967905, -8.000000000000000000 ) ) ;
#49456=DIRECTION ( 'NONE',  ( -0.000000000000000000, 1.000000000000000000, -0.000000000000000000 ) ) ;
#49467=CARTESIAN_POINT ( 'NONE',  ( 5.656854249492379694, 113.9375000000000000, -5.656854249492380582 ) ) ;
#49473=CARTESIAN_POINT ( 'NONE',  ( 3.313708498984762052, 18.09374999590322375, -8.000000000000000000 ) ) ;
#49484=DIRECTION ( 'NONE',  ( -0.000000000000000000, 1.000000000000000000, -0.000000000000000000 ) ) ;
#49497=CARTESIAN_POINT ( 'NONE',  ( 7.188101187500002709, 115.8125000020483952, 2.977408999572649151 ) ) ;
#49498=CARTESIAN_POINT ( 'NONE',  ( 5.656854249492381470, 119.5625000000000000, 5.656854249492379694 ) ) ;
#49503=CARTESIAN_POINT ( 'NONE',  ( -7.188101187500001821, 92.56250000204838102, -2.977408999572650483 ) ) ;
#49525=ORIENTED_EDGE ( 'NONE', *, *, #58545, .T. ) ;
#49529=CARTESIAN_POINT ( 'NONE',  ( -1.320432766682874540E-15, 24.09374999795161543, 7.188101187500000044 ) ) ;
#49533=CARTESIAN_POINT ( 'NONE',  ( 5.082755093536324154, 20.15624999795161543, 5.082755093536326818 ) ) ;
#49559=CARTESIAN_POINT ( 'NONE',  ( -5.082755093536325930, 91.34375000204838102, -5.082755093536325930 ) ) ;
#49564=CARTESIAN_POINT ( 'NONE',  ( 5.656854249492378806, 8.624999995903221972, 5.656854249492381470 ) ) ;
#49580=EDGE_LOOP ( 'NONE', ( #53088, #47591, #69653, #2889 ) ) ;
#49582=VECTOR ( 'NONE', #54284, 1000.000000000000114 ) ;
#49587=CARTESIAN_POINT ( 'NONE',  ( -4.898587196589412829E-16, 115.6250000000000000, -8.000000000000000000 ) ) ;
#49591=CARTESIAN_POINT ( 'NONE',  ( -7.188101187500001821, 110.5625000020483810, -2.977408999572650483 ) ) ;
#49616=CYLINDRICAL_SURFACE ( 'NONE', #52113, 8.000000000000000000 ) ;
#49619=CARTESIAN_POINT ( 'NONE',  ( 7.188101187500000933, 15.93749999795161365, -2.977408999572650483 ) ) ;
#49624=CARTESIAN_POINT ( 'NONE',  ( -4.898587196589412829E-16, 96.31250000409677625, -8.000000000000000000 ) ) ;
#49629=CARTESIAN_POINT ( 'NONE',  ( -7.188101187500000044, 1.218749997951610098, -8.802885111219163269E-16 ) ) ;
#49631=CARTESIAN_POINT ( 'NONE',  ( 0.000000000000000000, 125.0000000000000000, 8.000000000000000000 ) ) ;
#49632=CARTESIAN_POINT ( 'NONE',  ( -8.000000000000000000, 16.96874999590322730, -3.313708498984762496 ) ) ;
#49636=ADVANCED_FACE ( 'NONE', ( #44422 ), #67437, .T. ) ;
#49638=CARTESIAN_POINT ( 'NONE',  ( 8.000000000000000000, 27.00000000000000355, 0.000000000000000000 ) ) ;
#49640=ORIENTED_EDGE ( 'NONE', *, *, #8071, .F. ) ;
#49646=VERTEX_POINT ( 'NONE', #62141 ) ;
#49647=CARTESIAN_POINT ( 'NONE',  ( -7.188101187500000044, 13.21874999795161187, -8.802885111219163269E-16 ) ) ;
#49651=CARTESIAN_POINT ( 'NONE',  ( -7.188101187500000044, 114.0312500020483952, 0.000000000000000000 ) ) ;
#49664=CYLINDRICAL_SURFACE ( 'NONE', #26897, 8.000000000000000000 ) ;
#49666=CARTESIAN_POINT ( 'NONE',  ( -3.313708498984762052, 94.71874999999998579, -8.000000000000000000 ) ) ;
#49668=CARTESIAN_POINT ( 'NONE',  ( 8.000000000000000000, 98.84375000000000000, -3.313708498984762496 ) ) ;
#49694=CARTESIAN_POINT ( 'NONE',  ( -5.082755093536325042, 17.53124999795161187, -5.082755093536325930 ) ) ;
#49703=CARTESIAN_POINT ( 'NONE',  ( 3.313708498984697215, 117.9687499999999858, 8.000000000000063949 ) ) ;
#49704=CARTESIAN_POINT ( 'NONE',  ( 1.469576158976823947E-15, 121.0625000040967763, 8.000000000000000000 ) ) ;
#49728=CARTESIAN_POINT ( 'NONE',  ( -8.000000000000000000, 14.15625000000000355, -3.313708498984762496 ) ) ;
#49730=CARTESIAN_POINT ( 'NONE',  ( -5.656854249492380582, 90.50000000409677625, -5.656854249492380582 ) ) ;
#49733=( BOUNDED_CURVE ( )  B_SPLINE_CURVE ( 2, ( #23213, #57566, #5875, #28871, #51891, #15682, #69989, #34932, #12263 ),
 .UNSPECIFIED., .F., .F. ) 
 B_SPLINE_CURVE_WITH_KNOTS ( ( 3, 2, 2, 2, 3 ),
 ( 0.3229166666666665186, 0.3281249999999998335, 0.3333333333333331483, 0.3385416666666665186, 0.3437499999999998335 ),
 .UNSPECIFIED. ) 
 CURVE ( )  GEOMETRIC_REPRESENTATION_ITEM ( )  RATIONAL_B_SPLINE_CURVE ( ( 1.000000000000002442, 0.9238795325112842960, 1.000000000000000000, 0.9238795325112867385, 1.000000000000000000, 0.9238795325112867385, 1.000000000000000000, 0.9238795325112891810, 0.9999999999999975575 ) ) 
 REPRESENTATION_ITEM ( '' )  );
#49741=CARTESIAN_POINT ( 'NONE',  ( -2.977408999572650927, 92.37500000204839523, -7.188101187500001821 ) ) ;
#49743=CARTESIAN_POINT ( 'NONE',  ( 1.469576158976823947E-15, 109.0625000040967905, 8.000000000000000000 ) ) ;
#49746=ADVANCED_FACE ( 'NONE', ( #4814 ), #38024, .T. ) ;
#49753=CARTESIAN_POINT ( 'NONE',  ( -4.898587196589412829E-16, 105.3125000040967763, -8.000000000000000000 ) ) ;
#49762=CARTESIAN_POINT ( 'NONE',  ( -3.313708498984760720, 10.78124999590322197, -8.000000000000000000 ) ) ;
#49765=CARTESIAN_POINT ( 'NONE',  ( 7.188101187500001821, 14.43749999795161365, -2.977408999572650483 ) ) ;
#49768=CARTESIAN_POINT ( 'NONE',  ( -5.082755093536325930, 106.3437500020483810, -5.082755093536325930 ) ) ;
#49770=CYLINDRICAL_SURFACE ( 'NONE', #11283, 8.000000000000000000 ) ;
#49788=CARTESIAN_POINT ( 'NONE',  ( 7.188101187500000044, 99.40625000204838102, -8.802885111219163269E-16 ) ) ;
#49794=CARTESIAN_POINT ( 'NONE',  ( 5.082755093536325042, 104.4687500020483952, -5.082755093536325930 ) ) ;
#49809=DIRECTION ( 'NONE',  ( 0.000000000000000000, -1.000000000000000000, 0.000000000000000000 ) ) ;
#49817=CARTESIAN_POINT ( 'NONE',  ( -1.320432766682874540E-15, 7.593749997951611874, 7.188101187500000044 ) ) ;
#49818=CARTESIAN_POINT ( 'NONE',  ( 3.313708498984765161, 112.1562500040967763, 7.999999999999998224 ) ) ;
#49844=CARTESIAN_POINT ( 'NONE',  ( -8.000000000000000000, 114.4999999999999858, 0.000000000000000000 ) ) ;
#49850=CARTESIAN_POINT ( 'NONE',  ( -3.313708498984765161, 21.84374999590322375, 7.999999999999998224 ) ) ;
#49854=CARTESIAN_POINT ( 'NONE',  ( -4.898587196589412829E-16, 121.6250000000000000, -8.000000000000000000 ) ) ;
#49875=CARTESIAN_POINT ( 'NONE',  ( -2.977408999572650927, 117.8750000020483810, -7.188101187500000933 ) ) ;
#49880=CARTESIAN_POINT ( 'NONE',  ( 7.188101187500000044, 119.2812500020483810, -8.802885111219163269E-16 ) ) ;
#49906=CARTESIAN_POINT ( 'NONE',  ( 2.977408999572651815, 24.18749999795161543, 7.188101187500000933 ) ) ;
#49909=CARTESIAN_POINT ( 'NONE',  ( 7.188101187500001821, 20.43749999795161187, -2.977408999572650483 ) ) ;
#49924=VERTEX_POINT ( 'NONE', #23642 ) ;
#49934=CARTESIAN_POINT ( 'NONE',  ( -2.977408999572650927, 94.25000000204838102, -7.188101187500001821 ) ) ;
#49956=ORIENTED_EDGE ( 'NONE', *, *, #25598, .T. ) ;
#49959=CARTESIAN_POINT ( 'NONE',  ( -4.898587196589412829E-16, 97.62499999999998579, -8.000000000000000000 ) ) ;
#49965=CARTESIAN_POINT ( 'NONE',  ( 5.082755093536325042, 107.0937500020483810, -5.082755093536325930 ) ) ;
#49989=CARTESIAN_POINT ( 'NONE',  ( 4.401442555609581635E-16, 17.71874999795161187, -7.188101187500000044 ) ) ;
#49997=CARTESIAN_POINT ( 'NONE',  ( 7.188101187500001821, 2.062499997951610098, -2.977408999572650483 ) ) ;
#50000=CARTESIAN_POINT ( 'NONE',  ( 7.188101187500001821, 0.9374999979516100979, -2.977408999572650483 ) ) ;
#50013=CARTESIAN_POINT ( 'NONE',  ( 4.898587196589412829E-16, 6.375000000000000888, -8.000000000000000000 ) ) ;
#50014=VERTEX_POINT ( 'NONE', #63252 ) ;
#50015=CARTESIAN_POINT ( 'NONE',  ( 5.082755093536325930, 11.15624999795161187, -5.082755093536325930 ) ) ;
#50020=CARTESIAN_POINT ( 'NONE',  ( 5.082755093536326818, 114.5937500020483810, 5.082755093536325042 ) ) ;
#50036=CARTESIAN_POINT ( 'NONE',  ( 8.000000000000000000, 91.34375000000000000, -3.313708498984762496 ) ) ;
#50050=CARTESIAN_POINT ( 'NONE',  ( 0.000000000000000000, 125.0000000000000000, 0.000000000000000000 ) ) ;
#50061=CARTESIAN_POINT ( 'NONE',  ( -2.977408999572654480, 20.99999999795161898, 7.188101187499999156 ) ) ;
#50096=CARTESIAN_POINT ( 'NONE',  ( 3.313708498984762496, 11.71875000000000000, 7.999999999999998224 ) ) ;
#50099=CARTESIAN_POINT ( 'NONE',  ( -5.656854249492378806, 90.87500000409677625, 5.656854249492381470 ) ) ;
#50111=CARTESIAN_POINT ( 'NONE',  ( 7.188101187500000044, 94.90625000204838102, -8.802885111219163269E-16 ) ) ;
#50120=VERTEX_POINT ( 'NONE', #64743 ) ;
#50124=DIRECTION ( 'NONE',  ( 0.000000000000000000, -1.000000000000000000, 0.000000000000000000 ) ) ;
#50132=CARTESIAN_POINT ( 'NONE',  ( 3.313708498984762052, 10.59374999590322020, -8.000000000000000000 ) ) ;
#50136=CARTESIAN_POINT ( 'NONE',  ( -7.188101187500001821, 14.99999999795161187, -2.977408999572651371 ) ) ;
#50139=CARTESIAN_POINT ( 'NONE',  ( -2.977408999572650927, 106.2500000020484094, -7.188101187500000933 ) ) ;
#50146=CARTESIAN_POINT ( 'NONE',  ( 4.898587196589412829E-16, 21.37500000000000355, -8.000000000000000000 ) ) ;
#50151=CARTESIAN_POINT ( 'NONE',  ( -3.313708498984800688, 22.78124999590322020, -7.999999999999958256 ) ) ;
#50157=CARTESIAN_POINT ( 'NONE',  ( -7.188101187500000044, 97.15625000204839523, 0.000000000000000000 ) ) ;
#50164=CARTESIAN_POINT ( 'NONE',  ( -2.977408999572650927, 104.7500000020483810, -7.188101187500001821 ) ) ;
#50175=CARTESIAN_POINT ( 'NONE',  ( 5.656854249492378806, 8.812500000000000000, 5.656854249492381470 ) ) ;
#50179=ORIENTED_EDGE ( 'NONE', *, *, #3343, .T. ) ;
#50187=CARTESIAN_POINT ( 'NONE',  ( 7.188101187500000044, 6.468749997951610986, 0.000000000000000000 ) ) ;
#50188=CARTESIAN_POINT ( 'NONE',  ( -3.313708498984762052, 112.9062500040967763, -8.000000000000000000 ) ) ;
#50213=CARTESIAN_POINT ( 'NONE',  ( 3.313708498984760720, 108.0312499999999858, -8.000000000000000000 ) ) ;
#50220=CARTESIAN_POINT ( 'NONE',  ( 4.898587196589412829E-16, 24.18749999590322375, -8.000000000000000000 ) ) ;
#50222=CARTESIAN_POINT ( 'NONE',  ( -5.082755093536324154, 123.2187500020483952, 5.082755093536326818 ) ) ;
#50235=CARTESIAN_POINT ( 'NONE',  ( 8.000000000000000000, 102.0312500040967763, -3.313708498984762496 ) ) ;
#50242=CARTESIAN_POINT ( 'NONE',  ( -7.188101187500000933, 116.5625000020483810, -2.977408999572650483 ) ) ;
#50248=CARTESIAN_POINT ( 'NONE',  ( 2.977408999572650039, 121.0625000020483668, -7.188101187500001821 ) ) ;
#50274=AXIS2_PLACEMENT_3D ( 'NONE', #74454, #34496, #17104 ) ;
#50276=CARTESIAN_POINT ( 'NONE',  ( -8.000000000000001776, 0.8437500000000000000, 3.313708498984759387 ) ) ;
#50279=CARTESIAN_POINT ( 'NONE',  ( -7.188101187500001821, 19.49999999795161898, -2.977408999572651371 ) ) ;
#50282=DIRECTION ( 'NONE',  ( -0.8660271417563482066, 1.588872886645881945E-06, -0.4999969897297438237 ) ) ;
#50302=CARTESIAN_POINT ( 'NONE',  ( 1.926036052266958176, 89.59560469603701449, -7.188101187500001821 ) ) ;
#50305=ADVANCED_FACE ( 'NONE', ( #21311 ), #49616, .T. ) ;
#50306=EDGE_LOOP ( 'NONE', ( #20903, #19173, #71062, #69185 ) ) ;
#50307=CARTESIAN_POINT ( 'NONE',  ( 7.999999999999998224, 8.718749995903221972, 3.313708498984766049 ) ) ;
#50308=CARTESIAN_POINT ( 'NONE',  ( 0.000000000000000000, 54.99999999999999289, 8.000000000000000000 ) ) ;
#50321=CARTESIAN_POINT ( 'NONE',  ( 8.000000000000000000, 109.5312500040968047, -3.313708498984762496 ) ) ;
#50330=CARTESIAN_POINT ( 'NONE',  ( -5.082755093536324154, 103.3437500020483668, 5.082755093536326818 ) ) ;
#50350=ORIENTED_EDGE ( 'NONE', *, *, #58559, .F. ) ;
#50357=CARTESIAN_POINT ( 'NONE',  ( -5.082755093536325042, 19.40624999795161543, -5.082755093536325930 ) ) ;
#50361=CARTESIAN_POINT ( 'NONE',  ( -8.000000000000000000, 96.59375000409679046, -3.313708498984761164 ) ) ;
#50367=CARTESIAN_POINT ( 'NONE',  ( -5.082755093536325042, 5.531249997951610986, -5.082755093536325930 ) ) ;
#50369=CARTESIAN_POINT ( 'NONE',  ( -8.000000000000000000, 17.06249999590322375, -9.797174393178825657E-16 ) ) ;
#50385=CARTESIAN_POINT ( 'NONE',  ( -5.656854249492379694, 21.56250000000000355, -5.656854249492380582 ) ) ;
#50387=CARTESIAN_POINT ( 'NONE',  ( 5.082755093536325930, 12.65624999795161187, -5.082755093536325930 ) ) ;
#50392=CARTESIAN_POINT ( 'NONE',  ( 7.188101187500002709, 104.1875000020483668, 2.977408999572649151 ) ) ;
#50397=VERTEX_POINT ( 'NONE', #69948 ) ;
#50408=CARTESIAN_POINT ( 'NONE',  ( 5.656854249492381470, 97.06250000000000000, 5.656854249492379694 ) ) ;
#50416=CARTESIAN_POINT ( 'NONE',  ( 4.898587196589412829E-16, 19.87500000000000355, -8.000000000000000000 ) ) ;
#50420=CARTESIAN_POINT ( 'NONE',  ( -7.188101187499999156, 122.7500000020483952, 2.977408999572654924 ) ) ;
#50425=CARTESIAN_POINT ( 'NONE',  ( -8.000000000000001776, 12.84375000000000355, 3.313708498984759387 ) ) ;
#50429=CARTESIAN_POINT ( 'NONE',  ( -7.188101187500002709, 20.81249999795161543, 2.977408999572649151 ) ) ;
#50430=CARTESIAN_POINT ( 'NONE',  ( 0.000000000000000000, 125.0000000000000000, 8.000000000000000000 ) ) ;
#50434=ADVANCED_FACE ( 'NONE', ( #70674 ), #6939, .T. ) ;
#50442=CARTESIAN_POINT ( 'NONE',  ( -3.313708498984765161, 21.84374999590322375, 7.999999999999998224 ) ) ;
#50462=CARTESIAN_POINT ( 'NONE',  ( -3.313708498984760720, 10.96875000000000178, -8.000000000000000000 ) ) ;
#50464=CARTESIAN_POINT ( 'NONE',  ( 5.656854249492379694, 93.12500000409677625, -5.656854249492380582 ) ) ;
#50476=CARTESIAN_POINT ( 'NONE',  ( 7.188101187500001821, 92.00000000204838102, -2.977408999572651371 ) ) ;
#50485=ORIENTED_EDGE ( 'NONE', *, *, #73863, .T. ) ;
#50499=CARTESIAN_POINT ( 'NONE',  ( -3.313708498984760720, 6.281249995903221084, -8.000000000000000000 ) ) ;
#50502=CARTESIAN_POINT ( 'NONE',  ( 4.401442555609581635E-16, 14.71874999795161187, -7.188101187500000044 ) ) ;
#50504=CARTESIAN_POINT ( 'NONE',  ( 1.469576158976823947E-15, 105.8750000000000000, 8.000000000000000000 ) ) ;
#50505=CARTESIAN_POINT ( 'NONE',  ( 2.977408999572650039, 101.5625000020483952, -7.188101187500000933 ) ) ;
#50516=CARTESIAN_POINT ( 'NONE',  ( -8.000000000000000000, 23.06249999590322020, -9.797174393178825657E-16 ) ) ;
#50522=CARTESIAN_POINT ( 'NONE',  ( -7.188101187500000933, 94.06250000204838102, -2.977408999572650483 ) ) ;
#50530=CARTESIAN_POINT ( 'NONE',  ( -2.977408999572651815, 103.8125000020483952, 7.188101187500000933 ) ) ;
#50531=CARTESIAN_POINT ( 'NONE',  ( -3.360070523760016581, 0.4865809706466538986, -7.253681227061384185 ) ) ;
#50549=EDGE_CURVE ( 'NONE', #46167, #38779, #3242, .T. ) ;
#50551=LINE ( 'NONE', #15466, #41201 ) ;
#50558=CARTESIAN_POINT ( 'NONE',  ( -5.082755093536325042, 14.53124999795161187, -5.082755093536325930 ) ) ;
#50559=CARTESIAN_POINT ( 'NONE',  ( 5.656854249492381470, 107.7500000040967763, 5.656854249492379694 ) ) ;
#50567=CARTESIAN_POINT ( 'NONE',  ( 7.188101187500002709, 109.8125000020483952, 2.977408999572649151 ) ) ;
#50573=ORIENTED_EDGE ( 'NONE', *, *, #70067, .T. ) ;
#50580=DIRECTION ( 'NONE',  ( -0.000000000000000000, 1.000000000000000000, -0.000000000000000000 ) ) ;
#50582=CARTESIAN_POINT ( 'NONE',  ( 8.000000000000000000, 106.2500000000000000, -9.797174393178825657E-16 ) ) ;
#50588=CARTESIAN_POINT ( 'NONE',  ( 4.898587196589412829E-16, 27.18749999590322375, -8.000000000000000000 ) ) ;
#50590=CARTESIAN_POINT ( 'NONE',  ( -5.082755093536325930, 122.8437500020483952, -5.082755093536325930 ) ) ;
#50612=CARTESIAN_POINT ( 'NONE',  ( 2.977408999572650039, 114.6875000020484094, -7.188101187500000933 ) ) ;
#50618=CARTESIAN_POINT ( 'NONE',  ( -5.082755093536325930, 119.8437500020483810, -5.082755093536325930 ) ) ;
#50639=ORIENTED_EDGE ( 'NONE', *, *, #10268, .T. ) ;
#50643=CARTESIAN_POINT ( 'NONE',  ( -1.469576158976823947E-15, 2.625000000000000444, 8.000000000000000000 ) ) ;
#50645=CARTESIAN_POINT ( 'NONE',  ( -2.977408999572654480, 16.87499999795161543, 7.188101187499999156 ) ) ;
#50654=AXIS2_PLACEMENT_3D ( 'NONE', #50050, #15708, #9701 ) ;
#50659=CARTESIAN_POINT ( 'NONE',  ( 8.000000000000000000, 94.43750000409679046, -9.797174393178825657E-16 ) ) ;
#50669=CARTESIAN_POINT ( 'NONE',  ( 8.000000000000001776, 122.6562500000000000, 3.313708498984759387 ) ) ;
#50693=FACE_OUTER_BOUND ( 'NONE', #68730, .T. ) ;
#50695=CARTESIAN_POINT ( 'NONE',  ( 0.000000000000000000, 125.0000000000000000, 0.000000000000000000 ) ) ;
#50700=CARTESIAN_POINT ( 'NONE',  ( 1.320432766682874540E-15, 102.0312500020483810, 7.188101187500000044 ) ) ;
#50705=ORIENTED_EDGE ( 'NONE', *, *, #27957, .T. ) ;
#50706=EDGE_LOOP ( 'NONE', ( #35677, #404, #7059, #70360 ) ) ;
#50707=( BOUNDED_CURVE ( )  B_SPLINE_CURVE ( 2, ( #47901, #23419, #18505, #24525, #70556, #17759, #64530, #53212, #40773 ),
 .UNSPECIFIED., .F., .F. ) 
 B_SPLINE_CURVE_WITH_KNOTS ( ( 3, 2, 2, 2, 3 ),
 ( 0.3472222222222222099, 0.3541666666666666852, 0.3611111111111111049, 0.3680555555555555802, 0.3750000000000000000 ),
 .UNSPECIFIED. ) 
 CURVE ( )  GEOMETRIC_REPRESENTATION_ITEM ( )  RATIONAL_B_SPLINE_CURVE ( ( 1.000000000000000000, 0.9238795325112867385, 1.000000000000000000, 0.9238795325112867385, 1.000000000000000000, 0.9238795325112867385, 1.000000000000000000, 0.9238795325112867385, 1.000000000000000000 ) ) 
 REPRESENTATION_ITEM ( '' )  );
#50708=( BOUNDED_CURVE ( )  B_SPLINE_CURVE ( 2, ( #13587, #62770, #59631, #7947, #51092, #39768, #11113, #21122, #54726 ),
 .UNSPECIFIED., .F., .F. ) 
 B_SPLINE_CURVE_WITH_KNOTS ( ( 3, 2, 2, 2, 3 ),
 ( 0.01847903363950017044, 0.02083333333333333218, 0.02777777777777777624, 0.03472222222222222376, 0.04166666666666666435 ),
 .UNSPECIFIED. ) 
 CURVE ( )  GEOMETRIC_REPRESENTATION_ITEM ( )  RATIONAL_B_SPLINE_CURVE ( ( 0.9658850645339662755, 0.9741937033643515154, 1.000000000000000000, 0.9238795325112867385, 1.000000000000000000, 0.9238795325112867385, 1.000000000000000000, 0.9238795325112867385, 1.000000000000000000 ) ) 
 REPRESENTATION_ITEM ( '' )  );
#50719=CARTESIAN_POINT ( 'NONE',  ( -1.469576158976823947E-15, 18.93749999590322020, 8.000000000000000000 ) ) ;
#50721=AXIS2_PLACEMENT_3D ( 'NONE', #35424, #69367, #39410 ) ;
#50722=CARTESIAN_POINT ( 'NONE',  ( -4.898587196589412829E-16, 100.6249999999999858, -8.000000000000000000 ) ) ;
#50729=CARTESIAN_POINT ( 'NONE',  ( -2.977408999572654480, 21.37499999795161543, 7.188101187499999156 ) ) ;
#50735=CARTESIAN_POINT ( 'NONE',  ( 9.797174393178825657E-16, 125.0000000000000000, -8.000000000000000000 ) ) ;
#50738=CARTESIAN_POINT ( 'NONE',  ( -2.977408999572654480, 7.499999997951610986, 7.188101187499999156 ) ) ;
#50741=CARTESIAN_POINT ( 'NONE',  ( 5.082755093536325930, 2.531249997951610542, -5.082755093536325930 ) ) ;
#50744=ADVANCED_BREP_SHAPE_REPRESENTATION ( '', ( #67548, #57354 ), #51355 ) ;
#50755=CARTESIAN_POINT ( 'NONE',  ( -1.320432766682874540E-15, 9.093749997951610098, 7.188101187500000044 ) ) ;
#50759=CARTESIAN_POINT ( 'NONE',  ( -5.082755093536324154, 105.2187500020483952, 5.082755093536326818 ) ) ;
#50774=LINE ( 'NONE', #8930, #42567 ) ;
#50792=CARTESIAN_POINT ( 'NONE',  ( 1.320432766682874540E-15, 118.5312500020483810, 7.188101187500000044 ) ) ;
#50801=CARTESIAN_POINT ( 'NONE',  ( 2.977408999572651815, 19.68749999795161543, 7.188101187500000933 ) ) ;
#50812=CARTESIAN_POINT ( 'NONE',  ( 5.656854249492379694, 118.4375000000000000, -5.656854249492380582 ) ) ;
#50821=DIRECTION ( 'NONE',  ( 0.000000000000000000, 0.000000000000000000, 1.000000000000000000 ) ) ;
#50827=EDGE_LOOP ( 'NONE', ( #30948, #59104 ) ) ;
#50835=ORIENTED_EDGE ( 'NONE', *, *, #27022, .T. ) ;
#50840=CARTESIAN_POINT ( 'NONE',  ( -5.656854249492379694, 11.06250000000000178, -5.656854249492380582 ) ) ;
#50841=VERTEX_POINT ( 'NONE', #73651 ) ;
#50842=CARTESIAN_POINT ( 'NONE',  ( -7.999999999999998224, 90.78125000409681888, 3.313708498984766493 ) ) ;
#50853=CARTESIAN_POINT ( 'NONE',  ( -7.188101187500001821, 122.9375000020483810, -2.977408999572650483 ) ) ;
#50863=ORIENTED_EDGE ( 'NONE', *, *, #21425, .F. ) ;
#50872=CARTESIAN_POINT ( 'NONE',  ( 1.469576158976823947E-15, 114.8750000000000000, 8.000000000000000000 ) ) ;
#50873=CARTESIAN_POINT ( 'NONE',  ( 9.491012693392001592E-16, 125.0000000000000000, 7.500000000000020428 ) ) ;
#50875=CARTESIAN_POINT ( 'NONE',  ( 3.313708498984762496, 8.531249995903221972, 7.999999999999998224 ) ) ;
#50876=ORIENTED_EDGE ( 'NONE', *, *, #26969, .F. ) ;
#50878=CARTESIAN_POINT ( 'NONE',  ( -7.188101187500001821, 17.99999999795161898, -2.977408999572651371 ) ) ;
#50881=CARTESIAN_POINT ( 'NONE',  ( 0.000000000000000000, 125.0000000000000000, 0.000000000000000000 ) ) ;
#50882=CARTESIAN_POINT ( 'NONE',  ( -5.082755093536325930, 103.3437500020483668, -5.082755093536325930 ) ) ;
#50898=CARTESIAN_POINT ( 'NONE',  ( -7.188101187499999156, 91.25000000204838102, 2.977408999572654924 ) ) ;
#50902=CARTESIAN_POINT ( 'NONE',  ( -4.898587196589412829E-16, 115.6250000000000000, -8.000000000000000000 ) ) ;
#50906=CARTESIAN_POINT ( 'NONE',  ( -5.082755093536325930, 104.8437500020483810, -5.082755093536325930 ) ) ;
#50911=CARTESIAN_POINT ( 'NONE',  ( 1.469576158976823947E-15, 100.0625000040967763, 8.000000000000000000 ) ) ;
#50914=CARTESIAN_POINT ( 'NONE',  ( 4.898587196589412829E-16, 16.87500000000000000, -8.000000000000000000 ) ) ;
#50925=VECTOR ( 'NONE', #13503, 1000.000000000000000 ) ;
#50929=( BOUNDED_CURVE ( )  B_SPLINE_CURVE ( 2, ( #17507, #67715, #62775, #68816, #40154, #10369, #34142, #22785, #33396 ),
 .UNSPECIFIED., .F., .F. ) 
 B_SPLINE_CURVE_WITH_KNOTS ( ( 3, 2, 2, 2, 3 ),
 ( 0.1770833333333334259, 0.1822916666666667407, 0.1875000000000001110, 0.1927083333333334814, 0.1979166666666667962 ),
 .UNSPECIFIED. ) 
 CURVE ( )  GEOMETRIC_REPRESENTATION_ITEM ( )  RATIONAL_B_SPLINE_CURVE ( ( 0.9999999999999987788, 0.9238795325112879597, 1.000000000000000000, 0.9238795325112867385, 1.000000000000000000, 0.9238795325112867385, 1.000000000000000000, 0.9238795325112847401, 1.000000000000001998 ) ) 
 REPRESENTATION_ITEM ( '' )  );
#50934=CARTESIAN_POINT ( 'NONE',  ( -1.320432766682874540E-15, 13.59374999795161187, 7.188101187500000044 ) ) ;
#50935=CARTESIAN_POINT ( 'NONE',  ( -5.656854249492378806, 110.3750000040967763, 5.656854249492381470 ) ) ;
#50938=( BOUNDED_CURVE ( )  B_SPLINE_CURVE ( 2, ( #67599, #67227, #43834, #50235, #21561, #44587, #21928, #34032, #27976 ),
 .UNSPECIFIED., .F., .F. ) 
 B_SPLINE_CURVE_WITH_KNOTS ( ( 3, 2, 2, 2, 3 ),
 ( 0.5937500000000000000, 0.5989583333333333703, 0.6041666666666666297, 0.6093750000000000000, 0.6145833333333333703 ),
 .UNSPECIFIED. ) 
 CURVE ( )  GEOMETRIC_REPRESENTATION_ITEM ( )  RATIONAL_B_SPLINE_CURVE ( ( 1.000000000000000000, 0.9238795325112867385, 1.000000000000000000, 0.9238795325112867385, 1.000000000000000000, 0.9238795325112867385, 1.000000000000000000, 0.9238795325112867385, 1.000000000000000000 ) ) 
 REPRESENTATION_ITEM ( '' )  );
#50942=ORIENTED_EDGE ( 'NONE', *, *, #9011, .T. ) ;
#50944=CARTESIAN_POINT ( 'NONE',  ( 7.188101187500000044, 102.4062500020483810, -8.802885111219163269E-16 ) ) ;
#50959=VECTOR ( 'NONE', #56790, 1000.000000000000000 ) ;
#50960=CARTESIAN_POINT ( 'NONE',  ( -8.000000000000000000, 105.4062500000000000, -3.313708498984761608 ) ) ;
#50966=CARTESIAN_POINT ( 'NONE',  ( -7.188101187500002709, 1.687499997951610098, 2.977408999572649151 ) ) ;
#50975=CARTESIAN_POINT ( 'NONE',  ( 8.000000000000000000, 122.7500000000000000, -9.797174393178825657E-16 ) ) ;
#50988=CARTESIAN_POINT ( 'NONE',  ( -1.469576158976823947E-15, 6.937499995903221084, 8.000000000000000000 ) ) ;
#50989=CARTESIAN_POINT ( 'NONE',  ( 7.188101187500000044, 112.9062500020483952, -8.802885111219163269E-16 ) ) ;
#50995=CARTESIAN_POINT ( 'NONE',  ( -4.401442555609581635E-16, 118.1562500020483810, -7.188101187500000044 ) ) ;
#51004=CARTESIAN_POINT ( 'NONE',  ( 5.656854249492379694, 107.9374999999999858, -5.656854249492380582 ) ) ;
#51022=CARTESIAN_POINT ( 'NONE',  ( 2.977408999572650927, 26.24999999795161898, -7.188101187500001821 ) ) ;
#51025=CARTESIAN_POINT ( 'NONE',  ( -2.977408999572654480, 24.37499999795161543, 7.188101187499999156 ) ) ;
#51026=DIRECTION ( 'NONE',  ( 0.000000000000000000, 0.000000000000000000, 1.000000000000000000 ) ) ;
#51036=( BOUNDED_CURVE ( )  B_SPLINE_CURVE ( 2, ( #32607, #3932, #20888, #39368, #43909, #73693, #67670, #62364, #38997 ),
 .UNSPECIFIED., .F., .F. ) 
 B_SPLINE_CURVE_WITH_KNOTS ( ( 3, 2, 2, 2, 3 ),
 ( 0.8437500000000002220, 0.8489583333333335924, 0.8541666666666668517, 0.8593750000000002220, 0.8645833333333335924 ),
 .UNSPECIFIED. ) 
 CURVE ( )  GEOMETRIC_REPRESENTATION_ITEM ( )  RATIONAL_B_SPLINE_CURVE ( ( 0.9999999999999967804, 0.9238795325112899581, 1.000000000000000000, 0.9238795325112867385, 1.000000000000000000, 0.9238795325112867385, 1.000000000000000000, 0.9238795325112835188, 1.000000000000003331 ) ) 
 REPRESENTATION_ITEM ( '' )  );
#51042=ORIENTED_EDGE ( 'NONE', *, *, #25483, .F. ) ;
#51044=ORIENTED_EDGE ( 'NONE', *, *, #60187, .T. ) ;
#51050=CARTESIAN_POINT ( 'NONE',  ( -7.999999999999998224, 122.0937500000000000, 3.313708498984766493 ) ) ;
#51059=EDGE_CURVE ( 'NONE', #46167, #493, #42279, .T. ) ;
#51068=AXIS2_PLACEMENT_3D ( 'NONE', #59711, #59346, #19701 ) ;
#51078=CARTESIAN_POINT ( 'NONE',  ( 2.977408999572654480, 103.6250000020483810, 7.188101187499999156 ) ) ;
#51085=EDGE_CURVE ( 'NONE', #64471, #26128, #2783, .T. ) ;
#51092=CARTESIAN_POINT ( 'NONE',  ( -8.000000000000000000, 0.7500000000000000000, -9.797174393178825657E-16 ) ) ;
#51097=CARTESIAN_POINT ( 'NONE',  ( 3.594044162775203777, 89.15552387383502264, -6.225081946264263699 ) ) ;
#51105=CARTESIAN_POINT ( 'NONE',  ( 7.188101187499999156, 26.24999999795161543, 2.977408999572654924 ) ) ;
#51113=CARTESIAN_POINT ( 'NONE',  ( -7.188101187500002709, 11.81249999795161187, 2.977408999572649151 ) ) ;
#51116=CARTESIAN_POINT ( 'NONE',  ( 2.977408999572650927, 4.124999997951610986, -7.188101187500001821 ) ) ;
#51132=CARTESIAN_POINT ( 'NONE',  ( 7.188101187499999156, 15.37499999795161187, 2.977408999572654924 ) ) ;
#51133=LINE ( 'NONE', #51503, #36395 ) ;
#51136=CARTESIAN_POINT ( 'NONE',  ( -2.977408999572651815, 105.3125000020483668, 7.188101187500000933 ) ) ;
#51140=CARTESIAN_POINT ( 'NONE',  ( -7.999999999999998224, 95.28125000409677625, 3.313708498984766049 ) ) ;
#51143=PRODUCT ( 'stud', 'stud', '', ( #44833 ) ) ;
#51147=CARTESIAN_POINT ( 'NONE',  ( 0.000000000000000000, 125.0000000000000000, 0.000000000000000000 ) ) ;
#51154=CARTESIAN_POINT ( 'NONE',  ( -7.999999999999998224, 90.59375000000000000, 3.313708498984766493 ) ) ;
#51166=CARTESIAN_POINT ( 'NONE',  ( -5.082755093536324154, 118.3437500020483810, 5.082755093536326818 ) ) ;
#51173=DIRECTION ( 'NONE',  ( 0.000000000000000000, 0.000000000000000000, 1.000000000000000000 ) ) ;
#51174=CARTESIAN_POINT ( 'NONE',  ( -5.082755093536326818, 26.90624999795161543, 5.082755093536325042 ) ) ;
#51197=CARTESIAN_POINT ( 'NONE',  ( 2.977408999572650927, 4.124999997951610986, -7.188101187500000933 ) ) ;
#51208=ORIENTED_EDGE ( 'NONE', *, *, #9530, .F. ) ;
#51210=ADVANCED_FACE ( 'NONE', ( #43393, #55482 ), #31715, .T. ) ;
#51215=CARTESIAN_POINT ( 'NONE',  ( -8.000000000000000000, 20.25000000000000355, -9.797174393178825657E-16 ) ) ;
#51216=ORIENTED_EDGE ( 'NONE', *, *, #5578, .T. ) ;
#51218=CARTESIAN_POINT ( 'NONE',  ( 8.000000000000000000, 89.93750000409677625, -9.797174393178825657E-16 ) ) ;
#51226=CARTESIAN_POINT ( 'NONE',  ( 5.082755093536325042, 122.4687500020483952, -5.082755093536325930 ) ) ;
#51227=EDGE_CURVE ( 'NONE', #69151, #31186, #10501, .T. ) ;
#51248=( BOUNDED_CURVE ( )  B_SPLINE_CURVE ( 2, ( #20870, #15579, #72937, #20489, #50659, #38619, #43506, #37491, #67654 ),
 .UNSPECIFIED., .F., .F. ) 
 B_SPLINE_CURVE_WITH_KNOTS ( ( 3, 2, 2, 2, 3 ),
 ( 0.8020833333333334814, 0.8072916666666667407, 0.8125000000000001110, 0.8177083333333334814, 0.8229166666666667407 ),
 .UNSPECIFIED. ) 
 CURVE ( )  GEOMETRIC_REPRESENTATION_ITEM ( )  RATIONAL_B_SPLINE_CURVE ( ( 0.9999999999999983347, 0.9238795325112884038, 1.000000000000000000, 0.9238795325112867385, 1.000000000000000000, 0.9238795325112867385, 1.000000000000000000, 0.9238795325112850731, 1.000000000000001554 ) ) 
 REPRESENTATION_ITEM ( '' )  );
#51250=CARTESIAN_POINT ( 'NONE',  ( 8.000000000000000000, 8.812499995903221972, 0.000000000000000000 ) ) ;
#51253=CARTESIAN_POINT ( 'NONE',  ( -2.977408999572654480, 19.87499999795161543, 7.188101187499999156 ) ) ;
#51255=CARTESIAN_POINT ( 'NONE',  ( 3.313708498984762496, 7.218750000000000888, 7.999999999999998224 ) ) ;
#51256=CARTESIAN_POINT ( 'NONE',  ( 5.082755093536326818, 101.0937500020483810, 5.082755093536325042 ) ) ;
#51263=CARTESIAN_POINT ( 'NONE',  ( -5.656854249492378806, 119.3750000040967905, 5.656854249492381470 ) ) ;
#51266=CARTESIAN_POINT ( 'NONE',  ( -3.313708498984805573, 23.34374999590321664, 7.999999999999956479 ) ) ;
#51272=CARTESIAN_POINT ( 'NONE',  ( -4.401442555609581635E-16, 95.28125000204836681, -7.188101187500000044 ) ) ;
#51279=CARTESIAN_POINT ( 'NONE',  ( 7.188101187500002709, 104.1875000020483668, 2.977408999572649151 ) ) ;
#51300=ORIENTED_EDGE ( 'NONE', *, *, #25602, .T. ) ;
#51303=CARTESIAN_POINT ( 'NONE',  ( 5.082755093536325930, 15.65624999795161365, -5.082755093536325930 ) ) ;
#51305=CARTESIAN_POINT ( 'NONE',  ( 8.000000000000001776, 109.3437500040967905, 3.313708498984759387 ) ) ;
#51315=CARTESIAN_POINT ( 'NONE',  ( 7.188101187500002709, 102.3125000020483810, 2.977408999572649151 ) ) ;
#51316=ADVANCED_FACE ( 'NONE', ( #14343 ), #26030, .T. ) ;
#51333=CARTESIAN_POINT ( 'NONE',  ( 8.000000000000000000, 106.3437500000000000, -3.313708498984762496 ) ) ;
#51336=CARTESIAN_POINT ( 'NONE',  ( -5.656854249492380582, 102.5000000040967905, -5.656854249492380582 ) ) ;
#51338=CARTESIAN_POINT ( 'NONE',  ( -3.313708498984765161, 27.84374999590322375, 7.999999999999998224 ) ) ;
#51340=CARTESIAN_POINT ( 'NONE',  ( 7.188101187500002709, 122.1875000020483810, 2.977408999572649151 ) ) ;
#51355=( GEOMETRIC_REPRESENTATION_CONTEXT ( 3 ) GLOBAL_UNCERTAINTY_ASSIGNED_CONTEXT ( ( #581 ) ) GLOBAL_UNIT_ASSIGNED_CONTEXT ( ( #26051, #31737, #49072 ) ) REPRESENTATION_CONTEXT ( 'NONE', 'WORKASPACE' ) );
#51359=CARTESIAN_POINT ( 'NONE',  ( 2.977408999572654480, 114.1250000020483952, 7.188101187499999156 ) ) ;
#51364=CARTESIAN_POINT ( 'NONE',  ( 2.977408999572654480, 123.5000000020483952, 7.188101187499999156 ) ) ;
#51371=DIRECTION ( 'NONE',  ( -0.000000000000000000, 1.000000000000000000, -0.000000000000000000 ) ) ;
#51390=CARTESIAN_POINT ( 'NONE',  ( -7.188101187500002709, 25.31249999795161543, 2.977408999572649151 ) ) ;
#51393=CARTESIAN_POINT ( 'NONE',  ( -2.977408999572654480, 21.37499999795161543, 7.188101187499999156 ) ) ;
#51399=CARTESIAN_POINT ( 'NONE',  ( 0.000000000000000000, 125.0000000000000000, 0.000000000000000000 ) ) ;
#51418=CARTESIAN_POINT ( 'NONE',  ( -3.313708498984762052, 124.7187500000000000, -8.000000000000000000 ) ) ;
#51427=CARTESIAN_POINT ( 'NONE',  ( -5.656854249492379694, 23.06250000000000355, -5.656854249492380582 ) ) ;
#51436=CARTESIAN_POINT ( 'NONE',  ( 8.000000000000000000, 10.40624999590321842, -3.313708498984761164 ) ) ;
#51447=CARTESIAN_POINT ( 'NONE',  ( -7.188101187500001821, 103.0625000020483810, -2.977408999572650483 ) ) ;
#51452=ORIENTED_EDGE ( 'NONE', *, *, #31376, .F. ) ;
#51462=CARTESIAN_POINT ( 'NONE',  ( 8.000000000000000000, 4.593750000000000888, -3.313708498984761164 ) ) ;
#51464=CARTESIAN_POINT ( 'NONE',  ( -8.000000000000001776, 18.65624999590322375, 3.313708498984759387 ) ) ;
#51474=CARTESIAN_POINT ( 'NONE',  ( 7.188101187500000933, 26.43749999795162253, -2.977408999572650483 ) ) ;
#51483=CARTESIAN_POINT ( 'NONE',  ( -5.082755093536326818, 8.906249997951610098, 5.082755093536325042 ) ) ;
#51486=CARTESIAN_POINT ( 'NONE',  ( 2.977408999572650927, 5.624999997951610986, -7.188101187500001821 ) ) ;
#51494=ORIENTED_EDGE ( 'NONE', *, *, #40075, .T. ) ;
#51502=CARTESIAN_POINT ( 'NONE',  ( 7.188101187499999156, 19.87499999795161543, 2.977408999572654924 ) ) ;
#51503=CARTESIAN_POINT ( 'NONE',  ( 9.797174393178825657E-16, 125.0000000000000000, -8.000000000000000000 ) ) ;
#51507=CARTESIAN_POINT ( 'NONE',  ( -4.401442555609581635E-16, 106.1562500020483810, -7.188101187500000044 ) ) ;
#51510=CARTESIAN_POINT ( 'NONE',  ( 9.797174393178825657E-16, 125.0000000000000000, -8.000000000000000000 ) ) ;
#51521=CARTESIAN_POINT ( 'NONE',  ( 8.000000000000000000, 91.25000000000000000, -9.797174393178825657E-16 ) ) ;
#51522=CARTESIAN_POINT ( 'NONE',  ( 5.656854249492381470, 91.06249999999998579, 5.656854249492379694 ) ) ;
#51535=CARTESIAN_POINT ( 'NONE',  ( -5.082755093536325930, 123.9687500020483952, -5.082755093536325930 ) ) ;
#51542=ORIENTED_EDGE ( 'NONE', *, *, #27632, .T. ) ;
#51544=CARTESIAN_POINT ( 'NONE',  ( 5.082755093536324154, 22.78124999795161187, 5.082755093536326818 ) ) ;
#51558=CARTESIAN_POINT ( 'NONE',  ( -3.313708498984805573, 27.84374999590322020, 7.999999999999956479 ) ) ;
#51561=DIRECTION ( 'NONE',  ( 0.000000000000000000, 0.000000000000000000, 1.000000000000000000 ) ) ;
#51565=CARTESIAN_POINT ( 'NONE',  ( -7.188101187500002709, 6.187499997951610986, 2.977408999572649151 ) ) ;
#51572=CARTESIAN_POINT ( 'NONE',  ( -7.999999999999998224, 120.5937500000000000, 3.313708498984766049 ) ) ;
#51576=ORIENTED_EDGE ( 'NONE', *, *, #39210, .F. ) ;
#51582=CARTESIAN_POINT ( 'NONE',  ( 8.000000000000000000, 16.59375000000000711, -3.313708498984761608 ) ) ;
#51586=CARTESIAN_POINT ( 'NONE',  ( 5.082755093536326818, 121.7187500020483952, 5.082755093536325042 ) ) ;
#51599=CARTESIAN_POINT ( 'NONE',  ( -7.188101187500000044, 124.5312500020483810, 0.000000000000000000 ) ) ;
#51619=VERTEX_POINT ( 'NONE', #65491 ) ;
#51628=CARTESIAN_POINT ( 'NONE',  ( -2.977408999572650039, 14.81249999795161543, -7.188101187500001821 ) ) ;
#51631=CARTESIAN_POINT ( 'NONE',  ( -2.977408999572650927, 100.2500000020483810, -7.188101187500000933 ) ) ;
#51632=DIRECTION ( 'NONE',  ( 0.000000000000000000, 0.000000000000000000, 1.000000000000000000 ) ) ;
#51640=ORIENTED_EDGE ( 'NONE', *, *, #41790, .T. ) ;
#51648=CARTESIAN_POINT ( 'NONE',  ( -2.977408999572652260, 92.93750000204839523, 7.188101187500000044 ) ) ;
#51655=CARTESIAN_POINT ( 'NONE',  ( -2.977408999572651815, 99.31250000204839523, 7.188101187500000933 ) ) ;
#51674=ORIENTED_EDGE ( 'NONE', *, *, #53996, .F. ) ;
#51676=CARTESIAN_POINT ( 'NONE',  ( -7.188101187500000044, 14.71874999795161187, -8.802885111219163269E-16 ) ) ;
#51677=CARTESIAN_POINT ( 'NONE',  ( 3.313708498984760720, 103.7187500040967763, -8.000000000000000000 ) ) ;
#51686=CARTESIAN_POINT ( 'NONE',  ( -4.898587196589412829E-16, 99.31250000409677625, -8.000000000000000000 ) ) ;
#51687=CARTESIAN_POINT ( 'NONE',  ( 5.082755093536325042, 102.5937500020483668, -5.082755093536325930 ) ) ;
#51694=ORIENTED_EDGE ( 'NONE', *, *, #64252, .T. ) ;
#51704=CARTESIAN_POINT ( 'NONE',  ( 3.313708498984760720, 100.5312500000000000, -8.000000000000000000 ) ) ;
#51707=CARTESIAN_POINT ( 'NONE',  ( -8.000000000000000000, 102.5937500040967763, -3.313708498984761164 ) ) ;
#51710=CARTESIAN_POINT ( 'NONE',  ( 7.999999999999998224, 28.21874999590322375, 3.313708498984766493 ) ) ;
#51712=CARTESIAN_POINT ( 'NONE',  ( -2.977408999572650927, 121.2500000020483952, -7.188101187500000933 ) ) ;
#51728=ADVANCED_FACE ( 'NONE', ( #42836 ), #13056, .T. ) ;
#51734=CARTESIAN_POINT ( 'NONE',  ( 7.188101187500000044, 109.9062500020483810, -8.802885111219163269E-16 ) ) ;
#51740=CARTESIAN_POINT ( 'NONE',  ( 5.082755093536326818, 114.5937500020483810, 5.082755093536325042 ) ) ;
#51766=CARTESIAN_POINT ( 'NONE',  ( 2.977408999572651815, 27.18749999795161898, 7.188101187500000933 ) ) ;
#51769=CARTESIAN_POINT ( 'NONE',  ( -2.977408999572654480, 25.87499999795161543, 7.188101187499999156 ) ) ;
#51795=CARTESIAN_POINT ( 'NONE',  ( 1.320432766682874540E-15, 90.40625000204838102, 7.188101187500000044 ) ) ;
#51803=CARTESIAN_POINT ( 'NONE',  ( 5.656854249492378806, 5.624999995903220196, 5.656854249492381470 ) ) ;
#51817=EDGE_CURVE ( 'NONE', #64471, #69918, #38319, .T. ) ;
#51827=CARTESIAN_POINT ( 'NONE',  ( -2.977408999572651815, 104.9375000020483810, 7.188101187500000933 ) ) ;
#51832=VERTEX_POINT ( 'NONE', #56051 ) ;
#51843=CYLINDRICAL_SURFACE ( 'NONE', #20483, 8.000000000000000000 ) ;
#51849=CARTESIAN_POINT ( 'NONE',  ( 1.469576158976823947E-15, 96.87499999999998579, 8.000000000000000000 ) ) ;
#51853=CARTESIAN_POINT ( 'NONE',  ( 7.188101187500000933, 24.93749999795161543, -2.977408999572650483 ) ) ;
#51865=CARTESIAN_POINT ( 'NONE',  ( -7.188101187500000044, 7.218749997951610986, -8.802885111219163269E-16 ) ) ;
#51868=CARTESIAN_POINT ( 'NONE',  ( 7.188101187499999156, 3.749999997951610542, 2.977408999572654924 ) ) ;
#51883=ORIENTED_EDGE ( 'NONE', *, *, #34911, .T. ) ;
#51884=CARTESIAN_POINT ( 'NONE',  ( -7.188101187500000933, 14.62499999795161187, -2.977408999572651371 ) ) ;
#51888=CARTESIAN_POINT ( 'NONE',  ( 2.977408999572654480, 108.5000000020483810, 7.188101187499999156 ) ) ;
#51891=CARTESIAN_POINT ( 'NONE',  ( -8.000000000000000000, 111.6875000040967905, 0.000000000000000000 ) ) ;
#51899=CYLINDRICAL_SURFACE ( 'NONE', #2969, 8.000000000000000000 ) ;
#51911=EDGE_LOOP ( 'NONE', ( #22855, #19993, #40996, #38038 ) ) ;
#51919=CARTESIAN_POINT ( 'NONE',  ( -2.977408999572651815, 121.4375000020483668, 7.188101187500000933 ) ) ;
#51929=CARTESIAN_POINT ( 'NONE',  ( 7.188101187500000044, 22.96874999795161543, 0.000000000000000000 ) ) ;
#51943=CARTESIAN_POINT ( 'NONE',  ( 4.898587196589412829E-16, 27.18749999590322375, -8.000000000000000000 ) ) ;
#51952=CARTESIAN_POINT ( 'NONE',  ( -2.977408999572654480, 4.874999997951610986, 7.188101187499999156 ) ) ;
#51955=ORIENTED_EDGE ( 'NONE', *, *, #15942, .F. ) ;
#51969=CARTESIAN_POINT ( 'NONE',  ( 8.000000000000000000, 18.09375000000000355, -3.313708498984761608 ) ) ;
#51971=CARTESIAN_POINT ( 'NONE',  ( 3.999985685286083115, 88.68677412680156635, -6.928211494859724873 ) ) ;
#51975=CARTESIAN_POINT ( 'NONE',  ( 4.898587196589412829E-16, 7.875000000000001776, -8.000000000000000000 ) ) ;
#51978=CARTESIAN_POINT ( 'NONE',  ( 8.000000000000001776, 113.6562500000000000, 3.313708498984759387 ) ) ;
#51996=PLANE ( 'NONE',  #45702 ) ;
#52000=CARTESIAN_POINT ( 'NONE',  ( 4.898587196589412829E-16, 1.875000000000000444, -8.000000000000000000 ) ) ;
#52001=VERTEX_POINT ( 'NONE', #22430 ) ;
#52007=CARTESIAN_POINT ( 'NONE',  ( 4.401442555609581635E-16, 23.71874999795161543, -7.188101187500000044 ) ) ;
#52010=CARTESIAN_POINT ( 'NONE',  ( -7.188101187499999156, 99.12500000204838102, 2.977408999572654924 ) ) ;
#52027=CARTESIAN_POINT ( 'NONE',  ( -4.401442555609581635E-16, 90.78125000204836681, -7.188101187500000044 ) ) ;
#52032=CARTESIAN_POINT ( 'NONE',  ( 2.977408999572654480, 96.50000000204838102, 7.188101187499999156 ) ) ;
#52058=CARTESIAN_POINT ( 'NONE',  ( -1.320432766682874540E-15, 15.09374999795161187, 7.188101187500000044 ) ) ;
#52059=CARTESIAN_POINT ( 'NONE',  ( 8.000000000000001776, 106.3437500040967763, 3.313708498984759387 ) ) ;
#52068=DIRECTION ( 'NONE',  ( 0.7071067811865525687, 0.7071067811865425767, -0.000000000000000000 ) ) ;
#52069=CARTESIAN_POINT ( 'NONE',  ( 7.188101187500000044, 103.9062500020483810, -8.802885111219163269E-16 ) ) ;
#52080=B_SPLINE_CURVE_WITH_KNOTS ( 'NONE', 3,
 ( #70738, #13743, #64718, #14120, #37155, #42430, #36052, #59797, #36787, #30750, #7007, #53030, #65447, #70381, #8110, #48459, #65067, #24346, #54142, #25071, #2451, #60156 ),
 .UNSPECIFIED., .F., .F.,
 ( 4, 2, 2, 2, 2, 2, 2, 2, 2, 2, 4 ),
 ( 0.000000000000000000, 0.001531360831348023465, 0.002297041247022034872, 0.003062721662696046062, 0.004594082494044070611, 0.006125443325392096461, 0.006891123741066107651, 0.007656804156740118841, 0.009188164988088146426, 0.01071952581943617401, 0.01225088665078420333 ),
 .UNSPECIFIED. ) ;
#52090=CARTESIAN_POINT ( 'NONE',  ( -7.999999999999998224, 99.59374999999998579, 3.313708498984766493 ) ) ;
#52093=CARTESIAN_POINT ( 'NONE',  ( 8.000000000000000000, 1.500000000000000000, 0.000000000000000000 ) ) ;
#52096=CARTESIAN_POINT ( 'NONE',  ( 5.082755093536325930, 5.531249997951610098, -5.082755093536325930 ) ) ;
#52099=CARTESIAN_POINT ( 'NONE',  ( -2.977408999572650927, 113.7500000020483810, -7.188101187500000933 ) ) ;
#52109=CARTESIAN_POINT ( 'NONE',  ( 8.000000000000000000, 124.2500000000000000, -9.797174393178825657E-16 ) ) ;
#52112=ORIENTED_EDGE ( 'NONE', *, *, #29418, .F. ) ;
#52113=AXIS2_PLACEMENT_3D ( 'NONE', #26212, #22047, #27715 ) ;
#52120=CARTESIAN_POINT ( 'NONE',  ( 7.188101187500000933, 114.5000000020483810, -2.977408999572651371 ) ) ;
#52125=CARTESIAN_POINT ( 'NONE',  ( -7.188101187500000044, 117.0312500020483810, 0.000000000000000000 ) ) ;
#52129=ORIENTED_EDGE ( 'NONE', *, *, #27395, .F. ) ;
#52131=CARTESIAN_POINT ( 'NONE',  ( 0.000000000000000000, 125.0000000000000000, 8.000000000000000000 ) ) ;
#52148=CARTESIAN_POINT ( 'NONE',  ( 8.000000000000000000, 6.093750000000000888, -3.313708498984761608 ) ) ;
#52149=CARTESIAN_POINT ( 'NONE',  ( -5.656854249492380582, 110.0000000040967763, -5.656854249492380582 ) ) ;
#52150=CARTESIAN_POINT ( 'NONE',  ( -7.188101187500000044, 24.09374999795161543, -8.802885111219163269E-16 ) ) ;
#52151=CARTESIAN_POINT ( 'NONE',  ( -3.313708498984762496, 120.9687500040967905, 7.999999999999998224 ) ) ;
#52160=EDGE_CURVE ( 'NONE', #3031, #30042, #59642, .T. ) ;
#52177=CARTESIAN_POINT ( 'NONE',  ( 8.000000000000000000, 119.8437500000000142, -3.313708498984762496 ) ) ;
#52206=CARTESIAN_POINT ( 'NONE',  ( 2.977408999572654480, 99.12500000204838102, 7.188101187499999156 ) ) ;
#52215=DIRECTION ( 'NONE',  ( -0.000000000000000000, 1.000000000000000000, -0.000000000000000000 ) ) ;
#52226=CARTESIAN_POINT ( 'NONE',  ( 3.313708498984762496, 17.53124999590322375, 7.999999999999998224 ) ) ;
#52230=CARTESIAN_POINT ( 'NONE',  ( -1.320432766682874540E-15, 25.96874999795161543, 7.188101187500000044 ) ) ;
#52233=ORIENTED_EDGE ( 'NONE', *, *, #61637, .F. ) ;
#52234=CARTESIAN_POINT ( 'NONE',  ( -8.000000000000000000, 125.0000000000000000, -1.469576158976823947E-15 ) ) ;
#52238=CARTESIAN_POINT ( 'NONE',  ( -1.320432766682874540E-15, 9.093749997951610098, 7.188101187500000044 ) ) ;
#52241=CARTESIAN_POINT ( 'NONE',  ( -7.188101187500000044, 3.093749997951610098, -8.802885111219163269E-16 ) ) ;
#52254=CARTESIAN_POINT ( 'NONE',  ( 7.188101187500000044, 114.4062500020483810, -8.802885111219163269E-16 ) ) ;
#52259=CARTESIAN_POINT ( 'NONE',  ( 4.401442555609581635E-16, 18.84374999795161187, -7.188101187500000044 ) ) ;
#52264=CARTESIAN_POINT ( 'NONE',  ( 5.082755093536325042, 98.46875000204838102, -5.082755093536325930 ) ) ;
#52277=DIRECTION ( 'NONE',  ( -0.000000000000000000, 1.000000000000000000, -0.000000000000000000 ) ) ;
#52293=CARTESIAN_POINT ( 'NONE',  ( 7.188101187500001821, 116.0000000020483810, -2.977408999572651371 ) ) ;
#52301=CARTESIAN_POINT ( 'NONE',  ( 0.000000000000000000, 125.0000000000000000, 0.000000000000000000 ) ) ;
#52302=CARTESIAN_POINT ( 'NONE',  ( -5.082755093536325042, 23.53124999795161543, -5.082755093536325930 ) ) ;
#52307=CARTESIAN_POINT ( 'NONE',  ( 4.898587196589412829E-16, 25.87500000000000711, -8.000000000000000000 ) ) ;
#52323=CARTESIAN_POINT ( 'NONE',  ( 7.188101187499999156, 6.749999997951610986, 2.977408999572654924 ) ) ;
#52333=CARTESIAN_POINT ( 'NONE',  ( 3.979266480698044450, 124.5000000000001137, -6.940132439340980675 ) ) ;
#52339=CARTESIAN_POINT ( 'NONE',  ( 4.898587196589412829E-16, 19.87500000000000355, -8.000000000000000000 ) ) ;
#52342=CARTESIAN_POINT ( 'NONE',  ( 5.082755093536325042, 122.0937500020483952, -5.082755093536325930 ) ) ;
#52344=EDGE_CURVE ( 'NONE', #61133, #64958, #65972, .T. ) ;
#52350=ORIENTED_EDGE ( 'NONE', *, *, #44508, .F. ) ;
#52351=CARTESIAN_POINT ( 'NONE',  ( -5.082755093536326818, 1.406249997951610320, 5.082755093536325042 ) ) ;
#52371=CARTESIAN_POINT ( 'NONE',  ( -1.469576158976823947E-15, 2.625000000000000444, 8.000000000000000000 ) ) ;
#52379=CARTESIAN_POINT ( 'NONE',  ( 2.977408999572650927, 20.62499999795161543, -7.188101187500001821 ) ) ;
#52382=CARTESIAN_POINT ( 'NONE',  ( 5.082755093536326818, 96.59375000204838102, 5.082755093536325042 ) ) ;
#52399=CARTESIAN_POINT ( 'NONE',  ( -2.977408999572652260, 89.93750000204839523, 7.188101187500000044 ) ) ;
#52402=CARTESIAN_POINT ( 'NONE',  ( 8.000000000000000000, 111.0312500040967763, -3.313708498984762496 ) ) ;
#52405=CARTESIAN_POINT ( 'NONE',  ( -5.082755093536325930, 94.34375000204838102, -5.082755093536325930 ) ) ;
#52413=CARTESIAN_POINT ( 'NONE',  ( -1.469576158976823947E-15, 12.93749999590322197, 8.000000000000000000 ) ) ;
#52428=CARTESIAN_POINT ( 'NONE',  ( -5.656854249492380582, 101.0000000040967905, -5.656854249492380582 ) ) ;
#52434=ORIENTED_EDGE ( 'NONE', *, *, #46821, .F. ) ;
#52436=CARTESIAN_POINT ( 'NONE',  ( -5.082755093536325930, 104.4687500020483952, -5.082755093536325930 ) ) ;
#52454=CARTESIAN_POINT ( 'NONE',  ( -5.656854249492378806, 101.1875000000000000, 5.656854249492381470 ) ) ;
#52459=CARTESIAN_POINT ( 'NONE',  ( 7.188101187500000044, 3.843749997951610542, 0.000000000000000000 ) ) ;
#52462=CARTESIAN_POINT ( 'NONE',  ( 7.188101187500002709, 114.6875000020484094, 2.977408999572649151 ) ) ;
#52483=CARTESIAN_POINT ( 'NONE',  ( 1.320432766682874540E-15, 109.5312500020483810, 7.188101187500000044 ) ) ;
#52488=CARTESIAN_POINT ( 'NONE',  ( -5.082755093536325930, 116.8437500020483810, -5.082755093536325930 ) ) ;
#52510=EDGE_LOOP ( 'NONE', ( #55221, #1985, #18178, #10681 ) ) ;
#52512=EDGE_CURVE ( 'NONE', #36620, #69862, #71457, .T. ) ;
#52516=CARTESIAN_POINT ( 'NONE',  ( 5.656854249492380582, 7.687500000000001776, -5.656854249492380582 ) ) ;
#52518=CARTESIAN_POINT ( 'NONE',  ( -5.082755093536325042, 26.90624999795161898, -5.082755093536325930 ) ) ;
#52519=CARTESIAN_POINT ( 'NONE',  ( -4.898587196589412829E-16, 121.8125000040967763, -8.000000000000000000 ) ) ;
#52540=CARTESIAN_POINT ( 'NONE',  ( -8.000000000000000000, 117.5000000000000000, 0.000000000000000000 ) ) ;
#52546=CARTESIAN_POINT ( 'NONE',  ( -3.313708498984765161, 14.34374999590322375, 7.999999999999998224 ) ) ;
#52548=CARTESIAN_POINT ( 'NONE',  ( 3.313708498984762496, 11.53124999590322375, 7.999999999999998224 ) ) ;
#52564=CARTESIAN_POINT ( 'NONE',  ( 3.313708498984757167, 4.031249995903219308, 8.000000000000001776 ) ) ;
#52565=CARTESIAN_POINT ( 'NONE',  ( -3.313708498984693218, 115.9062500040967620, -8.000000000000065725 ) ) ;
#52572=CARTESIAN_POINT ( 'NONE',  ( -7.188101187499999156, 97.25000000204839523, 2.977408999572654924 ) ) ;
#52575=CARTESIAN_POINT ( 'NONE',  ( 6.716570278246744685, 0.2636345205237095035, -3.927716332986086911 ) ) ;
#52604=CARTESIAN_POINT ( 'NONE',  ( -7.188101187500000044, 14.71874999795161187, -8.802885111219163269E-16 ) ) ;
#52609=CARTESIAN_POINT ( 'NONE',  ( 5.082755093536324154, 3.656249997951610542, 5.082755093536326818 ) ) ;
#52622=CARTESIAN_POINT ( 'NONE',  ( -2.977408999572650927, 114.8750000020483810, -7.188101187500001821 ) ) ;
#52627=CARTESIAN_POINT ( 'NONE',  ( -1.320432766682874540E-15, 18.09374999795161187, 7.188101187500000044 ) ) ;
#52632=CARTESIAN_POINT ( 'NONE',  ( 2.977408999572654480, 101.0000000020483810, 7.188101187499999156 ) ) ;
#52637=ORIENTED_EDGE ( 'NONE', *, *, #6709, .T. ) ;
#52643=FACE_OUTER_BOUND ( 'NONE', #47692, .T. ) ;
#52645=CARTESIAN_POINT ( 'NONE',  ( -1.469576158976823947E-15, 22.12500000000000355, 8.000000000000000000 ) ) ;
#52649=FACE_OUTER_BOUND ( 'NONE', #700, .T. ) ;
#52650=CARTESIAN_POINT ( 'NONE',  ( -8.000000000000000000, 5.250000000000000888, -9.797174393178825657E-16 ) ) ;
#52661=CARTESIAN_POINT ( 'NONE',  ( 7.188101187500001821, 114.5000000020483810, -2.977408999572651371 ) ) ;
#52669=CARTESIAN_POINT ( 'NONE',  ( -2.977408999572650039, 23.43749999795161898, -7.188101187500001821 ) ) ;
#52685=CARTESIAN_POINT ( 'NONE',  ( -8.000000000000000000, 27.56249999590322375, -9.797174393178825657E-16 ) ) ;
#52693=CARTESIAN_POINT ( 'NONE',  ( -7.188101187500000044, 9.093749997951611874, -8.802885111219163269E-16 ) ) ;
#52711=CARTESIAN_POINT ( 'NONE',  ( -8.000000000000000000, 17.15625000000000000, -3.313708498984762496 ) ) ;
#52714=CARTESIAN_POINT ( 'NONE',  ( -2.977408999572651815, 122.9375000020483810, 7.188101187500000933 ) ) ;
#52720=ORIENTED_EDGE ( 'NONE', *, *, #59637, .T. ) ;
#52721=CARTESIAN_POINT ( 'NONE',  ( 8.000000000000000000, 113.7500000000000000, -9.797174393178825657E-16 ) ) ;
#52724=CARTESIAN_POINT ( 'NONE',  ( -7.188101187499999156, 115.6250000020483810, 2.977408999572654924 ) ) ;
#52741=CARTESIAN_POINT ( 'NONE',  ( -8.000000000000000000, 2.156250000000000444, -3.313708498984762496 ) ) ;
#52749=CARTESIAN_POINT ( 'NONE',  ( -7.188101187500002709, 25.68749999795162253, 2.977408999572649151 ) ) ;
#52751=CARTESIAN_POINT ( 'NONE',  ( 2.977408999572650039, 98.56250000204838102, -7.188101187500000933 ) ) ;
#52760=LINE ( 'NONE', #25176, #57965 ) ;
#52765=CARTESIAN_POINT ( 'NONE',  ( 1.926037949307475072, 89.22060463630471361, -7.188101187500000933 ) ) ;
#52771=CARTESIAN_POINT ( 'NONE',  ( 1.320432766682874540E-15, 96.40625000204838102, 7.188101187500000044 ) ) ;
#52778=DIRECTION ( 'NONE',  ( -0.000000000000000000, 1.000000000000000000, -0.000000000000000000 ) ) ;
#52787=ORIENTED_EDGE ( 'NONE', *, *, #20488, .T. ) ;
#52795=CARTESIAN_POINT ( 'NONE',  ( 5.656854249492379694, 103.6250000040967763, -5.656854249492380582 ) ) ;
#52804=CARTESIAN_POINT ( 'NONE',  ( -5.082755093536324154, 98.84375000204838102, 5.082755093536326818 ) ) ;
#52806=CARTESIAN_POINT ( 'NONE',  ( 3.313708498984794915, 120.2187500040967905, -7.999999999999967137 ) ) ;
#52808=VERTEX_POINT ( 'NONE', #692 ) ;
#52822=CARTESIAN_POINT ( 'NONE',  ( 3.313708498984760720, 99.03124999999998579, -8.000000000000000000 ) ) ;
#52830=CARTESIAN_POINT ( 'NONE',  ( -7.188101187500000044, 6.093749997951610986, -8.802885111219163269E-16 ) ) ;
#52832=CARTESIAN_POINT ( 'NONE',  ( -4.401442555609581635E-16, 115.1562500020483810, -7.188101187500000044 ) ) ;
#52833=DIRECTION ( 'NONE',  ( 0.000000000000000000, 0.000000000000000000, 1.000000000000000000 ) ) ;
#52836=CARTESIAN_POINT ( 'NONE',  ( -3.313708498984708317, 90.78125000000002842, 8.000000000000053291 ) ) ;
#52853=CARTESIAN_POINT ( 'NONE',  ( -7.188101187500000933, 107.5625000020483810, -2.977408999572650483 ) ) ;
#52859=CARTESIAN_POINT ( 'NONE',  ( -2.977408999572651815, 115.8125000020484094, 7.188101187500000933 ) ) ;
#52872=CARTESIAN_POINT ( 'NONE',  ( 3.313708498984761608, 15.28125000000000355, -8.000000000000000000 ) ) ;
#52886=CARTESIAN_POINT ( 'NONE',  ( 3.313708498984762496, 2.718750000000000888, 7.999999999999998224 ) ) ;
#52889=CARTESIAN_POINT ( 'NONE',  ( 4.401442555609581635E-16, 2.343749997951610098, -7.188101187500000044 ) ) ;
#52890=CARTESIAN_POINT ( 'NONE',  ( 5.656854249492381470, 121.2500000040967905, 5.656854249492379694 ) ) ;
#52896=CARTESIAN_POINT ( 'NONE',  ( -1.469576158976823947E-15, 5.437499995903221084, 8.000000000000000000 ) ) ;
#52912=CARTESIAN_POINT ( 'NONE',  ( 5.656854249492379694, 118.4375000000000000, -5.656854249492380582 ) ) ;
#52919=CARTESIAN_POINT ( 'NONE',  ( 5.656854249492378806, 14.62499999590322020, 5.656854249492381470 ) ) ;
#52921=CARTESIAN_POINT ( 'NONE',  ( 8.000000000000000000, 11.81249999590322197, 0.000000000000000000 ) ) ;
#52935=ORIENTED_EDGE ( 'NONE', *, *, #57385, .T. ) ;
#52943=CARTESIAN_POINT ( 'NONE',  ( 2.977408999572654480, 121.6250000020483810, 7.188101187499999156 ) ) ;
#52947=CARTESIAN_POINT ( 'NONE',  ( -5.082755093536325930, 99.96875000204838102, -5.082755093536325930 ) ) ;
#52950=CARTESIAN_POINT ( 'NONE',  ( 6.155571212629570077, 0.2837926415812287440, -4.791828655132197134 ) ) ;
#52963=CARTESIAN_POINT ( 'NONE',  ( -5.656854249492378806, 113.1875000000000000, 5.656854249492381470 ) ) ;
#52964=DIRECTION ( 'NONE',  ( -0.000000000000000000, 1.000000000000000000, -0.000000000000000000 ) ) ;
#52974=CARTESIAN_POINT ( 'NONE',  ( -1.320432766682874540E-15, 18.09374999795161187, 7.188101187500000044 ) ) ;
#52977=CARTESIAN_POINT ( 'NONE',  ( 7.188101187500000044, 11.34374999795161187, 0.000000000000000000 ) ) ;
#52992=CARTESIAN_POINT ( 'NONE',  ( -2.977408999572651815, 115.4375000020483810, 7.188101187500000933 ) ) ;
#52997=CARTESIAN_POINT ( 'NONE',  ( 7.188101187500000044, 25.96874999795161543, 0.000000000000000000 ) ) ;
#53003=CARTESIAN_POINT ( 'NONE',  ( -5.082755093536324154, 97.71875000204838102, 5.082755093536326818 ) ) ;
#53008=ORIENTED_EDGE ( 'NONE', *, *, #20906, .T. ) ;
#53018=CARTESIAN_POINT ( 'NONE',  ( 8.000000000000001776, 91.15625000000000000, 3.313708498984759387 ) ) ;
#53030=CARTESIAN_POINT ( 'NONE',  ( -5.309927858096890496, 124.6926540804226988, -5.729198325116819035 ) ) ;
#53033=CARTESIAN_POINT ( 'NONE',  ( 5.082755093536325042, 113.0937500020483810, -5.082755093536325930 ) ) ;
#53062=CARTESIAN_POINT ( 'NONE',  ( 2.977408999572650927, 11.62499999795161187, -7.188101187500000933 ) ) ;
#53067=CARTESIAN_POINT ( 'NONE',  ( 5.656854249492379694, 99.12500000409677625, -5.656854249492380582 ) ) ;
#53080=CARTESIAN_POINT ( 'NONE',  ( 8.000000000000000000, 22.50000000000000355, 0.000000000000000000 ) ) ;
#53088=ORIENTED_EDGE ( 'NONE', *, *, #66976, .F. ) ;
#53089=CARTESIAN_POINT ( 'NONE',  ( 5.082755093536324154, 4.781249997951610986, 5.082755093536326818 ) ) ;
#53094=CARTESIAN_POINT ( 'NONE',  ( -7.188101187500000044, 115.5312500020483952, 0.000000000000000000 ) ) ;
#53113=CARTESIAN_POINT ( 'NONE',  ( -5.656854249492379694, 2.062500000000000444, -5.656854249492380582 ) ) ;
#53122=CARTESIAN_POINT ( 'NONE',  ( -1.320432766682874540E-15, 24.46874999795161543, 7.188101187500000044 ) ) ;
#53124=CARTESIAN_POINT ( 'NONE',  ( 5.082755093536325042, 95.46875000204838102, -5.082755093536325930 ) ) ;
#53145=CARTESIAN_POINT ( 'NONE',  ( -4.401442555609581635E-16, 95.65625000204838102, -7.188101187500000044 ) ) ;
#53148=( BOUNDED_SURFACE ( )  B_SPLINE_SURFACE ( 1, 2, ( 
 ( #51599, #62917, #62540, #33905, #5216, #691, #58033, #74614, #46313, #68954, #56530, #22544, #28217, #62171, #6341, #29346, #11243, #50853, #11986, #16888, #23674, #40283, #51226, #40657, #17264, #34273, #63284, #45566, #46680, #57653, #28963, #69704, #73867, #22172, #45197, #18016, #48150, #47779, #25135, #54205, #30077, #30449, #71159, #18389, #35385, #1428, #24037, #41401, #35744, #2513, #24768, #47046, #30809, #59132, #12352, #1058, #24412, #41035, #58761, #41765, #64773, #1783, #19115, #64042, #53832, #7441, #19480, #70442, #59856, #36850, #25507, #29710, #70801, #2141, #42495, #70082, #42120, #59494, #64414, #65131, #7807, #58398, #7071, #12712, #47417, #13443, #53465, #6703, #65510, #36480, #13805, #8170, #48520, #31180, #13076, #52724, #53094, #18757, #36111, #66623, #10039, #37593, #14928, #38720, #4379, #56070, #50020, #55701, #61718, #60592, #14556, #21346, #49651, #8917, #31555, #48892, #8541, #37970, #3261, #3631, #60969, #72282, #60217, #43993, #25872, #54579, #31929, #27372, #71526, #20217, #65875, #26249, #54951, #37219, #27007, #44367, #9289, #14182, #71903, #38339, #49267, #73035, #32312, #66251, #72667, #9672, #67379, #15679, #20594, #4017, #43236, #33074, #20969, #43610, #55326, #26628, #19853, #42857, #67003, #15302, #61346, #32692, #2884, #39448, #11155, #69238, #21711, #6247, #56809, #34179, #68121, #51888, #228, #56436, #62448, #40192, #27748, #5872, #10775, #44740, #45845, #33436, #23209, #45470, #5130, #4756, #34929, #45108, #22829, #16049, #39081, #57181, #11524, #63194, #34558, #33812, #51507, #62086, #68860, #57563, #28868, #17171, #46221, #5498, #68486, #51136, #50759, #73775, #22084, #63569, #17547, #16788, #40566, #39815, #67756, #28123, #16415, #50392, #11895, #57941, #22450, #10408, #73407, #74146, #62820, #74521, #28498, #42035, #59041, #58669, #64687, #967, #42400, #18295, #70356, #19387, #47329, #18667, #59403, #29251, #7718, #7348, #36388, #65417, #41311, #41678, #30721, #29619, #46589, #12623, #35294, #52632, #46959, #13715, #36024, #58308, #65041, #53376, #69610, #63950, #36759, #12986, #47688, #30355, #17926, #13350, #1336, #23950, #59772, #40941, #1700, #6612, #48062, #24678, #70710, #19028, #53742, #596, #52264, #29986, #23579, #64319, #69987, #35654, #12260, #6975, #53003, #2053, #24318, #25041, #71069, #37504, #72577, #15591, #42771, #38630, #38250, #54112, #43903, #20882, #8081, #43515, #14091, #65787, #60502, #9198, #20130, #66914, #8829, #31840, #60129, #8447, #37126, #21255, #3928, #49177, #15219, #72188, #2422, #43145, #54491, #31082, #26919, #49934, #54859, #25417, #55611, #3170, #72947, #32219, #2796, #61253, #37880, #26159, #66529, #25784, #44280, #71812, #20500, #67291, #14839, #60875, #9585, #48431, #32602, #55237, #71434, #19764, #66161, #3543, #31467, #48803, #14465, #26534, #49559, #61998, #4667, #46130, #68400, #15964, #74432, #11070, #27285, #21626, #51795, #5043, #5408, #62730, #4294, #45760, #33723, #56348, #69148, #50302, #34096, #38993, #5782 ),
 ( #44650, #39362, #10689, #51418, #45026, #33347, #73323, #16326, #22739, #17455, #67666, #61632, #17082, #32983, #68771, #40104, #9950, #22360, #10321, #27664, #62359, #57092, #73688, #63109, #56725, #50669, #11435, #28039, #68033, #22000, #55984, #51050, #28410, #74061, #45384, #16698, #34472, #57476, #28778, #39729, #142, #23118, #35935, #1612, #53287, #7260, #12899, #24224, #58580, #6888, #18942, #18208, #7626, #59321, #1966, #52177, #47238, #24595, #47601, #46500, #18578, #30270, #69520, #41589, #70624, #34841, #6523, #17834, #69897, #70265, #52912, #6154, #41948, #64602, #58952, #64956, #70988, #13266, #35567, #36303, #52540, #40848, #509, #29899, #53655, #29530, #1247, #30635, #47973, #24958, #40476, #63481, #11803, #878, #58224, #57848, #29162, #23864, #23488, #63856, #12171, #35207, #46874, #41222, #64230, #12539, #7993, #66445, #48343, #54023, #60038, #26830, #49844, #42684, #13634, #48715, #37037, #59684, #49467, #43813, #60413, #36672, #71350, #60788, #71721, #72487, #37414, #13998, #72100, #32128, #66828, #20796, #43053, #3452, #19672, #26442, #43430, #66070, #14378, #65696, #15130, #38162, #14752, #20413, #26065, #25695, #2707, #8358, #54771, #61164, #65330, #19304, #20037, #3081, #31374, #9495, #32509, #25328, #54400, #9112, #8739, #55522, #31751, #30999, #37792, #49086, #2331, #55147, #3834, #42314, #38906, #21907, #44938, #56639, #73973, #72862, #10978, #74341, #4208, #61908, #62645, #50213, #28323, #10233, #67204, #68315, #39277, #15502, #55894, #56260, #21167, #33261, #67945, #16239, #4954, #22278, #44191, #34013, #62278, #51333, #50582, #40020, #16993, #34382, #9863, #27954, #57008, #5321, #27197, #50960, #39648, #73234, #45300, #22650, #38539, #4576, #21540, #27574, #16612, #10605, #61540, #45670, #68684, #63023, #11347, #28690, #57382, #33633, #5692, #73600, #44564, #32892, #67576, #15873, #17740, #46779, #19865, #60231, #37233, #31194, #36862, #42871, #40755, #69431, #2529, #29812, #63764, #11713, #29070, #63389, #18119, #58133, #58494, #69803, #52454, #40391, #25149, #6063, #34753, #12082, #8556, #51704, #423, #46043, #6442, #35118, #17367, #8183, #25521, #41133, #69063, #52090, #19492, #29443, #54218, #64140, #46417, #52822, #65525, #48533, #71541, #792, #59870, #23402, #65890, #1157, #23776, #12450, #35480, #14196, #51, #48166, #71174, #6800, #42508, #13818, #23034, #57758, #50408, #2900, #62101, #37984, #15316, #49282, #33090, #60608, #66266, #72298, #39098, #31570, #54966, #25885, #60983, #20610, #71918, #61736, #56087, #72683, #48904, #8932, #73050, #9304, #10053, #49666, #26262, #9687, #44382, #4396, #27389, #55341, #15695, #31943, #38737, #55716, #3644, #26644, #3275, #73422, #21727, #4031, #32707, #38352, #32328, #14945, #43628, #67019, #44757, #20231, #54594, #20985, #61360, #66638, #67770, #16064, #37608, #44009, #21358, #27025, #43250, #50036, #14573, #67393, #51522, #4772, #68136, #68504, #33454, #51154, #34194, #57198, #68877, #11539, #10424, #23225, #74537, #63583, #62836 ) ),
 .UNSPECIFIED., .F., .F., .F. ) 
 B_SPLINE_SURFACE_WITH_KNOTS ( ( 2, 2 ),
 ( 3, 2, 2, 2, 2, 2, 2, 2, 2, 2, 2, 2, 2, 2, 2, 2, 2, 2, 2, 2, 2, 2, 2, 2, 2, 2, 2, 2, 2, 2, 2, 2, 2, 2, 2, 2, 2, 2, 2, 2, 2, 2, 2, 2, 2, 2, 2, 2, 2, 2, 2, 2, 2, 2, 2, 2, 2, 2, 2, 2, 2, 2, 2, 2, 2, 2, 2, 2, 2, 2, 2, 2, 2, 2, 2, 2, 2, 2, 2, 2, 2, 2, 2, 2, 2, 2, 2, 2, 2, 2, 2, 2, 2, 2, 2, 2, 2, 2, 2, 2, 2, 2, 2, 2, 2, 2, 2, 2, 2, 2, 2, 2, 2, 2, 2, 2, 2, 2, 2, 2, 2, 2, 2, 2, 2, 2, 2, 2, 2, 2, 2, 2, 2, 2, 2, 2, 2, 2, 2, 2, 2, 2, 2, 2, 2, 2, 2, 2, 2, 2, 2, 2, 2, 2, 2, 2, 2, 2, 2, 2, 2, 2, 2, 2, 2, 2, 2, 2, 2, 2, 2, 2, 2, 2, 2, 2, 2, 2, 2, 2, 2, 2, 2, 2, 2, 2, 2, 2, 3 ),
 ( 0.000000000000000000, 1.000000000000000000 ),
 ( 0.000000000000000000, 0.005208333333333333044, 0.01041666666666666609, 0.01562500000000000000, 0.02083333333333333218, 0.02604166666666666782, 0.03125000000000000000, 0.03645833333333333565, 0.04166666666666666435, 0.04687500000000000000, 0.05208333333333333565, 0.05729166666666666435, 0.06250000000000000000, 0.06770833333333332871, 0.07291666666666667129, 0.07812500000000000000, 0.08333333333333332871, 0.08854166666666667129, 0.09375000000000000000, 0.09895833333333332871, 0.1041666666666666713, 0.1093750000000000000, 0.1145833333333333287, 0.1197916666666666713, 0.1250000000000000000, 0.1302083333333333426, 0.1354166666666666574, 0.1406250000000000000, 0.1458333333333333426, 0.1510416666666666574, 0.1562500000000000000, 0.1614583333333333426, 0.1666666666666666574, 0.1718750000000000000, 0.1770833333333333426, 0.1822916666666666574, 0.1875000000000000000, 0.1927083333333333426, 0.1979166666666666574, 0.2031250000000000000, 0.2083333333333333426, 0.2135416666666666574, 0.2187500000000000000, 0.2239583333333333426, 0.2291666666666666574, 0.2343750000000000000, 0.2395833333333333426, 0.2447916666666666574, 0.2500000000000000000, 0.2552083333333333148, 0.2604166666666666852, 0.2656250000000000000, 0.2708333333333333148, 0.2760416666666666852, 0.2812500000000000000, 0.2864583333333333148, 0.2916666666666666852, 0.2968750000000000000, 0.3020833333333333148, 0.3072916666666666852, 0.3125000000000000000, 0.3177083333333333148, 0.3229166666666666852, 0.3281250000000000000, 0.3333333333333333148, 0.3385416666666666852, 0.3437500000000000000, 0.3489583333333333148, 0.3541666666666666852, 0.3593750000000000000, 0.3645833333333333148, 0.3697916666666666852, 0.3750000000000000000, 0.3802083333333333148, 0.3854166666666666852, 0.3906250000000000000, 0.3958333333333333148, 0.4010416666666666852, 0.4062500000000000000, 0.4114583333333333148, 0.4166666666666666852, 0.4218750000000000000, 0.4270833333333333148, 0.4322916666666666852, 0.4375000000000000000, 0.4427083333333333148, 0.4479166666666666852, 0.4531250000000000000, 0.4583333333333333148, 0.4635416666666666852, 0.4687500000000000000, 0.4739583333333333148, 0.4791666666666666852, 0.4843750000000000000, 0.4895833333333333148, 0.4947916666666666852, 0.5000000000000000000, 0.5052083333333333703, 0.5104166666666666297, 0.5156250000000000000, 0.5208333333333333703, 0.5260416666666666297, 0.5312500000000000000, 0.5364583333333333703, 0.5416666666666666297, 0.5468750000000000000, 0.5520833333333333703, 0.5572916666666666297, 0.5625000000000000000, 0.5677083333333333703, 0.5729166666666666297, 0.5781250000000000000, 0.5833333333333333703, 0.5885416666666666297, 0.5937500000000000000, 0.5989583333333333703, 0.6041666666666666297, 0.6093750000000000000, 0.6145833333333333703, 0.6197916666666666297, 0.6250000000000000000, 0.6302083333333333703, 0.6354166666666666297, 0.6406250000000000000, 0.6458333333333333703, 0.6510416666666666297, 0.6562500000000000000, 0.6614583333333333703, 0.6666666666666666297, 0.6718750000000000000, 0.6770833333333333703, 0.6822916666666666297, 0.6875000000000000000, 0.6927083333333333703, 0.6979166666666666297, 0.7031250000000000000, 0.7083333333333333703, 0.7135416666666666297, 0.7187500000000000000, 0.7239583333333333703, 0.7291666666666666297, 0.7343750000000000000, 0.7395833333333333703, 0.7447916666666666297, 0.7500000000000000000, 0.7552083333333333703, 0.7604166666666666297, 0.7656250000000000000, 0.7708333333333333703, 0.7760416666666666297, 0.7812500000000000000, 0.7864583333333333703, 0.7916666666666666297, 0.7968750000000000000, 0.8020833333333333703, 0.8072916666666666297, 0.8125000000000000000, 0.8177083333333333703, 0.8229166666666666297, 0.8281250000000000000, 0.8333333333333333703, 0.8385416666666666297, 0.8437500000000000000, 0.8489583333333333703, 0.8541666666666666297, 0.8593750000000000000, 0.8645833333333333703, 0.8697916666666666297, 0.8750000000000000000, 0.8802083333333333703, 0.8854166666666666297, 0.8906250000000000000, 0.8958333333333333703, 0.9010416666666666297, 0.9062500000000000000, 0.9114583333333333703, 0.9166666666666666297, 0.9218750000000000000, 0.9270833333333333703, 0.9322916666666666297, 0.9375000000000000000, 0.9427083333333333703, 0.9479166666666666297, 0.9531250000000000000, 0.9583333333333333703, 0.9635416666666666297, 0.9687500000000000000, 0.9722122468226729319, 0.9819343692908996113 ),
 .UNSPECIFIED. ) 
 GEOMETRIC_REPRESENTATION_ITEM ( )  RATIONAL_B_SPLINE_SURFACE ( (
 ( 1.000000000000000000, 0.9238795325112867385, 1.000000000000000000, 0.9238795325112867385, 1.000000000000000000, 0.9238795325112867385, 1.000000000000000000, 0.9238795325112867385, 1.000000000000000000, 0.9238795325112867385, 1.000000000000000000, 0.9238795325112867385, 1.000000000000000000, 0.9238795325112867385, 1.000000000000000000, 0.9238795325112867385, 1.000000000000000000, 0.9238795325112867385, 1.000000000000000000, 0.9238795325112867385, 1.000000000000000000, 0.9238795325112867385, 1.000000000000000000, 0.9238795325112867385, 1.000000000000000000, 0.9238795325112867385, 1.000000000000000000, 0.9238795325112867385, 1.000000000000000000, 0.9238795325112867385, 1.000000000000000000, 0.9238795325112867385, 1.000000000000000000, 0.9238795325112867385, 1.000000000000000000, 0.9238795325112867385, 1.000000000000000000, 0.9238795325112867385, 1.000000000000000000, 0.9238795325112867385, 1.000000000000000000, 0.9238795325112867385, 1.000000000000000000, 0.9238795325112867385, 1.000000000000000000, 0.9238795325112867385, 1.000000000000000000, 0.9238795325112867385, 1.000000000000000000, 0.9238795325112867385, 1.000000000000000000, 0.9238795325112867385, 1.000000000000000000, 0.9238795325112867385, 1.000000000000000000, 0.9238795325112867385, 1.000000000000000000, 0.9238795325112867385, 1.000000000000000000, 0.9238795325112867385, 1.000000000000000000, 0.9238795325112867385, 1.000000000000000000, 0.9238795325112867385, 1.000000000000000000, 0.9238795325112867385, 1.000000000000000000, 0.9238795325112867385, 1.000000000000000000, 0.9238795325112867385, 1.000000000000000000, 0.9238795325112867385, 1.000000000000000000, 0.9238795325112867385, 1.000000000000000000, 0.9238795325112867385, 1.000000000000000000, 0.9238795325112867385, 1.000000000000000000, 0.9238795325112867385, 1.000000000000000000, 0.9238795325112867385, 1.000000000000000000, 0.9238795325112867385, 1.000000000000000000, 0.9238795325112867385, 1.000000000000000000, 0.9238795325112867385, 1.000000000000000000, 0.9238795325112867385, 1.000000000000000000, 0.9238795325112867385, 1.000000000000000000, 0.9238795325112867385, 1.000000000000000000, 0.9238795325112867385, 1.000000000000000000, 0.9238795325112867385, 1.000000000000000000, 0.9238795325112867385, 1.000000000000000000, 0.9238795325112867385, 1.000000000000000000, 0.9238795325112867385, 1.000000000000000000, 0.9238795325112867385, 1.000000000000000000, 0.9238795325112867385, 1.000000000000000000, 0.9238795325112867385, 1.000000000000000000, 0.9238795325112867385, 1.000000000000000000, 0.9238795325112867385, 1.000000000000000000, 0.9238795325112867385, 1.000000000000000000, 0.9238795325112867385, 1.000000000000000000, 0.9238795325112867385, 1.000000000000000000, 0.9238795325112867385, 1.000000000000000000, 0.9238795325112867385, 1.000000000000000000, 0.9238795325112867385, 1.000000000000000000, 0.9238795325112867385, 1.000000000000000000, 0.9238795325112867385, 1.000000000000000000, 0.9238795325112867385, 1.000000000000000000, 0.9238795325112867385, 1.000000000000000000, 0.9238795325112867385, 1.000000000000000000, 0.9238795325112867385, 1.000000000000000000, 0.9238795325112867385, 1.000000000000000000, 0.9238795325112867385, 1.000000000000000000, 0.9238795325112867385, 1.000000000000000000, 0.9238795325112867385, 1.000000000000000000, 0.9238795325112867385, 1.000000000000000000, 0.9238795325112867385, 1.000000000000000000, 0.9238795325112867385, 1.000000000000000000, 0.9238795325112867385, 1.000000000000000000, 0.9238795325112867385, 1.000000000000000000, 0.9238795325112867385, 1.000000000000000000, 0.9238795325112867385, 1.000000000000000000, 0.9238795325112867385, 1.000000000000000000, 0.9238795325112867385, 1.000000000000000000, 0.9238795325112867385, 1.000000000000000000, 0.9238795325112867385, 1.000000000000000000, 0.9238795325112867385, 1.000000000000000000, 0.9238795325112867385, 1.000000000000000000, 0.9238795325112867385, 1.000000000000000000, 0.9238795325112867385, 1.000000000000000000, 0.9238795325112867385, 1.000000000000000000, 0.9238795325112867385, 1.000000000000000000, 0.9238795325112867385, 1.000000000000000000, 0.9238795325112867385, 1.000000000000000000, 0.9238795325112867385, 1.000000000000000000, 0.9238795325112867385, 1.000000000000000000, 0.9238795325112867385, 1.000000000000000000, 0.9238795325112867385, 1.000000000000000000, 0.9238795325112867385, 1.000000000000000000, 0.9238795325112867385, 1.000000000000000000, 0.9238795325112867385, 1.000000000000000000, 0.9238795325112867385, 1.000000000000000000, 0.9238795325112867385, 1.000000000000000000, 0.9238795325112867385, 1.000000000000000000, 0.9238795325112867385, 1.000000000000000000, 0.9238795325112867385, 1.000000000000000000, 0.9238795325112867385, 1.000000000000000000, 0.9238795325112867385, 1.000000000000000000, 0.9238795325112867385, 1.000000000000000000, 0.9238795325112867385, 1.000000000000000000, 0.9238795325112867385, 1.000000000000000000, 0.9238795325112867385, 1.000000000000000000, 0.9238795325112867385, 1.000000000000000000, 0.9238795325112867385, 1.000000000000000000, 0.9238795325112867385, 1.000000000000000000, 0.9238795325112867385, 1.000000000000000000, 0.9238795325112867385, 1.000000000000000000, 0.9238795325112867385, 1.000000000000000000, 0.9238795325112867385, 1.000000000000000000, 0.9238795325112867385, 1.000000000000000000, 0.9238795325112867385, 1.000000000000000000, 0.9238795325112867385, 1.000000000000000000, 0.9238795325112867385, 1.000000000000000000, 0.9238795325112867385, 1.000000000000000000, 0.9238795325112867385, 1.000000000000000000, 0.9238795325112867385, 1.000000000000000000, 0.9238795325112867385, 1.000000000000000000, 0.9238795325112867385, 1.000000000000000000, 0.9238795325112867385, 1.000000000000000000, 0.9238795325112867385, 1.000000000000000000, 0.9238795325112867385, 1.000000000000000000, 0.9238795325112867385, 1.000000000000000000, 0.9238795325112867385, 1.000000000000000000, 0.9238795325112867385, 1.000000000000000000, 0.9238795325112867385, 1.000000000000000000, 0.9238795325112867385, 1.000000000000000000, 0.9238795325112867385, 1.000000000000000000, 0.9238795325112867385, 1.000000000000000000, 0.9238795325112867385, 1.000000000000000000, 0.9238795325112867385, 1.000000000000000000, 0.9238795325112867385, 1.000000000000000000, 0.9238795325112867385, 1.000000000000000000, 0.9238795325112867385, 1.000000000000000000, 0.9238795325112867385, 1.000000000000000000, 0.9238795325112867385, 1.000000000000000000, 0.9238795325112867385, 1.000000000000000000, 0.9238795325112867385, 1.000000000000000000, 0.9238795325112867385, 1.000000000000000000, 0.9238795325112867385, 1.000000000000000000, 0.9238795325112867385, 1.000000000000000000, 0.9238795325112867385, 1.000000000000000000, 0.9238795325112867385, 1.000000000000000000, 0.9238795325112867385, 1.000000000000000000, 0.9238795325112867385, 1.000000000000000000, 0.9238795325112867385, 1.000000000000000000, 0.9238795325112867385, 1.000000000000000000, 0.9238795325112867385, 1.000000000000000000, 0.9238795325112867385, 1.000000000000000000, 0.9238795325112867385, 1.000000000000000000, 0.9238795325112867385, 1.000000000000000000, 0.9238795325112867385, 1.000000000000000000, 0.9238795325112867385, 1.000000000000000000, 0.9238795325112867385, 1.000000000000000000, 0.9238795325112867385, 1.000000000000000000, 0.9238795325112867385, 1.000000000000000000, 0.9238795325112867385, 1.000000000000000000, 0.9238795325112867385, 1.000000000000000000, 0.9238795325112867385, 1.000000000000000000, 0.9238795325112867385, 1.000000000000000000, 0.9238795325112867385, 1.000000000000000000, 0.9238795325112867385, 1.000000000000000000, 0.9238795325112867385, 1.000000000000000000, 0.9238795325112867385, 1.000000000000000000, 0.9238795325112867385, 1.000000000000000000, 0.9238795325112867385, 1.000000000000000000, 0.9238795325112867385, 1.000000000000000000, 0.9238795325112867385, 1.000000000000000000, 0.9238795325112867385, 1.000000000000000000, 0.9238795325112867385, 1.000000000000000000, 0.9238795325112867385, 1.000000000000000000, 0.9238795325112867385, 1.000000000000000000, 0.9238795325112867385, 1.000000000000000000, 0.9238795325112867385, 1.000000000000000000, 0.9238795325112867385, 1.000000000000000000, 0.9238795325112867385, 1.000000000000000000, 0.9238795325112867385, 1.000000000000000000, 0.9238795325112867385, 1.000000000000000000, 0.9238795325112867385, 1.000000000000000000, 0.9493988134329905959, 0.9660720450733824016, 0.9660720450733824016, 0.9660720450733824016),
 ( 1.000000000000000000, 0.9238795325112867385, 1.000000000000000000, 0.9238795325112867385, 1.000000000000000000, 0.9238795325112867385, 1.000000000000000000, 0.9238795325112867385, 1.000000000000000000, 0.9238795325112867385, 1.000000000000000000, 0.9238795325112867385, 1.000000000000000000, 0.9238795325112867385, 1.000000000000000000, 0.9238795325112867385, 1.000000000000000000, 0.9238795325112867385, 1.000000000000000000, 0.9238795325112867385, 1.000000000000000000, 0.9238795325112867385, 1.000000000000000000, 0.9238795325112867385, 1.000000000000000000, 0.9238795325112867385, 1.000000000000000000, 0.9238795325112867385, 1.000000000000000000, 0.9238795325112867385, 1.000000000000000000, 0.9238795325112867385, 1.000000000000000000, 0.9238795325112867385, 1.000000000000000000, 0.9238795325112867385, 1.000000000000000000, 0.9238795325112867385, 1.000000000000000000, 0.9238795325112867385, 1.000000000000000000, 0.9238795325112867385, 1.000000000000000000, 0.9238795325112867385, 1.000000000000000000, 0.9238795325112867385, 1.000000000000000000, 0.9238795325112867385, 1.000000000000000000, 0.9238795325112867385, 1.000000000000000000, 0.9238795325112867385, 1.000000000000000000, 0.9238795325112867385, 1.000000000000000000, 0.9238795325112867385, 1.000000000000000000, 0.9238795325112867385, 1.000000000000000000, 0.9238795325112867385, 1.000000000000000000, 0.9238795325112867385, 1.000000000000000000, 0.9238795325112867385, 1.000000000000000000, 0.9238795325112867385, 1.000000000000000000, 0.9238795325112867385, 1.000000000000000000, 0.9238795325112867385, 1.000000000000000000, 0.9238795325112867385, 1.000000000000000000, 0.9238795325112867385, 1.000000000000000000, 0.9238795325112867385, 1.000000000000000000, 0.9238795325112867385, 1.000000000000000000, 0.9238795325112867385, 1.000000000000000000, 0.9238795325112867385, 1.000000000000000000, 0.9238795325112867385, 1.000000000000000000, 0.9238795325112867385, 1.000000000000000000, 0.9238795325112867385, 1.000000000000000000, 0.9238795325112867385, 1.000000000000000000, 0.9238795325112867385, 1.000000000000000000, 0.9238795325112867385, 1.000000000000000000, 0.9238795325112867385, 1.000000000000000000, 0.9238795325112867385, 1.000000000000000000, 0.9238795325112867385, 1.000000000000000000, 0.9238795325112867385, 1.000000000000000000, 0.9238795325112867385, 1.000000000000000000, 0.9238795325112867385, 1.000000000000000000, 0.9238795325112867385, 1.000000000000000000, 0.9238795325112867385, 1.000000000000000000, 0.9238795325112867385, 1.000000000000000000, 0.9238795325112867385, 1.000000000000000000, 0.9238795325112867385, 1.000000000000000000, 0.9238795325112867385, 1.000000000000000000, 0.9238795325112867385, 1.000000000000000000, 0.9238795325112867385, 1.000000000000000000, 0.9238795325112867385, 1.000000000000000000, 0.9238795325112867385, 1.000000000000000000, 0.9238795325112867385, 1.000000000000000000, 0.9238795325112867385, 1.000000000000000000, 0.9238795325112867385, 1.000000000000000000, 0.9238795325112867385, 1.000000000000000000, 0.9238795325112867385, 1.000000000000000000, 0.9238795325112867385, 1.000000000000000000, 0.9238795325112867385, 1.000000000000000000, 0.9238795325112867385, 1.000000000000000000, 0.9238795325112867385, 1.000000000000000000, 0.9238795325112867385, 1.000000000000000000, 0.9238795325112867385, 1.000000000000000000, 0.9238795325112867385, 1.000000000000000000, 0.9238795325112867385, 1.000000000000000000, 0.9238795325112867385, 1.000000000000000000, 0.9238795325112867385, 1.000000000000000000, 0.9238795325112867385, 1.000000000000000000, 0.9238795325112867385, 1.000000000000000000, 0.9238795325112867385, 1.000000000000000000, 0.9238795325112867385, 1.000000000000000000, 0.9238795325112867385, 1.000000000000000000, 0.9238795325112867385, 1.000000000000000000, 0.9238795325112867385, 1.000000000000000000, 0.9238795325112867385, 1.000000000000000000, 0.9238795325112867385, 1.000000000000000000, 0.9238795325112867385, 1.000000000000000000, 0.9238795325112867385, 1.000000000000000000, 0.9238795325112867385, 1.000000000000000000, 0.9238795325112867385, 1.000000000000000000, 0.9238795325112867385, 1.000000000000000000, 0.9238795325112867385, 1.000000000000000000, 0.9238795325112867385, 1.000000000000000000, 0.9238795325112867385, 1.000000000000000000, 0.9238795325112867385, 1.000000000000000000, 0.9238795325112867385, 1.000000000000000000, 0.9238795325112867385, 1.000000000000000000, 0.9238795325112867385, 1.000000000000000000, 0.9238795325112867385, 1.000000000000000000, 0.9238795325112867385, 1.000000000000000000, 0.9238795325112867385, 1.000000000000000000, 0.9238795325112867385, 1.000000000000000000, 0.9238795325112867385, 1.000000000000000000, 0.9238795325112867385, 1.000000000000000000, 0.9238795325112867385, 1.000000000000000000, 0.9238795325112867385, 1.000000000000000000, 0.9238795325112867385, 1.000000000000000000, 0.9238795325112867385, 1.000000000000000000, 0.9238795325112867385, 1.000000000000000000, 0.9238795325112867385, 1.000000000000000000, 0.9238795325112867385, 1.000000000000000000, 0.9238795325112867385, 1.000000000000000000, 0.9238795325112867385, 1.000000000000000000, 0.9238795325112867385, 1.000000000000000000, 0.9238795325112867385, 1.000000000000000000, 0.9238795325112867385, 1.000000000000000000, 0.9238795325112867385, 1.000000000000000000, 0.9238795325112867385, 1.000000000000000000, 0.9238795325112867385, 1.000000000000000000, 0.9238795325112867385, 1.000000000000000000, 0.9238795325112867385, 1.000000000000000000, 0.9238795325112867385, 1.000000000000000000, 0.9238795325112867385, 1.000000000000000000, 0.9238795325112867385, 1.000000000000000000, 0.9238795325112867385, 1.000000000000000000, 0.9238795325112867385, 1.000000000000000000, 0.9238795325112867385, 1.000000000000000000, 0.9238795325112867385, 1.000000000000000000, 0.9238795325112867385, 1.000000000000000000, 0.9238795325112867385, 1.000000000000000000, 0.9238795325112867385, 1.000000000000000000, 0.9238795325112867385, 1.000000000000000000, 0.9238795325112867385, 1.000000000000000000, 0.9238795325112867385, 1.000000000000000000, 0.9238795325112867385, 1.000000000000000000, 0.9238795325112867385, 1.000000000000000000, 0.9238795325112867385, 1.000000000000000000, 0.9238795325112867385, 1.000000000000000000, 0.9238795325112867385, 1.000000000000000000, 0.9238795325112867385, 1.000000000000000000, 0.9238795325112867385, 1.000000000000000000, 0.9238795325112867385, 1.000000000000000000, 0.9238795325112867385, 1.000000000000000000, 0.9238795325112867385, 1.000000000000000000, 0.9238795325112867385, 1.000000000000000000, 0.9238795325112867385, 1.000000000000000000, 0.9238795325112867385, 1.000000000000000000, 0.9238795325112867385, 1.000000000000000000, 0.9238795325112867385, 1.000000000000000000, 0.9238795325112867385, 1.000000000000000000, 0.9238795325112867385, 1.000000000000000000, 0.9238795325112867385, 1.000000000000000000, 0.9238795325112867385, 1.000000000000000000, 0.9238795325112867385, 1.000000000000000000, 0.9238795325112867385, 1.000000000000000000, 0.9238795325112867385, 1.000000000000000000, 0.9238795325112867385, 1.000000000000000000, 0.9238795325112867385, 1.000000000000000000, 0.9238795325112867385, 1.000000000000000000, 0.9238795325112867385, 1.000000000000000000, 0.9238795325112867385, 1.000000000000000000, 0.9238795325112867385, 1.000000000000000000, 0.9238795325112867385, 1.000000000000000000, 0.9238795325112867385, 1.000000000000000000, 0.9238795325112867385, 1.000000000000000000, 0.9238795325112867385, 1.000000000000000000, 0.9238795325112867385, 1.000000000000000000, 0.9238795325112867385, 1.000000000000000000, 0.9238795325112867385, 1.000000000000000000, 0.9238795325112867385, 1.000000000000000000, 0.9238795325112867385, 1.000000000000000000, 0.9238795325112867385, 1.000000000000000000, 0.9238795325112867385, 1.000000000000000000, 0.9238795325112867385, 1.000000000000000000, 0.9238795325112867385, 1.000000000000000000, 0.9238795325112867385, 1.000000000000000000, 0.9238795325112867385, 1.000000000000000000, 0.9238795325112867385, 1.000000000000000000, 0.9238795325112867385, 1.000000000000000000, 0.9238795325112867385, 1.000000000000000000, 0.9238795325112867385, 1.000000000000000000, 0.9238795325112867385, 1.000000000000000000, 0.9238795325112867385, 1.000000000000000000, 0.9238795325112867385, 1.000000000000000000, 0.9238795325112867385, 1.000000000000000000, 0.9493988134329905959, 0.9660720450733824016, 0.9660720450733824016, 0.9660720450733824016) ) ) 
 REPRESENTATION_ITEM ( '' )  SURFACE ( )  );
#53164=CARTESIAN_POINT ( 'NONE',  ( 3.594042629939374400, 89.53052393364181683, -6.225082831242716885 ) ) ;
#53168=CARTESIAN_POINT ( 'NONE',  ( 1.469576158976823947E-15, 101.5625000040967763, 8.000000000000000000 ) ) ;
#53177=CARTESIAN_POINT ( 'NONE',  ( -7.188101187500001821, 95.56250000204838102, -2.977408999572650483 ) ) ;
#53201=CARTESIAN_POINT ( 'NONE',  ( 5.082755093536324154, 3.656249997951610542, 5.082755093536326818 ) ) ;
#53202=AXIS2_PLACEMENT_3D ( 'NONE', #62464, #22099, #45862 ) ;
#53205=CARTESIAN_POINT ( 'NONE',  ( -7.188101187500000044, 117.0312500020483810, 0.000000000000000000 ) ) ;
#53206=CARTESIAN_POINT ( 'NONE',  ( 4.898587196589412829E-16, 3.187499995903220640, -8.000000000000000000 ) ) ;
#53210=DIRECTION ( 'NONE',  ( 0.000000000000000000, 0.000000000000000000, 1.000000000000000000 ) ) ;
#53212=CARTESIAN_POINT ( 'NONE',  ( -3.313708498984765161, 10.03125000000000178, 7.999999999999998224 ) ) ;
#53214=CARTESIAN_POINT ( 'NONE',  ( 8.000000000000000000, 112.3437499999999858, -3.313708498984762496 ) ) ;
#53215=CARTESIAN_POINT ( 'NONE',  ( -1.469576158976823947E-15, 24.93749999590322375, 8.000000000000000000 ) ) ;
#53225=CARTESIAN_POINT ( 'NONE',  ( -1.469576158976823947E-15, 2.625000000000000444, 8.000000000000000000 ) ) ;
#53226=CARTESIAN_POINT ( 'NONE',  ( -5.082755093536324154, 103.3437500020483668, 5.082755093536326818 ) ) ;
#53231=ADVANCED_FACE ( 'NONE', ( #2885 ), #25873, .F. ) ;
#53232=CARTESIAN_POINT ( 'NONE',  ( 1.320432766682874540E-15, 114.4062500020483810, 7.188101187500000044 ) ) ;
#53238=LINE ( 'NONE', #52131, #43775 ) ;
#53239=CARTESIAN_POINT ( 'NONE',  ( -4.898587196589412829E-16, 108.1250000000000000, -8.000000000000000000 ) ) ;
#53250=DIRECTION ( 'NONE',  ( -0.000000000000000000, 1.000000000000000000, -0.000000000000000000 ) ) ;
#53256=CARTESIAN_POINT ( 'NONE',  ( 4.898587196589412829E-16, 3.375000000000000444, -8.000000000000000000 ) ) ;
#53258=CARTESIAN_POINT ( 'NONE',  ( -2.977408999572650039, 0.9374999979516102089, -7.188101187500001821 ) ) ;
#53260=( BOUNDED_CURVE ( )  B_SPLINE_CURVE ( 2, ( #35523, #62774, #16372, #4341, #68083, #51464, #16012, #21304, #50719 ),
 .UNSPECIFIED., .F., .F. ) 
 B_SPLINE_CURVE_WITH_KNOTS ( ( 3, 2, 2, 2, 3 ),
 ( 0.6249999999999998890, 0.6319444444444443088, 0.6388888888888888395, 0.6458333333333333703, 0.6527777777777777901 ),
 .UNSPECIFIED. ) 
 CURVE ( )  GEOMETRIC_REPRESENTATION_ITEM ( )  RATIONAL_B_SPLINE_CURVE ( ( 1.000000000000001110, 0.9238795325112855172, 1.000000000000000000, 0.9238795325112867385, 1.000000000000000000, 0.9238795325112867385, 1.000000000000000000, 0.9238795325112867385, 1.000000000000000000 ) ) 
 REPRESENTATION_ITEM ( '' )  );
#53263=EDGE_CURVE ( 'NONE', #31201, #20088, #68588, .T. ) ;
#53264=CARTESIAN_POINT ( 'NONE',  ( -8.000000000000001776, 6.843750000000000888, 3.313708498984759387 ) ) ;
#53287=CARTESIAN_POINT ( 'NONE',  ( 1.469576158976823947E-15, 120.8750000000000000, 8.000000000000000000 ) ) ;
#53293=CARTESIAN_POINT ( 'NONE',  ( -3.313708498984760720, 15.28124999590322197, -8.000000000000000000 ) ) ;
#53315=CARTESIAN_POINT ( 'NONE',  ( -4.401442555609581635E-16, 123.7812500020483810, -7.188101187500000044 ) ) ;
#53319=CARTESIAN_POINT ( 'NONE',  ( -2.977408999572651815, 98.93750000204838102, 7.188101187500000933 ) ) ;
#53322=CARTESIAN_POINT ( 'NONE',  ( 4.519822870821364802, 0.3270240920704938770, -6.395220799012816038 ) ) ;
#53341=VERTEX_POINT ( 'NONE', #63016 ) ;
#53347=CARTESIAN_POINT ( 'NONE',  ( -7.188101187500002709, 14.81249999795161543, 2.977408999572649151 ) ) ;
#53350=CARTESIAN_POINT ( 'NONE',  ( 2.977408999572650927, 14.62499999795161010, -7.188101187500001821 ) ) ;
#53363=CARTESIAN_POINT ( 'NONE',  ( -7.188101187500001821, 115.0625000020483952, -2.977408999572650483 ) ) ;
#53369=CARTESIAN_POINT ( 'NONE',  ( 4.401442555609581635E-16, 23.34374999795161543, -7.188101187500000044 ) ) ;
#53376=CARTESIAN_POINT ( 'NONE',  ( -7.188101187500001821, 100.4375000020483668, -2.977408999572650483 ) ) ;
#53406=CARTESIAN_POINT ( 'NONE',  ( 5.082755093536326818, 117.2187500020483810, 5.082755093536325042 ) ) ;
#53436=CARTESIAN_POINT ( 'NONE',  ( -1.320432766682874540E-15, 13.96874999795161187, 7.188101187500000044 ) ) ;
#53453=CARTESIAN_POINT ( 'NONE',  ( -3.313708498984765161, 26.53125000000000355, 7.999999999999998224 ) ) ;
#53463=CARTESIAN_POINT ( 'NONE',  ( -5.082755093536326818, 7.406249997951610986, 5.082755093536325042 ) ) ;
#53465=CARTESIAN_POINT ( 'NONE',  ( 5.082755093536325042, 116.4687500020483810, -5.082755093536325930 ) ) ;
#53474=AXIS2_PLACEMENT_3D ( 'NONE', #66142, #9179, #15201 ) ;
#53477=CARTESIAN_POINT ( 'NONE',  ( 3.313708498984760276, 105.2187500040967905, -8.000000000000000000 ) ) ;
#53490=CARTESIAN_POINT ( 'NONE',  ( 2.977408999572651815, 21.56249999795161898, 7.188101187500000933 ) ) ;
#53492=CARTESIAN_POINT ( 'NONE',  ( 5.082755093536326818, 93.59375000204838102, 5.082755093536325042 ) ) ;
#53509=CARTESIAN_POINT ( 'NONE',  ( -5.656854249492380582, 123.5000000040967905, -5.656854249492380582 ) ) ;
#53514=ADVANCED_FACE ( 'NONE', ( #38443 ), #22743, .T. ) ;
#53516=CARTESIAN_POINT ( 'NONE',  ( 3.594050593751920264, 89.53052362291684574, -6.225078233346985179 ) ) ;
#53538=CARTESIAN_POINT ( 'NONE',  ( -4.898587196589412829E-16, 96.31250000409677625, -8.000000000000000000 ) ) ;
#53545=ORIENTED_EDGE ( 'NONE', *, *, #25483, .T. ) ;
#53547=CARTESIAN_POINT ( 'NONE',  ( -7.188101187500001821, 100.0625000020483952, -2.977408999572650483 ) ) ;
#53552=CARTESIAN_POINT ( 'NONE',  ( 7.188101187500000044, 27.46874999795161543, 0.000000000000000000 ) ) ;
#53567=CARTESIAN_POINT ( 'NONE',  ( -5.656854249492381470, 2.249999995903220196, 5.656854249492379694 ) ) ;
#53569=CARTESIAN_POINT ( 'NONE',  ( -7.188101187500001821, 5.999999997951610098, -2.977408999572651371 ) ) ;
#53573=CARTESIAN_POINT ( 'NONE',  ( -4.401442555609581635E-16, 113.6562500020483952, -7.188101187500000044 ) ) ;
#53597=CARTESIAN_POINT ( 'NONE',  ( -7.188101187500000044, 103.1562500020483810, 0.000000000000000000 ) ) ;
#53602=CARTESIAN_POINT ( 'NONE',  ( -7.188101187500000044, 109.5312500020483810, 0.000000000000000000 ) ) ;
#53609=CARTESIAN_POINT ( 'NONE',  ( -3.313708498984708317, 108.7812500000000142, 8.000000000000053291 ) ) ;
#53613=EDGE_CURVE ( 'NONE', #9713, #54330, #28782, .T. ) ;
#53626=CARTESIAN_POINT ( 'NONE',  ( 8.000000000000000000, 7.593750000000001776, -3.313708498984761608 ) ) ;
#53628=CARTESIAN_POINT ( 'NONE',  ( 5.082755093536324154, 4.781249997951610986, 5.082755093536326818 ) ) ;
#53631=CARTESIAN_POINT ( 'NONE',  ( 3.313708498984765161, 122.6562500040968047, 7.999999999999998224 ) ) ;
#53634=VECTOR ( 'NONE', #4309, 1000.000000000000000 ) ;
#53635=CARTESIAN_POINT ( 'NONE',  ( -3.313708498984760276, 6.468750000000001776, -8.000000000000000000 ) ) ;
#53655=CARTESIAN_POINT ( 'NONE',  ( -4.898587196589412829E-16, 117.1250000000000000, -8.000000000000000000 ) ) ;
#53657=VERTEX_POINT ( 'NONE', #35031 ) ;
#53659=CARTESIAN_POINT ( 'NONE',  ( 8.000000000000000000, 17.81249999590322375, 0.000000000000000000 ) ) ;
#53673=ADVANCED_FACE ( 'NONE', ( #70095 ), #51996, .T. ) ;
#53681=CARTESIAN_POINT ( 'NONE',  ( 2.977408999572650039, 120.6875000020483952, -7.188101187500000933 ) ) ;
#53688=CARTESIAN_POINT ( 'NONE',  ( -4.401442555609581635E-16, 90.78125000204836681, -7.188101187500000044 ) ) ;
#53692=ORIENTED_EDGE ( 'NONE', *, *, #63473, .F. ) ;
#53693=ORIENTED_EDGE ( 'NONE', *, *, #16099, .T. ) ;
#53704=CARTESIAN_POINT ( 'NONE',  ( -3.313708498984842432, 112.7187499999999858, -7.999999999999920064 ) ) ;
#53714=CARTESIAN_POINT ( 'NONE',  ( 7.188101187499999156, 13.87499999795161187, 2.977408999572654924 ) ) ;
#53717=CARTESIAN_POINT ( 'NONE',  ( 2.977408999572651815, 9.562499997951608322, 7.188101187500000933 ) ) ;
#53731=CARTESIAN_POINT ( 'NONE',  ( -7.188101187500000044, 116.6562500020483810, 0.000000000000000000 ) ) ;
#53736=CARTESIAN_POINT ( 'NONE',  ( -7.188101187500002709, 20.81249999795161543, 2.977408999572649151 ) ) ;
#53738=LINE ( 'NONE', #9194, #32805 ) ;
#53742=CARTESIAN_POINT ( 'NONE',  ( -4.401442555609581635E-16, 98.65625000204838102, -7.188101187500000044 ) ) ;
#53752=PLANE ( 'NONE',  #74017 ) ;
#53758=CARTESIAN_POINT ( 'NONE',  ( 1.469576158976823947E-15, 108.8750000000000000, 8.000000000000000000 ) ) ;
#53759=FACE_OUTER_BOUND ( 'NONE', #39336, .T. ) ;
#53766=CARTESIAN_POINT ( 'NONE',  ( 2.143584681480918963, 88.75185463835309463, -8.000000000000000000 ) ) ;
#53771=CARTESIAN_POINT ( 'NONE',  ( -5.656854249492381470, 5.249999995903221084, 5.656854249492379694 ) ) ;
#53773=CARTESIAN_POINT ( 'NONE',  ( 5.082755093536325042, 114.5937500020483810, -5.082755093536325930 ) ) ;
#53779=EDGE_CURVE ( 'NONE', #61205, #11312, #69716, .T. ) ;
#53781=CARTESIAN_POINT ( 'NONE',  ( 5.656854249492381470, 109.0624999999999858, 5.656854249492379694 ) ) ;
#53789=CARTESIAN_POINT ( 'NONE',  ( 0.000000000000000000, 75.00000000000000000, 11.00000000000000000 ) ) ;
#53800=CARTESIAN_POINT ( 'NONE',  ( -5.082755093536325042, 14.90624999795161187, -5.082755093536325930 ) ) ;
#53810=CARTESIAN_POINT ( 'NONE',  ( -3.313708498984816231, 93.96875000409676204, 7.999999999999943157 ) ) ;
#53814=AXIS2_PLACEMENT_3D ( 'NONE', #32085, #9821, #55106 ) ;
#53816=ADVANCED_FACE ( 'NONE', ( #54220 ), #24424, .T. ) ;
#53819=CARTESIAN_POINT ( 'NONE',  ( 7.999999999999998224, 23.90625000000000000, 3.313708498984766493 ) ) ;
#53829=CARTESIAN_POINT ( 'NONE',  ( 2.977408999572650927, 2.249999997951610098, -7.188101187500000933 ) ) ;
#53832=CARTESIAN_POINT ( 'NONE',  ( -7.188101187500000044, 118.5312500020483810, 0.000000000000000000 ) ) ;
#53838=ORIENTED_EDGE ( 'NONE', *, *, #22351, .T. ) ;
#53841=CARTESIAN_POINT ( 'NONE',  ( -1.469576158976823947E-15, 15.93749999590322197, 8.000000000000000000 ) ) ;
#53856=CARTESIAN_POINT ( 'NONE',  ( -5.082755093536325042, 26.90624999795161898, -5.082755093536325930 ) ) ;
#53858=CARTESIAN_POINT ( 'NONE',  ( 1.320432766682874540E-15, 94.90625000204838102, 7.188101187500000044 ) ) ;
#53878=CARTESIAN_POINT ( 'NONE',  ( -8.000000000000000000, 123.6875000040967905, 0.000000000000000000 ) ) ;
#53883=CARTESIAN_POINT ( 'NONE',  ( -5.082755093536324154, 90.21875000204838102, 5.082755093536326818 ) ) ;
#53890=CARTESIAN_POINT ( 'NONE',  ( -3.313708498984727413, 121.7187499999999858, -8.000000000000033751 ) ) ;
#53897=ORIENTED_EDGE ( 'NONE', *, *, #71055, .F. ) ;
#53903=CARTESIAN_POINT ( 'NONE',  ( -8.000000000000000000, 98.18750000409677625, 0.000000000000000000 ) ) ;
#53912=CARTESIAN_POINT ( 'NONE',  ( 5.082755093536325042, 99.59375000204838102, -5.082755093536325930 ) ) ;
#53914=CARTESIAN_POINT ( 'NONE',  ( 5.656854249492381470, 119.7500000040967905, 5.656854249492379694 ) ) ;
#53935=CARTESIAN_POINT ( 'NONE',  ( -3.313708498984765161, 2.343749995903220196, 7.999999999999998224 ) ) ;
#53937=CARTESIAN_POINT ( 'NONE',  ( -7.188101187500000044, 12.09374999795161187, -8.802885111219163269E-16 ) ) ;
#53940=CARTESIAN_POINT ( 'NONE',  ( 5.082755093536325042, 110.4687500020483810, -5.082755093536325930 ) ) ;
#53960=CARTESIAN_POINT ( 'NONE',  ( -5.082755093536325930, 104.4687500020483952, -5.082755093536325930 ) ) ;
#53967=CARTESIAN_POINT ( 'NONE',  ( 2.977408999572654480, 108.5000000020483810, 7.188101187499999156 ) ) ;
#53972=ORIENTED_EDGE ( 'NONE', *, *, #44154, .T. ) ;
#53977=CARTESIAN_POINT ( 'NONE',  ( -7.188101187500000933, 1.499999997951610098, -2.977408999572651371 ) ) ;
#53982=ORIENTED_EDGE ( 'NONE', *, *, #27022, .F. ) ;
#53983=CARTESIAN_POINT ( 'NONE',  ( 3.313708498984721640, 20.53124999590322020, 8.000000000000039080 ) ) ;
#53989=ORIENTED_EDGE ( 'NONE', *, *, #10880, .T. ) ;
#53990=CARTESIAN_POINT ( 'NONE',  ( 8.000000000000000000, 13.50000000000000178, 0.000000000000000000 ) ) ;
#53992=CARTESIAN_POINT ( 'NONE',  ( 4.401442555609581635E-16, 5.343749997951610986, -7.188101187500000044 ) ) ;
#53993=CARTESIAN_POINT ( 'NONE',  ( 8.000000000000001776, 118.3437500040967763, 3.313708498984759387 ) ) ;
#53996=EDGE_CURVE ( 'NONE', #43418, #69933, #55309, .T. ) ;
#54005=CARTESIAN_POINT ( 'NONE',  ( -3.313708498984765161, 16.03125000000000355, 7.999999999999998224 ) ) ;
#54019=CARTESIAN_POINT ( 'NONE',  ( -3.313708498984765161, 12.84374999590322197, 7.999999999999998224 ) ) ;
#54023=CARTESIAN_POINT ( 'NONE',  ( -3.313708498984762496, 114.7812500000000000, 7.999999999999998224 ) ) ;
#54028=CARTESIAN_POINT ( 'NONE',  ( 3.313708498984762052, 12.09374999590322020, -8.000000000000000000 ) ) ;
#54051=CARTESIAN_POINT ( 'NONE',  ( -7.188101187500000044, 124.1562500020483810, 0.000000000000000000 ) ) ;
#54052=CARTESIAN_POINT ( 'NONE',  ( 8.000000000000001776, 119.6562499999999858, 3.313708498984759387 ) ) ;
#54057=CARTESIAN_POINT ( 'NONE',  ( 7.188101187500001821, 92.00000000204838102, -2.977408999572651371 ) ) ;
#54076=CARTESIAN_POINT ( 'NONE',  ( 2.977408999572652260, 27.56249999795161187, 7.188101187500000044 ) ) ;
#54084=CARTESIAN_POINT ( 'NONE',  ( -7.188101187500000044, 20.71874999795161543, -8.802885111219163269E-16 ) ) ;
#54086=CARTESIAN_POINT ( 'NONE',  ( 1.714702201362999334, 124.5469634165301898, -7.773580895186444906 ) ) ;
#54087=CARTESIAN_POINT ( 'NONE',  ( 2.977408999572650927, 11.62499999795161365, -7.188101187500001821 ) ) ;
#54091=CARTESIAN_POINT ( 'NONE',  ( 4.898587196589412829E-16, 12.37500000000000178, -8.000000000000000000 ) ) ;
#54094=EDGE_CURVE ( 'NONE', #25519, #51832, #15772, .T. ) ;
#54099=AXIS2_PLACEMENT_3D ( 'NONE', #58776, #65527, #18773 ) ;
#54100=CARTESIAN_POINT ( 'NONE',  ( 5.082755093536325042, 111.5937500020483810, -5.082755093536325930 ) ) ;
#54104=CARTESIAN_POINT ( 'NONE',  ( -1.320432766682874540E-15, 25.59374999795161543, 7.188101187500000044 ) ) ;
#54105=VERTEX_POINT ( 'NONE', #55718 ) ;
#54112=CARTESIAN_POINT ( 'NONE',  ( 7.188101187500002709, 96.68750000204836681, 2.977408999572649151 ) ) ;
#54130=CARTESIAN_POINT ( 'NONE',  ( 3.313708498984815343, 97.71875000409676204, -7.999999999999944933 ) ) ;
#54139=CARTESIAN_POINT ( 'NONE',  ( -7.999999999999998224, 116.0937500000000000, 3.313708498984766049 ) ) ;
#54142=CARTESIAN_POINT ( 'NONE',  ( -2.009711600462664727, 124.6176558922824569, -7.638752868991079303 ) ) ;
#54145=CARTESIAN_POINT ( 'NONE',  ( -5.082755093536325930, 108.9687500020483810, -5.082755093536325930 ) ) ;
#54164=CARTESIAN_POINT ( 'NONE',  ( 0.000000000000000000, 125.0000000000000000, 0.000000000000000000 ) ) ;
#54169=ORIENTED_EDGE ( 'NONE', *, *, #5832, .T. ) ;
#54176=CARTESIAN_POINT ( 'NONE',  ( 7.188101187500000044, 12.84374999795161187, 0.000000000000000000 ) ) ;
#54186=CARTESIAN_POINT ( 'NONE',  ( -7.999999999999998224, 93.78125000409679046, 3.313708498984766049 ) ) ;
#54192=CARTESIAN_POINT ( 'NONE',  ( 8.000000000000000000, 21.00000000000000355, 0.000000000000000000 ) ) ;
#54202=CARTESIAN_POINT ( 'NONE',  ( -7.188101187500000933, 5.624999997951610986, -2.977408999572651371 ) ) ;
#54205=CARTESIAN_POINT ( 'NONE',  ( 7.188101187500001821, 120.8750000020483810, -2.977408999572651371 ) ) ;
#54209=DIRECTION ( 'NONE',  ( 0.000000000000000000, 0.000000000000000000, 1.000000000000000000 ) ) ;
#54218=CARTESIAN_POINT ( 'NONE',  ( -5.656854249492380582, 99.31250000000000000, -5.656854249492380582 ) ) ;
#54220=FACE_OUTER_BOUND ( 'NONE', #67656, .T. ) ;
#54233=CARTESIAN_POINT ( 'NONE',  ( -1.320432766682874540E-15, 27.46874999795161543, 7.188101187500000044 ) ) ;
#54235=CARTESIAN_POINT ( 'NONE',  ( -5.082755093536324154, 93.21875000204838102, 5.082755093536326818 ) ) ;
#54240=DIRECTION ( 'NONE',  ( 0.000000000000000000, 0.000000000000000000, 1.000000000000000000 ) ) ;
#54252=CARTESIAN_POINT ( 'NONE',  ( 7.999999999999998224, 23.71874999590322020, 3.313708498984766049 ) ) ;
#54259=CARTESIAN_POINT ( 'NONE',  ( -2.977408999572650927, 89.75000000204839523, -7.188101187500001821 ) ) ;
#54278=CARTESIAN_POINT ( 'NONE',  ( 1.469576158976823947E-15, 110.5625000040967905, 8.000000000000000000 ) ) ;
#54282=CARTESIAN_POINT ( 'NONE',  ( 3.313708498984760720, 99.21875000409680467, -8.000000000000000000 ) ) ;
#54283=ADVANCED_FACE ( 'NONE', ( #52649 ), #63967, .T. ) ;
#54284=DIRECTION ( 'NONE',  ( -0.8660254037844397068, -0.4999999999999981126, 0.000000000000000000 ) ) ;
#54292=CARTESIAN_POINT ( 'NONE',  ( -2.977408999572650927, 98.37500000204840944, -7.188101187500001821 ) ) ;
#54293=CARTESIAN_POINT ( 'NONE',  ( 3.313708498984761608, 16.59374999590322375, -8.000000000000000000 ) ) ;
#54294=CARTESIAN_POINT ( 'NONE',  ( 8.000000000000000000, 119.9375000040967763, -9.797174393178825657E-16 ) ) ;
#54314=CARTESIAN_POINT ( 'NONE',  ( -5.656854249492381470, 5.249999995903221084, 5.656854249492379694 ) ) ;
#54317=CARTESIAN_POINT ( 'NONE',  ( 2.977408999572650927, 10.12499999795161187, -7.188101187500001821 ) ) ;
#54320=CARTESIAN_POINT ( 'NONE',  ( -7.188101187500000044, 109.5312500020483810, 0.000000000000000000 ) ) ;
#54330=VERTEX_POINT ( 'NONE', #33830 ) ;
#54338=CARTESIAN_POINT ( 'NONE',  ( -5.082755093536324154, 107.8437500020483810, 5.082755093536326818 ) ) ;
#54343=CARTESIAN_POINT ( 'NONE',  ( 5.082755093536326818, 107.0937500020483810, 5.082755093536325042 ) ) ;
#54353=CARTESIAN_POINT ( 'NONE',  ( 9.797174393178825657E-16, 125.0000000000000000, -8.000000000000000000 ) ) ;
#54372=CARTESIAN_POINT ( 'NONE',  ( 5.082755093536325930, 0.6562499979516100979, -5.082755093536325930 ) ) ;
#54373=CARTESIAN_POINT ( 'NONE',  ( 3.313708498984765161, 116.6562500040968047, 7.999999999999998224 ) ) ;
#54377=CARTESIAN_POINT ( 'NONE',  ( 0.000000000000000000, 125.0000000000000000, 0.000000000000000000 ) ) ;
#54386=DIRECTION ( 'NONE',  ( 0.000000000000000000, 0.000000000000000000, 1.000000000000000000 ) ) ;
#54400=CARTESIAN_POINT ( 'NONE',  ( -5.656854249492378806, 110.1875000000000000, 5.656854249492381470 ) ) ;
#54405=CARTESIAN_POINT ( 'NONE',  ( -5.656854249492381470, 18.74999999590322020, 5.656854249492379694 ) ) ;
#54408=CARTESIAN_POINT ( 'NONE',  ( 5.656854249492379694, 114.1250000040967763, -5.656854249492380582 ) ) ;
#54418=CARTESIAN_POINT ( 'NONE',  ( -5.656854249492378806, 107.3750000040967763, 5.656854249492381470 ) ) ;
#54433=CARTESIAN_POINT ( 'NONE',  ( -2.977408999572651815, 91.43750000204838102, 7.188101187500000933 ) ) ;
#54450=AXIS2_PLACEMENT_3D ( 'NONE', #17797, #53250, #28742 ) ;
#54462=ORIENTED_EDGE ( 'NONE', *, *, #25789, .T. ) ;
#54464=CARTESIAN_POINT ( 'NONE',  ( -5.082755093536325042, 20.53124999795161543, -5.082755093536325930 ) ) ;
#54467=CARTESIAN_POINT ( 'NONE',  ( -2.977408999572650039, 13.31249999795161187, -7.188101187500001821 ) ) ;
#54480=CARTESIAN_POINT ( 'NONE',  ( -7.188101187500000044, 110.6562500020483810, 0.000000000000000000 ) ) ;
#54484=CARTESIAN_POINT ( 'NONE',  ( -7.188101187500000044, 23.71874999795161543, -8.802885111219163269E-16 ) ) ;
#54491=CARTESIAN_POINT ( 'NONE',  ( -7.188101187500000044, 94.53125000204836681, 0.000000000000000000 ) ) ;
#54517=CIRCLE ( 'NONE', #11122, 8.000000000000000000 ) ;
#54519=CARTESIAN_POINT ( 'NONE',  ( 1.320432766682874540E-15, 111.0312500020483810, 7.188101187500000044 ) ) ;
#54546=CARTESIAN_POINT ( 'NONE',  ( -7.188101187500000933, 11.99999999795161187, -2.977408999572651371 ) ) ;
#54549=VERTEX_POINT ( 'NONE', #53758 ) ;
#54563=CARTESIAN_POINT ( 'NONE',  ( 4.898587196589412829E-16, 24.37500000000000355, -8.000000000000000000 ) ) ;
#54565=VERTEX_POINT ( 'NONE', #42417 ) ;
#54574=CARTESIAN_POINT ( 'NONE',  ( -5.082755093536325042, 4.031249997951610986, -5.082755093536325930 ) ) ;
#54579=CARTESIAN_POINT ( 'NONE',  ( -2.977408999572651815, 112.8125000020483952, 7.188101187500000933 ) ) ;
#54589=DIRECTION ( 'NONE',  ( -0.000000000000000000, 1.000000000000000000, -0.000000000000000000 ) ) ;
#54594=CARTESIAN_POINT ( 'NONE',  ( 1.469576158976823947E-15, 92.37499999999998579, 8.000000000000000000 ) ) ;
#54596=DIRECTION ( 'NONE',  ( -0.000000000000000000, 1.000000000000000000, -0.000000000000000000 ) ) ;
#54608=CARTESIAN_POINT ( 'NONE',  ( 5.082755093536325042, 90.96875000204838102, -5.082755093536325930 ) ) ;
#54617=DIRECTION ( 'NONE',  ( 0.000000000000000000, 0.000000000000000000, 1.000000000000000000 ) ) ;
#54624=CARTESIAN_POINT ( 'NONE',  ( -5.656854249492378806, 102.6875000000000000, 5.656854249492381470 ) ) ;
#54626=CARTESIAN_POINT ( 'NONE',  ( 5.656854249492379694, 121.6250000040967905, -5.656854249492380582 ) ) ;
#54631=CARTESIAN_POINT ( 'NONE',  ( -2.977408999572651815, 90.31250000204838102, 7.188101187500000933 ) ) ;
#54653=CARTESIAN_POINT ( 'NONE',  ( 3.313708498984765161, 95.65625000409679046, 7.999999999999998224 ) ) ;
#54661=CARTESIAN_POINT ( 'NONE',  ( -4.898587196589412829E-16, 93.12499999999998579, -8.000000000000000000 ) ) ;
#54664=CARTESIAN_POINT ( 'NONE',  ( 7.188101187500002709, 94.81250000204838102, 2.977408999572649151 ) ) ;
#54674=( BOUNDED_CURVE ( )  B_SPLINE_CURVE ( 2, ( #63050, #44966, #83, #23060, #11375, #69089, #17395, #67972, #40419 ),
 .UNSPECIFIED., .F., .F. ) 
 B_SPLINE_CURVE_WITH_KNOTS ( ( 3, 2, 2, 2, 3 ),
 ( 0.2083333333333333148, 0.2152777777777777624, 0.2222222222222221821, 0.2291666666666666574, 0.2361111111111111049 ),
 .UNSPECIFIED. ) 
 CURVE ( )  GEOMETRIC_REPRESENTATION_ITEM ( )  RATIONAL_B_SPLINE_CURVE ( ( 1.000000000000000222, 0.9238795325112864054, 1.000000000000000000, 0.9238795325112867385, 1.000000000000000000, 0.9238795325112867385, 1.000000000000000000, 0.9238795325112867385, 1.000000000000000000 ) ) 
 REPRESENTATION_ITEM ( '' )  );
#54689=CARTESIAN_POINT ( 'NONE',  ( -1.320432766682874540E-15, 12.46874999795161187, 7.188101187500000044 ) ) ;
#54691=DIRECTION ( 'NONE',  ( -0.000000000000000000, 1.000000000000000000, -0.000000000000000000 ) ) ;
#54692=CARTESIAN_POINT ( 'NONE',  ( 2.977408999572654480, 113.0000000020483810, 7.188101187499999156 ) ) ;
#54702=VERTEX_POINT ( 'NONE', #66931 ) ;
#54711=CARTESIAN_POINT ( 'NONE',  ( 7.188101187500000044, 100.9062500020483810, -8.802885111219163269E-16 ) ) ;
#54719=CARTESIAN_POINT ( 'NONE',  ( -2.977408999572651815, 111.3125000020483810, 7.188101187500000933 ) ) ;
#54726=CARTESIAN_POINT ( 'NONE',  ( -1.469576158976823947E-15, 1.125000000000000222, 8.000000000000000000 ) ) ;
#54731=CARTESIAN_POINT ( 'NONE',  ( 5.082755093536324154, 2.156249997951610542, 5.082755093536326818 ) ) ;
#54742=VERTEX_POINT ( 'NONE', #9600 ) ;
#54746=CARTESIAN_POINT ( 'NONE',  ( -2.977408999572654480, 10.49999999795161010, 7.188101187499999156 ) ) ;
#54747=CARTESIAN_POINT ( 'NONE',  ( 5.656854249492379694, 114.1250000040967763, -5.656854249492380582 ) ) ;
#54754=CARTESIAN_POINT ( 'NONE',  ( 8.000000000000000000, 95.75000000000000000, -9.797174393178825657E-16 ) ) ;
#54765=CARTESIAN_POINT ( 'NONE',  ( 7.999999999999998224, 26.71874999590322375, 3.313708498984766049 ) ) ;
#54771=CARTESIAN_POINT ( 'NONE',  ( -4.898587196589412829E-16, 111.1250000000000000, -8.000000000000000000 ) ) ;
#54776=CARTESIAN_POINT ( 'NONE',  ( 3.313708498984762496, 19.03124999590322375, 7.999999999999998224 ) ) ;
#54779=CARTESIAN_POINT ( 'NONE',  ( 4.898587196589412829E-16, 1.875000000000000444, -8.000000000000000000 ) ) ;
#54799=CARTESIAN_POINT ( 'NONE',  ( -7.188101187500000044, 119.6562500020483810, 0.000000000000000000 ) ) ;
#54806=CARTESIAN_POINT ( 'NONE',  ( -7.188101187499999156, 89.75000000204839523, 2.977408999572654924 ) ) ;
#54823=EDGE_LOOP ( 'NONE', ( #47507, #1148, #71165, #2103 ) ) ;
#54831=ORIENTED_EDGE ( 'NONE', *, *, #11595, .T. ) ;
#54836=CARTESIAN_POINT ( 'NONE',  ( 2.977408999572650927, 23.24999999795161187, -7.188101187500001821 ) ) ;
#54839=CARTESIAN_POINT ( 'NONE',  ( 7.188101187500001821, 15.93749999795161543, -2.977408999572650483 ) ) ;
#54848=CARTESIAN_POINT ( 'NONE',  ( -2.977408999572650927, 108.8750000020483810, -7.188101187500001821 ) ) ;
#54859=CARTESIAN_POINT ( 'NONE',  ( -4.401442555609581635E-16, 94.15625000204838102, -7.188101187500000044 ) ) ;
#54891=CARTESIAN_POINT ( 'NONE',  ( -7.188101187500001821, 107.5625000020483810, -2.977408999572650483 ) ) ;
#54901=CARTESIAN_POINT ( 'NONE',  ( 3.313708498984721640, 26.71875000000000000, 8.000000000000039080 ) ) ;
#54904=ORIENTED_EDGE ( 'NONE', *, *, #40791, .F. ) ;
#54919=CARTESIAN_POINT ( 'NONE',  ( -1.320432766682874540E-15, 16.96874999795161543, 7.188101187500000044 ) ) ;
#54928=CARTESIAN_POINT ( 'NONE',  ( 7.188101187499999156, 4.874999997951610098, 2.977408999572654924 ) ) ;
#54933=EDGE_LOOP ( 'NONE', ( #61168, #2163, #9855, #40778 ) ) ;
#54945=CARTESIAN_POINT ( 'NONE',  ( -3.313708498984762496, 104.2812499999999858, 7.999999999999998224 ) ) ;
#54946=ORIENTED_EDGE ( 'NONE', *, *, #7668, .F. ) ;
#54947=CARTESIAN_POINT ( 'NONE',  ( 5.082755093536325930, 9.656249997951610098, -5.082755093536325930 ) ) ;
#54951=CARTESIAN_POINT ( 'NONE',  ( -4.401442555609581635E-16, 112.1562500020483952, -7.188101187500000044 ) ) ;
#54966=CARTESIAN_POINT ( 'NONE',  ( 5.656854249492379694, 95.93750000000000000, -5.656854249492380582 ) ) ;
#54983=CARTESIAN_POINT ( 'NONE',  ( -5.082755093536325930, 91.34375000204838102, -5.082755093536325930 ) ) ;
#54992=CARTESIAN_POINT ( 'NONE',  ( 1.469576158976823947E-15, 92.37499999999998579, 8.000000000000000000 ) ) ;
#54993=CARTESIAN_POINT ( 'NONE',  ( -5.082755093536326818, 19.40624999795161543, 5.082755093536325042 ) ) ;
#55019=CARTESIAN_POINT ( 'NONE',  ( 7.999999999999998224, 2.718749995903220640, 3.313708498984766049 ) ) ;
#55027=VERTEX_POINT ( 'NONE', #16713 ) ;
#55029=CARTESIAN_POINT ( 'NONE',  ( -8.000000000000000000, 95.09375000409679046, -3.313708498984761608 ) ) ;
#55039=CARTESIAN_POINT ( 'NONE',  ( 1.320432766682874540E-15, 90.03125000204838102, 7.188101187500000044 ) ) ;
#55045=CARTESIAN_POINT ( 'NONE',  ( -3.313708498984707429, 100.9062500040967905, -8.000000000000055067 ) ) ;
#55056=CYLINDRICAL_SURFACE ( 'NONE', #29673, 8.000000000000000000 ) ;
#55057=CARTESIAN_POINT ( 'NONE',  ( -5.656854249492378806, 90.87500000409677625, 5.656854249492381470 ) ) ;
#55060=CARTESIAN_POINT ( 'NONE',  ( 5.656854249492378806, 2.624999995903220196, 5.656854249492381470 ) ) ;
#55062=CARTESIAN_POINT ( 'NONE',  ( 5.082755093536325930, 8.531249997951611874, -5.082755093536325930 ) ) ;
#55065=CARTESIAN_POINT ( 'NONE',  ( -4.401442555609581635E-16, 109.1562500020483810, -7.188101187500000044 ) ) ;
#55084=CARTESIAN_POINT ( 'NONE',  ( -4.898587196589412829E-16, 114.3125000040967905, -8.000000000000000000 ) ) ;
#55085=FACE_OUTER_BOUND ( 'NONE', #10657, .T. ) ;
#55086=CARTESIAN_POINT ( 'NONE',  ( 2.977408999572650039, 98.18750000204835260, -7.188101187500000933 ) ) ;
#55092=EDGE_CURVE ( 'NONE', #38802, #7386, #30774, .T. ) ;
#55094=CARTESIAN_POINT ( 'NONE',  ( 2.977408999572650039, 106.0625000020483668, -7.188101187500001821 ) ) ;
#55098=ORIENTED_EDGE ( 'NONE', *, *, #59311, .T. ) ;
#55106=DIRECTION ( 'NONE',  ( 0.000000000000000000, 0.000000000000000000, 1.000000000000000000 ) ) ;
#55120=CARTESIAN_POINT ( 'NONE',  ( 7.188101187500001821, 11.06249999795161187, -2.977408999572650483 ) ) ;
#55121=CARTESIAN_POINT ( 'NONE',  ( -7.999999999999998224, 117.7812500040967905, 3.313708498984766493 ) ) ;
#55124=FACE_OUTER_BOUND ( 'NONE', #60581, .T. ) ;
#55138=EDGE_CURVE ( 'NONE', #44243, #53657, #4782, .T. ) ;
#55147=CARTESIAN_POINT ( 'NONE',  ( 8.000000000000000000, 109.3437499999999858, -3.313708498984762496 ) ) ;
#55153=CARTESIAN_POINT ( 'NONE',  ( -1.469576158976823947E-15, 21.93749999590322375, 8.000000000000000000 ) ) ;
#55171=EDGE_LOOP ( 'NONE', ( #68884, #25495, #18480, #39784, #1285, #50863, #63562, #68438, #65506, #45131, #69014, #27319, #26922, #34311, #19838, #32264, #17194, #59775, #73106, #44454, #51576, #57130, #70171, #52434, #65870, #35008, #46929, #62180, #21349, #11161, #67263, #41479, #26333, #71772, #11704, #41069, #59558, #57648, #37525, #32057 ) ) ;
#55178=CARTESIAN_POINT ( 'NONE',  ( 2.977408999572654480, 118.6250000020483810, 7.188101187499999156 ) ) ;
#55179=CARTESIAN_POINT ( 'NONE',  ( 3.313708498984800688, 120.0312499999999716, -7.999999999999958256 ) ) ;
#55184=CARTESIAN_POINT ( 'NONE',  ( 5.082755093536325042, 93.59375000204838102, -5.082755093536325930 ) ) ;
#55188=ORIENTED_EDGE ( 'NONE', *, *, #48641, .F. ) ;
#55194=CARTESIAN_POINT ( 'NONE',  ( 4.898587196589412829E-16, 24.37500000000000355, -8.000000000000000000 ) ) ;
#55210=CARTESIAN_POINT ( 'NONE',  ( 4.401442555609581635E-16, 23.34374999795161543, -7.188101187500000044 ) ) ;
#55214=CARTESIAN_POINT ( 'NONE',  ( 5.082755093536324154, 17.15624999795161543, 5.082755093536326818 ) ) ;
#55221=ORIENTED_EDGE ( 'NONE', *, *, #32514, .F. ) ;
#55226=CARTESIAN_POINT ( 'NONE',  ( 2.977408999572654480, 111.1250000020483810, 7.188101187499999156 ) ) ;
#55232=ORIENTED_EDGE ( 'NONE', *, *, #17317, .F. ) ;
#55237=CARTESIAN_POINT ( 'NONE',  ( 7.188101187500002709, 92.18750000204838102, 2.977408999572649151 ) ) ;
#55259=CARTESIAN_POINT ( 'NONE',  ( 5.656854249492379694, 109.6250000040967763, -5.656854249492380582 ) ) ;
#55264=DIRECTION ( 'NONE',  ( -0.000000000000000000, 1.000000000000000000, -0.000000000000000000 ) ) ;
#55270=CARTESIAN_POINT ( 'NONE',  ( -4.401442555609581635E-16, 108.7812500020483810, -7.188101187500000044 ) ) ;
#55285=CARTESIAN_POINT ( 'NONE',  ( -5.656854249492378806, 93.68750000000000000, 5.656854249492381470 ) ) ;
#55289=FACE_OUTER_BOUND ( 'NONE', #15933, .T. ) ;
#55290=ORIENTED_EDGE ( 'NONE', *, *, #22173, .T. ) ;
#55294=CARTESIAN_POINT ( 'NONE',  ( 7.188101187499999156, 15.74999999795161365, 2.977408999572654924 ) ) ;
#55301=CARTESIAN_POINT ( 'NONE',  ( 7.188101187500000044, 1.968749997951610320, 0.000000000000000000 ) ) ;
#55309=CIRCLE ( 'NONE', #54099, 11.00000000000000000 ) ;
#55313=ORIENTED_EDGE ( 'NONE', *, *, #66578, .F. ) ;
#55314=VECTOR ( 'NONE', #1508, 1000.000000000000000 ) ;
#55321=ORIENTED_EDGE ( 'NONE', *, *, #38204, .T. ) ;
#55322=CARTESIAN_POINT ( 'NONE',  ( 7.188101187500000044, 12.46874999795161187, 0.000000000000000000 ) ) ;
#55326=CARTESIAN_POINT ( 'NONE',  ( 5.082755093536326818, 110.0937500020483810, 5.082755093536325042 ) ) ;
#55334=CARTESIAN_POINT ( 'NONE',  ( 3.313708498984765161, 105.9687500000000000, 7.999999999999998224 ) ) ;
#55340=CARTESIAN_POINT ( 'NONE',  ( -1.469576158976823947E-15, 23.62500000000000355, 8.000000000000000000 ) ) ;
#55341=CARTESIAN_POINT ( 'NONE',  ( 8.000000000000001776, 94.15624999999998579, 3.313708498984759387 ) ) ;
#55349=CARTESIAN_POINT ( 'NONE',  ( 8.000000000000000000, 100.3437500000000000, -3.313708498984762496 ) ) ;
#55353=CARTESIAN_POINT ( 'NONE',  ( -2.977408999572650039, 26.81249999795161543, -7.188101187500001821 ) ) ;
#55360=CARTESIAN_POINT ( 'NONE',  ( -8.000000000000000000, 12.75000000000000178, -9.797174393178825657E-16 ) ) ;
#55363=( BOUNDED_CURVE ( )  B_SPLINE_CURVE ( 2, ( #18330, #41345, #64355, #12658, #35689, #58704, #30023, #2459, #65454 ),
 .UNSPECIFIED., .F., .F. ) 
 B_SPLINE_CURVE_WITH_KNOTS ( ( 3, 2, 2, 2, 3 ),
 ( 0.8472222222222222099, 0.8541666666666666297, 0.8611111111111111605, 0.8680555555555555802, 0.8750000000000000000 ),
 .UNSPECIFIED. ) 
 CURVE ( )  GEOMETRIC_REPRESENTATION_ITEM ( )  RATIONAL_B_SPLINE_CURVE ( ( 1.000000000000000000, 0.9238795325112867385, 1.000000000000000000, 0.9238795325112867385, 1.000000000000000000, 0.9238795325112867385, 1.000000000000000000, 0.9238795325112867385, 1.000000000000000000 ) ) 
 REPRESENTATION_ITEM ( '' )  );
#55365=CARTESIAN_POINT ( 'NONE',  ( 7.188101187500000044, 16.96874999795161543, 0.000000000000000000 ) ) ;
#55374=CARTESIAN_POINT ( 'NONE',  ( 3.313708498984800688, 118.5312499999999858, -7.999999999999958256 ) ) ;
#55379=CARTESIAN_POINT ( 'NONE',  ( -8.000000000000001776, 21.65624999590322375, 3.313708498984759387 ) ) ;
#55400=CARTESIAN_POINT ( 'NONE',  ( -8.000000000000000000, 12.65625000000000178, -3.313708498984762496 ) ) ;
#55403=CARTESIAN_POINT ( 'NONE',  ( -8.000000000000000000, 90.59375000409677625, -3.313708498984761608 ) ) ;
#55406=ORIENTED_EDGE ( 'NONE', *, *, #18760, .F. ) ;
#55413=CARTESIAN_POINT ( 'NONE',  ( 5.082755093536325042, 93.59375000204838102, -5.082755093536325930 ) ) ;
#55433=CARTESIAN_POINT ( 'NONE',  ( 5.656854249492380582, 11.99999999590322197, -5.656854249492380582 ) ) ;
#55436=CARTESIAN_POINT ( 'NONE',  ( 7.188101187499999156, 14.24999999795161010, 2.977408999572654924 ) ) ;
#55438=DIRECTION ( 'NONE',  ( 0.000000000000000000, 0.000000000000000000, 1.000000000000000000 ) ) ;
#55439=CARTESIAN_POINT ( 'NONE',  ( 7.188101187500002709, 107.1875000020483810, 2.977408999572649151 ) ) ;
#55456=CARTESIAN_POINT ( 'NONE',  ( 3.313708498984762496, 25.03124999590322375, 7.999999999999998224 ) ) ;
#55457=CARTESIAN_POINT ( 'NONE',  ( 1.320432766682874540E-15, 97.53125000204838102, 7.188101187500000044 ) ) ;
#55465=CARTESIAN_POINT ( 'NONE',  ( 5.082755093536325042, 101.4687500020483810, -5.082755093536325930 ) ) ;
#55474=VECTOR ( 'NONE', #5157, 1000.000000000000000 ) ;
#55482=FACE_OUTER_BOUND ( 'NONE', #38764, .T. ) ;
#55491=CARTESIAN_POINT ( 'NONE',  ( 2.977408999572650927, 11.24999999795161187, -7.188101187500001821 ) ) ;
#55492=CARTESIAN_POINT ( 'NONE',  ( 5.656854249492381470, 116.7500000040967905, 5.656854249492379694 ) ) ;
#55496=ADVANCED_FACE ( 'NONE', ( #5390 ), #61979, .T. ) ;
#55498=( LENGTH_UNIT ( ) NAMED_UNIT ( * ) SI_UNIT ( .MILLI., .METRE. ) );
#55522=CARTESIAN_POINT ( 'NONE',  ( -8.000000000000000000, 109.9062499999999858, -3.313708498984761608 ) ) ;
#55530=CARTESIAN_POINT ( 'NONE',  ( -5.656854249492379694, 22.87499999590322375, -5.656854249492380582 ) ) ;
#55536=CARTESIAN_POINT ( 'NONE',  ( -4.898587196589412829E-16, 114.3125000040967905, -8.000000000000000000 ) ) ;
#55544=CARTESIAN_POINT ( 'NONE',  ( -8.000000000000000000, 107.1875000040967905, 0.000000000000000000 ) ) ;
#55552=CARTESIAN_POINT ( 'NONE',  ( 2.977408999572654480, 120.1250000020484094, 7.188101187499999156 ) ) ;
#55557=CARTESIAN_POINT ( 'NONE',  ( 1.320432766682874540E-15, 118.9062500020483810, 7.188101187500000044 ) ) ;
#55559=CARTESIAN_POINT ( 'NONE',  ( 0.000000000000000000, 75.00000000000000000, 11.00000000000000000 ) ) ;
#55568=CARTESIAN_POINT ( 'NONE',  ( -4.898587196589412829E-16, 103.6250000000000000, -8.000000000000000000 ) ) ;
#55571=CARTESIAN_POINT ( 'NONE',  ( 5.656854249492378806, 22.12499999590322375, 5.656854249492381470 ) ) ;
#55581=CARTESIAN_POINT ( 'NONE',  ( -7.188101187500001821, 20.62499999795161543, -2.977408999572651371 ) ) ;
#55585=CARTESIAN_POINT ( 'NONE',  ( 7.188101187500001821, 17.43749999795161543, -2.977408999572650483 ) ) ;
#55604=VERTEX_POINT ( 'NONE', #74041 ) ;
#55611=CARTESIAN_POINT ( 'NONE',  ( 5.082755093536325042, 93.96875000204838102, -5.082755093536325930 ) ) ;
#55631=CARTESIAN_POINT ( 'NONE',  ( -8.000000000000000000, 17.15625000000000000, -3.313708498984762496 ) ) ;
#55642=CARTESIAN_POINT ( 'NONE',  ( -2.977408999572650927, 107.3750000020484094, -7.188101187500001821 ) ) ;
#55649=ORIENTED_EDGE ( 'NONE', *, *, #28766, .T. ) ;
#55660=CARTESIAN_POINT ( 'NONE',  ( -7.999999999999998224, 95.09375000000000000, 3.313708498984766049 ) ) ;
#55669=CARTESIAN_POINT ( 'NONE',  ( -7.188101187500002709, 16.68749999795161543, 2.977408999572649151 ) ) ;
#55679=CARTESIAN_POINT ( 'NONE',  ( -7.188101187500000044, 4.218749997951610986, -8.802885111219163269E-16 ) ) ;
#55690=VERTEX_POINT ( 'NONE', #64938 ) ;
#55695=CARTESIAN_POINT ( 'NONE',  ( 8.000000000000000000, 6.000000000000000888, 0.000000000000000000 ) ) ;
#55697=CARTESIAN_POINT ( 'NONE',  ( 4.401442555609581635E-16, 9.843749997951610098, -7.188101187500000044 ) ) ;
#55701=CARTESIAN_POINT ( 'NONE',  ( 2.977408999572654480, 114.5000000020483810, 7.188101187499999156 ) ) ;
#55706=ORIENTED_EDGE ( 'NONE', *, *, #37107, .T. ) ;
#55711=CARTESIAN_POINT ( 'NONE',  ( 7.999999999999998224, 19.21874999590322020, 3.313708498984766049 ) ) ;
#55716=CARTESIAN_POINT ( 'NONE',  ( -3.313708498984762496, 93.78125000000000000, 7.999999999999998224 ) ) ;
#55718=CARTESIAN_POINT ( 'NONE',  ( 1.469576158976823947E-15, 104.3750000000000000, 8.000000000000000000 ) ) ;
#55725=CARTESIAN_POINT ( 'NONE',  ( -3.313708498984719864, 19.96874999999999645, -8.000000000000040856 ) ) ;
#55730=CARTESIAN_POINT ( 'NONE',  ( 4.898587196589412829E-16, 3.375000000000000444, -8.000000000000000000 ) ) ;
#55739=CARTESIAN_POINT ( 'NONE',  ( 7.188101187499999156, 18.37499999795161187, 2.977408999572654924 ) ) ;
#55740=CARTESIAN_POINT ( 'NONE',  ( -5.656854249492378806, 108.8750000040967763, 5.656854249492381470 ) ) ;
#55748=CARTESIAN_POINT ( 'NONE',  ( 8.000000000000001776, 118.1562500000000000, 3.313708498984759387 ) ) ;
#55753=EDGE_CURVE ( 'NONE', #38779, #47140, #69876, .T. ) ;
#55773=CARTESIAN_POINT ( 'NONE',  ( 5.656854249492380582, 10.68750000000000178, -5.656854249492380582 ) ) ;
#55776=CARTESIAN_POINT ( 'NONE',  ( 3.313708498984765161, 91.15625000409676204, 7.999999999999998224 ) ) ;
#55779=( BOUNDED_CURVE ( )  B_SPLINE_CURVE ( 2, ( #70006, #54130, #58688, #47708, #70728, #47347, #42418, #42051, #70371 ),
 .UNSPECIFIED., .F., .F. ) 
 B_SPLINE_CURVE_WITH_KNOTS ( ( 3, 2, 2, 2, 3 ),
 ( 0.7187500000000001110, 0.7239583333333334814, 0.7291666666666667407, 0.7343750000000001110, 0.7395833333333334814 ),
 .UNSPECIFIED. ) 
 CURVE ( )  GEOMETRIC_REPRESENTATION_ITEM ( )  RATIONAL_B_SPLINE_CURVE ( ( 0.9999999999999983347, 0.9238795325112884038, 1.000000000000000000, 0.9238795325112867385, 1.000000000000000000, 0.9238795325112867385, 1.000000000000000000, 0.9238795325112850731, 1.000000000000001554 ) ) 
 REPRESENTATION_ITEM ( '' )  );
#55787=CARTESIAN_POINT ( 'NONE',  ( -7.188101187500000044, 91.15625000204838102, 0.000000000000000000 ) ) ;
#55792=ORIENTED_EDGE ( 'NONE', *, *, #15942, .T. ) ;
#55809=CARTESIAN_POINT ( 'NONE',  ( 7.999999999999998224, 10.21874999590321842, 3.313708498984766493 ) ) ;
#55813=CARTESIAN_POINT ( 'NONE',  ( -1.320432766682874540E-15, 18.46874999795161187, 7.188101187500000044 ) ) ;
#55815=FACE_OUTER_BOUND ( 'NONE', #58665, .T. ) ;
#55816=CARTESIAN_POINT ( 'NONE',  ( -4.401442555609581635E-16, 104.6562500020483810, -7.188101187500000044 ) ) ;
#55829=CARTESIAN_POINT ( 'NONE',  ( -1.469576158976823947E-15, 20.43749999590322375, 8.000000000000000000 ) ) ;
#55836=CARTESIAN_POINT ( 'NONE',  ( -4.401442555609581635E-16, 99.78125000204838102, -7.188101187500000044 ) ) ;
#55842=CARTESIAN_POINT ( 'NONE',  ( -5.082755093536325930, 101.8437500020483810, -5.082755093536325930 ) ) ;
#55867=CARTESIAN_POINT ( 'NONE',  ( -2.977408999572650039, 9.937499997951610098, -7.188101187500001821 ) ) ;
#55868=CARTESIAN_POINT ( 'NONE',  ( 3.313708498984765161, 110.6562500040967905, 7.999999999999998224 ) ) ;
#55882=DIRECTION ( 'NONE',  ( 0.000000000000000000, 0.000000000000000000, 1.000000000000000000 ) ) ;
#55887=CARTESIAN_POINT ( 'NONE',  ( 5.656854249492379694, 91.62500000409677625, -5.656854249492380582 ) ) ;
#55893=EDGE_CURVE ( 'NONE', #52001, #17336, #38501, .T. ) ;
#55894=CARTESIAN_POINT ( 'NONE',  ( 1.469576158976823947E-15, 107.3750000000000000, 8.000000000000000000 ) ) ;
#55898=( BOUNDED_CURVE ( )  B_SPLINE_CURVE ( 2, ( #24849, #12797, #12430, #35830, #36563, #48238, #59578, #30532, #25594 ),
 .UNSPECIFIED., .F., .F. ) 
 B_SPLINE_CURVE_WITH_KNOTS ( ( 3, 2, 2, 2, 3 ),
 ( 0.8645833333333335924, 0.8697916666666668517, 0.8750000000000002220, 0.8802083333333337034, 0.8854166666666669627 ),
 .UNSPECIFIED. ) 
 CURVE ( )  GEOMETRIC_REPRESENTATION_ITEM ( )  RATIONAL_B_SPLINE_CURVE ( ( 0.9999999999999967804, 0.9238795325112899581, 1.000000000000000000, 0.9238795325112867385, 1.000000000000000000, 0.9238795325112867385, 1.000000000000000000, 0.9238795325112818535, 1.000000000000004885 ) ) 
 REPRESENTATION_ITEM ( '' )  );
#55899=CARTESIAN_POINT ( 'NONE',  ( -5.656854249492378806, 102.8750000040967763, 5.656854249492381470 ) ) ;
#55902=CARTESIAN_POINT ( 'NONE',  ( -1.469576158976823947E-15, 18.93749999590322020, 8.000000000000000000 ) ) ;
#55905=CARTESIAN_POINT ( 'NONE',  ( 5.082755093536325042, 119.4687500020483810, -5.082755093536325930 ) ) ;
#55922=EDGE_CURVE ( 'NONE', #31066, #64829, #61617, .T. ) ;
#55928=CARTESIAN_POINT ( 'NONE',  ( 1.320432766682874540E-15, 117.0312500020483810, 7.188101187500000044 ) ) ;
#55933=CARTESIAN_POINT ( 'NONE',  ( 2.977408999572654480, 119.0000000020483810, 7.188101187499999156 ) ) ;
#55935=CARTESIAN_POINT ( 'NONE',  ( 0.000000000000000000, 125.0000000000000000, 0.000000000000000000 ) ) ;
#55947=VERTEX_POINT ( 'NONE', #9190 ) ;
#55958=CARTESIAN_POINT ( 'NONE',  ( -8.000000000000000000, 0.7500000000000000000, -9.797174393178825657E-16 ) ) ;
#55961=CARTESIAN_POINT ( 'NONE',  ( 2.977408999572651815, 18.56249999795161187, 7.188101187500000933 ) ) ;
#55962=DIRECTION ( 'NONE',  ( 0.000000000000000000, 0.000000000000000000, 1.000000000000000000 ) ) ;
#55968=ORIENTED_EDGE ( 'NONE', *, *, #35527, .F. ) ;
#55979=LINE ( 'NONE', #16693, #28003 ) ;
#55984=CARTESIAN_POINT ( 'NONE',  ( -5.656854249492378806, 122.1875000000000000, 5.656854249492381470 ) ) ;
#55991=CARTESIAN_POINT ( 'NONE',  ( -3.313708498984760276, 22.96875000000000355, -8.000000000000000000 ) ) ;
#56000=CARTESIAN_POINT ( 'NONE',  ( 0.000000000000000000, 75.00000000000000000, 0.000000000000000000 ) ) ;
#56002=CARTESIAN_POINT ( 'NONE',  ( -3.313708498984719864, 16.96874999999999289, -8.000000000000040856 ) ) ;
#56013=CARTESIAN_POINT ( 'NONE',  ( -7.188101187500000044, 101.6562500020483810, 0.000000000000000000 ) ) ;
#56041=CARTESIAN_POINT ( 'NONE',  ( 2.977408999572650927, 16.12499999795161543, -7.188101187500000933 ) ) ;
#56045=CARTESIAN_POINT ( 'NONE',  ( 5.656854249492379694, 90.12500000409677625, -5.656854249492380582 ) ) ;
#56049=CARTESIAN_POINT ( 'NONE',  ( 7.188101187500001821, 5.062499997951610098, -2.977408999572650483 ) ) ;
#56051=CARTESIAN_POINT ( 'NONE',  ( 1.469576158976823947E-15, 98.37499999999998579, 8.000000000000000000 ) ) ;
#56052=CARTESIAN_POINT ( 'NONE',  ( -1.469576158976823947E-15, 17.43749999590322375, 8.000000000000000000 ) ) ;
#56053=VERTEX_POINT ( 'NONE', #38986 ) ;
#56066=CARTESIAN_POINT ( 'NONE',  ( 7.188101187499999156, 12.37499999795161187, 2.977408999572654924 ) ) ;
#56070=CARTESIAN_POINT ( 'NONE',  ( 7.188101187500002709, 114.6875000020484094, 2.977408999572649151 ) ) ;
#56087=CARTESIAN_POINT ( 'NONE',  ( 1.469576158976823947E-15, 95.37499999999998579, 8.000000000000000000 ) ) ;
#56089=CARTESIAN_POINT ( 'NONE',  ( 8.000000000000001776, 98.65625000000001421, 3.313708498984759387 ) ) ;
#56100=CARTESIAN_POINT ( 'NONE',  ( -2.977408999572650927, 119.3750000020483810, -7.188101187500001821 ) ) ;
#56108=CARTESIAN_POINT ( 'NONE',  ( -7.188101187500001821, 17.62499999795161187, -2.977408999572651371 ) ) ;
#56110=( BOUNDED_CURVE ( )  B_SPLINE_CURVE ( 2, ( #44803, #33140, #16483, #27436, #39520, #67816, #22518, #45538, #34247 ),
 .UNSPECIFIED., .F., .F. ) 
 B_SPLINE_CURVE_WITH_KNOTS ( ( 3, 2, 2, 2, 3 ),
 ( 0.01388888888888889159, 0.02083333333333333565, 0.02777777777777777624, 0.03472222222222222376, 0.04166666666666666435 ),
 .UNSPECIFIED. ) 
 CURVE ( )  GEOMETRIC_REPRESENTATION_ITEM ( )  RATIONAL_B_SPLINE_CURVE ( ( 1.000000000000000000, 0.9238795325112867385, 1.000000000000000000, 0.9238795325112867385, 1.000000000000000000, 0.9238795325112867385, 1.000000000000000000, 0.9238795325112867385, 1.000000000000000000 ) ) 
 REPRESENTATION_ITEM ( '' )  );
#56127=CIRCLE ( 'NONE', #59715, 7.500000000000020428 ) ;
#56140=ORIENTED_EDGE ( 'NONE', *, *, #34546, .F. ) ;
#56142=( BOUNDED_CURVE ( )  B_SPLINE_CURVE ( 2, ( #14130, #48469, #47365, #71474, #35691, #25454, #18706, #59806, #1736 ),
 .UNSPECIFIED., .F., .F. ) 
 B_SPLINE_CURVE_WITH_KNOTS ( ( 3, 2, 2, 2, 3 ),
 ( 0.8437500000000002220, 0.8489583333333335924, 0.8541666666666668517, 0.8593750000000002220, 0.8645833333333335924 ),
 .UNSPECIFIED. ) 
 CURVE ( )  GEOMETRIC_REPRESENTATION_ITEM ( )  RATIONAL_B_SPLINE_CURVE ( ( 0.9999999999999967804, 0.9238795325112899581, 1.000000000000000000, 0.9238795325112867385, 1.000000000000000000, 0.9238795325112867385, 1.000000000000000000, 0.9238795325112835188, 1.000000000000003331 ) ) 
 REPRESENTATION_ITEM ( '' )  );
#56145=CARTESIAN_POINT ( 'NONE',  ( 8.000000000000000000, 9.093750000000001776, -3.313708498984761608 ) ) ;
#56147=CARTESIAN_POINT ( 'NONE',  ( 8.000000000000001776, 89.84375000409677625, 3.313708498984759387 ) ) ;
#56156=CARTESIAN_POINT ( 'NONE',  ( -7.188101187500000044, 89.65625000204838102, 0.000000000000000000 ) ) ;
#56165=AXIS2_PLACEMENT_3D ( 'NONE', #63125, #6170, #69915 ) ;
#56169=VERTEX_POINT ( 'NONE', #70528 ) ;
#56180=CARTESIAN_POINT ( 'NONE',  ( -8.000000000000000000, 7.968749995903221972, -3.313708498984762496 ) ) ;
#56184=CARTESIAN_POINT ( 'NONE',  ( 2.977408999572650927, 14.62499999795161010, -7.188101187500001821 ) ) ;
#56186=CARTESIAN_POINT ( 'NONE',  ( 8.000000000000000000, 7.593750000000001776, -3.313708498984761164 ) ) ;
#56187=CARTESIAN_POINT ( 'NONE',  ( 7.188101187500000933, 102.8750000020483810, -2.977408999572651371 ) ) ;
#56204=CARTESIAN_POINT ( 'NONE',  ( 1.320432766682874540E-15, 99.03125000204838102, 7.188101187500000044 ) ) ;
#56210=CARTESIAN_POINT ( 'NONE',  ( -7.188101187499999156, 102.1250000020483810, 2.977408999572654924 ) ) ;
#56222=CARTESIAN_POINT ( 'NONE',  ( 5.656854249492380582, 9.187500000000001776, -5.656854249492380582 ) ) ;
#56234=CARTESIAN_POINT ( 'NONE',  ( 4.401442555609581635E-16, 6.843749997951611874, -7.188101187500000044 ) ) ;
#56235=CARTESIAN_POINT ( 'NONE',  ( -5.656854249492380582, 111.5000000040967763, -5.656854249492380582 ) ) ;
#56241=( BOUNDED_SURFACE ( )  B_SPLINE_SURFACE ( 1, 2, ( 
 ( #9268, #50000, #14910, #20950, #66982, #15657, #38320, #38698, #32290, #61699, #10021, #33053, #4361, #44719, #16030, #39063, #56415, #4736, #50741, #73755, #45088, #68103, #16393, #62430, #52241, #22431, #57543, #45827, #68467, #74497, #52609, #51868, #45450, #16767, #28845, #51116, #5852, #40174, #41287, #57160, #63177, #12236, #35273, #575, #11872, #11504, #18272, #23557, #35631, #945, #209, #51486, #63926, #46568, #12604, #23187, #29596, #68838, #40915, #58646, #39794, #64297, #69589, #62798, #6589, #17525, #17151, #22806, #28101, #74128, #17902, #11138, #34160, #58286, #46198, #34908, #6225, #5476, #28478, #34537, #69214, #40542, #23927, #63547, #57916, #46936, #29228, #69964, #14442, #37477, #1675, #13693, #19739, #53717, #36365, #19005, #36735, #42379, #6953, #30699, #71788, #29964, #37102, #31441, #43119, #59746, #8057, #20107, #31059, #59018, #42011, #47665, #52977, #14067, #25017, #54087, #1311, #24294, #7692, #47305, #59381, #65018, #66137, #36001, #13329, #65764, #60106, #2397, #65396, #2031, #70330, #25395, #18645, #54467, #48037, #30331, #42748, #48409, #41653, #71046, #8424, #70687, #2774, #64663, #12963, #7327, #71415, #53350, #25760, #19366, #48781, #24655, #21973, #73665, #32955, #60477, #8807, #67641, #32576, #67271, #38604, #54839, #43494, #43876, #31818, #49153, #33324, #3519, #26893, #44627, #61604, #50645, #68004, #16300, #55214, #15565, #73299, #55585, #15198, #72553, #9923, #21233, #3148, #9561, #45001, #26134, #15937, #10298, #72163, #55961, #4271, #20473, #27261, #37858, #20858, #26508, #66505, #38966, #3899, #50279, #66892, #61233, #14816, #60855, #9175, #38227, #49533, #32194, #21601, #49909, #72923, #44259, #61970, #56323, #4644, #27638, #16675, #74406, #11044, #51393, #855, #68745, #68377, #34074, #45361, #17430, #23840, #46847, #39705, #46106, #69869, #40823, #74032, #63829, #39340, #23466, #63453, #33697, #17059, #57071, #5018, #5383, #12144, #63086, #62705, #40081, #28384, #22714, #52150, #11778, #28014, #51025, #46478, #34817, #35181, #45731, #22335, #62337, #69125, #6129, #11410, #34447, #58196, #57446, #5754, #10665, #28754, #51769, #116, #23095, #40454, #57823, #29507, #29135, #486, #69498, #17807, #6501, #52518, #56702, #1587, #48688, #25669, #59653, #60013, #30973, #65302, #8331, #24571 ),
 ( #6862, #47576, #54372, #24199, #70243, #53258, #64576, #30240, #2682, #70599, #47210, #12873, #18553, #70961, #18182, #41197, #41559, #24929, #64207, #19646, #52889, #42659, #12511, #2303, #42288, #35542, #18916, #35910, #58557, #58929, #65670, #41922, #29874, #1220, #64933, #7236, #13242, #36276, #31341, #59292, #7600, #25300, #48319, #13607, #1940, #30608, #53628, #36645, #47943, #13969, #19278, #7970, #53992, #71325, #37011, #49439, #73209, #37765, #9836, #27544, #8709, #33235, #44164, #31724, #50187, #61135, #60764, #20386, #56234, #10206, #67178, #71693, #20012, #4184, #43784, #26803, #49817, #26038, #72834, #38512, #61513, #38879, #9465, #3424, #20766, #15101, #4549, #14353, #26413, #43401, #44536, #32862, #43023, #27170, #61883, #72459, #21514, #66044, #14725, #67547, #66798, #55867, #37381, #72068, #15845, #60383, #49059, #54746, #38134, #3054, #66416, #9086, #32100, #55120, #32483, #55491, #3805, #21140, #15474, #67917, #39248, #23008, #11321, #17338, #4928, #62248, #393, #16967, #5664, #10575, #33605, #40360, #56614, #45276, #6035, #62620, #73946, #39620, #27925, #10950, #50934, #34724, #56981, #68657, #57353, #22, #46014, #39993, #33986, #16584, #50558, #73572, #51676, #29040, #69035, #28661, #52058, #5295, #28297, #63360, #62997, #22248, #51303, #74315, #45642, #11686, #57728, #68287, #21882, #22623, #34354, #44911, #16209, #4795, #43653, #62123, #55365, #37637, #67043, #31968, #16084, #21382, #49694, #56108, #15717, #26286, #72323, #9331, #27789, #10447, #73444, #55739, #27048, #61383, #44035, #20637, #10077, #4056, #15343, #49307, #32351, #4418, #54993, #73814, #3300, #50801, #38759, #66664, #21751, #32731, #3671, #14970, #43275, #56479, #61759, #66291, #14597, #50429, #38379, #50061, #44405, #60635, #38007, #26669, #8956, #61005, #39119, #72707, #9709, #27413, #67418, #33477, #21010, #73075, #33114, #44779, #67793, #68901, #51544, #34220, #51929, #57600, #29654, #45887, #12302, #52669, #52302, #46629, #58347, #28912, #266, #35335, #23249, #74184, #57221, #62858, #22121, #29292, #40230, #46257, #28536, #22874, #6652, #45146, #68157, #74562, #11192, #16456, #40605, #33851, #39493, #17211, #10816, #63233, #62488, #28164, #22489, #5535, #68527, #11560, #56849, #34593, #51174, #16830, #45510, #69276, #5168, #39857, #5910 ) ),
 .UNSPECIFIED., .F., .F., .F. ) 
 B_SPLINE_SURFACE_WITH_KNOTS ( ( 2, 2 ),
 ( 3, 2, 2, 2, 2, 2, 2, 2, 2, 2, 2, 2, 2, 2, 2, 2, 2, 2, 2, 2, 2, 2, 2, 2, 2, 2, 2, 2, 2, 2, 2, 2, 2, 2, 2, 2, 2, 2, 2, 2, 2, 2, 2, 2, 2, 2, 2, 2, 2, 2, 2, 2, 2, 2, 2, 2, 2, 2, 2, 2, 2, 2, 2, 2, 2, 2, 2, 2, 2, 2, 2, 2, 2, 2, 2, 2, 2, 2, 2, 2, 2, 2, 2, 2, 2, 2, 2, 2, 2, 2, 2, 2, 2, 2, 2, 2, 2, 2, 2, 2, 2, 2, 2, 2, 2, 2, 2, 2, 2, 2, 2, 2, 2, 2, 2, 2, 2, 2, 2, 2, 2, 2, 2, 2, 2, 2, 2, 2, 2, 2, 2, 2, 2, 2, 2, 2, 2, 2, 2, 2, 2, 2, 2, 2, 3 ),
 ( 0.000000000000000000, 1.000000000000000000 ),
 ( 0.000000000000000000, 0.006944444444444444059, 0.01388888888888888812, 0.02083333333333333218, 0.02777777777777777624, 0.03472222222222222376, 0.04166666666666666435, 0.04861111111111111188, 0.05555555555555555247, 0.06250000000000000000, 0.06944444444444444753, 0.07638888888888889506, 0.08333333333333332871, 0.09027777777777777624, 0.09722222222222222376, 0.1041666666666666713, 0.1111111111111111049, 0.1180555555555555525, 0.1250000000000000000, 0.1319444444444444475, 0.1388888888888888951, 0.1458333333333333426, 0.1527777777777777901, 0.1597222222222222099, 0.1666666666666666574, 0.1736111111111111049, 0.1805555555555555525, 0.1875000000000000000, 0.1944444444444444475, 0.2013888888888888951, 0.2083333333333333426, 0.2152777777777777901, 0.2222222222222222099, 0.2291666666666666574, 0.2361111111111111049, 0.2430555555555555525, 0.2500000000000000000, 0.2569444444444444198, 0.2638888888888888951, 0.2708333333333333148, 0.2777777777777777901, 0.2847222222222222099, 0.2916666666666666852, 0.2986111111111111049, 0.3055555555555555802, 0.3125000000000000000, 0.3194444444444444198, 0.3263888888888888951, 0.3333333333333333148, 0.3402777777777777901, 0.3472222222222222099, 0.3541666666666666852, 0.3611111111111111049, 0.3680555555555555802, 0.3750000000000000000, 0.3819444444444444198, 0.3888888888888888951, 0.3958333333333333148, 0.4027777777777777901, 0.4097222222222222099, 0.4166666666666666852, 0.4236111111111111049, 0.4305555555555555802, 0.4375000000000000000, 0.4444444444444444198, 0.4513888888888888951, 0.4583333333333333148, 0.4652777777777777901, 0.4722222222222222099, 0.4791666666666666852, 0.4861111111111111049, 0.4930555555555555802, 0.5000000000000000000, 0.5069444444444444198, 0.5138888888888888395, 0.5208333333333333703, 0.5277777777777777901, 0.5347222222222222099, 0.5416666666666666297, 0.5486111111111111605, 0.5555555555555555802, 0.5625000000000000000, 0.5694444444444444198, 0.5763888888888888395, 0.5833333333333333703, 0.5902777777777777901, 0.5972222222222222099, 0.6041666666666666297, 0.6111111111111111605, 0.6180555555555555802, 0.6250000000000000000, 0.6319444444444444198, 0.6388888888888888395, 0.6458333333333333703, 0.6527777777777777901, 0.6597222222222222099, 0.6666666666666666297, 0.6736111111111111605, 0.6805555555555555802, 0.6875000000000000000, 0.6944444444444444198, 0.7013888888888888395, 0.7083333333333333703, 0.7152777777777777901, 0.7222222222222222099, 0.7291666666666666297, 0.7361111111111111605, 0.7430555555555555802, 0.7500000000000000000, 0.7569444444444444198, 0.7638888888888888395, 0.7708333333333333703, 0.7777777777777777901, 0.7847222222222222099, 0.7916666666666666297, 0.7986111111111111605, 0.8055555555555555802, 0.8125000000000000000, 0.8194444444444444198, 0.8263888888888888395, 0.8333333333333333703, 0.8402777777777777901, 0.8472222222222222099, 0.8541666666666666297, 0.8611111111111111605, 0.8680555555555555802, 0.8750000000000000000, 0.8819444444444444198, 0.8888888888888888395, 0.8958333333333333703, 0.9027777777777777901, 0.9097222222222222099, 0.9166666666666666297, 0.9236111111111111605, 0.9305555555555555802, 0.9375000000000000000, 0.9444444444444444198, 0.9513888888888888395, 0.9583333333333333703, 0.9652777777777777901, 0.9722222222222222099, 0.9791666666666666297, 0.9861111111111111605, 0.9930555555555555802, 1.000000000000000000 ),
 .UNSPECIFIED. ) 
 GEOMETRIC_REPRESENTATION_ITEM ( )  RATIONAL_B_SPLINE_SURFACE ( (
 ( 1.000000000000000000, 0.9238795325112867385, 1.000000000000000000, 0.9238795325112867385, 1.000000000000000000, 0.9238795325112867385, 1.000000000000000000, 0.9238795325112867385, 1.000000000000000000, 0.9238795325112867385, 1.000000000000000000, 0.9238795325112867385, 1.000000000000000000, 0.9238795325112867385, 1.000000000000000000, 0.9238795325112867385, 1.000000000000000000, 0.9238795325112867385, 1.000000000000000000, 0.9238795325112867385, 1.000000000000000000, 0.9238795325112867385, 1.000000000000000000, 0.9238795325112867385, 1.000000000000000000, 0.9238795325112867385, 1.000000000000000000, 0.9238795325112867385, 1.000000000000000000, 0.9238795325112867385, 1.000000000000000000, 0.9238795325112867385, 1.000000000000000000, 0.9238795325112867385, 1.000000000000000000, 0.9238795325112867385, 1.000000000000000000, 0.9238795325112867385, 1.000000000000000000, 0.9238795325112867385, 1.000000000000000000, 0.9238795325112867385, 1.000000000000000000, 0.9238795325112867385, 1.000000000000000000, 0.9238795325112867385, 1.000000000000000000, 0.9238795325112867385, 1.000000000000000000, 0.9238795325112867385, 1.000000000000000000, 0.9238795325112867385, 1.000000000000000000, 0.9238795325112867385, 1.000000000000000000, 0.9238795325112867385, 1.000000000000000000, 0.9238795325112867385, 1.000000000000000000, 0.9238795325112867385, 1.000000000000000000, 0.9238795325112867385, 1.000000000000000000, 0.9238795325112867385, 1.000000000000000000, 0.9238795325112867385, 1.000000000000000000, 0.9238795325112867385, 1.000000000000000000, 0.9238795325112867385, 1.000000000000000000, 0.9238795325112867385, 1.000000000000000000, 0.9238795325112867385, 1.000000000000000000, 0.9238795325112867385, 1.000000000000000000, 0.9238795325112867385, 1.000000000000000000, 0.9238795325112867385, 1.000000000000000000, 0.9238795325112867385, 1.000000000000000000, 0.9238795325112867385, 1.000000000000000000, 0.9238795325112867385, 1.000000000000000000, 0.9238795325112867385, 1.000000000000000000, 0.9238795325112867385, 1.000000000000000000, 0.9238795325112867385, 1.000000000000000000, 0.9238795325112867385, 1.000000000000000000, 0.9238795325112867385, 1.000000000000000000, 0.9238795325112867385, 1.000000000000000000, 0.9238795325112867385, 1.000000000000000000, 0.9238795325112867385, 1.000000000000000000, 0.9238795325112867385, 1.000000000000000000, 0.9238795325112867385, 1.000000000000000000, 0.9238795325112867385, 1.000000000000000000, 0.9238795325112867385, 1.000000000000000000, 0.9238795325112867385, 1.000000000000000000, 0.9238795325112867385, 1.000000000000000000, 0.9238795325112867385, 1.000000000000000000, 0.9238795325112867385, 1.000000000000000000, 0.9238795325112867385, 1.000000000000000000, 0.9238795325112867385, 1.000000000000000000, 0.9238795325112867385, 1.000000000000000000, 0.9238795325112867385, 1.000000000000000000, 0.9238795325112867385, 1.000000000000000000, 0.9238795325112867385, 1.000000000000000000, 0.9238795325112867385, 1.000000000000000000, 0.9238795325112867385, 1.000000000000000000, 0.9238795325112867385, 1.000000000000000000, 0.9238795325112867385, 1.000000000000000000, 0.9238795325112867385, 1.000000000000000000, 0.9238795325112867385, 1.000000000000000000, 0.9238795325112867385, 1.000000000000000000, 0.9238795325112867385, 1.000000000000000000, 0.9238795325112867385, 1.000000000000000000, 0.9238795325112867385, 1.000000000000000000, 0.9238795325112867385, 1.000000000000000000, 0.9238795325112867385, 1.000000000000000000, 0.9238795325112867385, 1.000000000000000000, 0.9238795325112867385, 1.000000000000000000, 0.9238795325112867385, 1.000000000000000000, 0.9238795325112867385, 1.000000000000000000, 0.9238795325112867385, 1.000000000000000000, 0.9238795325112867385, 1.000000000000000000, 0.9238795325112867385, 1.000000000000000000, 0.9238795325112867385, 1.000000000000000000, 0.9238795325112867385, 1.000000000000000000, 0.9238795325112867385, 1.000000000000000000, 0.9238795325112867385, 1.000000000000000000, 0.9238795325112867385, 1.000000000000000000, 0.9238795325112867385, 1.000000000000000000, 0.9238795325112867385, 1.000000000000000000, 0.9238795325112867385, 1.000000000000000000, 0.9238795325112867385, 1.000000000000000000, 0.9238795325112867385, 1.000000000000000000, 0.9238795325112867385, 1.000000000000000000, 0.9238795325112867385, 1.000000000000000000, 0.9238795325112867385, 1.000000000000000000, 0.9238795325112867385, 1.000000000000000000, 0.9238795325112867385, 1.000000000000000000, 0.9238795325112867385, 1.000000000000000000, 0.9238795325112867385, 1.000000000000000000, 0.9238795325112867385, 1.000000000000000000, 0.9238795325112867385, 1.000000000000000000, 0.9238795325112867385, 1.000000000000000000, 0.9238795325112867385, 1.000000000000000000, 0.9238795325112867385, 1.000000000000000000, 0.9238795325112867385, 1.000000000000000000, 0.9238795325112867385, 1.000000000000000000, 0.9238795325112867385, 1.000000000000000000, 0.9238795325112867385, 1.000000000000000000, 0.9238795325112867385, 1.000000000000000000, 0.9238795325112867385, 1.000000000000000000, 0.9238795325112867385, 1.000000000000000000, 0.9238795325112867385, 1.000000000000000000, 0.9238795325112867385, 1.000000000000000000, 0.9238795325112867385, 1.000000000000000000, 0.9238795325112867385, 1.000000000000000000, 0.9238795325112867385, 1.000000000000000000, 0.9238795325112867385, 1.000000000000000000, 0.9238795325112867385, 1.000000000000000000, 0.9238795325112867385, 1.000000000000000000, 0.9238795325112867385, 1.000000000000000000, 0.9238795325112867385, 1.000000000000000000, 0.9238795325112867385, 1.000000000000000000, 0.9238795325112867385, 1.000000000000000000, 0.9238795325112867385, 1.000000000000000000, 0.9238795325112867385, 1.000000000000000000, 0.9238795325112867385, 1.000000000000000000, 0.9238795325112867385, 1.000000000000000000, 0.9238795325112867385, 1.000000000000000000, 0.9238795325112867385, 1.000000000000000000, 0.9238795325112867385, 1.000000000000000000, 0.9238795325112867385, 1.000000000000000000, 0.9238795325112867385, 1.000000000000000000, 0.9238795325112867385, 1.000000000000000000, 0.9238795325112867385, 1.000000000000000000, 0.9238795325112867385, 1.000000000000000000, 0.9238795325112867385, 1.000000000000000000, 0.9238795325112867385, 1.000000000000000000, 0.9238795325112867385, 1.000000000000000000, 0.9238795325112867385, 1.000000000000000000, 0.9238795325112867385, 1.000000000000000000, 0.9238795325112867385, 1.000000000000000000, 0.9238795325112867385, 1.000000000000000000),
 ( 1.000000000000000000, 0.9238795325112867385, 1.000000000000000000, 0.9238795325112867385, 1.000000000000000000, 0.9238795325112867385, 1.000000000000000000, 0.9238795325112867385, 1.000000000000000000, 0.9238795325112867385, 1.000000000000000000, 0.9238795325112867385, 1.000000000000000000, 0.9238795325112867385, 1.000000000000000000, 0.9238795325112867385, 1.000000000000000000, 0.9238795325112867385, 1.000000000000000000, 0.9238795325112867385, 1.000000000000000000, 0.9238795325112867385, 1.000000000000000000, 0.9238795325112867385, 1.000000000000000000, 0.9238795325112867385, 1.000000000000000000, 0.9238795325112867385, 1.000000000000000000, 0.9238795325112867385, 1.000000000000000000, 0.9238795325112867385, 1.000000000000000000, 0.9238795325112867385, 1.000000000000000000, 0.9238795325112867385, 1.000000000000000000, 0.9238795325112867385, 1.000000000000000000, 0.9238795325112867385, 1.000000000000000000, 0.9238795325112867385, 1.000000000000000000, 0.9238795325112867385, 1.000000000000000000, 0.9238795325112867385, 1.000000000000000000, 0.9238795325112867385, 1.000000000000000000, 0.9238795325112867385, 1.000000000000000000, 0.9238795325112867385, 1.000000000000000000, 0.9238795325112867385, 1.000000000000000000, 0.9238795325112867385, 1.000000000000000000, 0.9238795325112867385, 1.000000000000000000, 0.9238795325112867385, 1.000000000000000000, 0.9238795325112867385, 1.000000000000000000, 0.9238795325112867385, 1.000000000000000000, 0.9238795325112867385, 1.000000000000000000, 0.9238795325112867385, 1.000000000000000000, 0.9238795325112867385, 1.000000000000000000, 0.9238795325112867385, 1.000000000000000000, 0.9238795325112867385, 1.000000000000000000, 0.9238795325112867385, 1.000000000000000000, 0.9238795325112867385, 1.000000000000000000, 0.9238795325112867385, 1.000000000000000000, 0.9238795325112867385, 1.000000000000000000, 0.9238795325112867385, 1.000000000000000000, 0.9238795325112867385, 1.000000000000000000, 0.9238795325112867385, 1.000000000000000000, 0.9238795325112867385, 1.000000000000000000, 0.9238795325112867385, 1.000000000000000000, 0.9238795325112867385, 1.000000000000000000, 0.9238795325112867385, 1.000000000000000000, 0.9238795325112867385, 1.000000000000000000, 0.9238795325112867385, 1.000000000000000000, 0.9238795325112867385, 1.000000000000000000, 0.9238795325112867385, 1.000000000000000000, 0.9238795325112867385, 1.000000000000000000, 0.9238795325112867385, 1.000000000000000000, 0.9238795325112867385, 1.000000000000000000, 0.9238795325112867385, 1.000000000000000000, 0.9238795325112867385, 1.000000000000000000, 0.9238795325112867385, 1.000000000000000000, 0.9238795325112867385, 1.000000000000000000, 0.9238795325112867385, 1.000000000000000000, 0.9238795325112867385, 1.000000000000000000, 0.9238795325112867385, 1.000000000000000000, 0.9238795325112867385, 1.000000000000000000, 0.9238795325112867385, 1.000000000000000000, 0.9238795325112867385, 1.000000000000000000, 0.9238795325112867385, 1.000000000000000000, 0.9238795325112867385, 1.000000000000000000, 0.9238795325112867385, 1.000000000000000000, 0.9238795325112867385, 1.000000000000000000, 0.9238795325112867385, 1.000000000000000000, 0.9238795325112867385, 1.000000000000000000, 0.9238795325112867385, 1.000000000000000000, 0.9238795325112867385, 1.000000000000000000, 0.9238795325112867385, 1.000000000000000000, 0.9238795325112867385, 1.000000000000000000, 0.9238795325112867385, 1.000000000000000000, 0.9238795325112867385, 1.000000000000000000, 0.9238795325112867385, 1.000000000000000000, 0.9238795325112867385, 1.000000000000000000, 0.9238795325112867385, 1.000000000000000000, 0.9238795325112867385, 1.000000000000000000, 0.9238795325112867385, 1.000000000000000000, 0.9238795325112867385, 1.000000000000000000, 0.9238795325112867385, 1.000000000000000000, 0.9238795325112867385, 1.000000000000000000, 0.9238795325112867385, 1.000000000000000000, 0.9238795325112867385, 1.000000000000000000, 0.9238795325112867385, 1.000000000000000000, 0.9238795325112867385, 1.000000000000000000, 0.9238795325112867385, 1.000000000000000000, 0.9238795325112867385, 1.000000000000000000, 0.9238795325112867385, 1.000000000000000000, 0.9238795325112867385, 1.000000000000000000, 0.9238795325112867385, 1.000000000000000000, 0.9238795325112867385, 1.000000000000000000, 0.9238795325112867385, 1.000000000000000000, 0.9238795325112867385, 1.000000000000000000, 0.9238795325112867385, 1.000000000000000000, 0.9238795325112867385, 1.000000000000000000, 0.9238795325112867385, 1.000000000000000000, 0.9238795325112867385, 1.000000000000000000, 0.9238795325112867385, 1.000000000000000000, 0.9238795325112867385, 1.000000000000000000, 0.9238795325112867385, 1.000000000000000000, 0.9238795325112867385, 1.000000000000000000, 0.9238795325112867385, 1.000000000000000000, 0.9238795325112867385, 1.000000000000000000, 0.9238795325112867385, 1.000000000000000000, 0.9238795325112867385, 1.000000000000000000, 0.9238795325112867385, 1.000000000000000000, 0.9238795325112867385, 1.000000000000000000, 0.9238795325112867385, 1.000000000000000000, 0.9238795325112867385, 1.000000000000000000, 0.9238795325112867385, 1.000000000000000000, 0.9238795325112867385, 1.000000000000000000, 0.9238795325112867385, 1.000000000000000000, 0.9238795325112867385, 1.000000000000000000, 0.9238795325112867385, 1.000000000000000000, 0.9238795325112867385, 1.000000000000000000, 0.9238795325112867385, 1.000000000000000000, 0.9238795325112867385, 1.000000000000000000, 0.9238795325112867385, 1.000000000000000000, 0.9238795325112867385, 1.000000000000000000, 0.9238795325112867385, 1.000000000000000000, 0.9238795325112867385, 1.000000000000000000, 0.9238795325112867385, 1.000000000000000000, 0.9238795325112867385, 1.000000000000000000, 0.9238795325112867385, 1.000000000000000000, 0.9238795325112867385, 1.000000000000000000, 0.9238795325112867385, 1.000000000000000000, 0.9238795325112867385, 1.000000000000000000, 0.9238795325112867385, 1.000000000000000000, 0.9238795325112867385, 1.000000000000000000, 0.9238795325112867385, 1.000000000000000000, 0.9238795325112867385, 1.000000000000000000, 0.9238795325112867385, 1.000000000000000000, 0.9238795325112867385, 1.000000000000000000, 0.9238795325112867385, 1.000000000000000000, 0.9238795325112867385, 1.000000000000000000, 0.9238795325112867385, 1.000000000000000000, 0.9238795325112867385, 1.000000000000000000, 0.9238795325112867385, 1.000000000000000000, 0.9238795325112867385, 1.000000000000000000, 0.9238795325112867385, 1.000000000000000000) ) ) 
 REPRESENTATION_ITEM ( '' )  SURFACE ( )  );
#56258=CARTESIAN_POINT ( 'NONE',  ( -5.656854249492378806, 111.6875000000000000, 5.656854249492381470 ) ) ;
#56260=CARTESIAN_POINT ( 'NONE',  ( -3.313708498984762496, 107.2812499999999858, 7.999999999999998224 ) ) ;
#56266=CARTESIAN_POINT ( 'NONE',  ( -7.188101187500001821, 1.499999997951610542, -2.977408999572651371 ) ) ;
#56268=CARTESIAN_POINT ( 'NONE',  ( 7.188101187500000933, 120.8750000020483810, -2.977408999572651371 ) ) ;
#56288=CARTESIAN_POINT ( 'NONE',  ( -2.977408999572650927, 116.3750000020483810, -7.188101187500000933 ) ) ;
#56293=VECTOR ( 'NONE', #7369, 1000.000000000000000 ) ;
#56295=CARTESIAN_POINT ( 'NONE',  ( 7.188101187500002709, 122.1875000020483668, 2.977408999572649151 ) ) ;
#56305=CARTESIAN_POINT ( 'NONE',  ( 3.313708498984765161, 102.9687499999999858, 7.999999999999998224 ) ) ;
#56313=DIRECTION ( 'NONE',  ( -0.000000000000000000, 1.000000000000000000, -0.000000000000000000 ) ) ;
#56320=CARTESIAN_POINT ( 'NONE',  ( 3.313708498984762496, 1.218750000000000222, 7.999999999999998224 ) ) ;
#56321=CARTESIAN_POINT ( 'NONE',  ( -3.313708498984815343, 109.9062500040967905, -7.999999999999944933 ) ) ;
#56323=CARTESIAN_POINT ( 'NONE',  ( -2.977408999572650039, 20.81249999795161543, -7.188101187500001821 ) ) ;
#56331=ADVANCED_FACE ( 'NONE', ( #64863 ), #63102, .T. ) ;
#56341=CARTESIAN_POINT ( 'NONE',  ( -5.082755093536325042, 26.53124999795161543, -5.082755093536325930 ) ) ;
#56348=CARTESIAN_POINT ( 'NONE',  ( -2.977408999572650927, 89.75000000204839523, -7.188101187500001821 ) ) ;
#56350=EDGE_CURVE ( 'NONE', #45186, #35289, #35633, .T. ) ;
#56357=FACE_OUTER_BOUND ( 'NONE', #5425, .T. ) ;
#56361=CARTESIAN_POINT ( 'NONE',  ( 0.000000000000000000, 125.0000000000000000, 8.000000000000000000 ) ) ;
#56374=CYLINDRICAL_SURFACE ( 'NONE', #63921, 8.000000000000000000 ) ;
#56377=CARTESIAN_POINT ( 'NONE',  ( 5.082755093536325042, 102.5937500020483668, -5.082755093536325930 ) ) ;
#56404=CARTESIAN_POINT ( 'NONE',  ( 2.977408999572652260, 26.06249999795161543, 7.188101187500000044 ) ) ;
#56412=CARTESIAN_POINT ( 'NONE',  ( 7.188101187500001821, 9.562499997951608322, -2.977408999572650483 ) ) ;
#56415=CARTESIAN_POINT ( 'NONE',  ( 7.188101187500000044, 2.343749997951610098, 0.000000000000000000 ) ) ;
#56416=EDGE_LOOP ( 'NONE', ( #18963, #61510, #29902, #59914 ) ) ;
#56423=EDGE_CURVE ( 'NONE', #52808, #40745, #43313, .T. ) ;
#56431=CARTESIAN_POINT ( 'NONE',  ( -7.188101187500000933, 8.624999997951611874, -2.977408999572651371 ) ) ;
#56436=CARTESIAN_POINT ( 'NONE',  ( -2.977408999572651815, 108.3125000020483810, 7.188101187500000933 ) ) ;
#56440=FACE_OUTER_BOUND ( 'NONE', #32305, .T. ) ;
#56461=CARTESIAN_POINT ( 'NONE',  ( 0.000000000000000000, 0.5000000000000004441, 0.000000000000000000 ) ) ;
#56465=CARTESIAN_POINT ( 'NONE',  ( -1.469576158976823947E-15, 20.62500000000000355, 8.000000000000000000 ) ) ;
#56470=CARTESIAN_POINT ( 'NONE',  ( 7.188101187500000044, 118.9062500020483810, -8.802885111219163269E-16 ) ) ;
#56479=CARTESIAN_POINT ( 'NONE',  ( -2.977408999572650039, 20.43749999795161187, -7.188101187500001821 ) ) ;
#56483=ORIENTED_EDGE ( 'NONE', *, *, #64252, .F. ) ;
#56518=CARTESIAN_POINT ( 'NONE',  ( -3.313708498984760720, 9.468750000000000000, -8.000000000000000000 ) ) ;
#56520=CARTESIAN_POINT ( 'NONE',  ( 5.656854249492379694, 90.12500000409677625, -5.656854249492380582 ) ) ;
#56524=ORIENTED_EDGE ( 'NONE', *, *, #72397, .T. ) ;
#56530=CARTESIAN_POINT ( 'NONE',  ( 5.082755093536326818, 123.5937500020483952, 5.082755093536325042 ) ) ;
#56533=CARTESIAN_POINT ( 'NONE',  ( -1.469576158976823947E-15, 3.937499995903220640, 8.000000000000000000 ) ) ;
#56540=EDGE_CURVE ( 'NONE', #111, #17357, #43773, .T. ) ;
#56552=CARTESIAN_POINT ( 'NONE',  ( 3.313708498984765161, 101.4687500000000000, 7.999999999999998224 ) ) ;
#56555=CARTESIAN_POINT ( 'NONE',  ( -3.313708498984760720, 7.781249995903221972, -8.000000000000000000 ) ) ;
#56558=CARTESIAN_POINT ( 'NONE',  ( 5.082755093536325930, 14.53124999795161187, -5.082755093536325930 ) ) ;
#56561=CARTESIAN_POINT ( 'NONE',  ( 1.320432766682874540E-15, 106.9062500020483810, 7.188101187500000044 ) ) ;
#56571=CARTESIAN_POINT ( 'NONE',  ( 9.797174393178825657E-16, 125.0000000000000000, -8.000000000000000000 ) ) ;
#56578=CARTESIAN_POINT ( 'NONE',  ( 1.320432766682874540E-15, 93.03125000204836681, 7.188101187500000044 ) ) ;
#56586=CARTESIAN_POINT ( 'NONE',  ( -2.977408999572651815, 102.3125000020483810, 7.188101187500000933 ) ) ;
#56587=CARTESIAN_POINT ( 'NONE',  ( -1.714702201363321965, 0.4530365834698286132, -7.773580895186361417 ) ) ;
#56605=EDGE_CURVE ( 'NONE', #1872, #68569, #51036, .T. ) ;
#56614=CARTESIAN_POINT ( 'NONE',  ( 4.401442555609581635E-16, 12.84374999795161187, -7.188101187500000044 ) ) ;
#56615=CARTESIAN_POINT ( 'NONE',  ( -5.656854249492380582, 107.0000000040967763, -5.656854249492380582 ) ) ;
#56624=CARTESIAN_POINT ( 'NONE',  ( -2.977408999572651815, 112.4375000020483810, 7.188101187500000933 ) ) ;
#56639=CARTESIAN_POINT ( 'NONE',  ( -3.313708498984762496, 108.7812500000000000, 7.999999999999998224 ) ) ;
#56642=CARTESIAN_POINT ( 'NONE',  ( -5.656854249492380582, 97.81250000000000000, -5.656854249492380582 ) ) ;
#56645=CARTESIAN_POINT ( 'NONE',  ( 8.000000000000000000, 25.31249999590322375, 0.000000000000000000 ) ) ;
#56647=CARTESIAN_POINT ( 'NONE',  ( 7.188101187500000044, 122.2812500020483810, -8.802885111219163269E-16 ) ) ;
#56667=CARTESIAN_POINT ( 'NONE',  ( 7.188101187500000044, 111.4062500020483810, -8.802885111219163269E-16 ) ) ;
#56673=CARTESIAN_POINT ( 'NONE',  ( 7.188101187500000044, 120.7812500020483810, -8.802885111219163269E-16 ) ) ;
#56683=CARTESIAN_POINT ( 'NONE',  ( 0.000000000000000000, 125.0000000000000000, 8.000000000000000000 ) ) ;
#56699=CARTESIAN_POINT ( 'NONE',  ( 7.188101187499999156, 25.87499999795161543, 2.977408999572654924 ) ) ;
#56702=CARTESIAN_POINT ( 'NONE',  ( -7.188101187500001821, 26.99999999795161543, -2.977408999572651371 ) ) ;
#56725=CARTESIAN_POINT ( 'NONE',  ( 8.000000000000000000, 122.7500000000000000, -9.797174393178825657E-16 ) ) ;
#56753=CARTESIAN_POINT ( 'NONE',  ( 7.188101187500000044, 100.9062500020483810, -8.802885111219163269E-16 ) ) ;
#56774=CARTESIAN_POINT ( 'NONE',  ( 8.000000000000001776, 106.3437500040967763, 3.313708498984759387 ) ) ;
#56778=CARTESIAN_POINT ( 'NONE',  ( -2.977408999572654480, 22.87499999795161543, 7.188101187499999156 ) ) ;
#56787=CARTESIAN_POINT ( 'NONE',  ( -2.977408999572650039, 11.43749999795161010, -7.188101187500001821 ) ) ;
#56790=DIRECTION ( 'NONE',  ( -0.000000000000000000, 1.000000000000000000, -0.000000000000000000 ) ) ;
#56798=EDGE_LOOP ( 'NONE', ( #8085, #32788, #12804, #4702 ) ) ;
#56805=CARTESIAN_POINT ( 'NONE',  ( 4.401442555609581635E-16, 14.34374999795161187, -7.188101187500000044 ) ) ;
#56809=CARTESIAN_POINT ( 'NONE',  ( 7.188101187500000044, 108.7812500020483810, -8.802885111219163269E-16 ) ) ;
#56820=CARTESIAN_POINT ( 'NONE',  ( 0.000000000000000000, 125.0000000000000000, 0.000000000000000000 ) ) ;
#56836=DIRECTION ( 'NONE',  ( -0.000000000000000000, 1.000000000000000000, -0.000000000000000000 ) ) ;
#56840=CARTESIAN_POINT ( 'NONE',  ( -2.977408999572651815, 118.4375000020483810, 7.188101187500000933 ) ) ;
#56849=CARTESIAN_POINT ( 'NONE',  ( -7.188101187500000044, 26.71874999795161543, -8.802885111219163269E-16 ) ) ;
#56852=VECTOR ( 'NONE', #20334, 1000.000000000000000 ) ;
#56873=CARTESIAN_POINT ( 'NONE',  ( 4.401442555609581635E-16, 5.718749997951610986, -7.188101187500000044 ) ) ;
#56878=CARTESIAN_POINT ( 'NONE',  ( 5.656854249492379694, 115.6250000040967905, -5.656854249492380582 ) ) ;
#56890=CARTESIAN_POINT ( 'NONE',  ( 8.000000000000000000, 15.00000000000000355, 0.000000000000000000 ) ) ;
#56891=ORIENTED_EDGE ( 'NONE', *, *, #15182, .F. ) ;
#56893=CARTESIAN_POINT ( 'NONE',  ( 8.000000000000000000, 93.03125000409677625, -3.313708498984762496 ) ) ;
#56904=CARTESIAN_POINT ( 'NONE',  ( -4.401442555609581635E-16, 89.28125000204838102, -7.188101187500000044 ) ) ;
#56908=LINE ( 'NONE', #10873, #13295 ) ;
#56926=CARTESIAN_POINT ( 'NONE',  ( 8.000000000000000000, 10.31249999590322020, 0.000000000000000000 ) ) ;
#56929=CARTESIAN_POINT ( 'NONE',  ( 7.188101187500001821, 18.93749999795161187, -2.977408999572650483 ) ) ;
#56932=CARTESIAN_POINT ( 'NONE',  ( 5.082755093536325042, 104.4687500020483952, -5.082755093536325930 ) ) ;
#56948=CARTESIAN_POINT ( 'NONE',  ( -2.977408999572652260, 91.43750000204838102, 7.188101187500000044 ) ) ;
#56956=CARTESIAN_POINT ( 'NONE',  ( -7.188101187499999156, 105.1250000020483668, 2.977408999572654924 ) ) ;
#56962=CARTESIAN_POINT ( 'NONE',  ( 1.469576158976823947E-15, 107.3750000000000000, 8.000000000000000000 ) ) ;
#56969=AXIS2_PLACEMENT_3D ( 'NONE', #73093, #67809, #50821 ) ;
#56981=CARTESIAN_POINT ( 'NONE',  ( 5.082755093536324154, 13.78124999795161010, 5.082755093536326818 ) ) ;
#56982=CARTESIAN_POINT ( 'NONE',  ( -3.313708498984762052, 109.9062500040967905, -8.000000000000000000 ) ) ;
#56989=ORIENTED_EDGE ( 'NONE', *, *, #35268, .T. ) ;
#56990=CARTESIAN_POINT ( 'NONE',  ( -4.401442555609581635E-16, 102.7812500020483810, -7.188101187500000044 ) ) ;
#56993=CARTESIAN_POINT ( 'NONE',  ( -8.000000000000000000, 123.5000000000000000, 0.000000000000000000 ) ) ;
#57008=CARTESIAN_POINT ( 'NONE',  ( -5.656854249492378806, 105.6874999999999858, 5.656854249492381470 ) ) ;
#57015=CARTESIAN_POINT ( 'NONE',  ( -3.313708498984765161, 24.84374999590322020, 7.999999999999998224 ) ) ;
#57038=CARTESIAN_POINT ( 'NONE',  ( -7.188101187500000044, 113.6562500020483810, 0.000000000000000000 ) ) ;
#57043=CARTESIAN_POINT ( 'NONE',  ( -4.401442555609581635E-16, 121.1562500020483810, -7.188101187500000044 ) ) ;
#57044=CARTESIAN_POINT ( 'NONE',  ( -8.000000000000001776, 14.15624999590322730, 3.313708498984759387 ) ) ;
#57055=CARTESIAN_POINT ( 'NONE',  ( 1.469576158976823947E-15, 102.8750000000000000, 8.000000000000000000 ) ) ;
#57068=CARTESIAN_POINT ( 'NONE',  ( -5.082755093536325042, 26.53124999795161543, -5.082755093536325930 ) ) ;
#57071=CARTESIAN_POINT ( 'NONE',  ( 7.188101187499999156, 23.24999999795161187, 2.977408999572654924 ) ) ;
#57076=DIRECTION ( 'NONE',  ( 0.000000000000000000, 0.000000000000000000, 1.000000000000000000 ) ) ;
#57082=CIRCLE ( 'NONE', #72748, 7.499999999999992895 ) ;
#57092=CARTESIAN_POINT ( 'NONE',  ( 3.313708498984760720, 123.0312499999999858, -8.000000000000000000 ) ) ;
#57094=EDGE_CURVE ( 'NONE', #51619, #34267, #7630, .T. ) ;
#57111=CARTESIAN_POINT ( 'NONE',  ( 8.000000000000000000, 10.31249999590322020, 0.000000000000000000 ) ) ;
#57124=CARTESIAN_POINT ( 'NONE',  ( 5.082755093536325042, 104.0937500020483810, -5.082755093536325930 ) ) ;
#57127=CARTESIAN_POINT ( 'NONE',  ( 7.313652169806020176, 0.2330964041442518675, -2.525252314552933086 ) ) ;
#57130=ORIENTED_EDGE ( 'NONE', *, *, #33912, .F. ) ;
#57149=CARTESIAN_POINT ( 'NONE',  ( -5.082755093536326818, 24.28124999795161543, 5.082755093536325042 ) ) ;
#57157=CARTESIAN_POINT ( 'NONE',  ( 7.188101187499999156, 7.874999997951610986, 2.977408999572654924 ) ) ;
#57160=CARTESIAN_POINT ( 'NONE',  ( -7.188101187500001821, 4.499999997951610098, -2.977408999572651371 ) ) ;
#57165=DIRECTION ( 'NONE',  ( 0.000000000000000000, 0.000000000000000000, 1.000000000000000000 ) ) ;
#57177=CARTESIAN_POINT ( 'NONE',  ( 2.977408999572652260, 19.68749999795161543, 7.188101187500000044 ) ) ;
#57181=CARTESIAN_POINT ( 'NONE',  ( -7.188101187499999156, 106.6250000020483952, 2.977408999572654924 ) ) ;
#57184=CYLINDRICAL_SURFACE ( 'NONE', #67100, 8.000000000000000000 ) ;
#57185=CARTESIAN_POINT ( 'NONE',  ( -8.000000000000000000, 95.18750000409679046, 0.000000000000000000 ) ) ;
#57193=DIRECTION ( 'NONE',  ( -0.000000000000000000, 1.000000000000000000, -0.000000000000000000 ) ) ;
#57198=CARTESIAN_POINT ( 'NONE',  ( -8.000000000000000000, 90.40624999999998579, -3.313708498984761608 ) ) ;
#57212=CARTESIAN_POINT ( 'NONE',  ( 2.977408999572650039, 123.6875000020484094, -7.188101187500001821 ) ) ;
#57221=CARTESIAN_POINT ( 'NONE',  ( 5.082755093536324154, 24.28124999795161543, 5.082755093536326818 ) ) ;
#57222=DIRECTION ( 'NONE',  ( 0.000000000000000000, -1.000000000000000000, 0.000000000000000000 ) ) ;
#57244=CARTESIAN_POINT ( 'NONE',  ( -2.977408999572654480, 7.874999997951610986, 7.188101187499999156 ) ) ;
#57260=EDGE_CURVE ( 'NONE', #14040, #44316, #12902, .T. ) ;
#57263=CARTESIAN_POINT ( 'NONE',  ( -8.000000000000000000, 15.75000000000000355, -9.797174393178825657E-16 ) ) ;
#57265=CARTESIAN_POINT ( 'NONE',  ( 1.320432766682874540E-15, 120.0312500020483810, 7.188101187500000044 ) ) ;
#57268=CARTESIAN_POINT ( 'NONE',  ( -8.000000000000000000, 8.156250000000001776, -3.313708498984762496 ) ) ;
#57275=EDGE_CURVE ( 'NONE', #66991, #42278, #61169, .T. ) ;
#57303=CARTESIAN_POINT ( 'NONE',  ( -7.188101187500001821, 19.49999999795161898, -2.977408999572651371 ) ) ;
#57307=CARTESIAN_POINT ( 'NONE',  ( -5.082755093536325930, 100.3437500020483810, -5.082755093536325930 ) ) ;
#57315=CARTESIAN_POINT ( 'NONE',  ( -7.999999999999998224, 119.2812500040967905, 3.313708498984766049 ) ) ;
#57323=CARTESIAN_POINT ( 'NONE',  ( -4.401442555609581635E-16, 93.78125000204836681, -7.188101187500000044 ) ) ;
#57326=CARTESIAN_POINT ( 'NONE',  ( 3.313708498984679895, 111.2187500040967905, -8.000000000000081712 ) ) ;
#57329=CARTESIAN_POINT ( 'NONE',  ( -2.977408999572651815, 94.81250000204838102, 7.188101187500000933 ) ) ;
#57332=( BOUNDED_CURVE ( )  B_SPLINE_CURVE ( 2, ( #69676, #42094, #53067, #69303, #1401, #12329, #17989, #11585, #17614 ),
 .UNSPECIFIED., .F., .F. ) 
 B_SPLINE_CURVE_WITH_KNOTS ( ( 3, 2, 2, 2, 3 ),
 ( 0.6770833333333334814, 0.6822916666666667407, 0.6875000000000001110, 0.6927083333333334814, 0.6979166666666667407 ),
 .UNSPECIFIED. ) 
 CURVE ( )  GEOMETRIC_REPRESENTATION_ITEM ( )  RATIONAL_B_SPLINE_CURVE ( ( 0.9999999999999983347, 0.9238795325112884038, 1.000000000000000000, 0.9238795325112867385, 1.000000000000000000, 0.9238795325112867385, 1.000000000000000000, 0.9238795325112850731, 1.000000000000001554 ) ) 
 REPRESENTATION_ITEM ( '' )  );
#57350=ORIENTED_EDGE ( 'NONE', *, *, #14492, .T. ) ;
#57353=CARTESIAN_POINT ( 'NONE',  ( 7.188101187500000044, 13.96874999795161187, 0.000000000000000000 ) ) ;
#57354=AXIS2_PLACEMENT_3D ( 'NONE', #63097, #11422, #34459 ) ;
#57355=CARTESIAN_POINT ( 'NONE',  ( -8.000000000000000000, 105.5937500040967763, -3.313708498984761608 ) ) ;
#57365=DIRECTION ( 'NONE',  ( -0.000000000000000000, 1.000000000000000000, -0.000000000000000000 ) ) ;
#57366=CARTESIAN_POINT ( 'NONE',  ( -2.977408999572651815, 106.4375000020483810, 7.188101187500000933 ) ) ;
#57372=ORIENTED_EDGE ( 'NONE', *, *, #61207, .T. ) ;
#57382=CARTESIAN_POINT ( 'NONE',  ( -5.656854249492380582, 103.8125000000000000, -5.656854249492380582 ) ) ;
#57385=EDGE_CURVE ( 'NONE', #51832, #43757, #9635, .T. ) ;
#57389=CARTESIAN_POINT ( 'NONE',  ( -8.000000000000001776, 24.65624999590322730, 3.313708498984759387 ) ) ;
#57391=CARTESIAN_POINT ( 'NONE',  ( -7.188101187500000933, 121.4375000020483810, -2.977408999572650483 ) ) ;
#57398=CARTESIAN_POINT ( 'NONE',  ( 3.313708498984744732, 122.4687499999999858, 8.000000000000019540 ) ) ;
#57413=CARTESIAN_POINT ( 'NONE',  ( -4.401442555609581635E-16, 111.7812500020483810, -7.188101187500000044 ) ) ;
#57419=CARTESIAN_POINT ( 'NONE',  ( -4.401442555609581635E-16, 116.6562500020483810, -7.188101187500000044 ) ) ;
#57430=DIRECTION ( 'NONE',  ( -0.000000000000000000, 1.000000000000000000, -0.000000000000000000 ) ) ;
#57443=CARTESIAN_POINT ( 'NONE',  ( 7.188101187500000044, 27.46874999795161543, 0.000000000000000000 ) ) ;
#57446=CARTESIAN_POINT ( 'NONE',  ( -7.188101187500001821, 25.49999999795161898, -2.977408999572651371 ) ) ;
#57467=CARTESIAN_POINT ( 'NONE',  ( -5.656854249492378806, 104.3750000040967763, 5.656854249492381470 ) ) ;
#57476=CARTESIAN_POINT ( 'NONE',  ( 3.313708498984760720, 121.5312500000000142, -8.000000000000000000 ) ) ;
#57479=EDGE_LOOP ( 'NONE', ( #41384, #49525, #38984, #58465 ) ) ;
#57486=CARTESIAN_POINT ( 'NONE',  ( 5.656854249492380582, 5.999999995903221084, -5.656854249492380582 ) ) ;
#57494=CYLINDRICAL_SURFACE ( 'NONE', #56165, 8.000000000000000000 ) ;
#57504=DIRECTION ( 'NONE',  ( 0.000000000000000000, 0.000000000000000000, 1.000000000000000000 ) ) ;
#57508=CARTESIAN_POINT ( 'NONE',  ( -7.188101187499999156, 103.2500000020483810, 2.977408999572654924 ) ) ;
#57514=ORIENTED_EDGE ( 'NONE', *, *, #58132, .F. ) ;
#57527=ORIENTED_EDGE ( 'NONE', *, *, #2738, .F. ) ;
#57532=CARTESIAN_POINT ( 'NONE',  ( -7.188101187500000933, 23.99999999795161543, -2.977408999572651371 ) ) ;
#57540=CARTESIAN_POINT ( 'NONE',  ( 2.977408999572650927, 6.749999997951611874, -7.188101187500001821 ) ) ;
#57543=CARTESIAN_POINT ( 'NONE',  ( -5.082755093536326818, 3.281249997951610098, 5.082755093536325042 ) ) ;
#57558=( BOUNDED_CURVE ( )  B_SPLINE_CURVE ( 2, ( #44866, #67131, #15427, #73526, #38465, #32815, #4141, #27132, #50146 ),
 .UNSPECIFIED., .F., .F. ) 
 B_SPLINE_CURVE_WITH_KNOTS ( ( 3, 2, 2, 2, 3 ),
 ( 0.7638888888888888395, 0.7708333333333333703, 0.7777777777777779011, 0.7847222222222223209, 0.7916666666666667407 ),
 .UNSPECIFIED. ) 
 CURVE ( )  GEOMETRIC_REPRESENTATION_ITEM ( )  RATIONAL_B_SPLINE_CURVE ( ( 1.000000000000000000, 0.9238795325112867385, 1.000000000000000000, 0.9238795325112867385, 1.000000000000000000, 0.9238795325112867385, 1.000000000000000000, 0.9238795325112855172, 1.000000000000001110 ) ) 
 REPRESENTATION_ITEM ( '' )  );
#57559=CARTESIAN_POINT ( 'NONE',  ( -2.977408999572650039, 15.93749999795161365, -7.188101187500000933 ) ) ;
#57563=CARTESIAN_POINT ( 'NONE',  ( 7.188101187500001821, 105.8750000020483952, -2.977408999572651371 ) ) ;
#57566=CARTESIAN_POINT ( 'NONE',  ( -3.313708498984681672, 111.9687500040968047, 8.000000000000078160 ) ) ;
#57573=FACE_OUTER_BOUND ( 'NONE', #27151, .T. ) ;
#57580=CARTESIAN_POINT ( 'NONE',  ( 4.898587196589412829E-16, 4.875000000000000888, -8.000000000000000000 ) ) ;
#57585=CARTESIAN_POINT ( 'NONE',  ( 3.313708498984802020, 10.78125000000000000, -7.999999999999958256 ) ) ;
#57591=CARTESIAN_POINT ( 'NONE',  ( 5.082755093536325042, 122.0937500020483952, -5.082755093536325930 ) ) ;
#57600=CARTESIAN_POINT ( 'NONE',  ( 7.188101187500001821, 23.06249999795161187, -2.977408999572650483 ) ) ;
#57621=CARTESIAN_POINT ( 'NONE',  ( 7.188101187499999156, 8.249999997951611874, 2.977408999572654924 ) ) ;
#57639=CARTESIAN_POINT ( 'NONE',  ( 4.898587196589412829E-16, 15.37500000000000355, -8.000000000000000000 ) ) ;
#57642=CARTESIAN_POINT ( 'NONE',  ( -2.977408999572650927, 122.3750000020483952, -7.188101187500001821 ) ) ;
#57648=ORIENTED_EDGE ( 'NONE', *, *, #37676, .F. ) ;
#57650=CARTESIAN_POINT ( 'NONE',  ( 8.000000000000000000, 113.8437500000000000, -3.313708498984762496 ) ) ;
#57653=CARTESIAN_POINT ( 'NONE',  ( -2.977408999572651815, 121.8125000020483810, 7.188101187500000933 ) ) ;
#57663=EDGE_LOOP ( 'NONE', ( #72065, #28728, #45750, #777 ) ) ;
#57679=CARTESIAN_POINT ( 'NONE',  ( -2.977408999572650039, 22.31249999795161543, -7.188101187500001821 ) ) ;
#57682=CARTESIAN_POINT ( 'NONE',  ( 5.082755093536326818, 98.09375000204838102, 5.082755093536325042 ) ) ;
#57699=CARTESIAN_POINT ( 'NONE',  ( 7.188101187500000044, 94.90625000204838102, -8.802885111219163269E-16 ) ) ;
#57705=CARTESIAN_POINT ( 'NONE',  ( 7.188101187500001821, 98.37500000204840944, -2.977408999572651371 ) ) ;
#57728=CARTESIAN_POINT ( 'NONE',  ( -5.082755093536325042, 16.03124999795161543, -5.082755093536325930 ) ) ;
#57730=CARTESIAN_POINT ( 'NONE',  ( 8.000000000000001776, 104.8437500040967763, 3.313708498984759387 ) ) ;
#57737=DIRECTION ( 'NONE',  ( -0.000000000000000000, 1.000000000000000000, -0.000000000000000000 ) ) ;
#57741=CARTESIAN_POINT ( 'NONE',  ( 1.320432766682874540E-15, 106.5312500020483810, 7.188101187500000044 ) ) ;
#57754=CARTESIAN_POINT ( 'NONE',  ( 0.000000000000000000, 125.0000000000000000, 0.000000000000000000 ) ) ;
#57758=CARTESIAN_POINT ( 'NONE',  ( 8.000000000000001776, 97.15625000000000000, 3.313708498984759387 ) ) ;
#57763=CARTESIAN_POINT ( 'NONE',  ( -7.188101187500001821, 4.499999997951610098, -2.977408999572651371 ) ) ;
#57766=CARTESIAN_POINT ( 'NONE',  ( 5.082755093536325042, 114.9687500020483810, -5.082755093536325930 ) ) ;
#57770=CARTESIAN_POINT ( 'NONE',  ( -3.313708498984765161, 4.031250000000000888, 7.999999999999998224 ) ) ;
#57777=CARTESIAN_POINT ( 'NONE',  ( 8.000000000000000000, 124.3437500000000000, -3.313708498984762496 ) ) ;
#57787=CARTESIAN_POINT ( 'NONE',  ( -2.977408999572650927, 108.8750000020483952, -7.188101187500000933 ) ) ;
#57793=CARTESIAN_POINT ( 'NONE',  ( 2.977408999572650039, 116.5625000020483810, -7.188101187500001821 ) ) ;
#57820=CARTESIAN_POINT ( 'NONE',  ( -8.000000000000000000, 8.156250000000001776, -3.313708498984762496 ) ) ;
#57823=CARTESIAN_POINT ( 'NONE',  ( 7.188101187499999156, 26.24999999795161898, 2.977408999572654924 ) ) ;
#57825=CARTESIAN_POINT ( 'NONE',  ( 3.313708498984760720, 123.2187500040967763, -8.000000000000000000 ) ) ;
#57848=CARTESIAN_POINT ( 'NONE',  ( -7.999999999999998224, 116.0937500000000000, 3.313708498984766493 ) ) ;
#57856=CARTESIAN_POINT ( 'NONE',  ( 8.000000000000000000, 97.25000000000000000, -9.797174393178825657E-16 ) ) ;
#57878=CARTESIAN_POINT ( 'NONE',  ( -5.082755093536325930, 98.46875000204838102, -5.082755093536325930 ) ) ;
#57883=ORIENTED_EDGE ( 'NONE', *, *, #73598, .T. ) ;
#57887=CARTESIAN_POINT ( 'NONE',  ( 9.797174393178825657E-16, 125.0000000000000000, -8.000000000000000000 ) ) ;
#57890=CARTESIAN_POINT ( 'NONE',  ( -3.313708498984775375, 6.843749995903221084, 7.999999999999988454 ) ) ;
#57894=CYLINDRICAL_SURFACE ( 'NONE', #31373, 8.000000000000000000 ) ;
#57897=( BOUNDED_CURVE ( )  B_SPLINE_CURVE ( 2, ( #4996, #27995, #51004, #40060, #34423, #69102, #5732, #35160, #13220 ),
 .UNSPECIFIED., .F., .F. ) 
 B_SPLINE_CURVE_WITH_KNOTS ( ( 3, 2, 2, 2, 3 ),
 ( 0.4687499999999998890, 0.4739583333333332593, 0.4791666666666666297, 0.4843750000000000000, 0.4895833333333333148 ),
 .UNSPECIFIED. ) 
 CURVE ( )  GEOMETRIC_REPRESENTATION_ITEM ( )  RATIONAL_B_SPLINE_CURVE ( ( 1.000000000000001554, 0.9238795325112850731, 1.000000000000000000, 0.9238795325112867385, 1.000000000000000000, 0.9238795325112867385, 1.000000000000000000, 0.9238795325112867385, 1.000000000000000000 ) ) 
 REPRESENTATION_ITEM ( '' )  );
#57903=CARTESIAN_POINT ( 'NONE',  ( -2.977408999572650039, 25.31249999795161543, -7.188101187500000933 ) ) ;
#57911=VECTOR ( 'NONE', #61921, 1000.000000000000000 ) ;
#57913=CARTESIAN_POINT ( 'NONE',  ( -7.188101187500002709, 7.312499997951610986, 2.977408999572649151 ) ) ;
#57916=CARTESIAN_POINT ( 'NONE',  ( 4.401442555609581635E-16, 8.718749997951611874, -7.188101187500000044 ) ) ;
#57931=CARTESIAN_POINT ( 'NONE',  ( -7.188101187500000044, 115.1562500020483810, 0.000000000000000000 ) ) ;
#57936=CARTESIAN_POINT ( 'NONE',  ( 2.977408999572650927, 18.74999999795161543, -7.188101187500000933 ) ) ;
#57941=CARTESIAN_POINT ( 'NONE',  ( 2.977408999572654480, 104.0000000020483810, 7.188101187499999156 ) ) ;
#57965=VECTOR ( 'NONE', #18426, 1000.000000000000000 ) ;
#57971=CARTESIAN_POINT ( 'NONE',  ( 2.977408999572654480, 117.1250000020483952, 7.188101187499999156 ) ) ;
#57986=ORIENTED_EDGE ( 'NONE', *, *, #66956, .F. ) ;
#58004=CARTESIAN_POINT ( 'NONE',  ( -2.977408999572654480, 3.374999997951610986, 7.188101187499999156 ) ) ;
#58022=CARTESIAN_POINT ( 'NONE',  ( -3.313708498984765161, 17.53125000000000711, 7.999999999999998224 ) ) ;
#58024=CARTESIAN_POINT ( 'NONE',  ( 7.188101187500002709, 120.3125000020483668, 2.977408999572649151 ) ) ;
#58026=CARTESIAN_POINT ( 'NONE',  ( -8.000000000000001776, 8.343750000000001776, 3.313708498984759387 ) ) ;
#58033=CARTESIAN_POINT ( 'NONE',  ( 5.082755093536325042, 123.9687500020483952, -5.082755093536325930 ) ) ;
#58056=CARTESIAN_POINT ( 'NONE',  ( -5.082755093536325042, 25.40624999795161543, -5.082755093536325930 ) ) ;
#58058=CARTESIAN_POINT ( 'NONE',  ( 7.188101187500000044, 96.78125000204838102, -8.802885111219163269E-16 ) ) ;
#58067=CARTESIAN_POINT ( 'NONE',  ( -8.000000000000000000, 119.0937500040967905, -3.313708498984761164 ) ) ;
#58075=CARTESIAN_POINT ( 'NONE',  ( 1.320432766682874540E-15, 96.03125000204838102, 7.188101187500000044 ) ) ;
#58080=CARTESIAN_POINT ( 'NONE',  ( 7.188101187500001821, 93.87500000204836681, -2.977408999572651371 ) ) ;
#58085=EDGE_LOOP ( 'NONE', ( #15897, #5004, #4128, #59720 ) ) ;
#58091=CARTESIAN_POINT ( 'NONE',  ( -3.313708498984765161, 11.34374999590322197, 7.999999999999998224 ) ) ;
#58101=CARTESIAN_POINT ( 'NONE',  ( -8.000000000000000000, 101.1875000040967763, 0.000000000000000000 ) ) ;
#58110=CARTESIAN_POINT ( 'NONE',  ( 5.082755093536325042, 105.5937500020483810, -5.082755093536325930 ) ) ;
#58114=( BOUNDED_CURVE ( )  B_SPLINE_CURVE ( 2, ( #17464, #68407, #40485, #63490, #57856, #40858, #17842, #45768, #63865 ),
 .UNSPECIFIED., .F., .F. ) 
 B_SPLINE_CURVE_WITH_KNOTS ( ( 3, 2, 2, 2, 3 ),
 ( 0.7604166666666667407, 0.7656250000000001110, 0.7708333333333334814, 0.7760416666666667407, 0.7812500000000001110 ),
 .UNSPECIFIED. ) 
 CURVE ( )  GEOMETRIC_REPRESENTATION_ITEM ( )  RATIONAL_B_SPLINE_CURVE ( ( 0.9999999999999983347, 0.9238795325112884038, 1.000000000000000000, 0.9238795325112867385, 1.000000000000000000, 0.9238795325112867385, 1.000000000000000000, 0.9238795325112850731, 1.000000000000001554 ) ) 
 REPRESENTATION_ITEM ( '' )  );
#58117=EDGE_CURVE ( 'NONE', #21929, #38634, #48156, .T. ) ;
#58132=EDGE_CURVE ( 'NONE', #3567, #31249, #55898, .T. ) ;
#58133=CARTESIAN_POINT ( 'NONE',  ( 3.313708498984765161, 101.4687499999999858, 7.999999999999998224 ) ) ;
#58140=CARTESIAN_POINT ( 'NONE',  ( -2.977408999572650039, 4.312499997951610098, -7.188101187500001821 ) ) ;
#58143=CARTESIAN_POINT ( 'NONE',  ( -5.082755093536325930, 116.8437500020483810, -5.082755093536325930 ) ) ;
#58154=CARTESIAN_POINT ( 'NONE',  ( -3.313708498984816231, 96.78125000000002842, 7.999999999999943157 ) ) ;
#58164=CARTESIAN_POINT ( 'NONE',  ( 2.977408999572654480, 111.1250000020483810, 7.188101187499999156 ) ) ;
#58170=CARTESIAN_POINT ( 'NONE',  ( -5.082755093536325930, 113.8437500020483810, -5.082755093536325930 ) ) ;
#58171=CARTESIAN_POINT ( 'NONE',  ( -5.656854249492381470, 14.24999999590322375, 5.656854249492379694 ) ) ;
#58194=CARTESIAN_POINT ( 'NONE',  ( -5.656854249492379694, 8.062500000000001776, -5.656854249492380582 ) ) ;
#58196=CARTESIAN_POINT ( 'NONE',  ( -5.082755093536325042, 25.40624999795161543, -5.082755093536325930 ) ) ;
#58197=CARTESIAN_POINT ( 'NONE',  ( -3.313708498984762052, 123.4062500040967905, -8.000000000000000000 ) ) ;
#58203=B_SPLINE_CURVE_WITH_KNOTS ( 'NONE', 1,
 ( #45570, #6346 ),
 .UNSPECIFIED., .F., .F.,
 ( 2, 2 ),
 ( 0.000000000000000000, 1.000000000000000000 ),
 .UNSPECIFIED. ) ;
#58224=CARTESIAN_POINT ( 'NONE',  ( -5.656854249492378806, 116.1875000000000000, 5.656854249492381470 ) ) ;
#58227=ORIENTED_EDGE ( 'NONE', *, *, #58559, .T. ) ;
#58230=CARTESIAN_POINT ( 'NONE',  ( -3.313708498984760720, 13.78124999590322552, -8.000000000000000000 ) ) ;
#58254=CARTESIAN_POINT ( 'NONE',  ( -2.977408999572650927, 98.37500000204840944, -7.188101187500001821 ) ) ;
#58283=CARTESIAN_POINT ( 'NONE',  ( 2.977408999572650927, 14.24999999795161010, -7.188101187500001821 ) ) ;
#58286=CARTESIAN_POINT ( 'NONE',  ( -7.188101187500002709, 7.687499997951611874, 2.977408999572649151 ) ) ;
#58298=CARTESIAN_POINT ( 'NONE',  ( 5.082755093536325042, 117.5937500020483810, -5.082755093536325930 ) ) ;
#58302=CARTESIAN_POINT ( 'NONE',  ( -7.188101187500000044, 14.71874999795161187, -8.802885111219163269E-16 ) ) ;
#58308=CARTESIAN_POINT ( 'NONE',  ( -7.188101187499999156, 100.6250000020483810, 2.977408999572654924 ) ) ;
#58321=CYLINDRICAL_SURFACE ( 'NONE', #32960, 8.000000000000000000 ) ;
#58339=CARTESIAN_POINT ( 'NONE',  ( -7.188101187500001821, 113.5625000020483668, -2.977408999572650483 ) ) ;
#58347=CARTESIAN_POINT ( 'NONE',  ( -7.188101187500000044, 23.71874999795161543, -8.802885111219163269E-16 ) ) ;
#58351=ORIENTED_EDGE ( 'NONE', *, *, #37634, .F. ) ;
#58368=CARTESIAN_POINT ( 'NONE',  ( -1.320432766682874540E-15, 3.468749997951610986, 7.188101187500000044 ) ) ;
#58378=CARTESIAN_POINT ( 'NONE',  ( -8.000000000000000000, 93.59375000409677625, -3.313708498984761164 ) ) ;
#58385=CARTESIAN_POINT ( 'NONE',  ( 8.000000000000000000, 19.59375000000000711, -3.313708498984761608 ) ) ;
#58387=CARTESIAN_POINT ( 'NONE',  ( -7.188101187500000044, 122.6562500020483810, 0.000000000000000000 ) ) ;
#58394=ADVANCED_FACE ( 'NONE', ( #44457 ), #15768, .T. ) ;
#58398=CARTESIAN_POINT ( 'NONE',  ( -7.188101187500001821, 116.9375000020483952, -2.977408999572650483 ) ) ;
#58410=DIRECTION ( 'NONE',  ( 0.000000000000000000, 0.000000000000000000, 1.000000000000000000 ) ) ;
#58422=CARTESIAN_POINT ( 'NONE',  ( 7.188101187499999156, 24.74999999795161543, 2.977408999572654924 ) ) ;
#58424=CARTESIAN_POINT ( 'NONE',  ( 2.977408999572654480, 99.50000000204838102, 7.188101187499999156 ) ) ;
#58438=CARTESIAN_POINT ( 'NONE',  ( 2.977408999572654480, 90.12500000204836681, 7.188101187499999156 ) ) ;
#58444=CARTESIAN_POINT ( 'NONE',  ( 1.320432766682874540E-15, 94.90625000204838102, 7.188101187500000044 ) ) ;
#58453=CARTESIAN_POINT ( 'NONE',  ( 0.000000000000000000, 125.0000000000000000, 0.000000000000000000 ) ) ;
#58464=CARTESIAN_POINT ( 'NONE',  ( -8.000000000000000000, 3.468749995903220196, -3.313708498984762496 ) ) ;
#58465=ORIENTED_EDGE ( 'NONE', *, *, #8106, .F. ) ;
#58466=CARTESIAN_POINT ( 'NONE',  ( -3.313708498984762052, 106.9062500040967763, -8.000000000000000000 ) ) ;
#58473=CARTESIAN_POINT ( 'NONE',  ( -1.469576158976823947E-15, 10.12500000000000178, 8.000000000000000000 ) ) ;
#58476=CARTESIAN_POINT ( 'NONE',  ( 7.188101187500001821, 102.5000000020483810, -2.977408999572651371 ) ) ;
#58485=ORIENTED_EDGE ( 'NONE', *, *, #55893, .F. ) ;
#58494=CARTESIAN_POINT ( 'NONE',  ( 1.469576158976823947E-15, 101.3750000000000000, 8.000000000000000000 ) ) ;
#58498=CARTESIAN_POINT ( 'NONE',  ( 2.977408999572650927, 5.624999997951610986, -7.188101187500001821 ) ) ;
#58501=CARTESIAN_POINT ( 'NONE',  ( 5.082755093536326818, 116.0937500020483810, 5.082755093536325042 ) ) ;
#58502=CARTESIAN_POINT ( 'NONE',  ( 0.000000000000000000, 125.0000000000000000, 0.000000000000000000 ) ) ;
#58522=CARTESIAN_POINT ( 'NONE',  ( -5.082755093536325930, 105.9687500020483952, -5.082755093536325930 ) ) ;
#58527=CARTESIAN_POINT ( 'NONE',  ( -7.188101187499999156, 114.1250000020483952, 2.977408999572654924 ) ) ;
#58533=FACE_OUTER_BOUND ( 'NONE', #47474, .T. ) ;
#58545=EDGE_CURVE ( 'NONE', #16961, #33538, #36075, .T. ) ;
#58547=AXIS2_PLACEMENT_3D ( 'NONE', #3821, #48702, #44179 ) ;
#58555=CARTESIAN_POINT ( 'NONE',  ( -5.656854249492381470, 5.437500000000000888, 5.656854249492379694 ) ) ;
#58556=CARTESIAN_POINT ( 'NONE',  ( -4.898587196589412829E-16, 106.6250000000000000, -8.000000000000000000 ) ) ;
#58557=CARTESIAN_POINT ( 'NONE',  ( -1.320432766682874540E-15, 3.093749997951610542, 7.188101187500000044 ) ) ;
#58558=CARTESIAN_POINT ( 'NONE',  ( 8.000000000000000000, 121.4375000040967763, -9.797174393178825657E-16 ) ) ;
#58559=EDGE_CURVE ( 'NONE', #4846, #54105, #42862, .T. ) ;
#58565=CARTESIAN_POINT ( 'NONE',  ( -3.313708498984765161, 5.343749995903221084, 7.999999999999998224 ) ) ;
#58580=CARTESIAN_POINT ( 'NONE',  ( -8.000000000000000000, 120.5000000000000000, 0.000000000000000000 ) ) ;
#58587=CARTESIAN_POINT ( 'NONE',  ( -8.000000000000000000, 15.56249999590322197, -9.797174393178825657E-16 ) ) ;
#58614=CARTESIAN_POINT ( 'NONE',  ( -7.188101187499999156, 98.75000000204838102, 2.977408999572654924 ) ) ;
#58630=FACE_OUTER_BOUND ( 'NONE', #20459, .T. ) ;
#58643=CARTESIAN_POINT ( 'NONE',  ( 4.401442555609581635E-16, 14.34374999795161187, -7.188101187500000044 ) ) ;
#58646=CARTESIAN_POINT ( 'NONE',  ( -2.977408999572654480, 6.374999997951610098, 7.188101187499999156 ) ) ;
#58658=CARTESIAN_POINT ( 'NONE',  ( -5.082755093536325930, 119.4687500020483810, -5.082755093536325930 ) ) ;
#58663=CARTESIAN_POINT ( 'NONE',  ( 7.188101187499999156, 24.37499999795161543, 2.977408999572654924 ) ) ;
#58665=EDGE_LOOP ( 'NONE', ( #25948, #7447, #71342, #12880 ) ) ;
#58669=CARTESIAN_POINT ( 'NONE',  ( 2.977408999572650039, 103.0625000020483810, -7.188101187500001821 ) ) ;
#58688=CARTESIAN_POINT ( 'NONE',  ( 5.656854249492379694, 97.62500000409677625, -5.656854249492380582 ) ) ;
#58695=CARTESIAN_POINT ( 'NONE',  ( 1.469576158976823947E-15, 103.0625000040967763, 8.000000000000000000 ) ) ;
#58697=CARTESIAN_POINT ( 'NONE',  ( -5.656854249492379694, 4.874999995903221084, -5.656854249492380582 ) ) ;
#58699=CARTESIAN_POINT ( 'NONE',  ( 7.188101187500000044, 115.9062500020483810, -8.802885111219163269E-16 ) ) ;
#58704=CARTESIAN_POINT ( 'NONE',  ( -8.000000000000001776, 24.65624999590322730, 3.313708498984759387 ) ) ;
#58726=CARTESIAN_POINT ( 'NONE',  ( 8.000000000000000000, 112.5312500040967905, -3.313708498984762496 ) ) ;
#58730=CARTESIAN_POINT ( 'NONE',  ( 5.082755093536324154, 9.656249997951610098, 5.082755093536326818 ) ) ;
#58742=ORIENTED_EDGE ( 'NONE', *, *, #38256, .F. ) ;
#58748=CARTESIAN_POINT ( 'NONE',  ( 3.313708498984762496, 22.21875000000000355, 7.999999999999998224 ) ) ;
#58761=CARTESIAN_POINT ( 'NONE',  ( 5.082755093536326818, 119.0937500020483810, 5.082755093536325042 ) ) ;
#58776=CARTESIAN_POINT ( 'NONE',  ( 0.000000000000000000, 54.99999999999999289, 0.000000000000000000 ) ) ;
#58787=CARTESIAN_POINT ( 'NONE',  ( 7.188101187500000044, 26.34374999795161543, 0.000000000000000000 ) ) ;
#58789=CARTESIAN_POINT ( 'NONE',  ( 2.977408999572654480, 96.50000000204838102, 7.188101187499999156 ) ) ;
#58797=CARTESIAN_POINT ( 'NONE',  ( 0.000000000000000000, 125.0000000000000000, 0.000000000000000000 ) ) ;
#58811=CARTESIAN_POINT ( 'NONE',  ( 1.320432766682874540E-15, 97.90625000204839523, 7.188101187500000044 ) ) ;
#58825=ORIENTED_EDGE ( 'NONE', *, *, #60201, .T. ) ;
#58829=EDGE_CURVE ( 'NONE', #35953, #53341, #32507, .T. ) ;
#58833=CARTESIAN_POINT ( 'NONE',  ( 8.000000000000000000, 104.9375000040967763, -9.797174393178825657E-16 ) ) ;
#58835=EDGE_CURVE ( 'NONE', #5359, #50397, #45303, .T. ) ;
#58843=CARTESIAN_POINT ( 'NONE',  ( -5.082755093536324154, 100.3437500020483810, 5.082755093536326818 ) ) ;
#58846=ORIENTED_EDGE ( 'NONE', *, *, #60187, .F. ) ;
#58867=CARTESIAN_POINT ( 'NONE',  ( -1.320432766682874540E-15, 7.968749997951610986, 7.188101187500000044 ) ) ;
#58870=CARTESIAN_POINT ( 'NONE',  ( 5.082755093536326818, 117.5937500020483810, 5.082755093536325042 ) ) ;
#58874=CARTESIAN_POINT ( 'NONE',  ( -4.898587196589412829E-16, 90.12500000000000000, -8.000000000000000000 ) ) ;
#58893=CARTESIAN_POINT ( 'NONE',  ( 5.082755093536326818, 103.7187500020483810, 5.082755093536325042 ) ) ;
#58899=CARTESIAN_POINT ( 'NONE',  ( 7.188101187500001821, 111.8750000020483668, -2.977408999572651371 ) ) ;
#58905=EDGE_LOOP ( 'NONE', ( #14682, #54831, #23920, #26345 ) ) ;
#58908=CARTESIAN_POINT ( 'NONE',  ( -5.656854249492380582, 108.3124999999999858, -5.656854249492380582 ) ) ;
#58926=CARTESIAN_POINT ( 'NONE',  ( -5.656854249492379694, 6.562500000000001776, -5.656854249492380582 ) ) ;
#58928=VECTOR ( 'NONE', #70598, 1000.000000000000000 ) ;
#58929=CARTESIAN_POINT ( 'NONE',  ( 2.977408999572651815, 3.187499997951610098, 7.188101187500000933 ) ) ;
#58930=CARTESIAN_POINT ( 'NONE',  ( -8.000000000000000000, 119.0937500040967905, -3.313708498984761608 ) ) ;
#58940=CARTESIAN_POINT ( 'NONE',  ( 4.898587196589412829E-16, 15.37500000000000355, -8.000000000000000000 ) ) ;
#58944=ORIENTED_EDGE ( 'NONE', *, *, #45013, .T. ) ;
#58952=CARTESIAN_POINT ( 'NONE',  ( 5.656854249492381470, 118.0625000000000000, 5.656854249492379694 ) ) ;
#58957=VECTOR ( 'NONE', #54596, 1000.000000000000000 ) ;
#58958=CARTESIAN_POINT ( 'NONE',  ( -5.656854249492379694, 12.37499999590322197, -5.656854249492380582 ) ) ;
#58961=CARTESIAN_POINT ( 'NONE',  ( 5.656854249492381470, 113.7500000040967763, 5.656854249492379694 ) ) ;
#58987=CARTESIAN_POINT ( 'NONE',  ( 7.188101187500002709, 96.31250000204838102, 2.977408999572649151 ) ) ;
#59003=( BOUNDED_CURVE ( )  B_SPLINE_CURVE ( 2, ( #23952, #30357, #46592, #69614, #17929, #40944, #13352, #18670, #63953 ),
 .UNSPECIFIED., .F., .F. ) 
 B_SPLINE_CURVE_WITH_KNOTS ( ( 3, 2, 2, 2, 3 ),
 ( 0.9479166666666665186, 0.9531249999999998890, 0.9583333333333332593, 0.9635416666666666297, 0.9687500000000000000 ),
 .UNSPECIFIED. ) 
 CURVE ( )  GEOMETRIC_REPRESENTATION_ITEM ( )  RATIONAL_B_SPLINE_CURVE ( ( 1.000000000000001554, 0.9238795325112850731, 1.000000000000000000, 0.9238795325112867385, 1.000000000000000000, 0.9238795325112867385, 1.000000000000000000, 0.9238795325112867385, 1.000000000000000000 ) ) 
 REPRESENTATION_ITEM ( '' )  );
#59004=CARTESIAN_POINT ( 'NONE',  ( 7.999999999999998224, 17.71874999590322730, 3.313708498984766049 ) ) ;
#59015=CARTESIAN_POINT ( 'NONE',  ( 2.977408999572651815, 13.68749999795161365, 7.188101187500000933 ) ) ;
#59018=CARTESIAN_POINT ( 'NONE',  ( 2.977408999572651815, 11.06249999795161187, 7.188101187500000933 ) ) ;
#59031=CARTESIAN_POINT ( 'NONE',  ( 5.082755093536326818, 114.2187500020483810, 5.082755093536325042 ) ) ;
#59035=CARTESIAN_POINT ( 'NONE',  ( 7.188101187500000044, 21.46874999795161543, 0.000000000000000000 ) ) ;
#59041=CARTESIAN_POINT ( 'NONE',  ( -4.401442555609581635E-16, 103.1562500020483810, -7.188101187500000044 ) ) ;
#59064=CARTESIAN_POINT ( 'NONE',  ( 8.000000000000000000, 10.59375000000000178, -3.313708498984761164 ) ) ;
#59068=DIRECTION ( 'NONE',  ( -0.000000000000000000, 1.000000000000000000, -0.000000000000000000 ) ) ;
#59071=CARTESIAN_POINT ( 'NONE',  ( -2.977408999572651815, 113.9375000020483952, 7.188101187500000933 ) ) ;
#59088=CYLINDRICAL_SURFACE ( 'NONE', #70271, 8.000000000000000000 ) ;
#59091=ADVANCED_FACE ( 'NONE', ( #12078 ), #29439, .T. ) ;
#59093=CARTESIAN_POINT ( 'NONE',  ( -5.656854249492378806, 92.18749999999998579, 5.656854249492381470 ) ) ;
#59096=CARTESIAN_POINT ( 'NONE',  ( 8.000000000000001776, 112.3437500040967905, 3.313708498984759387 ) ) ;
#59100=CARTESIAN_POINT ( 'NONE',  ( -7.188101187500002709, 15.18749999795161365, 2.977408999572649151 ) ) ;
#59104=ORIENTED_EDGE ( 'NONE', *, *, #7688, .T. ) ;
#59109=CARTESIAN_POINT ( 'NONE',  ( 1.469576158976823947E-15, 115.0625000040967905, 8.000000000000000000 ) ) ;
#59117=CARTESIAN_POINT ( 'NONE',  ( -5.656854249492379694, 23.06250000000000355, -5.656854249492380582 ) ) ;
#59127=CARTESIAN_POINT ( 'NONE',  ( -1.320432766682874540E-15, 6.093749997951610986, 7.188101187500000044 ) ) ;
#59132=CARTESIAN_POINT ( 'NONE',  ( 2.977408999572650039, 119.5625000020483810, -7.188101187500001821 ) ) ;
#59159=CARTESIAN_POINT ( 'NONE',  ( 5.082755093536324154, 26.15624999795161543, 5.082755093536326818 ) ) ;
#59171=FACE_OUTER_BOUND ( 'NONE', #67359, .T. ) ;
#59177=CARTESIAN_POINT ( 'NONE',  ( -3.313708498984758055, 123.4062500040967905, -8.000000000000001776 ) ) ;
#59189=CARTESIAN_POINT ( 'NONE',  ( -4.898587196589412829E-16, 121.6250000000000000, -8.000000000000000000 ) ) ;
#59193=CARTESIAN_POINT ( 'NONE',  ( 3.313708498984762496, 2.531249995903220196, 7.999999999999998224 ) ) ;
#59204=CARTESIAN_POINT ( 'NONE',  ( -5.656854249492380582, 96.50000000409677625, -5.656854249492380582 ) ) ;
#59213=CARTESIAN_POINT ( 'NONE',  ( -7.188101187500000044, 98.65625000204838102, 0.000000000000000000 ) ) ;
#59217=ORIENTED_EDGE ( 'NONE', *, *, #882, .T. ) ;
#59235=CARTESIAN_POINT ( 'NONE',  ( -5.656854249492379694, 3.374999995903220640, -5.656854249492380582 ) ) ;
#59238=CARTESIAN_POINT ( 'NONE',  ( -1.320432766682874540E-15, 4.968749997951610986, 7.188101187500000044 ) ) ;
#59241=CARTESIAN_POINT ( 'NONE',  ( 7.188101187500000044, 116.2812500020483810, -8.802885111219163269E-16 ) ) ;
#59259=CARTESIAN_POINT ( 'NONE',  ( -5.082755093536324154, 104.8437500020483810, 5.082755093536326818 ) ) ;
#59265=CARTESIAN_POINT ( 'NONE',  ( 7.188101187500001821, 108.8750000020483810, -2.977408999572651371 ) ) ;
#59273=DIRECTION ( 'NONE',  ( -0.000000000000000000, 1.000000000000000000, -0.000000000000000000 ) ) ;
#59290=CARTESIAN_POINT ( 'NONE',  ( 7.999999999999998224, 7.406250000000000888, 3.313708498984766493 ) ) ;
#59291=CARTESIAN_POINT ( 'NONE',  ( -5.656854249492381470, 11.43750000000000178, 5.656854249492379694 ) ) ;
#59292=CARTESIAN_POINT ( 'NONE',  ( -7.188101187500001821, 4.124999997951610986, -2.977408999572651371 ) ) ;
#59305=CARTESIAN_POINT ( 'NONE',  ( -5.656854249492379694, 15.56250000000000355, -5.656854249492380582 ) ) ;
#59311=EDGE_CURVE ( 'NONE', #111, #66661, #61820, .T. ) ;
#59321=CARTESIAN_POINT ( 'NONE',  ( 3.313708498984760720, 120.0312500000000142, -8.000000000000000000 ) ) ;
#59325=CARTESIAN_POINT ( 'NONE',  ( 5.656854249492378806, 17.62499999590322375, 5.656854249492381470 ) ) ;
#59345=CARTESIAN_POINT ( 'NONE',  ( 7.188101187500000933, 122.0000000020483810, -2.977408999572651371 ) ) ;
#59346=DIRECTION ( 'NONE',  ( -0.000000000000000000, 1.000000000000000000, -0.000000000000000000 ) ) ;
#59351=CARTESIAN_POINT ( 'NONE',  ( 2.977408999572654480, 97.62500000204836681, 7.188101187499999156 ) ) ;
#59358=FACE_OUTER_BOUND ( 'NONE', #16717, .T. ) ;
#59365=DIRECTION ( 'NONE',  ( -0.000000000000000000, 1.000000000000000000, -0.000000000000000000 ) ) ;
#59370=CARTESIAN_POINT ( 'NONE',  ( 5.082755093536324154, 27.65624999795161543, 5.082755093536326818 ) ) ;
#59378=CARTESIAN_POINT ( 'NONE',  ( -5.082755093536325042, 13.03124999795161187, -5.082755093536325930 ) ) ;
#59381=CARTESIAN_POINT ( 'NONE',  ( -7.188101187500000044, 12.09374999795161187, -8.802885111219163269E-16 ) ) ;
#59392=CARTESIAN_POINT ( 'NONE',  ( -2.977408999572651815, 118.4375000020483810, 7.188101187500000933 ) ) ;
#59397=CARTESIAN_POINT ( 'NONE',  ( 2.977408999572652260, 24.18749999795161543, 7.188101187500000044 ) ) ;
#59403=CARTESIAN_POINT ( 'NONE',  ( -5.082755093536324154, 102.2187500020483810, 5.082755093536326818 ) ) ;
#59407=( BOUNDED_SURFACE ( )  B_SPLINE_SURFACE ( 1, 2, ( 
 ( #43969, #14162, #42833, #8894, #60945, #66978, #61696, #20192, #49629, #72644, #66229, #37195, #37571, #61323, #73014, #38317, #55301, #49997, #43211, #3994, #32287, #72259, #26983, #3609, #26605, #21324, #9649, #60195, #20947, #25850, #26223, #48870, #66601, #33050, #71878, #15280, #14907, #9265, #38695, #32669, #55679, #44345, #67355, #15654, #31907, #49243, #10018, #54928, #14531, #56049, #60570, #3237, #4358, #27350, #50367, #20572, #73384, #37946, #65852, #8517, #31534, #2862, #39791, #11869, #63175, #34157, #62061, #57540, #69210, #33790, #46195, #16764, #51865, #57913, #6222, #50738, #17148, #62795, #11501, #57157, #39060, #39428, #74125, #5849, #11134, #29225, #73752, #62427, #5473, #40538, #51483, #63544, #52238, #22058, #206, #21690, #44716, #56412, #23184, #4733, #34905, #16389, #68464, #28842, #17522, #28475, #67731, #33412, #40170, #34534, #45447, #10753, #27727, #16027, #10386, #45085, #68100, #56787, #5108, #74494, #28098, #51113, #22427, #22803, #45824, #68835, #69586, #41650, #63923, #17899, #35998, #6586, #64660, #70327, #59378, #1672, #12960, #35628, #47302, #7689, #30696, #59015, #7323, #53714, #19002, #40912, #30327, #58283, #58643, #29593, #24291, #65393, #52604, #53347, #18642, #24652, #71043, #47662, #70684, #2028, #42008, #65016, #41284, #6949, #19362, #64294, #942, #25014, #23924, #46933, #36362, #13325, #48034, #18269, #8053, #69961, #42376, #13690, #31056, #36732, #59743, #572, #23553, #46565, #12233, #35270, #12601, #29961, #52974, #1307, #9558, #15562, #32573, #26130, #49149, #48778, #60474, #20855, #38601, #2771, #72160, #8421, #71785, #31815, #15195, #20470, #61600, #31437, #20103, #43490, #72920, #9172, #21230, #9920, #54464, #55581, #54084, #2394, #14063, #3896, #37099, #44256, #43115, #66502, #38224, #61229, #14814, #25391, #65761, #72550, #43873, #3146, #66134, #60103, #48406, #71412, #26890, #66889, #67267, #19736, #37855, #42745, #25757, #54836, #55210, #14439, #37473, #8804, #60852, #32191, #3516, #26505, #49529, #49906, #28012, #17055, #34071, #22332, #68001, #5014, #40078, #63083, #68374, #16671, #11407, #51390, #27258, #45359, #15934, #16297, #38964, #56699, #23091, #61967, #39702, #51022, #74029, #28750, #57068, #5380, #34444, #62702, #74403, #73661, #39337, #51766, #21970, #10295, #57443 ),
 ( #11040, #4639, #63450, #28381, #5751, #22711, #44998, #62334, #55958, #50276, #113, #10661, #33694, #56320, #46103, #45728, #69122, #4268, #68742, #17427, #40451, #32952, #73296, #21598, #33321, #44624, #67639, #27635, #50643, #52886, #41195, #6860, #70958, #19276, #47941, #41920, #53256, #1938, #24927, #35540, #483, #17805, #12509, #12871, #35179, #42286, #6127, #1218, #23463, #29132, #47209, #40820, #24197, #29872, #70597, #35908, #70241, #46844, #58555, #18914, #64931, #18551, #41557, #13240, #30238, #52148, #64574, #69495, #69867, #63826, #58926, #11775, #12142, #7234, #1584, #24569, #7598, #47574, #36274, #59290, #30605, #53626, #52516, #18180, #34813, #853, #58194, #57820, #6499, #29505, #46475, #23838, #64205, #9366, #73852, #48317, #33151, #56145, #22157, #38417, #9746, #56518, #4456, #4090, #30971, #27447, #39156, #3710, #16118, #61418, #21785, #27830, #44814, #32766, #55773, #61042, #72744, #50462, #50840, #13966, #27084, #19644, #65300, #42657, #61794, #50096, #73477, #73112, #7968, #32386, #44072, #67825, #21419, #13605, #65668, #55400, #44443, #10482, #67455, #33514, #36643, #37009, #62159, #59650, #53990, #25298, #4833, #71323, #2300, #26709, #15750, #49728, #21047, #38791, #67081, #15380, #10112, #63646, #68938, #34259, #56890, #63271, #35374, #11975, #57639, #10854, #6328, #18003, #57263, #69690, #40270, #677, #6691, #23663, #17248, #11597, #39894, #51582, #35007, #29696, #68568, #34632, #74224, #52711, #22528, #40643, #5950, #58022, #28949, #62526, #62899, #22913, #29330, #51969, #1044, #45550, #11231, #306, #64028, #23285, #12341, #45185, #16868, #46668, #68196, #16492, #5204, #41021, #28202, #58385, #5576, #46295, #52339, #39530, #69316, #33888, #51215, #28576, #74601, #17625, #45925, #35731, #31542, #60203, #54192, #65496, #14170, #37204, #47766, #12700, #30066, #24756, #25119, #47405, #8527, #18375, #65118, #58748, #41389, #59481, #53080, #13428, #19102, #8157, #48137, #36465, #59117, #70787, #31165, #2499, #7794, #30797, #25493, #42480, #64402, #53819, #7058, #7426, #1414, #42107, #54563, #24399, #2127, #71145, #19467, #19836, #13791, #36837, #48508, #59843, #71513, #64761, #30433, #42844, #13062, #70428, #65862, #18745, #41753, #24024, #47033, #70068, #36100, #53453, #1772, #44354, #67365, #33421, #49638 ) ),
 .UNSPECIFIED., .F., .F., .F. ) 
 B_SPLINE_SURFACE_WITH_KNOTS ( ( 2, 2 ),
 ( 3, 2, 2, 2, 2, 2, 2, 2, 2, 2, 2, 2, 2, 2, 2, 2, 2, 2, 2, 2, 2, 2, 2, 2, 2, 2, 2, 2, 2, 2, 2, 2, 2, 2, 2, 2, 2, 2, 2, 2, 2, 2, 2, 2, 2, 2, 2, 2, 2, 2, 2, 2, 2, 2, 2, 2, 2, 2, 2, 2, 2, 2, 2, 2, 2, 2, 2, 2, 2, 2, 2, 2, 2, 2, 2, 2, 2, 2, 2, 2, 2, 2, 2, 2, 2, 2, 2, 2, 2, 2, 2, 2, 2, 2, 2, 2, 2, 2, 2, 2, 2, 2, 2, 2, 2, 2, 2, 2, 2, 2, 2, 2, 2, 2, 2, 2, 2, 2, 2, 2, 2, 2, 2, 2, 2, 2, 2, 2, 2, 2, 2, 2, 2, 2, 2, 2, 2, 2, 2, 2, 2, 2, 2, 2, 3 ),
 ( 0.000000000000000000, 1.000000000000000000 ),
 ( 0.000000000000000000, 0.006944444444444444059, 0.01388888888888888812, 0.02083333333333333218, 0.02777777777777777624, 0.03472222222222222376, 0.04166666666666666435, 0.04861111111111111188, 0.05555555555555555247, 0.06250000000000000000, 0.06944444444444444753, 0.07638888888888889506, 0.08333333333333332871, 0.09027777777777777624, 0.09722222222222222376, 0.1041666666666666713, 0.1111111111111111049, 0.1180555555555555525, 0.1250000000000000000, 0.1319444444444444475, 0.1388888888888888951, 0.1458333333333333426, 0.1527777777777777901, 0.1597222222222222099, 0.1666666666666666574, 0.1736111111111111049, 0.1805555555555555525, 0.1875000000000000000, 0.1944444444444444475, 0.2013888888888888951, 0.2083333333333333426, 0.2152777777777777901, 0.2222222222222222099, 0.2291666666666666574, 0.2361111111111111049, 0.2430555555555555525, 0.2500000000000000000, 0.2569444444444444198, 0.2638888888888888951, 0.2708333333333333148, 0.2777777777777777901, 0.2847222222222222099, 0.2916666666666666852, 0.2986111111111111049, 0.3055555555555555802, 0.3125000000000000000, 0.3194444444444444198, 0.3263888888888888951, 0.3333333333333333148, 0.3402777777777777901, 0.3472222222222222099, 0.3541666666666666852, 0.3611111111111111049, 0.3680555555555555802, 0.3750000000000000000, 0.3819444444444444198, 0.3888888888888888951, 0.3958333333333333148, 0.4027777777777777901, 0.4097222222222222099, 0.4166666666666666852, 0.4236111111111111049, 0.4305555555555555802, 0.4375000000000000000, 0.4444444444444444198, 0.4513888888888888951, 0.4583333333333333148, 0.4652777777777777901, 0.4722222222222222099, 0.4791666666666666852, 0.4861111111111111049, 0.4930555555555555802, 0.5000000000000000000, 0.5069444444444444198, 0.5138888888888888395, 0.5208333333333333703, 0.5277777777777777901, 0.5347222222222222099, 0.5416666666666666297, 0.5486111111111111605, 0.5555555555555555802, 0.5625000000000000000, 0.5694444444444444198, 0.5763888888888888395, 0.5833333333333333703, 0.5902777777777777901, 0.5972222222222222099, 0.6041666666666666297, 0.6111111111111111605, 0.6180555555555555802, 0.6250000000000000000, 0.6319444444444444198, 0.6388888888888888395, 0.6458333333333333703, 0.6527777777777777901, 0.6597222222222222099, 0.6666666666666666297, 0.6736111111111111605, 0.6805555555555555802, 0.6875000000000000000, 0.6944444444444444198, 0.7013888888888888395, 0.7083333333333333703, 0.7152777777777777901, 0.7222222222222222099, 0.7291666666666666297, 0.7361111111111111605, 0.7430555555555555802, 0.7500000000000000000, 0.7569444444444444198, 0.7638888888888888395, 0.7708333333333333703, 0.7777777777777777901, 0.7847222222222222099, 0.7916666666666666297, 0.7986111111111111605, 0.8055555555555555802, 0.8125000000000000000, 0.8194444444444444198, 0.8263888888888888395, 0.8333333333333333703, 0.8402777777777777901, 0.8472222222222222099, 0.8541666666666666297, 0.8611111111111111605, 0.8680555555555555802, 0.8750000000000000000, 0.8819444444444444198, 0.8888888888888888395, 0.8958333333333333703, 0.9027777777777777901, 0.9097222222222222099, 0.9166666666666666297, 0.9236111111111111605, 0.9305555555555555802, 0.9375000000000000000, 0.9444444444444444198, 0.9513888888888888395, 0.9583333333333333703, 0.9652777777777777901, 0.9722222222222222099, 0.9791666666666666297, 0.9861111111111111605, 0.9930555555555555802, 1.000000000000000000 ),
 .UNSPECIFIED. ) 
 GEOMETRIC_REPRESENTATION_ITEM ( )  RATIONAL_B_SPLINE_SURFACE ( (
 ( 1.000000000000000000, 0.9238795325112867385, 1.000000000000000000, 0.9238795325112867385, 1.000000000000000000, 0.9238795325112867385, 1.000000000000000000, 0.9238795325112867385, 1.000000000000000000, 0.9238795325112867385, 1.000000000000000000, 0.9238795325112867385, 1.000000000000000000, 0.9238795325112867385, 1.000000000000000000, 0.9238795325112867385, 1.000000000000000000, 0.9238795325112867385, 1.000000000000000000, 0.9238795325112867385, 1.000000000000000000, 0.9238795325112867385, 1.000000000000000000, 0.9238795325112867385, 1.000000000000000000, 0.9238795325112867385, 1.000000000000000000, 0.9238795325112867385, 1.000000000000000000, 0.9238795325112867385, 1.000000000000000000, 0.9238795325112867385, 1.000000000000000000, 0.9238795325112867385, 1.000000000000000000, 0.9238795325112867385, 1.000000000000000000, 0.9238795325112867385, 1.000000000000000000, 0.9238795325112867385, 1.000000000000000000, 0.9238795325112867385, 1.000000000000000000, 0.9238795325112867385, 1.000000000000000000, 0.9238795325112867385, 1.000000000000000000, 0.9238795325112867385, 1.000000000000000000, 0.9238795325112867385, 1.000000000000000000, 0.9238795325112867385, 1.000000000000000000, 0.9238795325112867385, 1.000000000000000000, 0.9238795325112867385, 1.000000000000000000, 0.9238795325112867385, 1.000000000000000000, 0.9238795325112867385, 1.000000000000000000, 0.9238795325112867385, 1.000000000000000000, 0.9238795325112867385, 1.000000000000000000, 0.9238795325112867385, 1.000000000000000000, 0.9238795325112867385, 1.000000000000000000, 0.9238795325112867385, 1.000000000000000000, 0.9238795325112867385, 1.000000000000000000, 0.9238795325112867385, 1.000000000000000000, 0.9238795325112867385, 1.000000000000000000, 0.9238795325112867385, 1.000000000000000000, 0.9238795325112867385, 1.000000000000000000, 0.9238795325112867385, 1.000000000000000000, 0.9238795325112867385, 1.000000000000000000, 0.9238795325112867385, 1.000000000000000000, 0.9238795325112867385, 1.000000000000000000, 0.9238795325112867385, 1.000000000000000000, 0.9238795325112867385, 1.000000000000000000, 0.9238795325112867385, 1.000000000000000000, 0.9238795325112867385, 1.000000000000000000, 0.9238795325112867385, 1.000000000000000000, 0.9238795325112867385, 1.000000000000000000, 0.9238795325112867385, 1.000000000000000000, 0.9238795325112867385, 1.000000000000000000, 0.9238795325112867385, 1.000000000000000000, 0.9238795325112867385, 1.000000000000000000, 0.9238795325112867385, 1.000000000000000000, 0.9238795325112867385, 1.000000000000000000, 0.9238795325112867385, 1.000000000000000000, 0.9238795325112867385, 1.000000000000000000, 0.9238795325112867385, 1.000000000000000000, 0.9238795325112867385, 1.000000000000000000, 0.9238795325112867385, 1.000000000000000000, 0.9238795325112867385, 1.000000000000000000, 0.9238795325112867385, 1.000000000000000000, 0.9238795325112867385, 1.000000000000000000, 0.9238795325112867385, 1.000000000000000000, 0.9238795325112867385, 1.000000000000000000, 0.9238795325112867385, 1.000000000000000000, 0.9238795325112867385, 1.000000000000000000, 0.9238795325112867385, 1.000000000000000000, 0.9238795325112867385, 1.000000000000000000, 0.9238795325112867385, 1.000000000000000000, 0.9238795325112867385, 1.000000000000000000, 0.9238795325112867385, 1.000000000000000000, 0.9238795325112867385, 1.000000000000000000, 0.9238795325112867385, 1.000000000000000000, 0.9238795325112867385, 1.000000000000000000, 0.9238795325112867385, 1.000000000000000000, 0.9238795325112867385, 1.000000000000000000, 0.9238795325112867385, 1.000000000000000000, 0.9238795325112867385, 1.000000000000000000, 0.9238795325112867385, 1.000000000000000000, 0.9238795325112867385, 1.000000000000000000, 0.9238795325112867385, 1.000000000000000000, 0.9238795325112867385, 1.000000000000000000, 0.9238795325112867385, 1.000000000000000000, 0.9238795325112867385, 1.000000000000000000, 0.9238795325112867385, 1.000000000000000000, 0.9238795325112867385, 1.000000000000000000, 0.9238795325112867385, 1.000000000000000000, 0.9238795325112867385, 1.000000000000000000, 0.9238795325112867385, 1.000000000000000000, 0.9238795325112867385, 1.000000000000000000, 0.9238795325112867385, 1.000000000000000000, 0.9238795325112867385, 1.000000000000000000, 0.9238795325112867385, 1.000000000000000000, 0.9238795325112867385, 1.000000000000000000, 0.9238795325112867385, 1.000000000000000000, 0.9238795325112867385, 1.000000000000000000, 0.9238795325112867385, 1.000000000000000000, 0.9238795325112867385, 1.000000000000000000, 0.9238795325112867385, 1.000000000000000000, 0.9238795325112867385, 1.000000000000000000, 0.9238795325112867385, 1.000000000000000000, 0.9238795325112867385, 1.000000000000000000, 0.9238795325112867385, 1.000000000000000000, 0.9238795325112867385, 1.000000000000000000, 0.9238795325112867385, 1.000000000000000000, 0.9238795325112867385, 1.000000000000000000, 0.9238795325112867385, 1.000000000000000000, 0.9238795325112867385, 1.000000000000000000, 0.9238795325112867385, 1.000000000000000000, 0.9238795325112867385, 1.000000000000000000, 0.9238795325112867385, 1.000000000000000000, 0.9238795325112867385, 1.000000000000000000, 0.9238795325112867385, 1.000000000000000000, 0.9238795325112867385, 1.000000000000000000, 0.9238795325112867385, 1.000000000000000000, 0.9238795325112867385, 1.000000000000000000, 0.9238795325112867385, 1.000000000000000000, 0.9238795325112867385, 1.000000000000000000, 0.9238795325112867385, 1.000000000000000000, 0.9238795325112867385, 1.000000000000000000, 0.9238795325112867385, 1.000000000000000000, 0.9238795325112867385, 1.000000000000000000, 0.9238795325112867385, 1.000000000000000000, 0.9238795325112867385, 1.000000000000000000, 0.9238795325112867385, 1.000000000000000000, 0.9238795325112867385, 1.000000000000000000, 0.9238795325112867385, 1.000000000000000000, 0.9238795325112867385, 1.000000000000000000, 0.9238795325112867385, 1.000000000000000000, 0.9238795325112867385, 1.000000000000000000, 0.9238795325112867385, 1.000000000000000000, 0.9238795325112867385, 1.000000000000000000, 0.9238795325112867385, 1.000000000000000000, 0.9238795325112867385, 1.000000000000000000, 0.9238795325112867385, 1.000000000000000000, 0.9238795325112867385, 1.000000000000000000, 0.9238795325112867385, 1.000000000000000000, 0.9238795325112867385, 1.000000000000000000, 0.9238795325112867385, 1.000000000000000000, 0.9238795325112867385, 1.000000000000000000, 0.9238795325112867385, 1.000000000000000000, 0.9238795325112867385, 1.000000000000000000),
 ( 1.000000000000000000, 0.9238795325112867385, 1.000000000000000000, 0.9238795325112867385, 1.000000000000000000, 0.9238795325112867385, 1.000000000000000000, 0.9238795325112867385, 1.000000000000000000, 0.9238795325112867385, 1.000000000000000000, 0.9238795325112867385, 1.000000000000000000, 0.9238795325112867385, 1.000000000000000000, 0.9238795325112867385, 1.000000000000000000, 0.9238795325112867385, 1.000000000000000000, 0.9238795325112867385, 1.000000000000000000, 0.9238795325112867385, 1.000000000000000000, 0.9238795325112867385, 1.000000000000000000, 0.9238795325112867385, 1.000000000000000000, 0.9238795325112867385, 1.000000000000000000, 0.9238795325112867385, 1.000000000000000000, 0.9238795325112867385, 1.000000000000000000, 0.9238795325112867385, 1.000000000000000000, 0.9238795325112867385, 1.000000000000000000, 0.9238795325112867385, 1.000000000000000000, 0.9238795325112867385, 1.000000000000000000, 0.9238795325112867385, 1.000000000000000000, 0.9238795325112867385, 1.000000000000000000, 0.9238795325112867385, 1.000000000000000000, 0.9238795325112867385, 1.000000000000000000, 0.9238795325112867385, 1.000000000000000000, 0.9238795325112867385, 1.000000000000000000, 0.9238795325112867385, 1.000000000000000000, 0.9238795325112867385, 1.000000000000000000, 0.9238795325112867385, 1.000000000000000000, 0.9238795325112867385, 1.000000000000000000, 0.9238795325112867385, 1.000000000000000000, 0.9238795325112867385, 1.000000000000000000, 0.9238795325112867385, 1.000000000000000000, 0.9238795325112867385, 1.000000000000000000, 0.9238795325112867385, 1.000000000000000000, 0.9238795325112867385, 1.000000000000000000, 0.9238795325112867385, 1.000000000000000000, 0.9238795325112867385, 1.000000000000000000, 0.9238795325112867385, 1.000000000000000000, 0.9238795325112867385, 1.000000000000000000, 0.9238795325112867385, 1.000000000000000000, 0.9238795325112867385, 1.000000000000000000, 0.9238795325112867385, 1.000000000000000000, 0.9238795325112867385, 1.000000000000000000, 0.9238795325112867385, 1.000000000000000000, 0.9238795325112867385, 1.000000000000000000, 0.9238795325112867385, 1.000000000000000000, 0.9238795325112867385, 1.000000000000000000, 0.9238795325112867385, 1.000000000000000000, 0.9238795325112867385, 1.000000000000000000, 0.9238795325112867385, 1.000000000000000000, 0.9238795325112867385, 1.000000000000000000, 0.9238795325112867385, 1.000000000000000000, 0.9238795325112867385, 1.000000000000000000, 0.9238795325112867385, 1.000000000000000000, 0.9238795325112867385, 1.000000000000000000, 0.9238795325112867385, 1.000000000000000000, 0.9238795325112867385, 1.000000000000000000, 0.9238795325112867385, 1.000000000000000000, 0.9238795325112867385, 1.000000000000000000, 0.9238795325112867385, 1.000000000000000000, 0.9238795325112867385, 1.000000000000000000, 0.9238795325112867385, 1.000000000000000000, 0.9238795325112867385, 1.000000000000000000, 0.9238795325112867385, 1.000000000000000000, 0.9238795325112867385, 1.000000000000000000, 0.9238795325112867385, 1.000000000000000000, 0.9238795325112867385, 1.000000000000000000, 0.9238795325112867385, 1.000000000000000000, 0.9238795325112867385, 1.000000000000000000, 0.9238795325112867385, 1.000000000000000000, 0.9238795325112867385, 1.000000000000000000, 0.9238795325112867385, 1.000000000000000000, 0.9238795325112867385, 1.000000000000000000, 0.9238795325112867385, 1.000000000000000000, 0.9238795325112867385, 1.000000000000000000, 0.9238795325112867385, 1.000000000000000000, 0.9238795325112867385, 1.000000000000000000, 0.9238795325112867385, 1.000000000000000000, 0.9238795325112867385, 1.000000000000000000, 0.9238795325112867385, 1.000000000000000000, 0.9238795325112867385, 1.000000000000000000, 0.9238795325112867385, 1.000000000000000000, 0.9238795325112867385, 1.000000000000000000, 0.9238795325112867385, 1.000000000000000000, 0.9238795325112867385, 1.000000000000000000, 0.9238795325112867385, 1.000000000000000000, 0.9238795325112867385, 1.000000000000000000, 0.9238795325112867385, 1.000000000000000000, 0.9238795325112867385, 1.000000000000000000, 0.9238795325112867385, 1.000000000000000000, 0.9238795325112867385, 1.000000000000000000, 0.9238795325112867385, 1.000000000000000000, 0.9238795325112867385, 1.000000000000000000, 0.9238795325112867385, 1.000000000000000000, 0.9238795325112867385, 1.000000000000000000, 0.9238795325112867385, 1.000000000000000000, 0.9238795325112867385, 1.000000000000000000, 0.9238795325112867385, 1.000000000000000000, 0.9238795325112867385, 1.000000000000000000, 0.9238795325112867385, 1.000000000000000000, 0.9238795325112867385, 1.000000000000000000, 0.9238795325112867385, 1.000000000000000000, 0.9238795325112867385, 1.000000000000000000, 0.9238795325112867385, 1.000000000000000000, 0.9238795325112867385, 1.000000000000000000, 0.9238795325112867385, 1.000000000000000000, 0.9238795325112867385, 1.000000000000000000, 0.9238795325112867385, 1.000000000000000000, 0.9238795325112867385, 1.000000000000000000, 0.9238795325112867385, 1.000000000000000000, 0.9238795325112867385, 1.000000000000000000, 0.9238795325112867385, 1.000000000000000000, 0.9238795325112867385, 1.000000000000000000, 0.9238795325112867385, 1.000000000000000000, 0.9238795325112867385, 1.000000000000000000, 0.9238795325112867385, 1.000000000000000000, 0.9238795325112867385, 1.000000000000000000, 0.9238795325112867385, 1.000000000000000000, 0.9238795325112867385, 1.000000000000000000, 0.9238795325112867385, 1.000000000000000000, 0.9238795325112867385, 1.000000000000000000, 0.9238795325112867385, 1.000000000000000000, 0.9238795325112867385, 1.000000000000000000, 0.9238795325112867385, 1.000000000000000000, 0.9238795325112867385, 1.000000000000000000, 0.9238795325112867385, 1.000000000000000000, 0.9238795325112867385, 1.000000000000000000, 0.9238795325112867385, 1.000000000000000000, 0.9238795325112867385, 1.000000000000000000, 0.9238795325112867385, 1.000000000000000000, 0.9238795325112867385, 1.000000000000000000, 0.9238795325112867385, 1.000000000000000000, 0.9238795325112867385, 1.000000000000000000, 0.9238795325112867385, 1.000000000000000000, 0.9238795325112867385, 1.000000000000000000, 0.9238795325112867385, 1.000000000000000000, 0.9238795325112867385, 1.000000000000000000, 0.9238795325112867385, 1.000000000000000000, 0.9238795325112867385, 1.000000000000000000, 0.9238795325112867385, 1.000000000000000000, 0.9238795325112867385, 1.000000000000000000, 0.9238795325112867385, 1.000000000000000000, 0.9238795325112867385, 1.000000000000000000) ) ) 
 REPRESENTATION_ITEM ( '' )  SURFACE ( )  );
#59428=CARTESIAN_POINT ( 'NONE',  ( 4.898587196589412829E-16, 7.687499995903221084, -8.000000000000000000 ) ) ;
#59432=( BOUNDED_CURVE ( )  B_SPLINE_CURVE ( 2, ( #59816, #9631, #42450, #55660, #14888, #37927, #65468, #43952, #48851 ),
 .UNSPECIFIED., .F., .F. ) 
 B_SPLINE_CURVE_WITH_KNOTS ( ( 3, 2, 2, 2, 3 ),
 ( 0.8229166666666667407, 0.8281250000000001110, 0.8333333333333334814, 0.8385416666666668517, 0.8437500000000002220 ),
 .UNSPECIFIED. ) 
 CURVE ( )  GEOMETRIC_REPRESENTATION_ITEM ( )  RATIONAL_B_SPLINE_CURVE ( ( 0.9999999999999983347, 0.9238795325112884038, 1.000000000000000000, 0.9238795325112867385, 1.000000000000000000, 0.9238795325112867385, 1.000000000000000000, 0.9238795325112835188, 1.000000000000003331 ) ) 
 REPRESENTATION_ITEM ( '' )  );
#59433=CARTESIAN_POINT ( 'NONE',  ( 4.898587196589412829E-16, 4.687499995903220196, -8.000000000000000000 ) ) ;
#59435=CARTESIAN_POINT ( 'NONE',  ( 5.082755093536326818, 114.2187500020483810, 5.082755093536325042 ) ) ;
#59439=CARTESIAN_POINT ( 'NONE',  ( 9.797174393178825657E-16, 125.0000000000000000, -8.000000000000000000 ) ) ;
#59441=ORIENTED_EDGE ( 'NONE', *, *, #35627, .T. ) ;
#59455=CARTESIAN_POINT ( 'NONE',  ( -8.000000000000000000, 92.00000000000000000, 0.000000000000000000 ) ) ;
#59458=CARTESIAN_POINT ( 'NONE',  ( -4.898587196589412829E-16, 99.12499999999998579, -8.000000000000000000 ) ) ;
#59463=CARTESIAN_POINT ( 'NONE',  ( 7.188101187500000933, 12.93749999795161187, -2.977408999572650483 ) ) ;
#59481=CARTESIAN_POINT ( 'NONE',  ( 7.999999999999998224, 22.40625000000000355, 3.313708498984766493 ) ) ;
#59483=ORIENTED_EDGE ( 'NONE', *, *, #67930, .T. ) ;
#59492=CARTESIAN_POINT ( 'NONE',  ( -5.082755093536325042, 2.531249997951610542, -5.082755093536325930 ) ) ;
#59494=CARTESIAN_POINT ( 'NONE',  ( -2.977408999572651815, 117.3125000020483810, 7.188101187500000933 ) ) ;
#59499=VERTEX_POINT ( 'NONE', #66732 ) ;
#59503=CARTESIAN_POINT ( 'NONE',  ( 8.000000000000000000, 3.093750000000000888, -3.313708498984761164 ) ) ;
#59513=CARTESIAN_POINT ( 'NONE',  ( 3.313708498984711426, 99.96875000000000000, 8.000000000000053291 ) ) ;
#59517=DIRECTION ( 'NONE',  ( -0.000000000000000000, 1.000000000000000000, -0.000000000000000000 ) ) ;
#59519=CARTESIAN_POINT ( 'NONE',  ( 2.977408999572650039, 92.56250000204838102, -7.188101187500000933 ) ) ;
#59526=( BOUNDED_CURVE ( )  B_SPLINE_CURVE ( 2, ( #11776, #10662, #33695, #69123, #68743, #5015, #52149, #56321, #29133 ),
 .UNSPECIFIED., .F., .F. ) 
 B_SPLINE_CURVE_WITH_KNOTS ( ( 3, 2, 2, 2, 3 ),
 ( 0.3645833333333331483, 0.3697916666666665186, 0.3749999999999998890, 0.3802083333333332038, 0.3854166666666665741 ),
 .UNSPECIFIED. ) 
 CURVE ( )  GEOMETRIC_REPRESENTATION_ITEM ( )  RATIONAL_B_SPLINE_CURVE ( ( 1.000000000000002442, 0.9238795325112842960, 1.000000000000000000, 0.9238795325112867385, 1.000000000000000000, 0.9238795325112867385, 1.000000000000000000, 0.9238795325112884038, 0.9999999999999983347 ) ) 
 REPRESENTATION_ITEM ( '' )  );
#59531=CARTESIAN_POINT ( 'NONE',  ( 1.469576158976823947E-15, 97.06250000409677625, 8.000000000000000000 ) ) ;
#59537=CARTESIAN_POINT ( 'NONE',  ( 8.000000000000000000, 23.90624999590322375, -3.313708498984761164 ) ) ;
#59543=CARTESIAN_POINT ( 'NONE',  ( 1.320432766682874540E-15, 91.90625000204838102, 7.188101187500000044 ) ) ;
#59551=FACE_OUTER_BOUND ( 'NONE', #60010, .T. ) ;
#59557=CARTESIAN_POINT ( 'NONE',  ( 9.797174393178825657E-16, 125.0000000000000000, -8.000000000000000000 ) ) ;
#59558=ORIENTED_EDGE ( 'NONE', *, *, #38204, .F. ) ;
#59565=CARTESIAN_POINT ( 'NONE',  ( -5.656854249492378806, 96.87500000409677625, 5.656854249492381470 ) ) ;
#59576=CARTESIAN_POINT ( 'NONE',  ( 7.188101187500000044, 100.9062500020483810, -8.802885111219163269E-16 ) ) ;
#59578=CARTESIAN_POINT ( 'NONE',  ( -5.656854249492380582, 92.00000000409677625, -5.656854249492380582 ) ) ;
#59579=CARTESIAN_POINT ( 'NONE',  ( 5.656854249492379694, 120.1250000040967905, -5.656854249492380582 ) ) ;
#59583=EDGE_LOOP ( 'NONE', ( #7879, #50179, #51955, #45561, #49034 ) ) ;
#59584=ORIENTED_EDGE ( 'NONE', *, *, #62454, .F. ) ;
#59595=CARTESIAN_POINT ( 'NONE',  ( 5.656854249492378806, 5.624999995903220196, 5.656854249492381470 ) ) ;
#59597=CARTESIAN_POINT ( 'NONE',  ( 5.082755093536324154, 11.15624999795161187, 5.082755093536326818 ) ) ;
#59600=CARTESIAN_POINT ( 'NONE',  ( -5.082755093536325930, 109.3437500020483810, -5.082755093536325930 ) ) ;
#59620=CARTESIAN_POINT ( 'NONE',  ( 7.188101187500002709, 106.8125000020483952, 2.977408999572649151 ) ) ;
#59625=CARTESIAN_POINT ( 'NONE',  ( -7.188101187499999156, 109.6250000020483952, 2.977408999572654924 ) ) ;
#59631=CARTESIAN_POINT ( 'NONE',  ( -5.656854249492379694, 0.5625000000000000000, -5.656854249492380582 ) ) ;
#59635=CARTESIAN_POINT ( 'NONE',  ( -5.082755093536325042, 1.406249997951610320, -5.082755093536325930 ) ) ;
#59637=EDGE_CURVE ( 'NONE', #2971, #69151, #41876, .T. ) ;
#59642=( BOUNDED_CURVE ( )  B_SPLINE_CURVE ( 2, ( #31440, #70329, #41652, #12962, #2773, #43118, #25016, #19365, #25759 ),
 .UNSPECIFIED., .F., .F. ) 
 B_SPLINE_CURVE_WITH_KNOTS ( ( 3, 2, 2, 2, 3 ),
 ( 0.1562500000000001110, 0.1614583333333334536, 0.1666666666666667407, 0.1718750000000000833, 0.1770833333333334259 ),
 .UNSPECIFIED. ) 
 CURVE ( )  GEOMETRIC_REPRESENTATION_ITEM ( )  RATIONAL_B_SPLINE_CURVE ( ( 0.9999999999999983347, 0.9238795325112884038, 1.000000000000000000, 0.9238795325112867385, 1.000000000000000000, 0.9238795325112867385, 1.000000000000000000, 0.9238795325112855172, 1.000000000000001110 ) ) 
 REPRESENTATION_ITEM ( '' )  );
#59650=CARTESIAN_POINT ( 'NONE',  ( 7.999999999999998224, 13.40625000000000178, 3.313708498984766493 ) ) ;
#59653=CARTESIAN_POINT ( 'NONE',  ( -2.977408999572654480, 27.37499999795161187, 7.188101187499999156 ) ) ;
#59655=CARTESIAN_POINT ( 'NONE',  ( 3.313708498984760720, 115.7187500040967763, -8.000000000000000000 ) ) ;
#59658=AXIS2_PLACEMENT_3D ( 'NONE', #37015, #60017, #2686 ) ;
#59674=ORIENTED_EDGE ( 'NONE', *, *, #53613, .F. ) ;
#59680=CARTESIAN_POINT ( 'NONE',  ( 3.313708498984765161, 104.4687500000000000, 7.999999999999998224 ) ) ;
#59683=ADVANCED_FACE ( 'NONE', ( #19232 ), #2259, .T. ) ;
#59684=CARTESIAN_POINT ( 'NONE',  ( 3.313708498984760720, 114.0312500000000000, -8.000000000000000000 ) ) ;
#59689=CARTESIAN_POINT ( 'NONE',  ( 5.656854249492380582, 17.99999999590322375, -5.656854249492380582 ) ) ;
#59691=CARTESIAN_POINT ( 'NONE',  ( 0.000000000000000000, 125.0000000000000000, 8.000000000000000000 ) ) ;
#59702=CARTESIAN_POINT ( 'NONE',  ( 5.656854249492380582, 10.49999999590322020, -5.656854249492380582 ) ) ;
#59711=CARTESIAN_POINT ( 'NONE',  ( 0.000000000000000000, 125.0000000000000000, 0.000000000000000000 ) ) ;
#59715=AXIS2_PLACEMENT_3D ( 'NONE', #4197, #49456, #55882 ) ;
#59716=CARTESIAN_POINT ( 'NONE',  ( -7.188101187500000044, 94.15625000204838102, 0.000000000000000000 ) ) ;
#59720=ORIENTED_EDGE ( 'NONE', *, *, #56350, .T. ) ;
#59721=ORIENTED_EDGE ( 'NONE', *, *, #58835, .T. ) ;
#59723=CARTESIAN_POINT ( 'NONE',  ( 8.000000000000000000, 28.31249999590322375, 0.000000000000000000 ) ) ;
#59730=CARTESIAN_POINT ( 'NONE',  ( -7.999999999999998224, 113.0937500000000000, 3.313708498984766049 ) ) ;
#59743=CARTESIAN_POINT ( 'NONE',  ( 4.401442555609581635E-16, 17.34374999795161187, -7.188101187500000044 ) ) ;
#59746=CARTESIAN_POINT ( 'NONE',  ( -7.188101187500002709, 10.68749999795161187, 2.977408999572649151 ) ) ;
#59760=CARTESIAN_POINT ( 'NONE',  ( 5.082755093536325042, 110.0937500020483810, -5.082755093536325930 ) ) ;
#59766=CARTESIAN_POINT ( 'NONE',  ( -5.082755093536326818, 25.40624999795161543, 5.082755093536325042 ) ) ;
#59767=ORIENTED_EDGE ( 'NONE', *, *, #45003, .T. ) ;
#59772=CARTESIAN_POINT ( 'NONE',  ( 1.320432766682874540E-15, 99.40625000204838102, 7.188101187500000044 ) ) ;
#59775=ORIENTED_EDGE ( 'NONE', *, *, #26049, .F. ) ;
#59793=LINE ( 'NONE', #30381, #17862 ) ;
#59797=CARTESIAN_POINT ( 'NONE',  ( -6.951749144819291182, 124.7465970749896229, -3.470743364672778331 ) ) ;
#59799=CARTESIAN_POINT ( 'NONE',  ( -7.188101187499999156, 110.7500000020483668, 2.977408999572654924 ) ) ;
#59804=CARTESIAN_POINT ( 'NONE',  ( -8.000000000000001776, 26.34375000000000711, 3.313708498984759387 ) ) ;
#59806=CARTESIAN_POINT ( 'NONE',  ( 3.313708498984657247, 92.65625000409677625, 8.000000000000106581 ) ) ;
#59816=CARTESIAN_POINT ( 'NONE',  ( 1.469576158976823947E-15, 95.37499999999998579, 8.000000000000000000 ) ) ;
#59820=ORIENTED_EDGE ( 'NONE', *, *, #55922, .F. ) ;
#59825=CARTESIAN_POINT ( 'NONE',  ( -5.082755093536326818, 10.78124999795161187, 5.082755093536325042 ) ) ;
#59843=CARTESIAN_POINT ( 'NONE',  ( 3.313708498984762496, 25.21875000000000711, 7.999999999999998224 ) ) ;
#59854=CARTESIAN_POINT ( 'NONE',  ( 2.977408999572650927, 6.749999997951611874, -7.188101187500000933 ) ) ;
#59856=CARTESIAN_POINT ( 'NONE',  ( -4.401442555609581635E-16, 118.1562500020483810, -7.188101187500000044 ) ) ;
#59868=ORIENTED_EDGE ( 'NONE', *, *, #46747, .T. ) ;
#59869=CARTESIAN_POINT ( 'NONE',  ( 8.000000000000000000, 24.00000000000000355, 0.000000000000000000 ) ) ;
#59870=CARTESIAN_POINT ( 'NONE',  ( 5.656854249492381470, 98.56250000000000000, 5.656854249492379694 ) ) ;
#59877=CARTESIAN_POINT ( 'NONE',  ( -4.898587196589412829E-16, 103.8125000040967763, -8.000000000000000000 ) ) ;
#59885=CARTESIAN_POINT ( 'NONE',  ( -2.977408999572652260, 91.81250000204838102, 7.188101187500000044 ) ) ;
#59898=ORIENTED_EDGE ( 'NONE', *, *, #29148, .F. ) ;
#59903=CARTESIAN_POINT ( 'NONE',  ( 1.469576158976823947E-15, 121.0625000040967763, 8.000000000000000000 ) ) ;
#59909=CARTESIAN_POINT ( 'NONE',  ( -5.656854249492378806, 113.3750000040967763, 5.656854249492381470 ) ) ;
#59914=ORIENTED_EDGE ( 'NONE', *, *, #38709, .F. ) ;
#59921=CARTESIAN_POINT ( 'NONE',  ( 5.656854249492380582, 2.999999995903220196, -5.656854249492380582 ) ) ;
#59929=CARTESIAN_POINT ( 'NONE',  ( 3.313708498984760720, 96.21875000409680467, -8.000000000000000000 ) ) ;
#59937=CARTESIAN_POINT ( 'NONE',  ( 2.977408999572654480, 100.6250000020483810, 7.188101187499999156 ) ) ;
#59941=CARTESIAN_POINT ( 'NONE',  ( -5.656854249492380582, 101.0000000040967905, -5.656854249492380582 ) ) ;
#59943=ORIENTED_EDGE ( 'NONE', *, *, #46641, .T. ) ;
#59957=CARTESIAN_POINT ( 'NONE',  ( 3.313708498984762052, 1.593749995903220196, -8.000000000000000000 ) ) ;
#59959=CARTESIAN_POINT ( 'NONE',  ( 2.977408999572651815, 12.56249999795161365, 7.188101187500000933 ) ) ;
#59962=CARTESIAN_POINT ( 'NONE',  ( 5.082755093536325042, 111.9687500020483810, -5.082755093536325930 ) ) ;
#59977=ADVANCED_FACE ( 'NONE', ( #25618 ), #42969, .T. ) ;
#59982=CARTESIAN_POINT ( 'NONE',  ( 5.656854249492380582, 25.49999999590322375, -5.656854249492380582 ) ) ;
#59983=CARTESIAN_POINT ( 'NONE',  ( 7.188101187500002709, 103.8125000020483952, 2.977408999572649151 ) ) ;
#59989=CARTESIAN_POINT ( 'NONE',  ( -7.188101187499999156, 108.1250000020483810, 2.977408999572654924 ) ) ;
#60001=FACE_OUTER_BOUND ( 'NONE', #25278, .T. ) ;
#60010=EDGE_LOOP ( 'NONE', ( #12163, #52112, #58944, #44555 ) ) ;
#60013=CARTESIAN_POINT ( 'NONE',  ( -1.320432766682874540E-15, 27.46874999795161543, 7.188101187500000044 ) ) ;
#60014=CARTESIAN_POINT ( 'NONE',  ( 3.313708498984765161, 113.6562500040967905, 7.999999999999998224 ) ) ;
#60017=DIRECTION ( 'NONE',  ( -0.000000000000000000, 1.000000000000000000, -0.000000000000000000 ) ) ;
#60038=CARTESIAN_POINT ( 'NONE',  ( -5.656854249492378806, 114.6875000000000000, 5.656854249492381470 ) ) ;
#60042=CARTESIAN_POINT ( 'NONE',  ( -8.000000000000000000, 19.96874999590322375, -3.313708498984762496 ) ) ;
#60045=CARTESIAN_POINT ( 'NONE',  ( 8.000000000000000000, 113.9375000040967763, -9.797174393178825657E-16 ) ) ;
#60057=VERTEX_POINT ( 'NONE', #13916 ) ;
#60065=CARTESIAN_POINT ( 'NONE',  ( 2.977408999572654480, 123.1250000020484094, 7.188101187499999156 ) ) ;
#60073=CARTESIAN_POINT ( 'NONE',  ( -4.401442555609581635E-16, 92.28125000204836681, -7.188101187500000044 ) ) ;
#60077=VERTEX_POINT ( 'NONE', #37332 ) ;
#60103=CARTESIAN_POINT ( 'NONE',  ( -7.188101187500002709, 22.31249999795161187, 2.977408999572649151 ) ) ;
#60106=CARTESIAN_POINT ( 'NONE',  ( 5.082755093536324154, 12.65624999795161187, 5.082755093536326818 ) ) ;
#60110=DIRECTION ( 'NONE',  ( -0.000000000000000000, 1.000000000000000000, -0.000000000000000000 ) ) ;
#60117=CARTESIAN_POINT ( 'NONE',  ( 5.082755093536326818, 111.2187500020483810, 5.082755093536325042 ) ) ;
#60121=CARTESIAN_POINT ( 'NONE',  ( -5.082755093536326818, 20.90624999795161543, 5.082755093536325042 ) ) ;
#60129=CARTESIAN_POINT ( 'NONE',  ( 5.082755093536325042, 95.46875000204838102, -5.082755093536325930 ) ) ;
#60139=CARTESIAN_POINT ( 'NONE',  ( 8.000000000000001776, 107.8437500040967905, 3.313708498984759387 ) ) ;
#60151=ADVANCED_FACE ( 'NONE', ( #55815 ), #38830, .T. ) ;
#60156=CARTESIAN_POINT ( 'NONE',  ( -4.850062511589670794E-16, 124.5792468245269475, -7.920753175473082663 ) ) ;
#60159=CARTESIAN_POINT ( 'NONE',  ( 7.188101187500001821, 111.5000000020483810, -2.977408999572651371 ) ) ;
#60185=CARTESIAN_POINT ( 'NONE',  ( 5.082755093536324154, 14.15624999795161187, 5.082755093536326818 ) ) ;
#60187=EDGE_CURVE ( 'NONE', #56169, #4846, #60733, .T. ) ;
#60195=CARTESIAN_POINT ( 'NONE',  ( -2.977408999572654480, 2.999999997951610542, 7.188101187499999156 ) ) ;
#60201=EDGE_CURVE ( 'NONE', #32974, #11019, #12051, .T. ) ;
#60203=CARTESIAN_POINT ( 'NONE',  ( 7.999999999999998224, 20.90625000000000355, 3.313708498984766493 ) ) ;
#60212=CARTESIAN_POINT ( 'NONE',  ( 7.188101187500000933, 5.062499997951610098, -2.977408999572650483 ) ) ;
#60217=CARTESIAN_POINT ( 'NONE',  ( 5.082755093536326818, 113.0937500020483810, 5.082755093536325042 ) ) ;
#60220=ADVANCED_FACE ( 'NONE', ( #44858 ), #21461, .T. ) ;
#60231=CARTESIAN_POINT ( 'NONE',  ( -3.313708498984762496, 102.7812499999999858, 7.999999999999998224 ) ) ;
#60233=DIRECTION ( 'NONE',  ( 0.000000000000000000, 0.000000000000000000, 1.000000000000000000 ) ) ;
#60245=CARTESIAN_POINT ( 'NONE',  ( 5.082755093536326818, 92.09375000204838102, 5.082755093536325042 ) ) ;
#60255=CARTESIAN_POINT ( 'NONE',  ( -1.469576158976823947E-15, 9.937499995903220196, 8.000000000000000000 ) ) ;
#60269=CARTESIAN_POINT ( 'NONE',  ( 1.926045908305006327, 89.59560438569886287, -7.188101187499999156 ) ) ;
#60276=DIRECTION ( 'NONE',  ( 0.000000000000000000, -1.000000000000000000, 0.000000000000000000 ) ) ;
#60278=CARTESIAN_POINT ( 'NONE',  ( 8.000000000000000000, 14.81249999590322020, 0.000000000000000000 ) ) ;
#60292=CARTESIAN_POINT ( 'NONE',  ( -3.313708498984762496, 99.96875000409676204, 7.999999999999998224 ) ) ;
#60299=VERTEX_POINT ( 'NONE', #34302 ) ;
#60301=CARTESIAN_POINT ( 'NONE',  ( 7.188101187500000044, 91.90625000204838102, -8.802885111219163269E-16 ) ) ;
#60311=ADVANCED_FACE ( 'NONE', ( #74645 ), #36049, .T. ) ;
#60327=CARTESIAN_POINT ( 'NONE',  ( -7.188101187500001821, 8.999999997951611874, -2.977408999572651371 ) ) ;
#60330=CARTESIAN_POINT ( 'NONE',  ( 5.082755093536326818, 110.0937500020483810, 5.082755093536325042 ) ) ;
#60347=VECTOR ( 'NONE', #1096, 1000.000000000000000 ) ;
#60349=CARTESIAN_POINT ( 'NONE',  ( -5.082755093536325930, 98.46875000204838102, -5.082755093536325930 ) ) ;
#60355=CARTESIAN_POINT ( 'NONE',  ( -4.401442555609581635E-16, 106.1562500020483810, -7.188101187500000044 ) ) ;
#60367=CARTESIAN_POINT ( 'NONE',  ( 2.977408999572652260, 2.062499997951610542, 7.188101187500000044 ) ) ;
#60373=ORIENTED_EDGE ( 'NONE', *, *, #31846, .T. ) ;
#60374=DIRECTION ( 'NONE',  ( -0.000000000000000000, 1.000000000000000000, -0.000000000000000000 ) ) ;
#60375=CARTESIAN_POINT ( 'NONE',  ( -4.898587196589412829E-16, 121.8125000040967763, -8.000000000000000000 ) ) ;
#60383=CARTESIAN_POINT ( 'NONE',  ( -7.188101187500002709, 10.31249999795161010, 2.977408999572649151 ) ) ;
#60384=CARTESIAN_POINT ( 'NONE',  ( 8.000000000000000000, 117.0312500040967905, -3.313708498984762496 ) ) ;
#60386=EDGE_CURVE ( 'NONE', #663, #38665, #59793, .T. ) ;
#60387=EDGE_CURVE ( 'NONE', #46386, #6290, #26564, .T. ) ;
#60413=CARTESIAN_POINT ( 'NONE',  ( 8.000000000000000000, 113.7500000000000000, -9.797174393178825657E-16 ) ) ;
#60419=CARTESIAN_POINT ( 'NONE',  ( -3.313708498984760720, 18.28124999590322020, -8.000000000000000000 ) ) ;
#60439=CARTESIAN_POINT ( 'NONE',  ( 7.188101187500000044, 120.4062500020483810, -8.802885111219163269E-16 ) ) ;
#60440=DIRECTION ( 'NONE',  ( -0.000000000000000000, 1.000000000000000000, -0.000000000000000000 ) ) ;
#60444=CARTESIAN_POINT ( 'NONE',  ( -5.082755093536324154, 91.34375000204838102, 5.082755093536326818 ) ) ;
#60457=CARTESIAN_POINT ( 'NONE',  ( 8.000000000000000000, 103.3437500000000000, -3.313708498984762496 ) ) ;
#60474=CARTESIAN_POINT ( 'NONE',  ( 4.401442555609581635E-16, 18.84374999795161187, -7.188101187500000044 ) ) ;
#60477=CARTESIAN_POINT ( 'NONE',  ( -2.977408999572654480, 15.37499999795161187, 7.188101187499999156 ) ) ;
#60484=EDGE_CURVE ( 'NONE', #55027, #111, #31867, .T. ) ;
#60491=CARTESIAN_POINT ( 'NONE',  ( 7.188101187500000044, 108.4062500020483810, -8.802885111219163269E-16 ) ) ;
#60494=EDGE_LOOP ( 'NONE', ( #27697, #10132, #16138, #69596 ) ) ;
#60502=CARTESIAN_POINT ( 'NONE',  ( -7.188101187500000044, 96.03125000204838102, 0.000000000000000000 ) ) ;
#60507=ORIENTED_EDGE ( 'NONE', *, *, #64674, .F. ) ;
#60508=( BOUNDED_CURVE ( )  B_SPLINE_CURVE ( 2, ( #63117, #16707, #51803, #74439, #151, #74069, #57486, #11443, #34851 ),
 .UNSPECIFIED., .F., .F. ) 
 B_SPLINE_CURVE_WITH_KNOTS ( ( 3, 2, 2, 2, 3 ),
 ( 0.1527777777777777901, 0.1597222222222222099, 0.1666666666666666574, 0.1736111111111111049, 0.1805555555555555525 ),
 .UNSPECIFIED. ) 
 CURVE ( )  GEOMETRIC_REPRESENTATION_ITEM ( )  RATIONAL_B_SPLINE_CURVE ( ( 1.000000000000000000, 0.9238795325112867385, 1.000000000000000000, 0.9238795325112867385, 1.000000000000000000, 0.9238795325112867385, 1.000000000000000000, 0.9238795325112867385, 1.000000000000000000 ) ) 
 REPRESENTATION_ITEM ( '' )  );
#60522=CARTESIAN_POINT ( 'NONE',  ( 9.797174393178825657E-16, 125.0000000000000000, -8.000000000000000000 ) ) ;
#60534=CARTESIAN_POINT ( 'NONE',  ( 7.188101187500002709, 106.8125000020484094, 2.977408999572649151 ) ) ;
#60540=ORIENTED_EDGE ( 'NONE', *, *, #57094, .F. ) ;
#60561=CARTESIAN_POINT ( 'NONE',  ( -2.977408999572650039, 17.81249999795161187, -7.188101187500000933 ) ) ;
#60570=CARTESIAN_POINT ( 'NONE',  ( 5.082755093536325930, 5.156249997951610986, -5.082755093536325930 ) ) ;
#60572=CARTESIAN_POINT ( 'NONE',  ( 0.000000000000000000, 125.0000000000000000, 0.000000000000000000 ) ) ;
#60579=CYLINDRICAL_SURFACE ( 'NONE', #36619, 8.000000000000000000 ) ;
#60581=EDGE_LOOP ( 'NONE', ( #17585, #39267, #68562, #30073 ) ) ;
#60587=CARTESIAN_POINT ( 'NONE',  ( 2.977408999572650927, 12.74999999795161187, -7.188101187500000933 ) ) ;
#60592=CARTESIAN_POINT ( 'NONE',  ( -2.977408999572651815, 114.3125000020483952, 7.188101187500000933 ) ) ;
#60603=CARTESIAN_POINT ( 'NONE',  ( 5.656854249492380582, 19.49999999590322020, -5.656854249492380582 ) ) ;
#60608=CARTESIAN_POINT ( 'NONE',  ( -8.000000000000000000, 96.40625000000000000, -3.313708498984761608 ) ) ;
#60615=ORIENTED_EDGE ( 'NONE', *, *, #21942, .T. ) ;
#60623=CARTESIAN_POINT ( 'NONE',  ( -2.977408999572652260, 90.31250000204838102, 7.188101187500000044 ) ) ;
#60635=CARTESIAN_POINT ( 'NONE',  ( 2.977408999572651815, 21.18749999795161187, 7.188101187500000933 ) ) ;
#60650=CARTESIAN_POINT ( 'NONE',  ( -5.082755093536324154, 91.71875000204838102, 5.082755093536326818 ) ) ;
#60662=FACE_OUTER_BOUND ( 'NONE', #58905, .T. ) ;
#60663=VECTOR ( 'NONE', #63602, 1000.000000000000000 ) ;
#60673=CARTESIAN_POINT ( 'NONE',  ( -8.000000000000000000, 98.09375000409679046, -3.313708498984761608 ) ) ;
#60685=CARTESIAN_POINT ( 'NONE',  ( 7.188101187500002709, 93.31250000204838102, 2.977408999572649151 ) ) ;
#60707=CARTESIAN_POINT ( 'NONE',  ( -3.313708498984765161, 3.843749995903220640, 7.999999999999998224 ) ) ;
#60709=CARTESIAN_POINT ( 'NONE',  ( 7.188101187500000044, 11.34374999795161187, 0.000000000000000000 ) ) ;
#60711=CARTESIAN_POINT ( 'NONE',  ( -7.188101187500000933, 107.9375000020483810, -2.977408999572650483 ) ) ;
#60713=DIRECTION ( 'NONE',  ( -0.000000000000000000, 1.000000000000000000, -0.000000000000000000 ) ) ;
#60729=CARTESIAN_POINT ( 'NONE',  ( 2.977408999572650039, 99.68750000204838102, -7.188101187500000933 ) ) ;
#60733=( BOUNDED_CURVE ( )  B_SPLINE_CURVE ( 2, ( #50504, #26749, #61081, #21091, #10152, #68239, #4875, #9409, #27870 ),
 .UNSPECIFIED., .F., .F. ) 
 B_SPLINE_CURVE_WITH_KNOTS ( ( 3, 2, 2, 2, 3 ),
 ( 0.5312500000000000000, 0.5364583333333333703, 0.5416666666666665186, 0.5468749999999998890, 0.5520833333333332593 ),
 .UNSPECIFIED. ) 
 CURVE ( )  GEOMETRIC_REPRESENTATION_ITEM ( )  RATIONAL_B_SPLINE_CURVE ( ( 1.000000000000000000, 0.9238795325112867385, 1.000000000000000000, 0.9238795325112867385, 1.000000000000000000, 0.9238795325112867385, 1.000000000000000000, 0.9238795325112884038, 0.9999999999999983347 ) ) 
 REPRESENTATION_ITEM ( '' )  );
#60736=CARTESIAN_POINT ( 'NONE',  ( 5.082755093536325042, 108.9687500020483810, -5.082755093536325930 ) ) ;
#60762=ORIENTED_EDGE ( 'NONE', *, *, #13232, .T. ) ;
#60764=CARTESIAN_POINT ( 'NONE',  ( 5.082755093536325930, 6.656249997951611874, -5.082755093536325930 ) ) ;
#60765=CARTESIAN_POINT ( 'NONE',  ( -3.313708498984762052, 114.4062500040967620, -8.000000000000000000 ) ) ;
#60771=ORIENTED_EDGE ( 'NONE', *, *, #3521, .F. ) ;
#60788=CARTESIAN_POINT ( 'NONE',  ( 3.313708498984765161, 113.4687500000000000, 7.999999999999998224 ) ) ;
#60793=CARTESIAN_POINT ( 'NONE',  ( -8.000000000000000000, 22.96874999590322020, -3.313708498984762496 ) ) ;
#60816=CARTESIAN_POINT ( 'NONE',  ( -7.188101187500000044, 118.1562500020483810, 0.000000000000000000 ) ) ;
#60820=ADVANCED_FACE ( 'NONE', ( #34782 ), #1183, .T. ) ;
#60823=CARTESIAN_POINT ( 'NONE',  ( -2.977408999572650927, 92.37500000204839523, -7.188101187500001821 ) ) ;
#60852=CARTESIAN_POINT ( 'NONE',  ( -7.188101187500000044, 23.71874999795161543, -8.802885111219163269E-16 ) ) ;
#60854=DIRECTION ( 'NONE',  ( 0.000000000000000000, 0.000000000000000000, 1.000000000000000000 ) ) ;
#60855=CARTESIAN_POINT ( 'NONE',  ( -2.977408999572654480, 19.87499999795161543, 7.188101187499999156 ) ) ;
#60858=CARTESIAN_POINT ( 'NONE',  ( -4.898587196589412829E-16, 118.8125000040967763, -8.000000000000000000 ) ) ;
#60864=CARTESIAN_POINT ( 'NONE',  ( 1.320432766682874540E-15, 112.5312500020483952, 7.188101187500000044 ) ) ;
#60875=CARTESIAN_POINT ( 'NONE',  ( 2.977408999572650039, 92.56250000204838102, -7.188101187500001821 ) ) ;
#60889=CARTESIAN_POINT ( 'NONE',  ( 1.469576158976823947E-15, 107.5625000040967905, 8.000000000000000000 ) ) ;
#60899=CARTESIAN_POINT ( 'NONE',  ( -8.000000000000000000, 17.25000000000000000, -9.797174393178825657E-16 ) ) ;
#60907=CARTESIAN_POINT ( 'NONE',  ( 5.082755093536326818, 108.2187500020483810, 5.082755093536325042 ) ) ;
#60917=CARTESIAN_POINT ( 'NONE',  ( -3.313708498984707429, 99.21875000000001421, -8.000000000000055067 ) ) ;
#60927=DIRECTION ( 'NONE',  ( -0.000000000000000000, 1.000000000000000000, -0.000000000000000000 ) ) ;
#60935=CARTESIAN_POINT ( 'NONE',  ( -7.188101187500000044, 21.09374999795161543, -8.802885111219163269E-16 ) ) ;
#60943=( BOUNDED_CURVE ( )  B_SPLINE_CURVE ( 2, ( #10844, #33878, #56878, #16858, #39884, #62886, #11219, #5562, #38257 ),
 .UNSPECIFIED., .F., .F. ) 
 B_SPLINE_CURVE_WITH_KNOTS ( ( 3, 2, 2, 2, 3 ),
 ( 0.2187500000000001388, 0.2239583333333333703, 0.2291666666666666019, 0.2343749999999998335, 0.2395833333333330928 ),
 .UNSPECIFIED. ) 
 CURVE ( )  GEOMETRIC_REPRESENTATION_ITEM ( )  RATIONAL_B_SPLINE_CURVE ( ( 0.9999999999999980016, 0.9238795325112887369, 1.000000000000000000, 0.9238795325112867385, 1.000000000000000000, 0.9238795325112867385, 1.000000000000000000, 0.9238795325112904022, 0.9999999999999963363 ) ) 
 REPRESENTATION_ITEM ( '' )  );
#60945=CARTESIAN_POINT ( 'NONE',  ( 4.401442555609581635E-16, 0.8437499979516099868, -7.188101187500000044 ) ) ;
#60950=FACE_OUTER_BOUND ( 'NONE', #26744, .T. ) ;
#60951=ORIENTED_EDGE ( 'NONE', *, *, #65112, .T. ) ;
#60965=CARTESIAN_POINT ( 'NONE',  ( -7.188101187500000933, 10.12499999795161187, -2.977408999572651371 ) ) ;
#60969=CARTESIAN_POINT ( 'NONE',  ( 7.188101187500000044, 113.2812500020483952, -8.802885111219163269E-16 ) ) ;
#60983=CARTESIAN_POINT ( 'NONE',  ( 8.000000000000000000, 95.75000000000000000, -9.797174393178825657E-16 ) ) ;
#60988=VERTEX_POINT ( 'NONE', #55084 ) ;
#60990=LINE ( 'NONE', #43257, #17879 ) ;
#61005=CARTESIAN_POINT ( 'NONE',  ( 7.188101187500001821, 21.56249999795161898, -2.977408999572650483 ) ) ;
#61006=DIRECTION ( 'NONE',  ( -0.000000000000000000, 1.000000000000000000, -0.000000000000000000 ) ) ;
#61021=EDGE_CURVE ( 'NONE', #54702, #64829, #15066, .T. ) ;
#61042=CARTESIAN_POINT ( 'NONE',  ( 3.313708498984762052, 10.78125000000000178, -8.000000000000000000 ) ) ;
#61043=VERTEX_POINT ( 'NONE', #65638 ) ;
#61045=CARTESIAN_POINT ( 'NONE',  ( 8.000000000000000000, 92.93750000409679046, -9.797174393178825657E-16 ) ) ;
#61056=CARTESIAN_POINT ( 'NONE',  ( 7.188101187500002709, 90.31250000204838102, 2.977408999572649151 ) ) ;
#61070=CARTESIAN_POINT ( 'NONE',  ( 0.000000000000000000, 125.0000000000000000, 0.000000000000000000 ) ) ;
#61077=CARTESIAN_POINT ( 'NONE',  ( 7.999999999999998224, 11.71874999590322197, 3.313708498984766493 ) ) ;
#61079=CARTESIAN_POINT ( 'NONE',  ( 2.977408999572651815, 11.06249999795161187, 7.188101187500000933 ) ) ;
#61081=CARTESIAN_POINT ( 'NONE',  ( -5.656854249492378806, 105.6874999999999858, 5.656854249492381470 ) ) ;
#61082=CARTESIAN_POINT ( 'NONE',  ( -2.977408999572650927, 109.2500000020483952, -7.188101187500000933 ) ) ;
#61100=CARTESIAN_POINT ( 'NONE',  ( 4.898587196589412829E-16, 25.68749999590322375, -8.000000000000000000 ) ) ;
#61101=CARTESIAN_POINT ( 'NONE',  ( -2.977408999572652260, 98.93750000204836681, 7.188101187500000044 ) ) ;
#61108=CARTESIAN_POINT ( 'NONE',  ( 5.082755093536326818, 105.5937500020483810, 5.082755093536325042 ) ) ;
#61119=CARTESIAN_POINT ( 'NONE',  ( -7.188101187500002709, 1.687499997951610098, 2.977408999572649151 ) ) ;
#61133=VERTEX_POINT ( 'NONE', #10914 ) ;
#61135=CARTESIAN_POINT ( 'NONE',  ( 7.188101187500001821, 6.562499997951610986, -2.977408999572650483 ) ) ;
#61136=CARTESIAN_POINT ( 'NONE',  ( 3.313708498984760720, 114.2187500040968047, -8.000000000000000000 ) ) ;
#61164=CARTESIAN_POINT ( 'NONE',  ( 3.313708498984760720, 111.0312499999999858, -8.000000000000000000 ) ) ;
#61168=ORIENTED_EDGE ( 'NONE', *, *, #765, .F. ) ;
#61169=( BOUNDED_CURVE ( )  B_SPLINE_CURVE ( 2, ( #45304, #16242, #16616, #40395, #52093, #426, #5324, #21910, #22281 ),
 .UNSPECIFIED., .F., .F. ) 
 B_SPLINE_CURVE_WITH_KNOTS ( ( 3, 2, 2, 2, 3 ),
 ( 0.04166666666666666435, 0.04861111111111111188, 0.05555555555555555247, 0.06250000000000000000, 0.06944444444444444753 ),
 .UNSPECIFIED. ) 
 CURVE ( )  GEOMETRIC_REPRESENTATION_ITEM ( )  RATIONAL_B_SPLINE_CURVE ( ( 1.000000000000000000, 0.9238795325112867385, 1.000000000000000000, 0.9238795325112867385, 1.000000000000000000, 0.9238795325112867385, 1.000000000000000000, 0.9238795325112867385, 1.000000000000000000 ) ) 
 REPRESENTATION_ITEM ( '' )  );
#61172=CARTESIAN_POINT ( 'NONE',  ( 5.656854249492380582, 22.49999999590322375, -5.656854249492380582 ) ) ;
#61196=CARTESIAN_POINT ( 'NONE',  ( -7.188101187499999156, 118.2500000020483952, 2.977408999572654924 ) ) ;
#61201=CARTESIAN_POINT ( 'NONE',  ( 5.082755093536326818, 91.71875000204838102, 5.082755093536325042 ) ) ;
#61205=VERTEX_POINT ( 'NONE', #734 ) ;
#61207=EDGE_CURVE ( 'NONE', #6290, #28600, #41075, .T. ) ;
#61229=CARTESIAN_POINT ( 'NONE',  ( 7.188101187500001821, 21.56249999795161898, -2.977408999572650483 ) ) ;
#61233=CARTESIAN_POINT ( 'NONE',  ( -7.188101187500002709, 19.68749999795161543, 2.977408999572649151 ) ) ;
#61245=ORIENTED_EDGE ( 'NONE', *, *, #13879, .T. ) ;
#61253=CARTESIAN_POINT ( 'NONE',  ( 2.977408999572654480, 93.50000000204838102, 7.188101187499999156 ) ) ;
#61256=ADVANCED_FACE ( 'NONE', ( #6006 ), #1472, .T. ) ;
#61275=CARTESIAN_POINT ( 'NONE',  ( -4.898587196589412829E-16, 109.8125000040967905, -8.000000000000000000 ) ) ;
#61286=CARTESIAN_POINT ( 'NONE',  ( -7.188101187500000044, 109.1562500020483810, 0.000000000000000000 ) ) ;
#61294=( BOUNDED_CURVE ( )  B_SPLINE_CURVE ( 2, ( #66200, #54901, #61298, #14504, #37543 ),
 .UNSPECIFIED., .F., .F. ) 
 B_SPLINE_CURVE_WITH_KNOTS ( ( 3, 2, 3 ),
 ( 0.9861111111111110494, 0.9930555555555555802, 1.000000000000000000 ),
 .UNSPECIFIED. ) 
 CURVE ( )  GEOMETRIC_REPRESENTATION_ITEM ( )  RATIONAL_B_SPLINE_CURVE ( ( 1.000000000000001110, 0.9238795325112855172, 1.000000000000000000, 0.9238795325112867385, 1.000000000000000000 ) ) 
 REPRESENTATION_ITEM ( '' )  );
#61296=CARTESIAN_POINT ( 'NONE',  ( 7.999999999999998224, 28.21874999590322375, 3.313708498984766049 ) ) ;
#61298=CARTESIAN_POINT ( 'NONE',  ( 5.656854249492378806, 26.81250000000000355, 5.656854249492381470 ) ) ;
#61315=CARTESIAN_POINT ( 'NONE',  ( -2.977408999572654480, 18.37499999795161187, 7.188101187499999156 ) ) ;
#61319=CARTESIAN_POINT ( 'NONE',  ( -5.656854249492378806, 96.87500000409677625, 5.656854249492381470 ) ) ;
#61323=CARTESIAN_POINT ( 'NONE',  ( 2.977408999572651815, 1.687499997951610098, 7.188101187500000933 ) ) ;
#61341=CARTESIAN_POINT ( 'NONE',  ( 7.188101187499999156, 10.87499999795161187, 2.977408999572654924 ) ) ;
#61346=CARTESIAN_POINT ( 'NONE',  ( -7.188101187500000044, 109.5312500020483810, 0.000000000000000000 ) ) ;
#61351=VERTEX_POINT ( 'NONE', #19525 ) ;
#61354=CARTESIAN_POINT ( 'NONE',  ( -4.898587196589412829E-16, 106.6250000000000000, -8.000000000000000000 ) ) ;
#61358=DIRECTION ( 'NONE',  ( 0.000000000000000000, 0.000000000000000000, 1.000000000000000000 ) ) ;
#61360=CARTESIAN_POINT ( 'NONE',  ( -5.656854249492378806, 92.18749999999998579, 5.656854249492381470 ) ) ;
#61366=CARTESIAN_POINT ( 'NONE',  ( 8.000000000000001776, 118.3437500040967763, 3.313708498984759387 ) ) ;
#61383=CARTESIAN_POINT ( 'NONE',  ( 7.188101187500001821, 18.56249999795161187, -2.977408999572650483 ) ) ;
#61384=( BOUNDED_CURVE ( )  B_SPLINE_CURVE ( 2, ( #20396, #7242, #66424, #25309, #54754, #65313, #37393, #64940, #14736 ),
 .UNSPECIFIED., .F., .F. ) 
 B_SPLINE_CURVE_WITH_KNOTS ( ( 3, 2, 2, 2, 3 ),
 ( 0.8020833333333334814, 0.8072916666666667407, 0.8125000000000001110, 0.8177083333333334814, 0.8229166666666667407 ),
 .UNSPECIFIED. ) 
 CURVE ( )  GEOMETRIC_REPRESENTATION_ITEM ( )  RATIONAL_B_SPLINE_CURVE ( ( 0.9999999999999983347, 0.9238795325112884038, 1.000000000000000000, 0.9238795325112867385, 1.000000000000000000, 0.9238795325112867385, 1.000000000000000000, 0.9238795325112850731, 1.000000000000001554 ) ) 
 REPRESENTATION_ITEM ( '' )  );
#61392=CARTESIAN_POINT ( 'NONE',  ( -4.898587196589412829E-16, 118.6250000000000000, -8.000000000000000000 ) ) ;
#61418=CARTESIAN_POINT ( 'NONE',  ( 3.313708498984762496, 10.21875000000000178, 7.999999999999998224 ) ) ;
#61419=ORIENTED_EDGE ( 'NONE', *, *, #44154, .F. ) ;
#61420=EDGE_CURVE ( 'NONE', #65598, #12358, #62707, .T. ) ;
#61421=CARTESIAN_POINT ( 'NONE',  ( 8.000000000000001776, 91.34375000409679046, 3.313708498984759387 ) ) ;
#61433=CARTESIAN_POINT ( 'NONE',  ( 7.188101187500001821, 95.00000000204836681, -2.977408999572651371 ) ) ;
#61443=ORIENTED_EDGE ( 'NONE', *, *, #30618, .T. ) ;
#61455=CARTESIAN_POINT ( 'NONE',  ( -3.313708498984760720, 9.281249995903221972, -8.000000000000000000 ) ) ;
#61458=CARTESIAN_POINT ( 'NONE',  ( -7.188101187500000044, 16.59374999795161543, -8.802885111219163269E-16 ) ) ;
#61461=CARTESIAN_POINT ( 'NONE',  ( 2.977408999572654480, 104.0000000020483810, 7.188101187499999156 ) ) ;
#61473=CARTESIAN_POINT ( 'NONE',  ( -3.313708498984805573, 20.34374999590321664, 7.999999999999956479 ) ) ;
#61479=CARTESIAN_POINT ( 'NONE',  ( -7.188101187500000933, 97.06250000204838102, -2.977408999572650483 ) ) ;
#61486=CARTESIAN_POINT ( 'NONE',  ( 7.188101187500000044, 101.2812500020483810, -8.802885111219163269E-16 ) ) ;
#61494=CARTESIAN_POINT ( 'NONE',  ( -4.898587196589412829E-16, 91.62499999999998579, -8.000000000000000000 ) ) ;
#61503=CARTESIAN_POINT ( 'NONE',  ( 4.898587196589412829E-16, 21.18749999590322375, -8.000000000000000000 ) ) ;
#61510=ORIENTED_EDGE ( 'NONE', *, *, #39210, .T. ) ;
#61513=CARTESIAN_POINT ( 'NONE',  ( 7.188101187500000044, 7.968749997951610986, 0.000000000000000000 ) ) ;
#61514=CARTESIAN_POINT ( 'NONE',  ( -8.000000000000000000, 111.5937500040967763, -3.313708498984761608 ) ) ;
#61524=CARTESIAN_POINT ( 'NONE',  ( 8.000000000000000000, 116.8437500000000000, -3.313708498984762496 ) ) ;
#61530=LINE ( 'NONE', #39, #44433 ) ;
#61540=CARTESIAN_POINT ( 'NONE',  ( 1.469576158976823947E-15, 104.3750000000000000, 8.000000000000000000 ) ) ;
#61545=ORIENTED_EDGE ( 'NONE', *, *, #7216, .T. ) ;
#61546=CARTESIAN_POINT ( 'NONE',  ( -3.313708498984762496, 102.9687500040967620, 7.999999999999998224 ) ) ;
#61549=CARTESIAN_POINT ( 'NONE',  ( -3.313708498984760720, 19.78124999590322375, -8.000000000000000000 ) ) ;
#61551=CARTESIAN_POINT ( 'NONE',  ( 5.082755093536326818, 123.5937500020483952, 5.082755093536325042 ) ) ;
#61572=CARTESIAN_POINT ( 'NONE',  ( 7.188101187500000933, 117.5000000020483810, -2.977408999572651371 ) ) ;
#61578=CARTESIAN_POINT ( 'NONE',  ( -4.401442555609581635E-16, 122.6562500020483810, -7.188101187500000044 ) ) ;
#61600=CARTESIAN_POINT ( 'NONE',  ( 5.082755093536324154, 19.78124999795161543, 5.082755093536326818 ) ) ;
#61604=CARTESIAN_POINT ( 'NONE',  ( -5.082755093536326818, 16.78124999795161543, 5.082755093536325042 ) ) ;
#61614=ORIENTED_EDGE ( 'NONE', *, *, #71956, .F. ) ;
#61617=( BOUNDED_CURVE ( )  B_SPLINE_CURVE ( 2, ( #6700, #39906, #29705, #17633, #40652, #68950, #6337, #64038, #62912, #17260, #52351, #40280, #687, #11607, #70078, #23671, #18385, #41398, #11241, #53829, #30807, #2139, #59492, #8537, #71157, #24408, #36476, #42118, #19478, #25867, #1781, #43232, #31551, #66247, #48517, #37589, #18754, #25132, #54574, #71523, #2510, #42854, #48148, #65871, #7068, #31176, #53089, #13074, #42491, #60212, #2880, #71898, #65507, #41763, #20212, #54202, #64771, #47414, #25504, #48887, #59127, #1424, #13803, #70438, #36109, #36848, #7438, #59854, #8168, #19848, #14550, #30074, #65130, #30445, #53463, #24766, #14180, #47776, #70799, #19113, #13440, #37215, #7805, #33431, #43989, #44734, #4752, #56431, #38716, #21342, #27744, #43605, #50755, #3627, #73403, #22078, #10034, #14924, #54947, #32688, #55697, #8913, #37966, #60965, #9284, #61714, #44363, #15674, #15297, #62082, #4012, #61341, #16411, #27001, #50015, #73771, #27368, #73031, #26244, #21707, #45104, #10405, #67375, #16044, #68117, #39077, #33070, #56066, #55322, #66999, #50387, #60587, #32307, #4375, #26623, #67752, #49647, #31925, #3256, #49263, #72277, #20590, #9668, #66618, #72661, #38335, #20966, #28864, #56805, #68856, #74515, #51884, #58302, #34175, #962, #40936, #23945, #6242, #69983, #51132, #34554, #22825, #11521, #23574, #591, #57559, #46583, #39443, #63564, #5867, #45466, #224, #23204, #28118, #10771, #68481, #46216, #17920, #63945, #29614, #69232, #29246, #46954, #16784, #17542, #40187, #40561, #62816, #52627, #33808, #11890, #74142, #5126, #34924, #39811, #57936, #52259, #69605, #12255, #35290, #45841, #6607, #62443, #22446, #11151, #57177, #5494, #51502, #28494, #17168, #63190, #65780, #1693, #2416, #37119, #14084, #71063, #53736, #60121, #1330, #8439, #64314, #31076, #30349, #59035, #24672, #31459, #7342, #25411, #41306, #47323, #70350, #18661, #19381, #2047, #48054, #47683, #19756, #36382, #19022, #48796, #25034, #48425, #42028, #53369, #70703, #12619, #35649, #54484, #65035, #13344, #41672, #71428, #59397, #42764, #58663, #42395, #13709, #2789, #7711, #30715, #65411, #64681, #36752, #12980, #25776, #59766, #8075, #54104, #18290, #6970, #29979, #52997, #24312, #36017, #43138, #32211, #72940, #56341, #26527, #21619, #66521, #33339, #73316, #4660, #38623, #27654, #8822, #66907 ),
 .UNSPECIFIED., .F., .F. ) 
 B_SPLINE_CURVE_WITH_KNOTS ( ( 3, 2, 2, 2, 2, 2, 2, 2, 2, 2, 2, 2, 2, 2, 2, 2, 2, 2, 2, 2, 2, 2, 2, 2, 2, 2, 2, 2, 2, 2, 2, 2, 2, 2, 2, 2, 2, 2, 2, 2, 2, 2, 2, 2, 2, 2, 2, 2, 2, 2, 2, 2, 2, 2, 2, 2, 2, 2, 2, 2, 2, 2, 2, 2, 2, 2, 2, 2, 2, 2, 2, 2, 2, 2, 2, 2, 2, 2, 2, 2, 2, 2, 2, 2, 2, 2, 2, 2, 2, 2, 2, 2, 2, 2, 2, 2, 2, 2, 2, 2, 2, 2, 2, 2, 2, 2, 2, 2, 2, 2, 2, 2, 2, 2, 2, 2, 2, 2, 2, 2, 2, 2, 2, 2, 2, 2, 2, 2, 2, 2, 2, 2, 2, 2, 2, 2, 2, 2, 2, 2, 2, 2, 2, 2, 3 ),
 ( 0.000000000000000000, 0.006944444444444444059, 0.01388888888888888812, 0.02083333333333333218, 0.02777777777777777624, 0.03472222222222222376, 0.04166666666666666435, 0.04861111111111111188, 0.05555555555555555247, 0.06250000000000000000, 0.06944444444444444753, 0.07638888888888889506, 0.08333333333333332871, 0.09027777777777777624, 0.09722222222222222376, 0.1041666666666666713, 0.1111111111111111049, 0.1180555555555555525, 0.1250000000000000000, 0.1319444444444444475, 0.1388888888888888951, 0.1458333333333333426, 0.1527777777777777901, 0.1597222222222222099, 0.1666666666666666574, 0.1736111111111111049, 0.1805555555555555525, 0.1875000000000000000, 0.1944444444444444475, 0.2013888888888888951, 0.2083333333333333426, 0.2152777777777777901, 0.2222222222222222099, 0.2291666666666666574, 0.2361111111111111049, 0.2430555555555555525, 0.2500000000000000000, 0.2569444444444444198, 0.2638888888888888951, 0.2708333333333333148, 0.2777777777777777901, 0.2847222222222222099, 0.2916666666666666852, 0.2986111111111111049, 0.3055555555555555802, 0.3125000000000000000, 0.3194444444444444198, 0.3263888888888888951, 0.3333333333333333148, 0.3402777777777777901, 0.3472222222222222099, 0.3541666666666666852, 0.3611111111111111049, 0.3680555555555555802, 0.3750000000000000000, 0.3819444444444444198, 0.3888888888888888951, 0.3958333333333333148, 0.4027777777777777901, 0.4097222222222222099, 0.4166666666666666852, 0.4236111111111111049, 0.4305555555555555802, 0.4375000000000000000, 0.4444444444444444198, 0.4513888888888888951, 0.4583333333333333148, 0.4652777777777777901, 0.4722222222222222099, 0.4791666666666666852, 0.4861111111111111049, 0.4930555555555555802, 0.5000000000000000000, 0.5069444444444444198, 0.5138888888888888395, 0.5208333333333333703, 0.5277777777777777901, 0.5347222222222222099, 0.5416666666666666297, 0.5486111111111111605, 0.5555555555555555802, 0.5625000000000000000, 0.5694444444444444198, 0.5763888888888888395, 0.5833333333333333703, 0.5902777777777777901, 0.5972222222222222099, 0.6041666666666666297, 0.6111111111111111605, 0.6180555555555555802, 0.6250000000000000000, 0.6319444444444444198, 0.6388888888888888395, 0.6458333333333333703, 0.6527777777777777901, 0.6597222222222222099, 0.6666666666666666297, 0.6736111111111111605, 0.6805555555555555802, 0.6875000000000000000, 0.6944444444444444198, 0.7013888888888888395, 0.7083333333333333703, 0.7152777777777777901, 0.7222222222222222099, 0.7291666666666666297, 0.7361111111111111605, 0.7430555555555555802, 0.7500000000000000000, 0.7569444444444444198, 0.7638888888888888395, 0.7708333333333333703, 0.7777777777777777901, 0.7847222222222222099, 0.7916666666666666297, 0.7986111111111111605, 0.8055555555555555802, 0.8125000000000000000, 0.8194444444444444198, 0.8263888888888888395, 0.8333333333333333703, 0.8402777777777777901, 0.8472222222222222099, 0.8541666666666666297, 0.8611111111111111605, 0.8680555555555555802, 0.8750000000000000000, 0.8819444444444444198, 0.8888888888888888395, 0.8958333333333333703, 0.9027777777777777901, 0.9097222222222222099, 0.9166666666666666297, 0.9236111111111111605, 0.9305555555555555802, 0.9375000000000000000, 0.9444444444444444198, 0.9513888888888888395, 0.9583333333333333703, 0.9652777777777777901, 0.9722222222222222099, 0.9791666666666666297, 0.9861111111111111605, 0.9930555555555555802, 1.000000000000000000 ),
 .UNSPECIFIED. ) 
 CURVE ( )  GEOMETRIC_REPRESENTATION_ITEM ( )  RATIONAL_B_SPLINE_CURVE ( ( 1.000000000000000000, 0.9238795325112867385, 1.000000000000000000, 0.9238795325112867385, 1.000000000000000000, 0.9238795325112867385, 1.000000000000000000, 0.9238795325112867385, 1.000000000000000000, 0.9238795325112867385, 1.000000000000000000, 0.9238795325112867385, 1.000000000000000000, 0.9238795325112867385, 1.000000000000000000, 0.9238795325112867385, 1.000000000000000000, 0.9238795325112867385, 1.000000000000000000, 0.9238795325112867385, 1.000000000000000000, 0.9238795325112867385, 1.000000000000000000, 0.9238795325112867385, 1.000000000000000000, 0.9238795325112867385, 1.000000000000000000, 0.9238795325112867385, 1.000000000000000000, 0.9238795325112867385, 1.000000000000000000, 0.9238795325112867385, 1.000000000000000000, 0.9238795325112867385, 1.000000000000000000, 0.9238795325112867385, 1.000000000000000000, 0.9238795325112867385, 1.000000000000000000, 0.9238795325112867385, 1.000000000000000000, 0.9238795325112867385, 1.000000000000000000, 0.9238795325112867385, 1.000000000000000000, 0.9238795325112867385, 1.000000000000000000, 0.9238795325112867385, 1.000000000000000000, 0.9238795325112867385, 1.000000000000000000, 0.9238795325112867385, 1.000000000000000000, 0.9238795325112867385, 1.000000000000000000, 0.9238795325112867385, 1.000000000000000000, 0.9238795325112867385, 1.000000000000000000, 0.9238795325112867385, 1.000000000000000000, 0.9238795325112867385, 1.000000000000000000, 0.9238795325112867385, 1.000000000000000000, 0.9238795325112867385, 1.000000000000000000, 0.9238795325112867385, 1.000000000000000000, 0.9238795325112867385, 1.000000000000000000, 0.9238795325112867385, 1.000000000000000000, 0.9238795325112867385, 1.000000000000000000, 0.9238795325112867385, 1.000000000000000000, 0.9238795325112867385, 1.000000000000000000, 0.9238795325112867385, 1.000000000000000000, 0.9238795325112867385, 1.000000000000000000, 0.9238795325112867385, 1.000000000000000000, 0.9238795325112867385, 1.000000000000000000, 0.9238795325112867385, 1.000000000000000000, 0.9238795325112867385, 1.000000000000000000, 0.9238795325112867385, 1.000000000000000000, 0.9238795325112867385, 1.000000000000000000, 0.9238795325112867385, 1.000000000000000000, 0.9238795325112867385, 1.000000000000000000, 0.9238795325112867385, 1.000000000000000000, 0.9238795325112867385, 1.000000000000000000, 0.9238795325112867385, 1.000000000000000000, 0.9238795325112867385, 1.000000000000000000, 0.9238795325112867385, 1.000000000000000000, 0.9238795325112867385, 1.000000000000000000, 0.9238795325112867385, 1.000000000000000000, 0.9238795325112867385, 1.000000000000000000, 0.9238795325112867385, 1.000000000000000000, 0.9238795325112867385, 1.000000000000000000, 0.9238795325112867385, 1.000000000000000000, 0.9238795325112867385, 1.000000000000000000, 0.9238795325112867385, 1.000000000000000000, 0.9238795325112867385, 1.000000000000000000, 0.9238795325112867385, 1.000000000000000000, 0.9238795325112867385, 1.000000000000000000, 0.9238795325112867385, 1.000000000000000000, 0.9238795325112867385, 1.000000000000000000, 0.9238795325112867385, 1.000000000000000000, 0.9238795325112867385, 1.000000000000000000, 0.9238795325112867385, 1.000000000000000000, 0.9238795325112867385, 1.000000000000000000, 0.9238795325112867385, 1.000000000000000000, 0.9238795325112867385, 1.000000000000000000, 0.9238795325112867385, 1.000000000000000000, 0.9238795325112867385, 1.000000000000000000, 0.9238795325112867385, 1.000000000000000000, 0.9238795325112867385, 1.000000000000000000, 0.9238795325112867385, 1.000000000000000000, 0.9238795325112867385, 1.000000000000000000, 0.9238795325112867385, 1.000000000000000000, 0.9238795325112867385, 1.000000000000000000, 0.9238795325112867385, 1.000000000000000000, 0.9238795325112867385, 1.000000000000000000, 0.9238795325112867385, 1.000000000000000000, 0.9238795325112867385, 1.000000000000000000, 0.9238795325112867385, 1.000000000000000000, 0.9238795325112867385, 1.000000000000000000, 0.9238795325112867385, 1.000000000000000000, 0.9238795325112867385, 1.000000000000000000, 0.9238795325112867385, 1.000000000000000000, 0.9238795325112867385, 1.000000000000000000, 0.9238795325112867385, 1.000000000000000000, 0.9238795325112867385, 1.000000000000000000, 0.9238795325112867385, 1.000000000000000000, 0.9238795325112867385, 1.000000000000000000, 0.9238795325112867385, 1.000000000000000000, 0.9238795325112867385, 1.000000000000000000, 0.9238795325112867385, 1.000000000000000000, 0.9238795325112867385, 1.000000000000000000, 0.9238795325112867385, 1.000000000000000000, 0.9238795325112867385, 1.000000000000000000, 0.9238795325112867385, 1.000000000000000000, 0.9238795325112867385, 1.000000000000000000, 0.9238795325112867385, 1.000000000000000000, 0.9238795325112867385, 1.000000000000000000, 0.9238795325112867385, 1.000000000000000000, 0.9238795325112867385, 1.000000000000000000, 0.9238795325112867385, 1.000000000000000000, 0.9238795325112867385, 1.000000000000000000, 0.9238795325112867385, 1.000000000000000000, 0.9238795325112867385, 1.000000000000000000, 0.9238795325112867385, 1.000000000000000000, 0.9238795325112867385, 1.000000000000000000, 0.9238795325112867385, 1.000000000000000000, 0.9238795325112867385, 1.000000000000000000, 0.9238795325112867385, 1.000000000000000000, 0.9238795325112867385, 1.000000000000000000, 0.9238795325112867385, 1.000000000000000000, 0.9238795325112867385, 1.000000000000000000, 0.9238795325112867385, 1.000000000000000000, 0.9238795325112867385, 1.000000000000000000, 0.9238795325112867385, 1.000000000000000000, 0.9238795325112867385, 1.000000000000000000, 0.9238795325112867385, 1.000000000000000000, 0.9238795325112867385, 1.000000000000000000, 0.9238795325112867385, 1.000000000000000000, 0.9238795325112867385, 1.000000000000000000, 0.9238795325112867385, 1.000000000000000000, 0.9238795325112867385, 1.000000000000000000, 0.9238795325112867385, 1.000000000000000000, 0.9238795325112867385, 1.000000000000000000, 0.9238795325112867385, 1.000000000000000000, 0.9238795325112867385, 1.000000000000000000, 0.9238795325112867385, 1.000000000000000000, 0.9238795325112867385, 1.000000000000000000, 0.9238795325112867385, 1.000000000000000000, 0.9238795325112867385, 1.000000000000000000, 0.9238795325112867385, 1.000000000000000000, 0.9238795325112867385, 1.000000000000000000, 0.9238795325112867385, 1.000000000000000000, 0.9238795325112867385, 1.000000000000000000, 0.9238795325112867385, 1.000000000000000000, 0.9238795325112867385, 1.000000000000000000, 0.9238795325112867385, 1.000000000000000000 ) ) 
 REPRESENTATION_ITEM ( '' )  );
#61632=CARTESIAN_POINT ( 'NONE',  ( 3.313708498984765161, 123.9687500000000142, 7.999999999999998224 ) ) ;
#61636=CARTESIAN_POINT ( 'NONE',  ( 8.000000000000000000, 8.812499995903221972, 0.000000000000000000 ) ) ;
#61637=EDGE_CURVE ( 'NONE', #55690, #25275, #19741, .T. ) ;
#61662=CARTESIAN_POINT ( 'NONE',  ( -4.401442555609581635E-16, 102.7812500020483810, -7.188101187500000044 ) ) ;
#61683=APPLICATION_CONTEXT ( 'automotive_design' ) ;
#61688=CARTESIAN_POINT ( 'NONE',  ( 4.401442555609581635E-16, 16.21874999795161543, -7.188101187500000044 ) ) ;
#61692=CARTESIAN_POINT ( 'NONE',  ( -4.898587196589412829E-16, 90.31250000409676204, -8.000000000000000000 ) ) ;
#61696=CARTESIAN_POINT ( 'NONE',  ( -5.082755093536325042, 1.031249997951609876, -5.082755093536325930 ) ) ;
#61699=CARTESIAN_POINT ( 'NONE',  ( -7.188101187500002709, 1.687499997951610098, 2.977408999572649151 ) ) ;
#61714=CARTESIAN_POINT ( 'NONE',  ( -7.188101187500002709, 10.31249999795161187, 2.977408999572649151 ) ) ;
#61718=CARTESIAN_POINT ( 'NONE',  ( 1.320432766682874540E-15, 114.4062500020483810, 7.188101187500000044 ) ) ;
#61736=CARTESIAN_POINT ( 'NONE',  ( 3.313708498984765161, 95.46875000000000000, 7.999999999999998224 ) ) ;
#61743=ORIENTED_EDGE ( 'NONE', *, *, #66578, .T. ) ;
#61755=LINE ( 'NONE', #45142, #11052 ) ;
#61759=CARTESIAN_POINT ( 'NONE',  ( -5.082755093536325042, 20.53124999795161543, -5.082755093536325930 ) ) ;
#61788=CARTESIAN_POINT ( 'NONE',  ( -4.898587196589412829E-16, 112.6250000000000000, -8.000000000000000000 ) ) ;
#61794=CARTESIAN_POINT ( 'NONE',  ( -1.469576158976823947E-15, 11.62500000000000178, 8.000000000000000000 ) ) ;
#61797=CARTESIAN_POINT ( 'NONE',  ( 3.313708498984765161, 94.15625000409677625, 7.999999999999998224 ) ) ;
#61806=CARTESIAN_POINT ( 'NONE',  ( 7.188101187500000044, 90.40625000204838102, -8.802885111219163269E-16 ) ) ;
#61807=CARTESIAN_POINT ( 'NONE',  ( 0.000000000000000000, 125.0000000000000000, 0.000000000000000000 ) ) ;
#61820=LINE ( 'NONE', #32033, #63644 ) ;
#61827=CARTESIAN_POINT ( 'NONE',  ( -5.656854249492379694, 10.87499999590322020, -5.656854249492380582 ) ) ;
#61831=CARTESIAN_POINT ( 'NONE',  ( 5.082755093536324154, 20.15624999795161543, 5.082755093536326818 ) ) ;
#61833=CARTESIAN_POINT ( 'NONE',  ( 8.000000000000000000, 7.500000000000001776, 0.000000000000000000 ) ) ;
#61834=CARTESIAN_POINT ( 'NONE',  ( -5.082755093536325930, 104.8437500020483810, -5.082755093536325930 ) ) ;
#61846=CARTESIAN_POINT ( 'NONE',  ( -8.000000000000001776, 20.15624999590322730, 3.313708498984759387 ) ) ;
#61852=CARTESIAN_POINT ( 'NONE',  ( 2.977408999572650039, 96.68750000204838102, -7.188101187500000933 ) ) ;
#61859=CARTESIAN_POINT ( 'NONE',  ( -7.188101187500000044, 100.5312500020483810, 0.000000000000000000 ) ) ;
#61860=CARTESIAN_POINT ( 'NONE',  ( -0.6939194017717918994, 0.4334809116420236252, -7.910544316330319958 ) ) ;
#61883=CARTESIAN_POINT ( 'NONE',  ( 5.082755093536324154, 9.281249997951610098, 5.082755093536326818 ) ) ;
#61884=ADVANCED_FACE ( 'NONE', ( #12670 ), #70400, .T. ) ;
#61885=CARTESIAN_POINT ( 'NONE',  ( 3.313708498984760720, 109.7187500040967763, -8.000000000000000000 ) ) ;
#61894=LINE ( 'NONE', #73583, #2958 ) ;
#61908=CARTESIAN_POINT ( 'NONE',  ( -3.313708498984762052, 108.2187500000000000, -8.000000000000000000 ) ) ;
#61914=CARTESIAN_POINT ( 'NONE',  ( -1.469576158976823947E-15, 26.43749999590322375, 8.000000000000000000 ) ) ;
#61917=CARTESIAN_POINT ( 'NONE',  ( -2.977408999572650927, 122.7500000020483668, -7.188101187500000933 ) ) ;
#61918=CARTESIAN_POINT ( 'NONE',  ( 8.000000000000001776, 121.1562500000000000, 3.313708498984759387 ) ) ;
#61921=DIRECTION ( 'NONE',  ( -0.000000000000000000, 1.000000000000000000, -0.000000000000000000 ) ) ;
#61929=ORIENTED_EDGE ( 'NONE', *, *, #26969, .T. ) ;
#61937=CARTESIAN_POINT ( 'NONE',  ( -7.188101187499999156, 115.2500000020483952, 2.977408999572654924 ) ) ;
#61939=CARTESIAN_POINT ( 'NONE',  ( -4.898587196589412829E-16, 106.8125000040967763, -8.000000000000000000 ) ) ;
#61942=CARTESIAN_POINT ( 'NONE',  ( 5.082755093536325042, 119.4687500020483810, -5.082755093536325930 ) ) ;
#61951=AXIS2_PLACEMENT_3D ( 'NONE', #12426, #57737, #64852 ) ;
#61957=CARTESIAN_POINT ( 'NONE',  ( 7.999999999999998224, 22.21874999590322375, 3.313708498984766049 ) ) ;
#61959=DIRECTION ( 'NONE',  ( -0.000000000000000000, 1.000000000000000000, -0.000000000000000000 ) ) ;
#61967=CARTESIAN_POINT ( 'NONE',  ( 7.188101187500001821, 26.06249999795161543, -2.977408999572650483 ) ) ;
#61970=CARTESIAN_POINT ( 'NONE',  ( 4.401442555609581635E-16, 20.71874999795161543, -7.188101187500000044 ) ) ;
#61972=CYLINDRICAL_SURFACE ( 'NONE', #1420, 8.000000000000000000 ) ;
#61979=CYLINDRICAL_SURFACE ( 'NONE', #44526, 8.000000000000000000 ) ;
#61998=CARTESIAN_POINT ( 'NONE',  ( -2.977408999572650927, 91.25000000204838102, -7.188101187500001821 ) ) ;
#62002=CARTESIAN_POINT ( 'NONE',  ( 8.000000000000000000, 8.906249995903221972, -3.313708498984761164 ) ) ;
#62006=DIRECTION ( 'NONE',  ( 0.000000000000000000, 0.000000000000000000, 1.000000000000000000 ) ) ;
#62028=CARTESIAN_POINT ( 'NONE',  ( 7.188101187500002709, 105.3125000020483668, 2.977408999572649151 ) ) ;
#62045=CARTESIAN_POINT ( 'NONE',  ( -4.898587196589412829E-16, 91.81250000409677625, -8.000000000000000000 ) ) ;
#62053=CARTESIAN_POINT ( 'NONE',  ( -2.977408999572654480, 19.87499999795161543, 7.188101187499999156 ) ) ;
#62061=CARTESIAN_POINT ( 'NONE',  ( 5.082755093536325930, 6.656249997951611874, -5.082755093536325930 ) ) ;
#62069=ADVANCED_FACE ( 'NONE', ( #25092, #8129 ), #30767, .T. ) ;
#62071=ADVANCED_FACE ( 'NONE', ( #36071 ), #59088, .T. ) ;
#62079=CARTESIAN_POINT ( 'NONE',  ( -8.000000000000001776, 21.84375000000000355, 3.313708498984759387 ) ) ;
#62082=CARTESIAN_POINT ( 'NONE',  ( 2.977408999572652260, 10.68749999795161187, 7.188101187500000044 ) ) ;
#62086=CARTESIAN_POINT ( 'NONE',  ( 2.977408999572650039, 106.0625000020483668, -7.188101187500001821 ) ) ;
#62095=LINE ( 'NONE', #5882, #17700 ) ;
#62101=CARTESIAN_POINT ( 'NONE',  ( 1.469576158976823947E-15, 96.87499999999998579, 8.000000000000000000 ) ) ;
#62103=CARTESIAN_POINT ( 'NONE',  ( 3.313708498984815343, 99.03124999999997158, -7.999999999999944933 ) ) ;
#62114=CARTESIAN_POINT ( 'NONE',  ( -5.082755093536325930, 122.4687500020483952, -5.082755093536325930 ) ) ;
#62123=CARTESIAN_POINT ( 'NONE',  ( 7.188101187499999156, 16.87499999795161543, 2.977408999572654924 ) ) ;
#62138=CARTESIAN_POINT ( 'NONE',  ( -3.313708498984719864, 21.28124999590322375, -8.000000000000040856 ) ) ;
#62141=CARTESIAN_POINT ( 'NONE',  ( -1.469576158976823947E-15, 26.62500000000000355, 8.000000000000000000 ) ) ;
#62159=CARTESIAN_POINT ( 'NONE',  ( 5.656854249492378806, 13.31250000000000178, 5.656854249492381470 ) ) ;
#62161=CARTESIAN_POINT ( 'NONE',  ( -8.000000000000000000, 93.68750000409679046, 0.000000000000000000 ) ) ;
#62166=( BOUNDED_CURVE ( )  B_SPLINE_CURVE ( 2, ( #32158, #55179, #30664, #3484, #48001, #54052, #49498, #65360, #13659 ),
 .UNSPECIFIED., .F., .F. ) 
 B_SPLINE_CURVE_WITH_KNOTS ( ( 3, 2, 2, 2, 3 ),
 ( 0.1354166666666667407, 0.1406250000000000833, 0.1458333333333334259, 0.1510416666666667684, 0.1562500000000001110 ),
 .UNSPECIFIED. ) 
 CURVE ( )  GEOMETRIC_REPRESENTATION_ITEM ( )  RATIONAL_B_SPLINE_CURVE ( ( 0.9999999999999987788, 0.9238795325112879597, 1.000000000000000000, 0.9238795325112867385, 1.000000000000000000, 0.9238795325112867385, 1.000000000000000000, 0.9238795325112850731, 1.000000000000001554 ) ) 
 REPRESENTATION_ITEM ( '' )  );
#62171=CARTESIAN_POINT ( 'NONE',  ( -2.977408999572651815, 123.3125000020483810, 7.188101187500000933 ) ) ;
#62180=ORIENTED_EDGE ( 'NONE', *, *, #7002, .F. ) ;
#62190=CARTESIAN_POINT ( 'NONE',  ( 5.656854249492381470, 101.5625000000000000, 5.656854249492379694 ) ) ;
#62193=CARTESIAN_POINT ( 'NONE',  ( -5.656854249492381470, 11.24999999590322197, 5.656854249492379694 ) ) ;
#62195=ORIENTED_EDGE ( 'NONE', *, *, #65405, .T. ) ;
#62197=CARTESIAN_POINT ( 'NONE',  ( 5.082755093536325930, 16.03124999795161543, -5.082755093536325930 ) ) ;
#62200=CARTESIAN_POINT ( 'NONE',  ( 7.188101187500002709, 105.6875000020483952, 2.977408999572649151 ) ) ;
#62201=CARTESIAN_POINT ( 'NONE',  ( 0.000000000000000000, 54.99999999999999289, 11.00000000000000000 ) ) ;
#62217=CARTESIAN_POINT ( 'NONE',  ( 7.188101187500002709, 94.81250000204838102, 2.977408999572649151 ) ) ;
#62223=CARTESIAN_POINT ( 'NONE',  ( -7.188101187499999156, 100.6250000020483810, 2.977408999572654924 ) ) ;
#62240=VERTEX_POINT ( 'NONE', #36438 ) ;
#62248=CARTESIAN_POINT ( 'NONE',  ( 2.977408999572651815, 12.18749999795161187, 7.188101187500000933 ) ) ;
#62249=CARTESIAN_POINT ( 'NONE',  ( -8.000000000000000000, 110.0937500040968047, -3.313708498984761608 ) ) ;
#62259=CARTESIAN_POINT ( 'NONE',  ( 7.188101187500002709, 108.3125000020483810, 2.977408999572649151 ) ) ;
#62274=CARTESIAN_POINT ( 'NONE',  ( -7.999999999999998224, 111.5937499999999858, 3.313708498984766049 ) ) ;
#62278=CARTESIAN_POINT ( 'NONE',  ( 5.656854249492379694, 106.4374999999999858, -5.656854249492380582 ) ) ;
#62284=CARTESIAN_POINT ( 'NONE',  ( 7.188101187500000044, 2.343749997951610098, 0.000000000000000000 ) ) ;
#62286=CARTESIAN_POINT ( 'NONE',  ( -7.188101187500000044, 123.0312500020483810, 0.000000000000000000 ) ) ;
#62307=CARTESIAN_POINT ( 'NONE',  ( -2.977408999572652260, 112.4375000020483810, 7.188101187500000044 ) ) ;
#62313=CARTESIAN_POINT ( 'NONE',  ( 7.188101187500000044, 117.7812500020483810, -8.802885111219163269E-16 ) ) ;
#62334=CARTESIAN_POINT ( 'NONE',  ( -8.000000000000000000, 0.6562500000000002220, -3.313708498984762496 ) ) ;
#62337=CARTESIAN_POINT ( 'NONE',  ( 7.188101187500001821, 24.93749999795161543, -2.977408999572650483 ) ) ;
#62346=AXIS2_PLACEMENT_3D ( 'NONE', #43072, #66848, #37055 ) ;
#62351=CARTESIAN_POINT ( 'NONE',  ( 0.000000000000000000, 125.0000000000000000, 0.000000000000000000 ) ) ;
#62359=CARTESIAN_POINT ( 'NONE',  ( -4.898587196589412829E-16, 123.1250000000000000, -8.000000000000000000 ) ) ;
#62362=VERTEX_POINT ( 'NONE', #14887 ) ;
#62364=CARTESIAN_POINT ( 'NONE',  ( 3.313708498984657247, 93.96875000000000000, 8.000000000000106581 ) ) ;
#62368=CARTESIAN_POINT ( 'NONE',  ( 5.656854249492380582, 13.49999999590322375, -5.656854249492380582 ) ) ;
#62371=( BOUNDED_CURVE ( )  B_SPLINE_CURVE ( 2, ( #25099, #47012, #70407, #13408, #13041, #24734, #64742, #42085, #19082 ),
 .UNSPECIFIED., .F., .F. ) 
 B_SPLINE_CURVE_WITH_KNOTS ( ( 3, 2, 2, 2, 3 ),
 ( 0.8194444444444443088, 0.8263888888888887285, 0.8333333333333332593, 0.8402777777777777901, 0.8472222222222222099 ),
 .UNSPECIFIED. ) 
 CURVE ( )  GEOMETRIC_REPRESENTATION_ITEM ( )  RATIONAL_B_SPLINE_CURVE ( ( 1.000000000000001110, 0.9238795325112855172, 1.000000000000000000, 0.9238795325112867385, 1.000000000000000000, 0.9238795325112867385, 1.000000000000000000, 0.9238795325112867385, 1.000000000000000000 ) ) 
 REPRESENTATION_ITEM ( '' )  );
#62380=ORIENTED_EDGE ( 'NONE', *, *, #19956, .F. ) ;
#62391=CARTESIAN_POINT ( 'NONE',  ( -4.401442555609581635E-16, 104.2812500020483810, -7.188101187500000044 ) ) ;
#62414=CARTESIAN_POINT ( 'NONE',  ( 5.656854249492379694, 106.6250000040967763, -5.656854249492380582 ) ) ;
#62419=CARTESIAN_POINT ( 'NONE',  ( 2.977408999572652260, 23.06249999795161543, 7.188101187500000044 ) ) ;
#62427=CARTESIAN_POINT ( 'NONE',  ( -7.188101187500001821, 8.624999997951611874, -2.977408999572651371 ) ) ;
#62430=CARTESIAN_POINT ( 'NONE',  ( -7.188101187500001821, 2.999999997951610098, -2.977408999572651371 ) ) ;
#62434=DIRECTION ( 'NONE',  ( -0.000000000000000000, 1.000000000000000000, -0.000000000000000000 ) ) ;
#62441=CARTESIAN_POINT ( 'NONE',  ( -5.656854249492378806, 104.1874999999999858, 5.656854249492381470 ) ) ;
#62443=CARTESIAN_POINT ( 'NONE',  ( -5.082755093536326818, 19.40624999795161543, 5.082755093536325042 ) ) ;
#62448=CARTESIAN_POINT ( 'NONE',  ( -5.082755093536324154, 108.2187500020483810, 5.082755093536326818 ) ) ;
#62454=EDGE_CURVE ( 'NONE', #17336, #54742, #43951, .T. ) ;
#62459=DIRECTION ( 'NONE',  ( 0.000000000000000000, 0.000000000000000000, 1.000000000000000000 ) ) ;
#62464=CARTESIAN_POINT ( 'NONE',  ( 0.000000000000000000, 125.0000000000000000, 0.000000000000000000 ) ) ;
#62476=EDGE_CURVE ( 'NONE', #29688, #72916, #57897, .T. ) ;
#62478=CARTESIAN_POINT ( 'NONE',  ( 2.977408999572654480, 121.6250000020483810, 7.188101187499999156 ) ) ;
#62487=FACE_OUTER_BOUND ( 'NONE', #47055, .T. ) ;
#62488=CARTESIAN_POINT ( 'NONE',  ( 5.082755093536325930, 26.15624999795161543, -5.082755093536325930 ) ) ;
#62497=CARTESIAN_POINT ( 'NONE',  ( 8.000000000000000000, 118.2500000000000000, -9.797174393178825657E-16 ) ) ;
#62503=ORIENTED_EDGE ( 'NONE', *, *, #8356, .T. ) ;
#62506=AXIS2_PLACEMENT_3D ( 'NONE', #29007, #41808, #64818 ) ;
#62512=CARTESIAN_POINT ( 'NONE',  ( 2.977408999572652260, 6.562499997951610098, 7.188101187500000044 ) ) ;
#62513=ADVANCED_FACE ( 'NONE', ( #58533 ), #41538, .T. ) ;
#62526=CARTESIAN_POINT ( 'NONE',  ( 3.313708498984762496, 17.71875000000000355, 7.999999999999998224 ) ) ;
#62529=CARTESIAN_POINT ( 'NONE',  ( -5.656854249492378806, 92.37500000409677625, 5.656854249492381470 ) ) ;
#62534=ORIENTED_EDGE ( 'NONE', *, *, #66343, .F. ) ;
#62535=EDGE_CURVE ( 'NONE', #72916, #63531, #17786, .T. ) ;
#62540=CARTESIAN_POINT ( 'NONE',  ( -5.082755093536325930, 124.3437500020483952, -5.082755093536325930 ) ) ;
#62549=ORIENTED_EDGE ( 'NONE', *, *, #17332, .F. ) ;
#62562=CARTESIAN_POINT ( 'NONE',  ( 3.313708498984762496, 11.53124999590322197, 7.999999999999998224 ) ) ;
#62566=CARTESIAN_POINT ( 'NONE',  ( -5.082755093536325042, 14.90624999795161187, -5.082755093536325930 ) ) ;
#62568=DIRECTION ( 'NONE',  ( 0.000000000000000000, 0.000000000000000000, 1.000000000000000000 ) ) ;
#62569=CARTESIAN_POINT ( 'NONE',  ( 5.082755093536325042, 101.4687500020483810, -5.082755093536325930 ) ) ;
#62584=CARTESIAN_POINT ( 'NONE',  ( 2.977408999572654480, 93.12500000204838102, 7.188101187499999156 ) ) ;
#62591=CARTESIAN_POINT ( 'NONE',  ( -7.188101187499999156, 103.6250000020483810, 2.977408999572654924 ) ) ;
#62601=CARTESIAN_POINT ( 'NONE',  ( 3.313708498984762496, 16.21875000000000355, 7.999999999999998224 ) ) ;
#62612=DIRECTION ( 'NONE',  ( 0.8660254037844395958, -0.4999999999999981681, 0.000000000000000000 ) ) ;
#62620=CARTESIAN_POINT ( 'NONE',  ( -7.188101187500001821, 13.12499999795161187, -2.977408999572651371 ) ) ;
#62621=CARTESIAN_POINT ( 'NONE',  ( 3.313708498984760720, 111.2187500040968047, -8.000000000000000000 ) ) ;
#62624=EDGE_CURVE ( 'NONE', #25866, #1937, #53238, .T. ) ;
#62631=CARTESIAN_POINT ( 'NONE',  ( 5.082755093536326818, 103.7187500020483810, 5.082755093536325042 ) ) ;
#62633=CARTESIAN_POINT ( 'NONE',  ( -4.898587196589412829E-16, 123.1250000000000000, -8.000000000000000000 ) ) ;
#62638=CARTESIAN_POINT ( 'NONE',  ( 8.000000000000001776, 91.34375000409679046, 3.313708498984759387 ) ) ;
#62645=CARTESIAN_POINT ( 'NONE',  ( -4.898587196589412829E-16, 108.1250000000000000, -8.000000000000000000 ) ) ;
#62651=CARTESIAN_POINT ( 'NONE',  ( -1.469576158976823947E-15, 27.93749999590322375, 8.000000000000000000 ) ) ;
#62653=CARTESIAN_POINT ( 'NONE',  ( -2.977408999572652260, 120.3125000020483810, 7.188101187500000044 ) ) ;
#62663=CARTESIAN_POINT ( 'NONE',  ( 5.656854249492381470, 124.0625000000000000, 5.656854249492379694 ) ) ;
#62666=ORIENTED_EDGE ( 'NONE', *, *, #39840, .T. ) ;
#62673=CARTESIAN_POINT ( 'NONE',  ( 7.188101187500000044, 114.4062500020483810, -8.802885111219163269E-16 ) ) ;
#62678=CARTESIAN_POINT ( 'NONE',  ( 5.082755093536325042, 120.9687500020483952, -5.082755093536325930 ) ) ;
#62687=CARTESIAN_POINT ( 'NONE',  ( -5.656854249492381470, 18.93750000000000355, 5.656854249492379694 ) ) ;
#62702=CARTESIAN_POINT ( 'NONE',  ( -7.188101187500002709, 26.81249999795161543, 2.977408999572649151 ) ) ;
#62703=CARTESIAN_POINT ( 'NONE',  ( -5.656854249492378806, 107.1874999999999858, 5.656854249492381470 ) ) ;
#62705=CARTESIAN_POINT ( 'NONE',  ( 4.401442555609581635E-16, 23.71874999795161543, -7.188101187500000044 ) ) ;
#62707=( BOUNDED_CURVE ( )  B_SPLINE_CURVE ( 2, ( #65177, #65555, #36527, #54252, #72332, #59537, #14227, #71575, #19897 ),
 .UNSPECIFIED., .F., .F. ) 
 B_SPLINE_CURVE_WITH_KNOTS ( ( 3, 2, 2, 2, 3 ),
 ( 0.8194444444444443088, 0.8263888888888887285, 0.8333333333333332593, 0.8402777777777777901, 0.8472222222222222099 ),
 .UNSPECIFIED. ) 
 CURVE ( )  GEOMETRIC_REPRESENTATION_ITEM ( )  RATIONAL_B_SPLINE_CURVE ( ( 1.000000000000001110, 0.9238795325112855172, 1.000000000000000000, 0.9238795325112867385, 1.000000000000000000, 0.9238795325112867385, 1.000000000000000000, 0.9238795325112867385, 1.000000000000000000 ) ) 
 REPRESENTATION_ITEM ( '' )  );
#62728=CARTESIAN_POINT ( 'NONE',  ( 4.898587196589412829E-16, 12.18749999590322197, -8.000000000000000000 ) ) ;
#62730=CARTESIAN_POINT ( 'NONE',  ( -7.188101187499999156, 90.12500000204836681, 2.977408999572654924 ) ) ;
#62745=CARTESIAN_POINT ( 'NONE',  ( 3.313708498984742068, 10.03124999590321842, 8.000000000000019540 ) ) ;
#62752=CARTESIAN_POINT ( 'NONE',  ( -4.898587196589412829E-16, 115.8125000040967763, -8.000000000000000000 ) ) ;
#62758=CARTESIAN_POINT ( 'NONE',  ( -7.188101187499999156, 104.7500000020483810, 2.977408999572654924 ) ) ;
#62770=CARTESIAN_POINT ( 'NONE',  ( -4.903509839973872353, 0.5323584527330150751, -6.410198659010889699 ) ) ;
#62772=CARTESIAN_POINT ( 'NONE',  ( -4.898587196589412829E-16, 93.12499999999998579, -8.000000000000000000 ) ) ;
#62774=CARTESIAN_POINT ( 'NONE',  ( -3.313708498984719864, 18.28124999590321664, -8.000000000000040856 ) ) ;
#62775=CARTESIAN_POINT ( 'NONE',  ( 5.656854249492379694, 117.1250000040967905, -5.656854249492380582 ) ) ;
#62777=CARTESIAN_POINT ( 'NONE',  ( -8.000000000000000000, 100.9999999999999858, 0.000000000000000000 ) ) ;
#62784=CARTESIAN_POINT ( 'NONE',  ( 2.977408999572650927, 25.12499999795161543, -7.188101187500000933 ) ) ;
#62788=CARTESIAN_POINT ( 'NONE',  ( 8.000000000000001776, 89.84375000409677625, 3.313708498984759387 ) ) ;
#62795=CARTESIAN_POINT ( 'NONE',  ( 2.977408999572651815, 7.687499997951611874, 7.188101187500000933 ) ) ;
#62798=CARTESIAN_POINT ( 'NONE',  ( 7.188101187499999156, 6.749999997951610986, 2.977408999572654924 ) ) ;
#62816=CARTESIAN_POINT ( 'NONE',  ( -2.977408999572654480, 17.99999999795161543, 7.188101187499999156 ) ) ;
#62820=CARTESIAN_POINT ( 'NONE',  ( -7.188101187500000044, 103.5312500020483810, 0.000000000000000000 ) ) ;
#62824=LINE ( 'NONE', #51510, #5723 ) ;
#62835=CARTESIAN_POINT ( 'NONE',  ( -1.469576158976823947E-15, 8.625000000000000000, 8.000000000000000000 ) ) ;
#62836=CARTESIAN_POINT ( 'NONE',  ( 14.24573139410703426, 89.64008544297853120, -1.012862405069980154 ) ) ;
#62849=CARTESIAN_POINT ( 'NONE',  ( -7.188101187500001821, 121.0625000020483668, -2.977408999572650483 ) ) ;
#62858=CARTESIAN_POINT ( 'NONE',  ( 7.188101187499999156, 24.37499999795161543, 2.977408999572654924 ) ) ;
#62865=CARTESIAN_POINT ( 'NONE',  ( 3.313708498984721640, 25.21875000000000000, 8.000000000000039080 ) ) ;
#62875=ORIENTED_EDGE ( 'NONE', *, *, #73598, .F. ) ;
#62881=CARTESIAN_POINT ( 'NONE',  ( -7.188101187500002709, 7.687499997951611874, 2.977408999572649151 ) ) ;
#62886=CARTESIAN_POINT ( 'NONE',  ( 8.000000000000001776, 115.3437500040967905, 3.313708498984759387 ) ) ;
#62899=CARTESIAN_POINT ( 'NONE',  ( 5.656854249492378806, 17.81250000000000355, 5.656854249492381470 ) ) ;
#62902=CARTESIAN_POINT ( 'NONE',  ( 2.977408999572650039, 120.6875000020483952, -7.188101187500001821 ) ) ;
#62912=CARTESIAN_POINT ( 'NONE',  ( -7.188101187500000044, 1.218749997951610098, -8.802885111219163269E-16 ) ) ;
#62917=CARTESIAN_POINT ( 'NONE',  ( -7.188101187500001821, 124.4375000020483810, -2.977408999572650483 ) ) ;
#62924=AXIS2_PLACEMENT_3D ( 'NONE', #1384, #12313, #47375 ) ;
#62939=CARTESIAN_POINT ( 'NONE',  ( -4.898587196589412829E-16, 102.1250000000000000, -8.000000000000000000 ) ) ;
#62944=CARTESIAN_POINT ( 'NONE',  ( 7.188101187499999156, 18.74999999795161898, 2.977408999572654924 ) ) ;
#62946=DIRECTION ( 'NONE',  ( -0.000000000000000000, 1.000000000000000000, -0.000000000000000000 ) ) ;
#62947=CARTESIAN_POINT ( 'NONE',  ( 5.082755093536325042, 102.9687500020483810, -5.082755093536325930 ) ) ;
#62958=CARTESIAN_POINT ( 'NONE',  ( -5.656854249492379694, 22.87499999590322375, -5.656854249492380582 ) ) ;
#62964=CARTESIAN_POINT ( 'NONE',  ( -7.188101187500000044, 94.15625000204838102, 0.000000000000000000 ) ) ;
#62968=CARTESIAN_POINT ( 'NONE',  ( 8.000000000000001776, 110.8437500040967763, 3.313708498984759387 ) ) ;
#62971=VECTOR ( 'NONE', #20545, 1000.000000000000000 ) ;
#62972=CARTESIAN_POINT ( 'NONE',  ( 2.977408999572654480, 99.50000000204838102, 7.188101187499999156 ) ) ;
#62975=EDGE_CURVE ( 'NONE', #38953, #30969, #70873, .T. ) ;
#62982=CARTESIAN_POINT ( 'NONE',  ( 5.656854249492380582, 16.68750000000000355, -5.656854249492380582 ) ) ;
#62997=CARTESIAN_POINT ( 'NONE',  ( 7.188101187500000044, 15.46874999795161187, 0.000000000000000000 ) ) ;
#62998=CARTESIAN_POINT ( 'NONE',  ( 1.469576158976823947E-15, 110.5625000040967905, 8.000000000000000000 ) ) ;
#63007=CARTESIAN_POINT ( 'NONE',  ( 2.977408999572650039, 104.1875000020483668, -7.188101187500001821 ) ) ;
#63016=CARTESIAN_POINT ( 'NONE',  ( -4.898587196589412829E-16, 109.8125000040967905, -8.000000000000000000 ) ) ;
#63023=CARTESIAN_POINT ( 'NONE',  ( -7.999999999999998224, 104.0937500000000284, 3.313708498984766493 ) ) ;
#63028=CARTESIAN_POINT ( 'NONE',  ( 8.000000000000000000, 25.40624999590323085, -3.313708498984761608 ) ) ;
#63030=CARTESIAN_POINT ( 'NONE',  ( 7.188101187500000933, 119.3750000020483810, -2.977408999572651371 ) ) ;
#63041=CARTESIAN_POINT ( 'NONE',  ( 1.469576158976823947E-15, 123.8750000000000000, 8.000000000000000000 ) ) ;
#63050=CARTESIAN_POINT ( 'NONE',  ( -1.469576158976823947E-15, 6.937499995903221084, 8.000000000000000000 ) ) ;
#63051=CARTESIAN_POINT ( 'NONE',  ( -7.188101187500000044, 110.6562500020483810, 0.000000000000000000 ) ) ;
#63057=CARTESIAN_POINT ( 'NONE',  ( 2.977408999572654480, 120.5000000020483810, 7.188101187499999156 ) ) ;
#63064=( BOUNDED_CURVE ( )  B_SPLINE_CURVE ( 2, ( #43270, #58154, #6820, #37631, #8951, #12470, #72319, #19885, #23799 ),
 .UNSPECIFIED., .F., .F. ) 
 B_SPLINE_CURVE_WITH_KNOTS ( ( 3, 2, 2, 2, 3 ),
 ( 0.7812500000000001110, 0.7864583333333334814, 0.7916666666666667407, 0.7968750000000001110, 0.8020833333333334814 ),
 .UNSPECIFIED. ) 
 CURVE ( )  GEOMETRIC_REPRESENTATION_ITEM ( )  RATIONAL_B_SPLINE_CURVE ( ( 0.9999999999999983347, 0.9238795325112884038, 1.000000000000000000, 0.9238795325112867385, 1.000000000000000000, 0.9238795325112867385, 1.000000000000000000, 0.9238795325112850731, 1.000000000000001554 ) ) 
 REPRESENTATION_ITEM ( '' )  );
#63083=CARTESIAN_POINT ( 'NONE',  ( -2.977408999572650039, 24.93749999795161543, -7.188101187500001821 ) ) ;
#63086=CARTESIAN_POINT ( 'NONE',  ( 2.977408999572650927, 23.62499999795161543, -7.188101187500001821 ) ) ;
#63097=CARTESIAN_POINT ( 'NONE',  ( 0.000000000000000000, 0.000000000000000000, 0.000000000000000000 ) ) ;
#63102=CYLINDRICAL_SURFACE ( 'NONE', #2400, 8.000000000000000000 ) ;
#63109=CARTESIAN_POINT ( 'NONE',  ( 8.000000000000000000, 122.8437500000000142, -3.313708498984762496 ) ) ;
#63112=EDGE_CURVE ( 'NONE', #48435, #40745, #48899, .T. ) ;
#63117=CARTESIAN_POINT ( 'NONE',  ( -1.469576158976823947E-15, 5.437499995903221084, 8.000000000000000000 ) ) ;
#63125=CARTESIAN_POINT ( 'NONE',  ( 0.000000000000000000, 125.0000000000000000, 0.000000000000000000 ) ) ;
#63135=CARTESIAN_POINT ( 'NONE',  ( -8.000000000000000000, 116.0937500040968047, -3.313708498984761164 ) ) ;
#63141=CARTESIAN_POINT ( 'NONE',  ( -4.401442555609581635E-16, 105.7812500020483810, -7.188101187500000044 ) ) ;
#63167=CARTESIAN_POINT ( 'NONE',  ( 4.401442555609581635E-16, 23.71874999795161543, -7.188101187500000044 ) ) ;
#63175=CARTESIAN_POINT ( 'NONE',  ( 7.188101187500000044, 6.468749997951610986, 0.000000000000000000 ) ) ;
#63177=CARTESIAN_POINT ( 'NONE',  ( -7.188101187500000044, 4.593749997951610098, -8.802885111219163269E-16 ) ) ;
#63190=CARTESIAN_POINT ( 'NONE',  ( 5.082755093536325930, 20.15624999795161543, -5.082755093536325930 ) ) ;
#63194=CARTESIAN_POINT ( 'NONE',  ( -7.188101187500001821, 106.4375000020483810, -2.977408999572650483 ) ) ;
#63209=CARTESIAN_POINT ( 'NONE',  ( 5.656854249492381470, 91.06249999999998579, 5.656854249492379694 ) ) ;
#63218=EDGE_CURVE ( 'NONE', #54565, #56169, #44881, .T. ) ;
#63224=CARTESIAN_POINT ( 'NONE',  ( 7.188101187500001821, 122.0000000020483668, -2.977408999572651371 ) ) ;
#63233=CARTESIAN_POINT ( 'NONE',  ( 7.188101187500001821, 26.06249999795161543, -2.977408999572650483 ) ) ;
#63237=ORIENTED_EDGE ( 'NONE', *, *, #56423, .F. ) ;
#63251=CARTESIAN_POINT ( 'NONE',  ( 8.000000000000000000, 115.3437500000000000, -3.313708498984762496 ) ) ;
#63252=CARTESIAN_POINT ( 'NONE',  ( 1.469576158976823947E-15, 101.3750000000000000, 8.000000000000000000 ) ) ;
#63255=CARTESIAN_POINT ( 'NONE',  ( 5.082755093536324154, 8.156249997951611874, 5.082755093536326818 ) ) ;
#63271=CARTESIAN_POINT ( 'NONE',  ( 8.000000000000000000, 15.09375000000000533, -3.313708498984761608 ) ) ;
#63273=CARTESIAN_POINT ( 'NONE',  ( 7.188101187500000044, 120.4062500020483810, -8.802885111219163269E-16 ) ) ;
#63276=CARTESIAN_POINT ( 'NONE',  ( -3.313708498984786033, 8.531250000000001776, 7.999999999999979572 ) ) ;
#63280=CARTESIAN_POINT ( 'NONE',  ( -4.898587196589412829E-16, 114.1250000000000000, -8.000000000000000000 ) ) ;
#63281=LINE ( 'NONE', #46310, #25783 ) ;
#63284=CARTESIAN_POINT ( 'NONE',  ( 5.082755093536326818, 122.0937500020483952, 5.082755093536325042 ) ) ;
#63311=CARTESIAN_POINT ( 'NONE',  ( 5.082755093536324154, 24.65624999795161543, 5.082755093536326818 ) ) ;
#63315=CARTESIAN_POINT ( 'NONE',  ( -2.977408999572650927, 97.25000000204839523, -7.188101187500000933 ) ) ;
#63331=CARTESIAN_POINT ( 'NONE',  ( -2.977408999572650927, 90.87500000204836681, -7.188101187500000933 ) ) ;
#63337=CARTESIAN_POINT ( 'NONE',  ( -5.082755093536324154, 97.71875000204838102, 5.082755093536326818 ) ) ;
#63342=ORIENTED_EDGE ( 'NONE', *, *, #40835, .F. ) ;
#63360=CARTESIAN_POINT ( 'NONE',  ( 7.188101187499999156, 15.37499999795161187, 2.977408999572654924 ) ) ;
#63361=CARTESIAN_POINT ( 'NONE',  ( 1.469576158976823947E-15, 104.5625000040967763, 8.000000000000000000 ) ) ;
#63370=CARTESIAN_POINT ( 'NONE',  ( 0.000000000000000000, 132.4999999999999147, 0.000000000000000000 ) ) ;
#63371=CARTESIAN_POINT ( 'NONE',  ( -5.082755093536324154, 106.3437500020483810, 5.082755093536326818 ) ) ;
#63373=CARTESIAN_POINT ( 'NONE',  ( -8.000000000000000000, 15.56249999590322197, -9.797174393178825657E-16 ) ) ;
#63389=CARTESIAN_POINT ( 'NONE',  ( 8.000000000000001776, 101.6562500000000142, 3.313708498984759387 ) ) ;
#63392=CARTESIAN_POINT ( 'NONE',  ( -8.000000000000000000, 98.00000000000000000, 0.000000000000000000 ) ) ;
#63395=CARTESIAN_POINT ( 'NONE',  ( -3.313708498984760720, 27.28124999590322730, -8.000000000000000000 ) ) ;
#63398=CARTESIAN_POINT ( 'NONE',  ( -5.082755093536325930, 118.3437500020483810, -5.082755093536325930 ) ) ;
#63406=CARTESIAN_POINT ( 'NONE',  ( 1.469576158976823947E-15, 100.0625000040967763, 8.000000000000000000 ) ) ;
#63418=CARTESIAN_POINT ( 'NONE',  ( -7.188101187500000044, 109.1562500020483810, 0.000000000000000000 ) ) ;
#63424=CARTESIAN_POINT ( 'NONE',  ( -2.977408999572651815, 112.8125000020483952, 7.188101187500000933 ) ) ;
#63434=CARTESIAN_POINT ( 'NONE',  ( 4.898587196589412829E-16, 12.18749999590322197, -8.000000000000000000 ) ) ;
#63436=CARTESIAN_POINT ( 'NONE',  ( 4.898587196589412829E-16, 18.37500000000000355, -8.000000000000000000 ) ) ;
#63448=ORIENTED_EDGE ( 'NONE', *, *, #68463, .F. ) ;
#63449=ORIENTED_EDGE ( 'NONE', *, *, #54094, .T. ) ;
#63450=CARTESIAN_POINT ( 'NONE',  ( 5.656854249492380582, 0.1874999999999999167, -5.656854249492380582 ) ) ;
#63453=CARTESIAN_POINT ( 'NONE',  ( -1.320432766682874540E-15, 22.96874999795161543, 7.188101187500000044 ) ) ;
#63472=( BOUNDED_CURVE ( )  B_SPLINE_CURVE ( 2, ( #51943, #39507, #10831, #11207, #52685, #28550, #281, #51558, #46272 ),
 .UNSPECIFIED., .F., .F. ) 
 B_SPLINE_CURVE_WITH_KNOTS ( ( 3, 2, 2, 2, 3 ),
 ( 0.9583333333333332593, 0.9652777777777776791, 0.9722222222222220989, 0.9791666666666665186, 0.9861111111111110494 ),
 .UNSPECIFIED. ) 
 CURVE ( )  GEOMETRIC_REPRESENTATION_ITEM ( )  RATIONAL_B_SPLINE_CURVE ( ( 1.000000000000001110, 0.9238795325112855172, 1.000000000000000000, 0.9238795325112867385, 1.000000000000000000, 0.9238795325112867385, 1.000000000000000000, 0.9238795325112879597, 0.9999999999999987788 ) ) 
 REPRESENTATION_ITEM ( '' )  );
#63473=EDGE_CURVE ( 'NONE', #32408, #3972, #15552, .T. ) ;
#63474=ORIENTED_EDGE ( 'NONE', *, *, #56423, .T. ) ;
#63481=CARTESIAN_POINT ( 'NONE',  ( 3.313708498984765161, 116.4687499999999858, 7.999999999999998224 ) ) ;
#63484=ORIENTED_EDGE ( 'NONE', *, *, #32546, .T. ) ;
#63490=CARTESIAN_POINT ( 'NONE',  ( 8.000000000000000000, 97.34374999999998579, -3.313708498984762496 ) ) ;
#63513=CARTESIAN_POINT ( 'NONE',  ( 7.188101187500000044, 94.90625000204838102, -8.802885111219163269E-16 ) ) ;
#63520=CARTESIAN_POINT ( 'NONE',  ( -4.898587196589412829E-16, 121.6250000000000000, -8.000000000000000000 ) ) ;
#63527=CARTESIAN_POINT ( 'NONE',  ( 8.000000000000000000, 4.500000000000000888, 0.000000000000000000 ) ) ;
#63531=VERTEX_POINT ( 'NONE', #35302 ) ;
#63536=CARTESIAN_POINT ( 'NONE',  ( 7.188101187500000044, 24.84374999795161543, 0.000000000000000000 ) ) ;
#63544=CARTESIAN_POINT ( 'NONE',  ( -2.977408999572654480, 8.999999997951610098, 7.188101187499999156 ) ) ;
#63547=CARTESIAN_POINT ( 'NONE',  ( 2.977408999572650927, 8.624999997951611874, -7.188101187500001821 ) ) ;
#63559=CARTESIAN_POINT ( 'NONE',  ( -4.401442555609581635E-16, 114.7812500020483952, -7.188101187500000044 ) ) ;
#63562=ORIENTED_EDGE ( 'NONE', *, *, #40997, .F. ) ;
#63563=ADVANCED_FACE ( 'NONE', ( #43586 ), #59407, .T. ) ;
#63564=CARTESIAN_POINT ( 'NONE',  ( -7.188101187500000044, 16.21874999795161543, -8.802885111219163269E-16 ) ) ;
#63569=CARTESIAN_POINT ( 'NONE',  ( -7.188101187500001821, 104.9375000020483810, -2.977408999572650483 ) ) ;
#63579=DIRECTION ( 'NONE',  ( 0.000000000000000000, 0.000000000000000000, 1.000000000000000000 ) ) ;
#63582=CARTESIAN_POINT ( 'NONE',  ( 8.000000000000000000, 91.34375000000000000, -3.313708498984762496 ) ) ;
#63583=CARTESIAN_POINT ( 'NONE',  ( 9.122856833726327608, 89.81967984264845484, -3.970537934901964494 ) ) ;
#63597=CARTESIAN_POINT ( 'NONE',  ( -2.977408999572651815, 116.9375000020483952, 7.188101187500000933 ) ) ;
#63602=DIRECTION ( 'NONE',  ( 8.659560562354994488E-17, 0.7071067811865426878, -0.7071067811865524577 ) ) ;
#63623=CARTESIAN_POINT ( 'NONE',  ( 5.656854249492381470, 115.0625000000000000, 5.656854249492379694 ) ) ;
#63627=CARTESIAN_POINT ( 'NONE',  ( -1.320432766682874540E-15, 7.968749997951610986, 7.188101187500000044 ) ) ;
#63631=CARTESIAN_POINT ( 'NONE',  ( 4.898587196589412829E-16, 10.87500000000000178, -8.000000000000000000 ) ) ;
#63644=VECTOR ( 'NONE', #21448, 1000.000000000000000 ) ;
#63646=CARTESIAN_POINT ( 'NONE',  ( 3.313708498984762496, 14.71875000000000355, 7.999999999999998224 ) ) ;
#63649=VECTOR ( 'NONE', #47988, 1000.000000000000000 ) ;
#63650=CARTESIAN_POINT ( 'NONE',  ( 2.977408999572654480, 121.6250000020483810, 7.188101187499999156 ) ) ;
#63661=ADVANCED_FACE ( 'NONE', ( #25857 ), #60579, .T. ) ;
#63684=CARTESIAN_POINT ( 'NONE',  ( -1.320432766682874540E-15, 22.96874999795161543, 7.188101187500000044 ) ) ;
#63686=CARTESIAN_POINT ( 'NONE',  ( 7.188101187500000044, 95.28125000204836681, -8.802885111219163269E-16 ) ) ;
#63694=B_SPLINE_CURVE_WITH_KNOTS ( 'NONE', 1,
 ( #38217, #4632 ),
 .UNSPECIFIED., .F., .F.,
 ( 2, 2 ),
 ( 0.000000000000000000, 0.6095729009238285423 ),
 .UNSPECIFIED. ) ;
#63695=CARTESIAN_POINT ( 'NONE',  ( -8.000000000000000000, 119.1875000040967763, 0.000000000000000000 ) ) ;
#63704=CARTESIAN_POINT ( 'NONE',  ( -7.188101187499999156, 92.75000000204839523, 2.977408999572654924 ) ) ;
#63710=CARTESIAN_POINT ( 'NONE',  ( -7.188101187500000044, 99.03125000204838102, 0.000000000000000000 ) ) ;
#63724=LINE ( 'NONE', #6403, #20068 ) ;
#63733=ORIENTED_EDGE ( 'NONE', *, *, #19393, .T. ) ;
#63737=CARTESIAN_POINT ( 'NONE',  ( 5.656854249492381470, 103.2500000040967905, 5.656854249492379694 ) ) ;
#63747=CARTESIAN_POINT ( 'NONE',  ( -7.188101187500001821, 101.5625000020483810, -2.977408999572650483 ) ) ;
#63752=ORIENTED_EDGE ( 'NONE', *, *, #7856, .F. ) ;
#63764=CARTESIAN_POINT ( 'NONE',  ( 5.656854249492379694, 101.9375000000000000, -5.656854249492380582 ) ) ;
#63770=CARTESIAN_POINT ( 'NONE',  ( -1.320432766682874540E-15, 3.468749997951610986, 7.188101187500000044 ) ) ;
#63773=CARTESIAN_POINT ( 'NONE',  ( -2.977408999572652260, 118.8125000020484094, 7.188101187500000044 ) ) ;
#63792=CARTESIAN_POINT ( 'NONE',  ( -7.188101187500000933, 110.5625000020483810, -2.977408999572650483 ) ) ;
#63798=CARTESIAN_POINT ( 'NONE',  ( 1.320432766682874540E-15, 117.4062500020483810, 7.188101187500000044 ) ) ;
#63826=CARTESIAN_POINT ( 'NONE',  ( -3.313708498984760720, 6.468750000000001776, -8.000000000000000000 ) ) ;
#63829=CARTESIAN_POINT ( 'NONE',  ( -7.188101187500002709, 22.68749999795161543, 2.977408999572649151 ) ) ;
#63830=CARTESIAN_POINT ( 'NONE',  ( -8.000000000000000000, 122.0937500040967905, -3.313708498984761608 ) ) ;
#63851=CARTESIAN_POINT ( 'NONE',  ( 1.469576158976823947E-15, 95.56250000409677625, 8.000000000000000000 ) ) ;
#63856=CARTESIAN_POINT ( 'NONE',  ( -3.313708498984762052, 115.7187499999999858, -8.000000000000000000 ) ) ;
#63862=CARTESIAN_POINT ( 'NONE',  ( -5.656854249492381470, 15.74999999590322197, 5.656854249492379694 ) ) ;
#63865=CARTESIAN_POINT ( 'NONE',  ( 1.469576158976823947E-15, 96.87499999999998579, 8.000000000000000000 ) ) ;
#63881=CARTESIAN_POINT ( 'NONE',  ( -4.898587196589412829E-16, 96.12499999999998579, -8.000000000000000000 ) ) ;
#63882=CARTESIAN_POINT ( 'NONE',  ( -8.000000000000000000, 116.1875000040967763, 0.000000000000000000 ) ) ;
#63887=CARTESIAN_POINT ( 'NONE',  ( 7.188101187500002709, 99.31250000204839523, 2.977408999572649151 ) ) ;
#63890=CARTESIAN_POINT ( 'NONE',  ( 6.949739821034066622, 0.2534984199823389073, -3.475076582212567100 ) ) ;
#63896=DIRECTION ( 'NONE',  ( 0.000000000000000000, 0.000000000000000000, 1.000000000000000000 ) ) ;
#63903=DIRECTION ( 'NONE',  ( -0.000000000000000000, 1.000000000000000000, -0.000000000000000000 ) ) ;
#63905=CARTESIAN_POINT ( 'NONE',  ( -3.313708498984762496, 101.2812499999999858, 7.999999999999998224 ) ) ;
#63908=CARTESIAN_POINT ( 'NONE',  ( 8.000000000000000000, 17.81249999590322375, 0.000000000000000000 ) ) ;
#63912=CARTESIAN_POINT ( 'NONE',  ( -7.188101187500000044, 27.09374999795161898, -8.802885111219163269E-16 ) ) ;
#63914=ADVANCED_FACE ( 'NONE', ( #16773 ), #5481, .T. ) ;
#63921=AXIS2_PLACEMENT_3D ( 'NONE', #50695, #73714, #36969 ) ;
#63923=CARTESIAN_POINT ( 'NONE',  ( 7.188101187500000044, 12.46874999795161187, 0.000000000000000000 ) ) ;
#63926=CARTESIAN_POINT ( 'NONE',  ( 4.401442555609581635E-16, 5.718749997951610986, -7.188101187500000044 ) ) ;
#63941=CARTESIAN_POINT ( 'NONE',  ( -7.188101187499999156, 118.2500000020483952, 2.977408999572654924 ) ) ;
#63945=CARTESIAN_POINT ( 'NONE',  ( 5.082755093536325930, 17.15624999795161543, -5.082755093536325930 ) ) ;
#63947=ORIENTED_EDGE ( 'NONE', *, *, #48375, .F. ) ;
#63950=CARTESIAN_POINT ( 'NONE',  ( -2.977408999572650927, 100.2500000020483952, -7.188101187500001821 ) ) ;
#63953=CARTESIAN_POINT ( 'NONE',  ( -4.898587196589412829E-16, 88.81250000409677625, -8.000000000000000000 ) ) ;
#63967=CYLINDRICAL_SURFACE ( 'NONE', #46879, 8.000000000000000000 ) ;
#63979=CARTESIAN_POINT ( 'NONE',  ( -7.188101187500000044, 115.1562500020483810, 0.000000000000000000 ) ) ;
#64006=CARTESIAN_POINT ( 'NONE',  ( 3.313708498984846429, 112.1562500040967763, 7.999999999999918288 ) ) ;
#64010=CARTESIAN_POINT ( 'NONE',  ( 5.082755093536325930, 5.531249997951610098, -5.082755093536325930 ) ) ;
#64023=VERTEX_POINT ( 'NONE', #54091 ) ;
#64028=CARTESIAN_POINT ( 'NONE',  ( -5.656854249492379694, 18.56250000000000355, -5.656854249492380582 ) ) ;
#64031=CARTESIAN_POINT ( 'NONE',  ( -7.188101187500001821, 122.5625000020483952, -2.977408999572650483 ) ) ;
#64038=CARTESIAN_POINT ( 'NONE',  ( -7.188101187500000933, 1.124999997951610098, -2.977408999572651371 ) ) ;
#64042=CARTESIAN_POINT ( 'NONE',  ( -7.188101187499999156, 118.6250000020483810, 2.977408999572654924 ) ) ;
#64068=CARTESIAN_POINT ( 'NONE',  ( -2.977408999572654480, 22.87499999795161187, 7.188101187499999156 ) ) ;
#64070=CARTESIAN_POINT ( 'NONE',  ( 7.188101187500000044, 98.28125000204838102, -8.802885111219163269E-16 ) ) ;
#64079=ORIENTED_EDGE ( 'NONE', *, *, #52344, .T. ) ;
#64086=CARTESIAN_POINT ( 'NONE',  ( 3.313708498984706985, 103.7187500040967905, -8.000000000000055067 ) ) ;
#64092=CARTESIAN_POINT ( 'NONE',  ( -5.082755093536325930, 97.34375000204838102, -5.082755093536325930 ) ) ;
#64113=CARTESIAN_POINT ( 'NONE',  ( -8.000000000000000000, 104.1875000040967763, 0.000000000000000000 ) ) ;
#64119=CYLINDRICAL_SURFACE ( 'NONE', #61951, 8.000000000000000000 ) ;
#64122=CARTESIAN_POINT ( 'NONE',  ( -2.977408999572650927, 105.8750000020483952, -7.188101187500001821 ) ) ;
#64123=CARTESIAN_POINT ( 'NONE',  ( -1.469576158976823947E-15, 15.93749999590322197, 8.000000000000000000 ) ) ;
#64140=CARTESIAN_POINT ( 'NONE',  ( -3.313708498984762052, 99.21875000000000000, -8.000000000000000000 ) ) ;
#64144=VECTOR ( 'NONE', #19878, 1000.000000000000000 ) ;
#64146=CARTESIAN_POINT ( 'NONE',  ( 7.188101187499999156, 3.749999997951610542, 2.977408999572654924 ) ) ;
#64149=CARTESIAN_POINT ( 'NONE',  ( 7.188101187500000933, 117.8750000020483810, -2.977408999572651371 ) ) ;
#64173=CARTESIAN_POINT ( 'NONE',  ( 1.469576158976823947E-15, 102.8750000000000000, 8.000000000000000000 ) ) ;
#64174=CARTESIAN_POINT ( 'NONE',  ( -4.401442555609581635E-16, 104.2812500020483810, -7.188101187500000044 ) ) ;
#64180=CARTESIAN_POINT ( 'NONE',  ( -5.082755093536324154, 117.2187500020483810, 5.082755093536326818 ) ) ;
#64185=VERTEX_POINT ( 'NONE', #6593 ) ;
#64205=CARTESIAN_POINT ( 'NONE',  ( -1.469576158976823947E-15, 8.625000000000000000, 8.000000000000000000 ) ) ;
#64207=CARTESIAN_POINT ( 'NONE',  ( 5.082755093536325930, 2.156249997951610098, -5.082755093536325930 ) ) ;
#64208=CARTESIAN_POINT ( 'NONE',  ( -8.000000000000000000, 123.5937500040967763, -3.313708498984761608 ) ) ;
#64222=EDGE_LOOP ( 'NONE', ( #48102, #51694 ) ) ;
#64230=CARTESIAN_POINT ( 'NONE',  ( 8.000000000000000000, 115.2499999999999858, -9.797174393178825657E-16 ) ) ;
#64235=CARTESIAN_POINT ( 'NONE',  ( 7.999999999999998224, 14.71874999590322020, 3.313708498984766493 ) ) ;
#64252=EDGE_CURVE ( 'NONE', #20088, #31201, #57082, .T. ) ;
#64257=DIRECTION ( 'NONE',  ( -0.000000000000000000, 1.000000000000000000, -0.000000000000000000 ) ) ;
#64262=CARTESIAN_POINT ( 'NONE',  ( 2.977408999572650039, 99.68750000204838102, -7.188101187500001821 ) ) ;
#64268=EDGE_LOOP ( 'NONE', ( #18331, #51640, #1568, #67094 ) ) ;
#64286=CARTESIAN_POINT ( 'NONE',  ( -1.320432766682874540E-15, 27.46874999795161543, 7.188101187500000044 ) ) ;
#64293=ADVANCED_FACE ( 'NONE', ( #3524 ), #32961, .T. ) ;
#64294=CARTESIAN_POINT ( 'NONE',  ( -2.977408999572650039, 15.93749999795161543, -7.188101187500001821 ) ) ;
#64297=CARTESIAN_POINT ( 'NONE',  ( 2.977408999572651815, 6.562499997951610098, 7.188101187500000933 ) ) ;
#64310=CARTESIAN_POINT ( 'NONE',  ( -5.082755093536325930, 114.9687500020483810, -5.082755093536325930 ) ) ;
#64311=CARTESIAN_POINT ( 'NONE',  ( 9.797174393178825657E-16, 125.0000000000000000, -8.000000000000000000 ) ) ;
#64314=CARTESIAN_POINT ( 'NONE',  ( 2.977408999572652260, 21.18749999795161543, 7.188101187500000044 ) ) ;
#64319=CARTESIAN_POINT ( 'NONE',  ( 7.188101187500002709, 98.18750000204838102, 2.977408999572649151 ) ) ;
#64338=CARTESIAN_POINT ( 'NONE',  ( -4.898587196589412829E-16, 117.1250000000000000, -8.000000000000000000 ) ) ;
#64347=ADVANCED_FACE ( 'NONE', ( #38608 ), #14819, .T. ) ;
#64350=CARTESIAN_POINT ( 'NONE',  ( 2.977408999572654480, 112.6250000020483668, 7.188101187499999156 ) ) ;
#64355=CARTESIAN_POINT ( 'NONE',  ( -5.656854249492379694, 24.37499999590322375, -5.656854249492380582 ) ) ;
#64356=VERTEX_POINT ( 'NONE', #60858 ) ;
#64373=CARTESIAN_POINT ( 'NONE',  ( -5.656854249492380582, 91.81249999999998579, -5.656854249492380582 ) ) ;
#64376=ADVANCED_FACE ( 'NONE', ( #2778 ), #48784, .T. ) ;
#64377=CARTESIAN_POINT ( 'NONE',  ( 1.469576158976823947E-15, 112.0625000040967905, 8.000000000000000000 ) ) ;
#64381=CARTESIAN_POINT ( 'NONE',  ( -7.188101187500000044, 10.59374999795161187, -8.802885111219163269E-16 ) ) ;
#64393=CARTESIAN_POINT ( 'NONE',  ( -3.313708498984653250, 93.40625000409676204, -8.000000000000108358 ) ) ;
#64399=ADVANCED_FACE ( 'NONE', ( #20862 ), #43881, .T. ) ;
#64402=CARTESIAN_POINT ( 'NONE',  ( 5.656854249492378806, 23.81250000000000355, 5.656854249492381470 ) ) ;
#64414=CARTESIAN_POINT ( 'NONE',  ( -5.082755093536324154, 117.2187500020483810, 5.082755093536326818 ) ) ;
#64419=CARTESIAN_POINT ( 'NONE',  ( 0.000000000000000000, 125.0000000000000000, 0.000000000000000000 ) ) ;
#64424=EDGE_CURVE ( 'NONE', #65034, #9708, #67275, .T. ) ;
#64440=CARTESIAN_POINT ( 'NONE',  ( -5.082755093536326818, 22.78124999795161187, 5.082755093536325042 ) ) ;
#64442=CARTESIAN_POINT ( 'NONE',  ( -4.401442555609581635E-16, 97.15625000204839523, -7.188101187500000044 ) ) ;
#64459=CARTESIAN_POINT ( 'NONE',  ( 5.656854249492381470, 103.2500000040967905, 5.656854249492379694 ) ) ;
#64465=CARTESIAN_POINT ( 'NONE',  ( -2.977408999572650927, 94.25000000204838102, -7.188101187500001821 ) ) ;
#64471=VERTEX_POINT ( 'NONE', #4648 ) ;
#64481=ORIENTED_EDGE ( 'NONE', *, *, #71887, .T. ) ;
#64484=CARTESIAN_POINT ( 'NONE',  ( 3.999982273345623174, 89.99927424231840689, -6.928213464733948612 ) ) ;
#64486=CARTESIAN_POINT ( 'NONE',  ( -4.898587196589412829E-16, 105.3125000040967763, -8.000000000000000000 ) ) ;
#64494=ORIENTED_EDGE ( 'NONE', *, *, #35464, .T. ) ;
#64495=CARTESIAN_POINT ( 'NONE',  ( 1.469576158976823947E-15, 92.37499999999998579, 8.000000000000000000 ) ) ;
#64496=CARTESIAN_POINT ( 'NONE',  ( -7.188101187499999156, 97.25000000204839523, 2.977408999572654924 ) ) ;
#64498=CARTESIAN_POINT ( 'NONE',  ( 3.313708498984762496, 16.03124999590322020, 7.999999999999998224 ) ) ;
#64499=CARTESIAN_POINT ( 'NONE',  ( -4.898587196589412829E-16, 120.3125000040967763, -8.000000000000000000 ) ) ;
#64519=CARTESIAN_POINT ( 'NONE',  ( -5.082755093536325042, 4.406249997951610098, -5.082755093536325930 ) ) ;
#64522=CARTESIAN_POINT ( 'NONE',  ( -7.188101187499999156, 114.1250000020483952, 2.977408999572654924 ) ) ;
#64530=CARTESIAN_POINT ( 'NONE',  ( -5.656854249492381470, 9.937500000000001776, 5.656854249492379694 ) ) ;
#64542=CARTESIAN_POINT ( 'NONE',  ( 1.320432766682874540E-15, 106.5312500020483810, 7.188101187500000044 ) ) ;
#64548=CARTESIAN_POINT ( 'NONE',  ( -5.082755093536325930, 112.3437500020483810, -5.082755093536325930 ) ) ;
#64553=ORIENTED_EDGE ( 'NONE', *, *, #34414, .T. ) ;
#64574=CARTESIAN_POINT ( 'NONE',  ( 5.656854249492380582, 6.187500000000000888, -5.656854249492380582 ) ) ;
#64576=CARTESIAN_POINT ( 'NONE',  ( -5.082755093536325042, 1.031249997951609876, -5.082755093536325930 ) ) ;
#64577=CARTESIAN_POINT ( 'NONE',  ( -7.999999999999998224, 119.2812500040967763, 3.313708498984766493 ) ) ;
#64595=ORIENTED_EDGE ( 'NONE', *, *, #66685, .F. ) ;
#64602=CARTESIAN_POINT ( 'NONE',  ( 8.000000000000001776, 118.1562500000000000, 3.313708498984759387 ) ) ;
#64609=CARTESIAN_POINT ( 'NONE',  ( -3.313708498984760720, 16.78124999590322375, -8.000000000000000000 ) ) ;
#64612=CARTESIAN_POINT ( 'NONE',  ( 3.313708498984652362, 114.2187500040967905, -8.000000000000108358 ) ) ;
#64634=CARTESIAN_POINT ( 'NONE',  ( 5.082755093536326818, 99.21875000204838102, 5.082755093536325042 ) ) ;
#64642=DIRECTION ( 'NONE',  ( -0.000000000000000000, 1.000000000000000000, -0.000000000000000000 ) ) ;
#64645=DIRECTION ( 'NONE',  ( 0.000000000000000000, 0.000000000000000000, 1.000000000000000000 ) ) ;
#64660=CARTESIAN_POINT ( 'NONE',  ( 4.401442555609581635E-16, 12.84374999795161187, -7.188101187500000044 ) ) ;
#64663=CARTESIAN_POINT ( 'NONE',  ( 7.188101187499999156, 14.24999999795161010, 2.977408999572654924 ) ) ;
#64670=ADVANCED_FACE ( 'NONE', ( #35185 ), #30243, .T. ) ;
#64674=EDGE_CURVE ( 'NONE', #43001, #32974, #39153, .T. ) ;
#64677=CARTESIAN_POINT ( 'NONE',  ( 5.082755093536325042, 114.5937500020483810, -5.082755093536325930 ) ) ;
#64681=CARTESIAN_POINT ( 'NONE',  ( -5.082755093536325042, 25.03124999795161543, -5.082755093536325930 ) ) ;
#64682=ORIENTED_EDGE ( 'NONE', *, *, #66976, .T. ) ;
#64687=CARTESIAN_POINT ( 'NONE',  ( 5.082755093536325042, 102.9687500020483810, -5.082755093536325930 ) ) ;
#64707=CYLINDRICAL_SURFACE ( 'NONE', #32534, 8.000000000000000000 ) ;
#64712=CARTESIAN_POINT ( 'NONE',  ( -1.469576158976823947E-15, 10.12500000000000178, 8.000000000000000000 ) ) ;
#64718=CARTESIAN_POINT ( 'NONE',  ( -7.651291526794159914, 124.7975115043635128, -1.023541575279288240 ) ) ;
#64720=CARTESIAN_POINT ( 'NONE',  ( 7.188101187500002709, 117.3125000020483810, 2.977408999572649151 ) ) ;
#64726=CARTESIAN_POINT ( 'NONE',  ( 0.000000000000000000, 124.5000000000000284, 0.000000000000000000 ) ) ;
#64739=CARTESIAN_POINT ( 'NONE',  ( -3.313708498984653250, 91.71874999999997158, -8.000000000000108358 ) ) ;
#64742=CARTESIAN_POINT ( 'NONE',  ( 5.656854249492380582, 22.68750000000000355, -5.656854249492380582 ) ) ;
#64743=CARTESIAN_POINT ( 'NONE',  ( -7.188101187500000044, 124.5312500020483810, 0.000000000000000000 ) ) ;
#64746=CARTESIAN_POINT ( 'NONE',  ( -5.082755093536326818, 12.28124999795161187, 5.082755093536325042 ) ) ;
#64761=CARTESIAN_POINT ( 'NONE',  ( 7.999999999999998224, 25.40625000000000355, 3.313708498984766493 ) ) ;
#64771=CARTESIAN_POINT ( 'NONE',  ( -7.188101187500000044, 5.718749997951611874, -8.802885111219163269E-16 ) ) ;
#64773=CARTESIAN_POINT ( 'NONE',  ( 1.320432766682874540E-15, 118.9062500020483810, 7.188101187500000044 ) ) ;
#64779=ORIENTED_EDGE ( 'NONE', *, *, #73863, .F. ) ;
#64799=CARTESIAN_POINT ( 'NONE',  ( 7.188101187499999156, 21.74999999795162253, 2.977408999572654924 ) ) ;
#64802=CARTESIAN_POINT ( 'NONE',  ( -5.082755093536325930, 95.84375000204838102, -5.082755093536325930 ) ) ;
#64818=DIRECTION ( 'NONE',  ( 0.000000000000000000, 0.000000000000000000, 1.000000000000000000 ) ) ;
#64819=CARTESIAN_POINT ( 'NONE',  ( 1.469576158976823947E-15, 103.0625000040967763, 8.000000000000000000 ) ) ;
#64829=VERTEX_POINT ( 'NONE', #53552 ) ;
#64831=CARTESIAN_POINT ( 'NONE',  ( 1.469576158976823947E-15, 122.5625000040967763, 8.000000000000000000 ) ) ;
#64836=VECTOR ( 'NONE', #49484, 1000.000000000000000 ) ;
#64839=ORIENTED_EDGE ( 'NONE', *, *, #15704, .F. ) ;
#64847=CARTESIAN_POINT ( 'NONE',  ( 8.000000000000000000, 101.9375000040967763, -9.797174393178825657E-16 ) ) ;
#64852=DIRECTION ( 'NONE',  ( 0.000000000000000000, 0.000000000000000000, 1.000000000000000000 ) ) ;
#64854=CARTESIAN_POINT ( 'NONE',  ( -1.469576158976823947E-15, 25.12500000000000355, 8.000000000000000000 ) ) ;
#64855=CARTESIAN_POINT ( 'NONE',  ( 5.082755093536326818, 99.21875000204838102, 5.082755093536325042 ) ) ;
#64863=FACE_OUTER_BOUND ( 'NONE', #35985, .T. ) ;
#64880=CARTESIAN_POINT ( 'NONE',  ( 5.082755093536325930, 7.031249997951610986, -5.082755093536325930 ) ) ;
#64883=CARTESIAN_POINT ( 'NONE',  ( -7.188101187500000933, 116.9375000020483952, -2.977408999572650483 ) ) ;
#64901=CARTESIAN_POINT ( 'NONE',  ( 2.977408999572654480, 105.1250000020483810, 7.188101187499999156 ) ) ;
#64906=CARTESIAN_POINT ( 'NONE',  ( 2.977408999572650039, 109.0625000020483810, -7.188101187500001821 ) ) ;
#64931=CARTESIAN_POINT ( 'NONE',  ( -1.469576158976823947E-15, 5.625000000000000888, 8.000000000000000000 ) ) ;
#64933=CARTESIAN_POINT ( 'NONE',  ( 5.082755093536325930, 3.656249997951610542, -5.082755093536325930 ) ) ;
#64934=CARTESIAN_POINT ( 'NONE',  ( 8.000000000000001776, 119.8437500040967763, 3.313708498984759387 ) ) ;
#64938=CARTESIAN_POINT ( 'NONE',  ( -4.898587196589412829E-16, 118.6250000000000000, -8.000000000000000000 ) ) ;
#64940=CARTESIAN_POINT ( 'NONE',  ( 3.313708498984711426, 95.46874999999998579, 8.000000000000053291 ) ) ;
#64943=CARTESIAN_POINT ( 'NONE',  ( 0.000000000000000000, 125.0000000000000000, 0.000000000000000000 ) ) ;
#64956=CARTESIAN_POINT ( 'NONE',  ( 3.313708498984765161, 117.9687500000000142, 7.999999999999998224 ) ) ;
#64958=VERTEX_POINT ( 'NONE', #52333 ) ;
#64960=CARTESIAN_POINT ( 'NONE',  ( -3.313708498984765161, 17.34374999590322375, 7.999999999999998224 ) ) ;
#64975=ORIENTED_EDGE ( 'NONE', *, *, #25955, .T. ) ;
#64989=CARTESIAN_POINT ( 'NONE',  ( -7.188101187499999156, 94.25000000204838102, 2.977408999572654924 ) ) ;
#65004=CARTESIAN_POINT ( 'NONE',  ( 0.000000000000000000, 125.0000000000000000, 0.000000000000000000 ) ) ;
#65016=CARTESIAN_POINT ( 'NONE',  ( 7.188101187500001821, 15.56249999795161365, -2.977408999572650483 ) ) ;
#65018=CARTESIAN_POINT ( 'NONE',  ( -7.188101187500002709, 12.18749999795161187, 2.977408999572649151 ) ) ;
#65031=CARTESIAN_POINT ( 'NONE',  ( -7.188101187500001821, 113.5625000020483668, -2.977408999572650483 ) ) ;
#65034=VERTEX_POINT ( 'NONE', #30790 ) ;
#65035=CARTESIAN_POINT ( 'NONE',  ( -7.188101187500002709, 23.81249999795161543, 2.977408999572649151 ) ) ;
#65041=CARTESIAN_POINT ( 'NONE',  ( -7.188101187500000044, 100.5312500020483810, 0.000000000000000000 ) ) ;
#65048=CARTESIAN_POINT ( 'NONE',  ( 4.898587196589412829E-16, 13.87500000000000178, -8.000000000000000000 ) ) ;
#65060=CARTESIAN_POINT ( 'NONE',  ( 8.000000000000001776, 110.6562500000000000, 3.313708498984759387 ) ) ;
#65067=CARTESIAN_POINT ( 'NONE',  ( -3.442279223133897670, 124.6480146498679034, -7.075733707437612985 ) ) ;
#65070=CARTESIAN_POINT ( 'NONE',  ( 7.188101187500002709, 115.8125000020484094, 2.977408999572649151 ) ) ;
#65079=CARTESIAN_POINT ( 'NONE',  ( 8.000000000000001776, 109.1562500000000000, 3.313708498984759387 ) ) ;
#65093=CARTESIAN_POINT ( 'NONE',  ( 0.000000000000000000, 125.0000000000000000, -7.500000000000020428 ) ) ;
#65097=CARTESIAN_POINT ( 'NONE',  ( 8.000000000000000000, 112.4375000040967905, -9.797174393178825657E-16 ) ) ;
#65101=CARTESIAN_POINT ( 'NONE',  ( 7.188101187500000933, 9.937499997951610098, -2.977408999572650483 ) ) ;
#65112=EDGE_CURVE ( 'NONE', #62240, #71473, #36278, .T. ) ;
#65115=AXIS2_PLACEMENT_3D ( 'NONE', #14468, #34011, #43907 ) ;
#65118=CARTESIAN_POINT ( 'NONE',  ( -1.469576158976823947E-15, 22.12500000000000355, 8.000000000000000000 ) ) ;
#65130=CARTESIAN_POINT ( 'NONE',  ( -7.188101187500000044, 7.218749997951610986, -8.802885111219163269E-16 ) ) ;
#65131=CARTESIAN_POINT ( 'NONE',  ( -7.188101187499999156, 117.1250000020483952, 2.977408999572654924 ) ) ;
#65160=CARTESIAN_POINT ( 'NONE',  ( -5.082755093536325930, 92.84375000204838102, -5.082755093536325930 ) ) ;
#65177=CARTESIAN_POINT ( 'NONE',  ( -1.469576158976823947E-15, 23.43749999590322020, 8.000000000000000000 ) ) ;
#65178=CARTESIAN_POINT ( 'NONE',  ( 8.000000000000000000, 103.5312500040967905, -3.313708498984762496 ) ) ;
#65183=CARTESIAN_POINT ( 'NONE',  ( 1.320432766682874540E-15, 93.40625000204838102, 7.188101187500000044 ) ) ;
#65190=CARTESIAN_POINT ( 'NONE',  ( 1.469576158976823947E-15, 122.3750000000000000, 8.000000000000000000 ) ) ;
#65194=CARTESIAN_POINT ( 'NONE',  ( -8.000000000000001776, 11.15624999590322020, 3.313708498984759387 ) ) ;
#65196=LINE ( 'NONE', #59557, #2302 ) ;
#65199=ORIENTED_EDGE ( 'NONE', *, *, #51059, .T. ) ;
#65204=CARTESIAN_POINT ( 'NONE',  ( 5.656854249492378806, 17.81250000000000355, 5.656854249492381470 ) ) ;
#65209=CARTESIAN_POINT ( 'NONE',  ( 3.313708498984760720, 100.7187500040967763, -8.000000000000000000 ) ) ;
#65219=CARTESIAN_POINT ( 'NONE',  ( -7.188101187500001821, 98.56250000204838102, -2.977408999572650483 ) ) ;
#65220=CARTESIAN_POINT ( 'NONE',  ( 8.000000000000000000, 16.31249999590322375, 0.000000000000000000 ) ) ;
#65237=AXIS2_PLACEMENT_3D ( 'NONE', #39389, #10713, #17107 ) ;
#65240=CARTESIAN_POINT ( 'NONE',  ( 8.000000000000000000, 1.406249995903220196, -3.313708498984761608 ) ) ;
#65242=CARTESIAN_POINT ( 'NONE',  ( -7.188101187500001821, 2.999999997951610542, -2.977408999572651371 ) ) ;
#65246=CARTESIAN_POINT ( 'NONE',  ( -2.977408999572652260, 112.8125000020483952, 7.188101187500000044 ) ) ;
#65267=CARTESIAN_POINT ( 'NONE',  ( -7.188101187500000044, 107.6562500020483810, 0.000000000000000000 ) ) ;
#65273=CARTESIAN_POINT ( 'NONE',  ( -2.977408999572650927, 109.2500000020483952, -7.188101187500001821 ) ) ;
#65288=LINE ( 'NONE', #70585, #38137 ) ;
#65300=CARTESIAN_POINT ( 'NONE',  ( -5.656854249492381470, 11.43750000000000178, 5.656854249492379694 ) ) ;
#65302=CARTESIAN_POINT ( 'NONE',  ( 5.082755093536324154, 27.65624999795161543, 5.082755093536326818 ) ) ;
#65303=CARTESIAN_POINT ( 'NONE',  ( -4.898587196589412829E-16, 115.8125000040967763, -8.000000000000000000 ) ) ;
#65309=CARTESIAN_POINT ( 'NONE',  ( -5.656854249492379694, 6.562500000000001776, -5.656854249492380582 ) ) ;
#65313=CARTESIAN_POINT ( 'NONE',  ( 8.000000000000001776, 95.65625000000001421, 3.313708498984759387 ) ) ;
#65320=ORIENTED_EDGE ( 'NONE', *, *, #48375, .T. ) ;
#65327=CARTESIAN_POINT ( 'NONE',  ( -5.656854249492379694, 12.37499999590322197, -5.656854249492380582 ) ) ;
#65330=CARTESIAN_POINT ( 'NONE',  ( 5.656854249492379694, 110.9375000000000000, -5.656854249492380582 ) ) ;
#65336=CARTESIAN_POINT ( 'NONE',  ( 7.999999999999998224, 17.71874999590322730, 3.313708498984766493 ) ) ;
#65350=DIRECTION ( 'NONE',  ( -0.000000000000000000, 1.000000000000000000, -0.000000000000000000 ) ) ;
#65359=CARTESIAN_POINT ( 'NONE',  ( -7.188101187500000044, 122.6562500020483810, 0.000000000000000000 ) ) ;
#65360=CARTESIAN_POINT ( 'NONE',  ( 3.313708498984711426, 119.4687500000000142, 8.000000000000053291 ) ) ;
#65365=CARTESIAN_POINT ( 'NONE',  ( -4.401442555609581635E-16, 93.78125000204836681, -7.188101187500000044 ) ) ;
#65372=CYLINDRICAL_SURFACE ( 'NONE', #32693, 8.000000000000000000 ) ;
#65393=CARTESIAN_POINT ( 'NONE',  ( -7.188101187500001821, 14.62499999795161010, -2.977408999572651371 ) ) ;
#65396=CARTESIAN_POINT ( 'NONE',  ( 7.188101187500000044, 12.84374999795161187, 0.000000000000000000 ) ) ;
#65405=EDGE_CURVE ( 'NONE', #62362, #20933, #48809, .T. ) ;
#65407=CARTESIAN_POINT ( 'NONE',  ( -7.188101187500001821, 107.5625000020483810, -2.977408999572650483 ) ) ;
#65411=CARTESIAN_POINT ( 'NONE',  ( -2.977408999572650039, 24.93749999795161543, -7.188101187500000933 ) ) ;
#65417=CARTESIAN_POINT ( 'NONE',  ( -2.977408999572650927, 101.7500000020483810, -7.188101187500001821 ) ) ;
#65425=CARTESIAN_POINT ( 'NONE',  ( -5.656854249492379694, 14.06250000000000178, -5.656854249492380582 ) ) ;
#65427=EDGE_CURVE ( 'NONE', #36065, #43001, #61894, .T. ) ;
#65440=VERTEX_POINT ( 'NONE', #51686 ) ;
#65443=CARTESIAN_POINT ( 'NONE',  ( -8.000000000000000000, 7.968749995903221972, -3.313708498984762496 ) ) ;
#65447=CARTESIAN_POINT ( 'NONE',  ( -5.123800378305636727, 124.6878826211476223, -5.902641312904766124 ) ) ;
#65449=CARTESIAN_POINT ( 'NONE',  ( -2.977408999572651815, 110.9375000020483810, 7.188101187500000933 ) ) ;
#65454=CARTESIAN_POINT ( 'NONE',  ( -1.469576158976823947E-15, 24.93749999590322375, 8.000000000000000000 ) ) ;
#65468=CARTESIAN_POINT ( 'NONE',  ( -5.656854249492380582, 94.81250000000000000, -5.656854249492380582 ) ) ;
#65479=CARTESIAN_POINT ( 'NONE',  ( -1.320432766682874540E-15, 10.96874999795161187, 7.188101187500000044 ) ) ;
#65491=CARTESIAN_POINT ( 'NONE',  ( -1.469576158976823947E-15, 19.12500000000000355, 8.000000000000000000 ) ) ;
#65496=CARTESIAN_POINT ( 'NONE',  ( 8.000000000000000000, 21.09375000000000355, -3.313708498984761608 ) ) ;
#65506=ORIENTED_EDGE ( 'NONE', *, *, #8356, .F. ) ;
#65507=CARTESIAN_POINT ( 'NONE',  ( 4.401442555609581635E-16, 5.343749997951610986, -7.188101187500000044 ) ) ;
#65509=EDGE_CURVE ( 'NONE', #36743, #33110, #69551, .T. ) ;
#65510=CARTESIAN_POINT ( 'NONE',  ( 7.188101187500000044, 116.2812500020483810, -8.802885111219163269E-16 ) ) ;
#65516=VERTEX_POINT ( 'NONE', #64495 ) ;
#65521=DIRECTION ( 'NONE',  ( -0.000000000000000000, 1.000000000000000000, -0.000000000000000000 ) ) ;
#65525=CARTESIAN_POINT ( 'NONE',  ( 5.656854249492379694, 98.93750000000000000, -5.656854249492380582 ) ) ;
#65527=DIRECTION ( 'NONE',  ( -0.000000000000000000, 1.000000000000000000, -0.000000000000000000 ) ) ;
#65540=CARTESIAN_POINT ( 'NONE',  ( 2.977408999572650039, 91.06250000204838102, -7.188101187500000933 ) ) ;
#65546=VERTEX_POINT ( 'NONE', #12064 ) ;
#65548=CARTESIAN_POINT ( 'NONE',  ( 0.000000000000000000, 125.0000000000000000, 8.000000000000000000 ) ) ;
#65554=CARTESIAN_POINT ( 'NONE',  ( 1.469576158976823947E-15, 102.8750000000000000, 8.000000000000000000 ) ) ;
#65555=CARTESIAN_POINT ( 'NONE',  ( 3.313708498984721640, 23.53124999590321664, 8.000000000000039080 ) ) ;
#65561=CARTESIAN_POINT ( 'NONE',  ( 1.469576158976823947E-15, 113.5625000040967905, 8.000000000000000000 ) ) ;
#65583=CARTESIAN_POINT ( 'NONE',  ( 5.656854249492379694, 100.6250000040967905, -5.656854249492380582 ) ) ;
#65594=CARTESIAN_POINT ( 'NONE',  ( -2.977408999572651815, 100.4375000020483668, 7.188101187500000933 ) ) ;
#65598=VERTEX_POINT ( 'NONE', #46025 ) ;
#65600=CARTESIAN_POINT ( 'NONE',  ( -7.999999999999998224, 101.2812500040967763, 3.313708498984766049 ) ) ;
#65616=CARTESIAN_POINT ( 'NONE',  ( -8.000000000000000000, 1.968749995903220196, -3.313708498984762496 ) ) ;
#65618=CARTESIAN_POINT ( 'NONE',  ( 5.082755093536325930, 10.03124999795161187, -5.082755093536325930 ) ) ;
#65621=CARTESIAN_POINT ( 'NONE',  ( 2.977408999572654480, 111.5000000020483810, 7.188101187499999156 ) ) ;
#65623=CYLINDRICAL_SURFACE ( 'NONE', #29117, 8.000000000000000000 ) ;
#65638=CARTESIAN_POINT ( 'NONE',  ( -4.898587196589412829E-16, 108.3125000040967905, -8.000000000000000000 ) ) ;
#65639=CARTESIAN_POINT ( 'NONE',  ( 5.656854249492378806, 25.12499999590322375, 5.656854249492381470 ) ) ;
#65640=CARTESIAN_POINT ( 'NONE',  ( 5.082755093536325042, 108.5937500020483810, -5.082755093536325930 ) ) ;
#65645=ADVANCED_FACE ( 'NONE', ( #34734 ), #40371, .T. ) ;
#65646=CARTESIAN_POINT ( 'NONE',  ( -7.188101187500001821, 106.4375000020483810, -2.977408999572650483 ) ) ;
#65661=DIRECTION ( 'NONE',  ( -0.000000000000000000, 1.000000000000000000, -0.000000000000000000 ) ) ;
#65662=CARTESIAN_POINT ( 'NONE',  ( -3.313708498984772710, 122.4687500040967620, 7.999999999999988454 ) ) ;
#65668=CARTESIAN_POINT ( 'NONE',  ( -5.656854249492379694, 12.56250000000000178, -5.656854249492380582 ) ) ;
#65670=CARTESIAN_POINT ( 'NONE',  ( 5.082755093536324154, 3.281249997951610098, 5.082755093536326818 ) ) ;
#65672=CARTESIAN_POINT ( 'NONE',  ( -3.313708498984762496, 113.4687500040967763, 7.999999999999998224 ) ) ;
#65683=EDGE_CURVE ( 'NONE', #18825, #12576, #31, .T. ) ;
#65696=CARTESIAN_POINT ( 'NONE',  ( 3.313708498984765161, 111.9687500000000142, 7.999999999999998224 ) ) ;
#65701=CARTESIAN_POINT ( 'NONE',  ( 8.000000000000000000, 22.40624999590322375, -3.313708498984761608 ) ) ;
#65731=CARTESIAN_POINT ( 'NONE',  ( -2.977408999572650927, 89.37500000204839523, -7.188101187500001821 ) ) ;
#65760=ADVANCED_FACE ( 'NONE', ( #48976 ), #8249, .T. ) ;
#65761=CARTESIAN_POINT ( 'NONE',  ( 4.401442555609581635E-16, 21.84374999795161543, -7.188101187500000044 ) ) ;
#65764=CARTESIAN_POINT ( 'NONE',  ( 2.977408999572651815, 12.56249999795161365, 7.188101187500000933 ) ) ;
#65776=CARTESIAN_POINT ( 'NONE',  ( -2.977408999572650927, 110.3750000020484094, -7.188101187500001821 ) ) ;
#65780=CARTESIAN_POINT ( 'NONE',  ( 2.977408999572650927, 20.24999999795161898, -7.188101187500000933 ) ) ;
#65787=CARTESIAN_POINT ( 'NONE',  ( -7.188101187499999156, 96.12500000204836681, 2.977408999572654924 ) ) ;
#65812=CARTESIAN_POINT ( 'NONE',  ( -3.313708498984869966, 115.7187500000000142, -7.999999999999892530 ) ) ;
#65816=CARTESIAN_POINT ( 'NONE',  ( 2.977408999572650039, 111.6875000020483810, -7.188101187500001821 ) ) ;
#65822=ORIENTED_EDGE ( 'NONE', *, *, #15091, .F. ) ;
#65843=CARTESIAN_POINT ( 'NONE',  ( -2.977408999572654480, 13.87499999795161187, 7.188101187499999156 ) ) ;
#65852=CARTESIAN_POINT ( 'NONE',  ( -5.082755093536326818, 5.906249997951610986, 5.082755093536325042 ) ) ;
#65854=DIRECTION ( 'NONE',  ( 0.000000000000000000, 0.000000000000000000, 1.000000000000000000 ) ) ;
#65862=CARTESIAN_POINT ( 'NONE',  ( 4.898587196589412829E-16, 25.87500000000000711, -8.000000000000000000 ) ) ;
#65870=ORIENTED_EDGE ( 'NONE', *, *, #58545, .F. ) ;
#65871=CARTESIAN_POINT ( 'NONE',  ( -2.977408999572654480, 4.499999997951610986, 7.188101187499999156 ) ) ;
#65875=CARTESIAN_POINT ( 'NONE',  ( -5.082755093536325930, 112.3437500020483810, -5.082755093536325930 ) ) ;
#65890=CARTESIAN_POINT ( 'NONE',  ( 1.469576158976823947E-15, 98.37499999999998579, 8.000000000000000000 ) ) ;
#65898=CARTESIAN_POINT ( 'NONE',  ( 3.313708498984815343, 100.5312499999999716, -7.999999999999944933 ) ) ;
#65905=CARTESIAN_POINT ( 'NONE',  ( 1.926045908305006549, 89.59560438569887708, -7.188101187499999156 ) ) ;
#65931=CARTESIAN_POINT ( 'NONE',  ( -8.000000000000000000, 113.1875000040967763, 0.000000000000000000 ) ) ;
#65955=CARTESIAN_POINT ( 'NONE',  ( 8.000000000000000000, 100.5312500040967905, -3.313708498984762496 ) ) ;
#65964=CARTESIAN_POINT ( 'NONE',  ( 2.977408999572654480, 96.12500000204836681, 7.188101187499999156 ) ) ;
#65972=B_SPLINE_CURVE_WITH_KNOTS ( 'NONE', 3,
 ( #36734, #13692, #1674, #19004, #54086, #2396, #42010, #47304, #7691, #48408 ),
 .UNSPECIFIED., .F., .F.,
 ( 4, 2, 2, 2, 4 ),
 ( 0.01225088665078420333, 0.01328571931158636227, 0.01432055197238852121, 0.01535538463319067841, 0.01639021729399283561 ),
 .UNSPECIFIED. ) ;
#65986=CARTESIAN_POINT ( 'NONE',  ( -8.000000000000000000, 3.562499995903220196, -9.797174393178825657E-16 ) ) ;
#65988=CARTESIAN_POINT ( 'NONE',  ( -7.188101187500002709, 9.187499997951611874, 2.977408999572649151 ) ) ;
#65991=CARTESIAN_POINT ( 'NONE',  ( 1.320432766682874540E-15, 111.4062500020483810, 7.188101187500000044 ) ) ;
#66009=CARTESIAN_POINT ( 'NONE',  ( -2.977408999572650927, 101.3750000020483952, -7.188101187500000933 ) ) ;
#66016=CARTESIAN_POINT ( 'NONE',  ( 5.082755093536326818, 108.5937500020483810, 5.082755093536325042 ) ) ;
#66034=VERTEX_POINT ( 'NONE', #22171 ) ;
#66044=CARTESIAN_POINT ( 'NONE',  ( 7.188101187500001821, 9.562499997951608322, -2.977408999572650483 ) ) ;
#66047=CARTESIAN_POINT ( 'NONE',  ( 1.469576158976823947E-15, 115.0625000040967905, 8.000000000000000000 ) ) ;
#66070=CARTESIAN_POINT ( 'NONE',  ( 8.000000000000001776, 112.1562500000000000, 3.313708498984759387 ) ) ;
#66075=CARTESIAN_POINT ( 'NONE',  ( 3.313708498984762052, 19.59374999590322020, -8.000000000000000000 ) ) ;
#66087=CARTESIAN_POINT ( 'NONE',  ( -4.898587196589412829E-16, 99.31250000409677625, -8.000000000000000000 ) ) ;
#66088=CARTESIAN_POINT ( 'NONE',  ( -4.898587196589412829E-16, 100.8125000040967763, -8.000000000000000000 ) ) ;
#66098=CARTESIAN_POINT ( 'NONE',  ( 5.082755093536325042, 122.0937500020483952, -5.082755093536325930 ) ) ;
#66099=DIRECTION ( 'NONE',  ( -0.000000000000000000, 1.000000000000000000, -0.000000000000000000 ) ) ;
#66104=CARTESIAN_POINT ( 'NONE',  ( 7.188101187500002709, 90.31250000204838102, 2.977408999572649151 ) ) ;
#66109=CARTESIAN_POINT ( 'NONE',  ( 1.469576158976823947E-15, 89.56250000409677625, 8.000000000000000000 ) ) ;
#66128=ORIENTED_EDGE ( 'NONE', *, *, #2962, .T. ) ;
#66134=CARTESIAN_POINT ( 'NONE',  ( -7.188101187500000044, 22.21874999795161187, -8.802885111219163269E-16 ) ) ;
#66137=CARTESIAN_POINT ( 'NONE',  ( -5.082755093536326818, 12.28124999795161187, 5.082755093536325042 ) ) ;
#66142=CARTESIAN_POINT ( 'NONE',  ( 0.000000000000000000, 125.0000000000000000, 0.000000000000000000 ) ) ;
#66149=CARTESIAN_POINT ( 'NONE',  ( 2.977408999572654480, 109.6250000020483952, 7.188101187499999156 ) ) ;
#66161=CARTESIAN_POINT ( 'NONE',  ( 1.320432766682874540E-15, 91.90625000204838102, 7.188101187500000044 ) ) ;
#66173=DIRECTION ( 'NONE',  ( 0.000000000000000000, -0.000000000000000000, -1.000000000000000000 ) ) ;
#66191=CARTESIAN_POINT ( 'NONE',  ( -2.977408999572651815, 106.4375000020483810, 7.188101187500000933 ) ) ;
#66200=CARTESIAN_POINT ( 'NONE',  ( -1.469576158976823947E-15, 26.62500000000000355, 8.000000000000000000 ) ) ;
#66218=CARTESIAN_POINT ( 'NONE',  ( 2.977408999572650927, 17.62499999795161543, -7.188101187500000933 ) ) ;
#66229=CARTESIAN_POINT ( 'NONE',  ( -5.082755093536326818, 1.406249997951610320, 5.082755093536325042 ) ) ;
#66238=CARTESIAN_POINT ( 'NONE',  ( 0.000000000000000000, 125.0000000000000000, 0.000000000000000000 ) ) ;
#66246=ORIENTED_EDGE ( 'NONE', *, *, #29186, .T. ) ;
#66247=CARTESIAN_POINT ( 'NONE',  ( 7.188101187500000933, 3.562499997951610542, -2.977408999572650483 ) ) ;
#66251=CARTESIAN_POINT ( 'NONE',  ( -7.188101187499999156, 111.1250000020483810, 2.977408999572654924 ) ) ;
#66252=DIRECTION ( 'NONE',  ( 1.000000000000000000, 0.000000000000000000, -0.000000000000000000 ) ) ;
#66259=SHAPE_REPRESENTATION ( 'stud', ( #57354 ), #51355 ) ;
#66266=CARTESIAN_POINT ( 'NONE',  ( -5.656854249492380582, 96.31250000000000000, -5.656854249492380582 ) ) ;
#66272=CARTESIAN_POINT ( 'NONE',  ( -4.898587196589412829E-16, 118.8125000040967763, -8.000000000000000000 ) ) ;
#66278=CARTESIAN_POINT ( 'NONE',  ( 5.082755093536324154, 27.65624999795161543, 5.082755093536326818 ) ) ;
#66280=CARTESIAN_POINT ( 'NONE',  ( -4.401442555609581635E-16, 91.15625000204838102, -7.188101187500000044 ) ) ;
#66291=CARTESIAN_POINT ( 'NONE',  ( -7.188101187500001821, 20.62499999795161543, -2.977408999572651371 ) ) ;
#66307=CARTESIAN_POINT ( 'NONE',  ( 7.188101187500002709, 90.68750000204838102, 2.977408999572649151 ) ) ;
#66319=CYLINDRICAL_SURFACE ( 'NONE', #39367, 8.000000000000000000 ) ;
#66329=CARTESIAN_POINT ( 'NONE',  ( 8.000000000000000000, 95.93750000409679046, -9.797174393178825657E-16 ) ) ;
#66338=CARTESIAN_POINT ( 'NONE',  ( -2.977408999572650927, 95.37500000204839523, -7.188101187500001821 ) ) ;
#66343=EDGE_CURVE ( 'NONE', #54330, #45186, #2568, .T. ) ;
#66348=( BOUNDED_CURVE ( )  B_SPLINE_CURVE ( 2, ( #52000, #1447, #53113, #52741, #30094, #47062, #41050, #16905, #52371 ),
 .UNSPECIFIED., .F., .F. ) 
 B_SPLINE_CURVE_WITH_KNOTS ( ( 3, 2, 2, 2, 3 ),
 ( 0.06944444444444444753, 0.07638888888888889506, 0.08333333333333331483, 0.09027777777777776236, 0.09722222222222220989 ),
 .UNSPECIFIED. ) 
 CURVE ( )  GEOMETRIC_REPRESENTATION_ITEM ( )  RATIONAL_B_SPLINE_CURVE ( ( 1.000000000000000000, 0.9238795325112867385, 1.000000000000000000, 0.9238795325112867385, 1.000000000000000000, 0.9238795325112867385, 1.000000000000000000, 0.9238795325112868495, 0.9999999999999998890 ) ) 
 REPRESENTATION_ITEM ( '' )  );
#66357=CARTESIAN_POINT ( 'NONE',  ( -3.313708498984653250, 90.40625000409677625, -8.000000000000108358 ) ) ;
#66361=CARTESIAN_POINT ( 'NONE',  ( -8.000000000000001776, 2.156249995903220196, 3.313708498984759387 ) ) ;
#66363=CARTESIAN_POINT ( 'NONE',  ( -7.188101187500002709, 10.68749999795161187, 2.977408999572649151 ) ) ;
#66366=CARTESIAN_POINT ( 'NONE',  ( 1.320432766682874540E-15, 109.9062500020483810, 7.188101187500000044 ) ) ;
#66368=CARTESIAN_POINT ( 'NONE',  ( 0.000000000000000000, 125.0000000000000000, 0.000000000000000000 ) ) ;
#66382=VECTOR ( 'NONE', #61006, 1000.000000000000000 ) ;
#66384=CARTESIAN_POINT ( 'NONE',  ( 5.082755093536325042, 99.59375000204838102, -5.082755093536325930 ) ) ;
#66390=CARTESIAN_POINT ( 'NONE',  ( 1.320432766682874540E-15, 109.9062500020483810, 7.188101187500000044 ) ) ;
#66402=CARTESIAN_POINT ( 'NONE',  ( 4.401442555609581635E-16, 2.718749997951610542, -7.188101187500000044 ) ) ;
#66416=CARTESIAN_POINT ( 'NONE',  ( 5.082755093536324154, 10.78124999795161187, 5.082755093536326818 ) ) ;
#66417=CARTESIAN_POINT ( 'NONE',  ( -8.000000000000000000, 114.6875000040967763, 0.000000000000000000 ) ) ;
#66424=CARTESIAN_POINT ( 'NONE',  ( 5.656854249492379694, 95.93750000000000000, -5.656854249492380582 ) ) ;
#66445=CARTESIAN_POINT ( 'NONE',  ( 3.313708498984765161, 114.9687500000000142, 7.999999999999998224 ) ) ;
#66451=CARTESIAN_POINT ( 'NONE',  ( 5.656854249492380582, 19.49999999590322020, -5.656854249492380582 ) ) ;
#66464=DIRECTION ( 'NONE',  ( -0.000000000000000000, 1.000000000000000000, -0.000000000000000000 ) ) ;
#66473=CARTESIAN_POINT ( 'NONE',  ( 7.188101187500000044, 117.4062500020483810, -8.802885111219163269E-16 ) ) ;
#66478=CARTESIAN_POINT ( 'NONE',  ( -5.082755093536324154, 89.84375000204839523, 5.082755093536326818 ) ) ;
#66496=CARTESIAN_POINT ( 'NONE',  ( 0.000000000000000000, 125.0000000000000000, 0.000000000000000000 ) ) ;
#66502=CARTESIAN_POINT ( 'NONE',  ( 7.188101187499999156, 21.37499999795161543, 2.977408999572654924 ) ) ;
#66505=CARTESIAN_POINT ( 'NONE',  ( 4.401442555609581635E-16, 19.21874999795161543, -7.188101187500000044 ) ) ;
#66511=AXIS2_PLACEMENT_3D ( 'NONE', #64726, #31124, #13390 ) ;
#66516=CARTESIAN_POINT ( 'NONE',  ( -5.082755093536325930, 108.9687500020483810, -5.082755093536325930 ) ) ;
#66521=CARTESIAN_POINT ( 'NONE',  ( -7.188101187500002709, 26.81249999795161898, 2.977408999572649151 ) ) ;
#66529=CARTESIAN_POINT ( 'NONE',  ( -5.082755093536324154, 93.21875000204838102, 5.082755093536326818 ) ) ;
#66542=CARTESIAN_POINT ( 'NONE',  ( 5.656854249492379694, 108.1250000040967763, -5.656854249492380582 ) ) ;
#66544=CARTESIAN_POINT ( 'NONE',  ( 0.000000000000000000, 125.0000000000000000, 0.000000000000000000 ) ) ;
#66558=CARTESIAN_POINT ( 'NONE',  ( -8.000000000000000000, 115.9062500000000000, -3.313708498984761164 ) ) ;
#66562=CARTESIAN_POINT ( 'NONE',  ( 7.188101187500000044, 109.9062500020483810, -8.802885111219163269E-16 ) ) ;
#66578=EDGE_CURVE ( 'NONE', #67997, #36743, #13542, .T. ) ;
#66588=CARTESIAN_POINT ( 'NONE',  ( 2.143582570168940826, 90.06435469398867610, -8.000000000000000000 ) ) ;
#66593=CARTESIAN_POINT ( 'NONE',  ( -5.082755093536325042, 16.40624999795161543, -5.082755093536325930 ) ) ;
#66596=VERTEX_POINT ( 'NONE', #30821 ) ;
#66600=CARTESIAN_POINT ( 'NONE',  ( 4.898587196589412829E-16, 13.87500000000000178, -8.000000000000000000 ) ) ;
#66601=CARTESIAN_POINT ( 'NONE',  ( 7.188101187500000044, 3.468749997951610542, 0.000000000000000000 ) ) ;
#66615=CARTESIAN_POINT ( 'NONE',  ( -1.469576158976823947E-15, 5.625000000000000888, 8.000000000000000000 ) ) ;
#66618=CARTESIAN_POINT ( 'NONE',  ( 7.188101187499999156, 13.87499999795161010, 2.977408999572654924 ) ) ;
#66623=CARTESIAN_POINT ( 'NONE',  ( -2.977408999572650927, 115.2500000020484094, -7.188101187500001821 ) ) ;
#66632=CARTESIAN_POINT ( 'NONE',  ( 8.000000000000001776, 106.1562500000000000, 3.313708498984759387 ) ) ;
#66638=CARTESIAN_POINT ( 'NONE',  ( -7.999999999999998224, 92.09375000000000000, 3.313708498984766493 ) ) ;
#66646=CARTESIAN_POINT ( 'NONE',  ( 9.797174393178825657E-16, 125.0000000000000000, -8.000000000000000000 ) ) ;
#66653=CARTESIAN_POINT ( 'NONE',  ( -2.977408999572652260, 94.81250000204838102, 7.188101187500000044 ) ) ;
#66661=VERTEX_POINT ( 'NONE', #62835 ) ;
#66664=CARTESIAN_POINT ( 'NONE',  ( 7.188101187499999156, 19.87499999795161543, 2.977408999572654924 ) ) ;
#66665=CARTESIAN_POINT ( 'NONE',  ( -7.999999999999998224, 108.7812500040967763, 3.313708498984766049 ) ) ;
#66666=( BOUNDED_CURVE ( )  B_SPLINE_CURVE ( 2, ( #59433, #24707, #58697, #36418, #42060, #7744, #53771, #58565, #52896 ),
 .UNSPECIFIED., .F., .F. ) 
 B_SPLINE_CURVE_WITH_KNOTS ( ( 3, 2, 2, 2, 3 ),
 ( 0.1250000000000000000, 0.1319444444444444475, 0.1388888888888888951, 0.1458333333333333426, 0.1527777777777777901 ),
 .UNSPECIFIED. ) 
 CURVE ( )  GEOMETRIC_REPRESENTATION_ITEM ( )  RATIONAL_B_SPLINE_CURVE ( ( 1.000000000000000000, 0.9238795325112867385, 1.000000000000000000, 0.9238795325112867385, 1.000000000000000000, 0.9238795325112867385, 1.000000000000000000, 0.9238795325112867385, 1.000000000000000000 ) ) 
 REPRESENTATION_ITEM ( '' )  );
#66679=CARTESIAN_POINT ( 'NONE',  ( -8.000000000000000000, 21.56249999590322375, -9.797174393178825657E-16 ) ) ;
#66685=EDGE_CURVE ( 'NONE', #65598, #67997, #73421, .T. ) ;
#66700=( BOUNDED_CURVE ( )  B_SPLINE_CURVE ( 2, ( #54051, #2361, #30295, #71014, #53315, #42342, #1639, #24620, #29925, #19700, #14408, #60065, #71750, #37065, #47629, #25355, #65359, #20064, #13658, #48371, #43082, #42712, #66098, #59345, #14027, #8387, #37440, #52943, #1273, #47265, #70292, #70651, #18606, #18970, #41973, #30663, #7657, #53681, #72890, #8769, #60439, #26860, #9526, #55552, #21197, #14781, #67235, #31779, #54799, #38192, #3111, #26095, #33291, #49116, #73264, #9140, #72128, #44222, #20442, #55178, #3865, #32541, #15531, #61196, #60816, #21568, #67973, #49875, #38572, #43458, #16268, #61572, #66473, #9892, #32922, #44967, #55928, #37821, #15904, #4239, #27226, #50242, #43842, #56288, #32157, #3483, #44595, #26473, #73632, #49497, #72516, #67607, #20825, #38935, #66856, #61937, #21937, #10264, #4606, #15161, #27601, #50612, #4983, #52120, #62673, #11008, #820, #51359, #17771, #17023, #69090, #28350, #57038, #33661, #69834, #40047, #34410, #34041, #12111, #46445, #50989, #35149, #69463, #84, #22304, #62307, #40786, #10634, #39309, #74369, #23431, #46070, #57413, #6470, #11746, #74001, #56667, #23807, #5349, #58164, #22680, #45698, #68712, #46810, #63051, #63792, #11376, #17396, #5719, #28719, #27984, #45329, #51734, #23061, #40420, #29473, #52483, #68345, #16641, #452, #63418, #34784, #39674, #57787, #6095, #29101, #65640, #13205, #36244, #70932, #29841, #35509, #13936, #41164, #54338, #13572, #65267, #52853, #19612, #19244, #1185, #2649, #25638, #36978, #48286, #59620, #47913, #30575, #64542, #47178, #42255, #2273, #24537, #18519, #58522, #1558, #24166, #48653, #24896, #31310, #7935, #18149, #36610, #64901, #42625, #1908, #59259, #30940, #70210, #18885, #53960, #12839, #64174, #12478, #7202, #25267, #47545, #59983, #58893, #41527, #70569, #7571, #53226, #41891, #53597, #71291, #8299, #35876, #30206, #6829, #73174, #8676, #26378, #15439, #14315, #72034, #43367, #26001, #67514, #44134, #3394, #26770, #71661, #66009, #32826, #3018, #20350, #49402, #54711, #37350, #49026, #38476, #31691, #43750, #15813, #37731, #42991, #9804, #9051, #10172, #55836, #60729, #66384, #27512, #49788, #19982, #21111, #38101, #56204, #61101, #14690, #27141, #9430, #72802, #60349, #32065, #4152, #55086, #72423, #20732, #66764, #33208, #15068, #32448, #55457, #4517, #3769, #67144, #50157, #61479, #21481, #44502, #38848, #61852, #10543, #69373, #22217, #45244, #22592, #26132, #58075, #29008, #28265, #5634, #39588, #68256, #44877, #6386, #51272, #45612, #73913, #23346, #57699, #62217, #46356, #11657, #16551, #27888, #10916, #17683, #62964, #50522, #33950, #34691, #57323, #68626, #40700, #22979, #33575, #73537, #35062, #62584, #56578, #51648, #16935, #63704, #11289, #69001, #12029, #21845, #67883, #5264, #28634, #39960, #45985, #34319, #16174, #17308, #364, #56948, #40327, #50898, #6007, #74282, #4891, #63331, #52027, #39217, #29392, #7487, #1473, #24454, #41809, #58438, #36157, #52399, #735, #7117, #23717, #46721, #2188, #69747, #42165, #52765, #18061 ),
 .UNSPECIFIED., .F., .F. ) 
 B_SPLINE_CURVE_WITH_KNOTS ( ( 3, 2, 2, 2, 2, 2, 2, 2, 2, 2, 2, 2, 2, 2, 2, 2, 2, 2, 2, 2, 2, 2, 2, 2, 2, 2, 2, 2, 2, 2, 2, 2, 2, 2, 2, 2, 2, 2, 2, 2, 2, 2, 2, 2, 2, 2, 2, 2, 2, 2, 2, 2, 2, 2, 2, 2, 2, 2, 2, 2, 2, 2, 2, 2, 2, 2, 2, 2, 2, 2, 2, 2, 2, 2, 2, 2, 2, 2, 2, 2, 2, 2, 2, 2, 2, 2, 2, 2, 2, 2, 2, 2, 2, 2, 2, 2, 2, 2, 2, 2, 2, 2, 2, 2, 2, 2, 2, 2, 2, 2, 2, 2, 2, 2, 2, 2, 2, 2, 2, 2, 2, 2, 2, 2, 2, 2, 2, 2, 2, 2, 2, 2, 2, 2, 2, 2, 2, 2, 2, 2, 2, 2, 2, 2, 2, 2, 2, 2, 2, 2, 2, 2, 2, 2, 2, 2, 2, 2, 2, 2, 2, 2, 2, 2, 2, 2, 2, 2, 2, 2, 2, 2, 2, 2, 2, 2, 2, 2, 2, 2, 2, 2, 2, 2, 2, 2, 2, 3 ),
 ( 0.000000000000000000, 0.005357197806354127741, 0.01071439561270825548, 0.01607159341906238409, 0.02142879122541651096, 0.02678598903177064131, 0.03214318683812476818, 0.03750038464447889852, 0.04285758245083302193, 0.04821478025718715227, 0.05357197806354128261, 0.05892917586989540601, 0.06428637367624953636, 0.06964357148260366670, 0.07500076928895779704, 0.08035796709531192739, 0.08571516490166604385, 0.09107236270802018807, 0.09642956051437430454, 0.1017867583207284349, 0.1071439561270825652, 0.1125011539334366956, 0.1178583517397908120, 0.1232155495461449562, 0.1285727473524990727, 0.1339299451588532308, 0.1392871429652073334, 0.1446443407715614637, 0.1500015385779155941, 0.1553587363842697244, 0.1607159341906238548, 0.1660731319969779851, 0.1714303298033320877, 0.1767875276096862458, 0.1821447254160403761, 0.1875019232223944787, 0.1928591210287486091, 0.1982163188351027672, 0.2035735166414568698, 0.2089307144478110001, 0.2142879122541651304, 0.2196451100605192608, 0.2250023078668733911, 0.2303595056732275215, 0.2357167034795816241, 0.2410739012859357822, 0.2464310990922899125, 0.2517882968986440151, 0.2571454947049981454, 0.2625026925113522758, 0.2678598903177064616, 0.2732170881240605365, 0.2785742859304146668, 0.2839314837367687971, 0.2892886815431229275, 0.2946458793494770578, 0.3000030771558311882, 0.3053602749621853185, 0.3107174727685394489, 0.3160746705748935792, 0.3214318683812477095, 0.3267890661876017844, 0.3321462639939559702, 0.3375034618003101006, 0.3428606596066641754, 0.3482178574130183613, 0.3535750552193724916, 0.3589322530257265664, 0.3642894508320807523, 0.3696466486384348271, 0.3750038464447889575, 0.3803610442511431433, 0.3857182420574972181, 0.3910754398638513485, 0.3964326376702055343, 0.4017898354765596092, 0.4071470332829137395, 0.4125042310892679254, 0.4178614288956220002, 0.4232186267019761305, 0.4285758245083302609, 0.4339330223146843912, 0.4392902201210385216, 0.4446474179273926519, 0.4500046157337467823, 0.4553618135401009126, 0.4607190113464550429, 0.4660762091528091733, 0.4714334069591632481, 0.4767906047655174340, 0.4821478025718715643, 0.4875050003782256391, 0.4928621981845798250, 0.4982193959909339553, 0.5035765937972880302, 0.5089337916036421605, 0.5142909894099962909, 0.5196481872163505322, 0.5250053850227045515, 0.5303625828290586819, 0.5357197806354129233, 0.5410769784417669426, 0.5464341762481210729, 0.5517913740544752033, 0.5571485718608293336, 0.5625057696671834639, 0.5678629674735375943, 0.5732201652798917246, 0.5785773630862458550, 0.5839345608925999853, 0.5892917586989541157, 0.5946489565053082460, 0.6000061543116623763, 0.6053633521180165067, 0.6107205499243706370, 0.6160777477307247674, 0.6214349455370788977, 0.6267921433434330281, 0.6321493411497871584, 0.6375065389561411777, 0.6428637367624954191, 0.6482209345688495494, 0.6535781323752035687, 0.6589353301815578101, 0.6642925279879119405, 0.6696497257942659598, 0.6750069236006202011, 0.6803641214069743315, 0.6857213192133283508, 0.6910785170196825922, 0.6964357148260367225, 0.7017929126323907418, 0.7071501104387449832, 0.7125073082450991135, 0.7178645060514531329, 0.7232217038578073742, 0.7285789016641615046, 0.7339360994705155239, 0.7392932972768696542, 0.7446504950832238956, 0.7500076928895779149, 0.7553648906959320453, 0.7607220885022862866, 0.7660792863086403059, 0.7714364841149944363, 0.7767936819213486777, 0.7821508797277026970, 0.7875080775340568273, 0.7928652753404110687, 0.7982224731467650880, 0.8035796709531192183, 0.8089368687594734597, 0.8142940665658274790, 0.8196512643721816094, 0.8250084621785358507, 0.8303656599848898701, 0.8357228577912440004, 0.8410800555975981307, 0.8464372534039522611, 0.8517944512103063914, 0.8571516490166605218, 0.8625088468230146521, 0.8678660446293687825, 0.8732232424357229128, 0.8785804402420770431, 0.8839376380484311735, 0.8892948358547853038, 0.8946520336611394342, 0.9000092314674935645, 0.9053664292738476949, 0.9107236270802018252, 0.9160808248865559555, 0.9214380226929100859, 0.9267952204992641052, 0.9321524183056183466, 0.9375096161119724769, 0.9428668139183264962, 0.9482240117246807376, 0.9535812095310348679, 0.9589384073373888873, 0.9642956051437431286, 0.9696528029500972590, 0.9750100007564512783, 0.9803671985628055197, 0.9857243963691596500, 0.9910815941755136693, 0.9964387919818679107, 1.000000000000000000 ),
 .UNSPECIFIED. ) 
 CURVE ( )  GEOMETRIC_REPRESENTATION_ITEM ( )  RATIONAL_B_SPLINE_CURVE ( ( 1.000000000000000000, 0.9238795325112867385, 1.000000000000000000, 0.9238795325112867385, 1.000000000000000000, 0.9238795325112867385, 1.000000000000000000, 0.9238795325112867385, 1.000000000000000000, 0.9238795325112867385, 1.000000000000000000, 0.9238795325112867385, 1.000000000000000000, 0.9238795325112867385, 1.000000000000000000, 0.9238795325112867385, 1.000000000000000000, 0.9238795325112867385, 1.000000000000000000, 0.9238795325112867385, 1.000000000000000000, 0.9238795325112867385, 1.000000000000000000, 0.9238795325112867385, 1.000000000000000000, 0.9238795325112867385, 1.000000000000000000, 0.9238795325112867385, 1.000000000000000000, 0.9238795325112867385, 1.000000000000000000, 0.9238795325112867385, 1.000000000000000000, 0.9238795325112867385, 1.000000000000000000, 0.9238795325112867385, 1.000000000000000000, 0.9238795325112867385, 1.000000000000000000, 0.9238795325112867385, 1.000000000000000000, 0.9238795325112867385, 1.000000000000000000, 0.9238795325112867385, 1.000000000000000000, 0.9238795325112867385, 1.000000000000000000, 0.9238795325112867385, 1.000000000000000000, 0.9238795325112867385, 1.000000000000000000, 0.9238795325112867385, 1.000000000000000000, 0.9238795325112867385, 1.000000000000000000, 0.9238795325112867385, 1.000000000000000000, 0.9238795325112867385, 1.000000000000000000, 0.9238795325112867385, 1.000000000000000000, 0.9238795325112867385, 1.000000000000000000, 0.9238795325112867385, 1.000000000000000000, 0.9238795325112867385, 1.000000000000000000, 0.9238795325112867385, 1.000000000000000000, 0.9238795325112867385, 1.000000000000000000, 0.9238795325112867385, 1.000000000000000000, 0.9238795325112867385, 1.000000000000000000, 0.9238795325112867385, 1.000000000000000000, 0.9238795325112867385, 1.000000000000000000, 0.9238795325112867385, 1.000000000000000000, 0.9238795325112867385, 1.000000000000000000, 0.9238795325112867385, 1.000000000000000000, 0.9238795325112867385, 1.000000000000000000, 0.9238795325112867385, 1.000000000000000000, 0.9238795325112867385, 1.000000000000000000, 0.9238795325112867385, 1.000000000000000000, 0.9238795325112867385, 1.000000000000000000, 0.9238795325112867385, 1.000000000000000000, 0.9238795325112867385, 1.000000000000000000, 0.9238795325112867385, 1.000000000000000000, 0.9238795325112867385, 1.000000000000000000, 0.9238795325112867385, 1.000000000000000000, 0.9238795325112867385, 1.000000000000000000, 0.9238795325112867385, 1.000000000000000000, 0.9238795325112867385, 1.000000000000000000, 0.9238795325112867385, 1.000000000000000000, 0.9238795325112867385, 1.000000000000000000, 0.9238795325112867385, 1.000000000000000000, 0.9238795325112867385, 1.000000000000000000, 0.9238795325112867385, 1.000000000000000000, 0.9238795325112867385, 1.000000000000000000, 0.9238795325112867385, 1.000000000000000000, 0.9238795325112867385, 1.000000000000000000, 0.9238795325112867385, 1.000000000000000000, 0.9238795325112867385, 1.000000000000000000, 0.9238795325112867385, 1.000000000000000000, 0.9238795325112867385, 1.000000000000000000, 0.9238795325112867385, 1.000000000000000000, 0.9238795325112867385, 1.000000000000000000, 0.9238795325112867385, 1.000000000000000000, 0.9238795325112867385, 1.000000000000000000, 0.9238795325112867385, 1.000000000000000000, 0.9238795325112867385, 1.000000000000000000, 0.9238795325112867385, 1.000000000000000000, 0.9238795325112867385, 1.000000000000000000, 0.9238795325112867385, 1.000000000000000000, 0.9238795325112867385, 1.000000000000000000, 0.9238795325112867385, 1.000000000000000000, 0.9238795325112867385, 1.000000000000000000, 0.9238795325112867385, 1.000000000000000000, 0.9238795325112867385, 1.000000000000000000, 0.9238795325112867385, 1.000000000000000000, 0.9238795325112867385, 1.000000000000000000, 0.9238795325112867385, 1.000000000000000000, 0.9238795325112867385, 1.000000000000000000, 0.9238795325112867385, 1.000000000000000000, 0.9238795325112867385, 1.000000000000000000, 0.9238795325112867385, 1.000000000000000000, 0.9238795325112867385, 1.000000000000000000, 0.9238795325112867385, 1.000000000000000000, 0.9238795325112867385, 1.000000000000000000, 0.9238795325112867385, 1.000000000000000000, 0.9238795325112867385, 1.000000000000000000, 0.9238795325112867385, 1.000000000000000000, 0.9238795325112867385, 1.000000000000000000, 0.9238795325112867385, 1.000000000000000000, 0.9238795325112867385, 1.000000000000000000, 0.9238795325112867385, 1.000000000000000000, 0.9238795325112867385, 1.000000000000000000, 0.9238795325112867385, 1.000000000000000000, 0.9238795325112867385, 1.000000000000000000, 0.9238795325112867385, 1.000000000000000000, 0.9238795325112867385, 1.000000000000000000, 0.9238795325112867385, 1.000000000000000000, 0.9238795325112867385, 1.000000000000000000, 0.9238795325112867385, 1.000000000000000000, 0.9238795325112867385, 1.000000000000000000, 0.9238795325112867385, 1.000000000000000000, 0.9238795325112867385, 1.000000000000000000, 0.9238795325112867385, 1.000000000000000000, 0.9238795325112867385, 1.000000000000000000, 0.9238795325112867385, 1.000000000000000000, 0.9238795325112867385, 1.000000000000000000, 0.9238795325112867385, 1.000000000000000000, 0.9238795325112867385, 1.000000000000000000, 0.9238795325112867385, 1.000000000000000000, 0.9238795325112867385, 1.000000000000000000, 0.9238795325112867385, 1.000000000000000000, 0.9238795325112867385, 1.000000000000000000, 0.9238795325112867385, 1.000000000000000000, 0.9238795325112867385, 1.000000000000000000, 0.9238795325112867385, 1.000000000000000000, 0.9238795325112867385, 1.000000000000000000, 0.9238795325112867385, 1.000000000000000000, 0.9238795325112867385, 1.000000000000000000, 0.9238795325112867385, 1.000000000000000000, 0.9238795325112867385, 1.000000000000000000, 0.9238795325112867385, 1.000000000000000000, 0.9238795325112867385, 1.000000000000000000, 0.9238795325112867385, 1.000000000000000000, 0.9238795325112867385, 1.000000000000000000, 0.9238795325112867385, 1.000000000000000000, 0.9238795325112867385, 1.000000000000000000, 0.9238795325112867385, 1.000000000000000000, 0.9238795325112867385, 1.000000000000000000, 0.9238795325112867385, 1.000000000000000000, 0.9238795325112867385, 1.000000000000000000, 0.9238795325112867385, 1.000000000000000000, 0.9238795325112867385, 1.000000000000000000, 0.9238795325112867385, 1.000000000000000000, 0.9238795325112867385, 1.000000000000000000, 0.9238795325112867385, 1.000000000000000000, 0.9238795325112867385, 1.000000000000000000, 0.9238795325112867385, 1.000000000000000000, 0.9238795325112867385, 1.000000000000000000, 0.9238795325112867385, 1.000000000000000000, 0.9238795325112867385, 1.000000000000000000, 0.9238795325112867385, 1.000000000000000000, 0.9238795325112867385, 1.000000000000000000, 0.9238795325112867385, 1.000000000000000000, 0.9238795325112867385, 1.000000000000000000, 0.9238795325112867385, 1.000000000000000000, 0.9238795325112867385, 1.000000000000000000, 0.9238795325112867385, 1.000000000000000000, 0.9238795325112867385, 1.000000000000000000, 0.9238795325112867385, 1.000000000000000000, 0.9238795325112867385, 1.000000000000000000, 0.9238795325112867385, 1.000000000000000000, 0.9238795325112867385, 1.000000000000000000, 0.9238795325112867385, 1.000000000000000000, 0.9238795325112867385, 1.000000000000000000, 0.9238795325112867385, 1.000000000000000000, 0.9238795325112867385, 1.000000000000000000, 0.9238795325112867385, 1.000000000000000000, 0.9238795325112867385, 1.000000000000000000, 0.9238795325112867385, 1.000000000000000000, 0.9238795325112867385, 1.000000000000000000, 0.9238795325112867385, 1.000000000000000000, 0.9238795325112867385, 1.000000000000000000, 0.9238795325112867385, 1.000000000000000000, 0.9238795325112867385, 1.000000000000000000, 0.9238795325112867385, 1.000000000000000000, 0.9238795325112867385, 1.000000000000000000, 0.9238795325112867385, 1.000000000000000000, 0.9238795325112867385, 1.000000000000000000, 0.9238795325112867385, 1.000000000000000000, 0.9238795325112867385, 1.000000000000000000, 0.9238795325112867385, 1.000000000000000000, 0.9238795325112867385, 1.000000000000000000, 0.9238795325112867385, 1.000000000000000000, 0.9238795325112867385, 1.000000000000000000, 0.9238795325112867385, 1.000000000000000000, 0.9238795325112867385, 1.000000000000000000, 0.9238795325112867385, 1.000000000000000000, 0.9238795325112867385, 1.000000000000000000, 0.9238795325112867385, 1.000000000000000000, 0.9493987661155159907, 0.9660720762559202868 ) ) 
 REPRESENTATION_ITEM ( '' )  );
#66705=CARTESIAN_POINT ( 'NONE',  ( -5.656854249492378806, 99.87500000409679046, 5.656854249492381470 ) ) ;
#66718=CARTESIAN_POINT ( 'NONE',  ( -7.188101187500001821, 91.06250000204838102, -2.977408999572650483 ) ) ;
#66723=ORIENTED_EDGE ( 'NONE', *, *, #47243, .T. ) ;
#66732=CARTESIAN_POINT ( 'NONE',  ( 1.469576158976823947E-15, 99.87499999999998579, 8.000000000000000000 ) ) ;
#66739=CARTESIAN_POINT ( 'NONE',  ( -3.313708498984765161, 9.843749995903220196, 7.999999999999998224 ) ) ;
#66741=CARTESIAN_POINT ( 'NONE',  ( 5.082755093536325930, 13.03124999795161187, -5.082755093536325930 ) ) ;
#66744=CARTESIAN_POINT ( 'NONE',  ( -2.977408999572650927, 112.2500000020483952, -7.188101187500000933 ) ) ;
#66764=CARTESIAN_POINT ( 'NONE',  ( 7.188101187500000044, 97.90625000204838102, -8.802885111219163269E-16 ) ) ;
#66770=CARTESIAN_POINT ( 'NONE',  ( 1.320432766682874540E-15, 105.4062500020483810, 7.188101187500000044 ) ) ;
#66781=CARTESIAN_POINT ( 'NONE',  ( -7.188101187500000044, 3.093749997951610542, -8.802885111219163269E-16 ) ) ;
#66798=CARTESIAN_POINT ( 'NONE',  ( 4.401442555609581635E-16, 9.843749997951610098, -7.188101187500000044 ) ) ;
#66800=CARTESIAN_POINT ( 'NONE',  ( 8.000000000000000000, 116.9375000040967763, -9.797174393178825657E-16 ) ) ;
#66804=DIRECTION ( 'NONE',  ( -0.000000000000000000, 1.000000000000000000, -0.000000000000000000 ) ) ;
#66807=( BOUNDED_CURVE ( )  B_SPLINE_CURVE ( 2, ( #3997, #26608, #43972, #49632, #50369, #33793, #72262, #72647, #56052 ),
 .UNSPECIFIED., .F., .F. ) 
 B_SPLINE_CURVE_WITH_KNOTS ( ( 3, 2, 2, 2, 3 ),
 ( 0.5694444444444444198, 0.5763888888888888395, 0.5833333333333333703, 0.5902777777777777901, 0.5972222222222222099 ),
 .UNSPECIFIED. ) 
 CURVE ( )  GEOMETRIC_REPRESENTATION_ITEM ( )  RATIONAL_B_SPLINE_CURVE ( ( 1.000000000000000000, 0.9238795325112867385, 1.000000000000000000, 0.9238795325112867385, 1.000000000000000000, 0.9238795325112867385, 1.000000000000000000, 0.9238795325112867385, 1.000000000000000000 ) ) 
 REPRESENTATION_ITEM ( '' )  );
#66828=CARTESIAN_POINT ( 'NONE',  ( -5.656854249492380582, 112.8125000000000000, -5.656854249492380582 ) ) ;
#66834=CARTESIAN_POINT ( 'NONE',  ( -8.000000000000001776, 21.65624999590322730, 3.313708498984759387 ) ) ;
#66840=CARTESIAN_POINT ( 'NONE',  ( -8.000000000000000000, 114.5937500040967905, -3.313708498984761164 ) ) ;
#66848=DIRECTION ( 'NONE',  ( -0.000000000000000000, 1.000000000000000000, -0.000000000000000000 ) ) ;
#66856=CARTESIAN_POINT ( 'NONE',  ( -5.082755093536324154, 115.3437500020483810, 5.082755093536326818 ) ) ;
#66860=CARTESIAN_POINT ( 'NONE',  ( -7.188101187500000044, 92.65625000204838102, 0.000000000000000000 ) ) ;
#66864=ORIENTED_EDGE ( 'NONE', *, *, #29784, .T. ) ;
#66871=CARTESIAN_POINT ( 'NONE',  ( -1.469576158976823947E-15, 9.937499995903220196, 8.000000000000000000 ) ) ;
#66889=CARTESIAN_POINT ( 'NONE',  ( 2.977408999572651815, 22.68749999795161543, 7.188101187500000933 ) ) ;
#66892=CARTESIAN_POINT ( 'NONE',  ( -7.188101187500000044, 19.59374999795161543, -8.802885111219163269E-16 ) ) ;
#66895=DIRECTION ( 'NONE',  ( 0.000000000000000000, 0.000000000000000000, 1.000000000000000000 ) ) ;
#66904=DIRECTION ( 'NONE',  ( -0.000000000000000000, 1.000000000000000000, -0.000000000000000000 ) ) ;
#66907=CARTESIAN_POINT ( 'NONE',  ( 7.188101187500000044, 27.46874999795161543, 0.000000000000000000 ) ) ;
#66908=EDGE_LOOP ( 'NONE', ( #4751, #64079, #10398, #40637, #29579, #38114, #17852, #17276, #30236, #41670, #20763, #38996, #62195, #11766, #22732, #18581, #18548, #64975, #47313, #59721, #51494, #51300, #53693, #5391, #4637, #61929, #18913, #51044, #58227, #14001, #60373, #3998, #51883, #28189, #27993, #42722, #63449, #52935, #59868, #5771, #6354, #59767, #31993, #27267, #22707, #55649, #64682, #66864, #49956, #9463, #20984, #34443 ) ) ;
#66914=CARTESIAN_POINT ( 'NONE',  ( -2.977408999572650927, 95.75000000204836681, -7.188101187500001821 ) ) ;
#66931=CARTESIAN_POINT ( 'NONE',  ( 8.000000000000000000, 27.00000000000000355, 0.000000000000000000 ) ) ;
#66935=ORIENTED_EDGE ( 'NONE', *, *, #71887, .F. ) ;
#66943=CARTESIAN_POINT ( 'NONE',  ( -7.188101187500001821, 112.0625000020483810, -2.977408999572650483 ) ) ;
#66956=EDGE_CURVE ( 'NONE', #29121, #55690, #10715, .T. ) ;
#66964=VERTEX_POINT ( 'NONE', #46603 ) ;
#66965=CARTESIAN_POINT ( 'NONE',  ( -4.898587196589412829E-16, 90.12500000000000000, -8.000000000000000000 ) ) ;
#66969=CARTESIAN_POINT ( 'NONE',  ( -1.320432766682874540E-15, 18.46874999795161187, 7.188101187500000044 ) ) ;
#66972=ORIENTED_EDGE ( 'NONE', *, *, #37107, .F. ) ;
#66976=EDGE_CURVE ( 'NONE', #45475, #31074, #26117, .T. ) ;
#66978=CARTESIAN_POINT ( 'NONE',  ( -2.977408999572650039, 0.9374999979516102089, -7.188101187500001821 ) ) ;
#66982=CARTESIAN_POINT ( 'NONE',  ( 4.401442555609581635E-16, 1.218749997951610098, -7.188101187500000044 ) ) ;
#66991=VERTEX_POINT ( 'NONE', #7730 ) ;
#66993=ADVANCED_FACE ( 'NONE', ( #30371 ), #72202, .T. ) ;
#66999=CARTESIAN_POINT ( 'NONE',  ( 7.188101187500000933, 12.56249999795161365, -2.977408999572650483 ) ) ;
#67003=CARTESIAN_POINT ( 'NONE',  ( -5.082755093536324154, 109.7187500020483810, 5.082755093536326818 ) ) ;
#67019=CARTESIAN_POINT ( 'NONE',  ( 8.000000000000001776, 92.65625000000001421, 3.313708498984759387 ) ) ;
#67041=ORIENTED_EDGE ( 'NONE', *, *, #55753, .F. ) ;
#67042=CARTESIAN_POINT ( 'NONE',  ( 8.000000000000001776, 92.65625000000001421, 3.313708498984759387 ) ) ;
#67043=CARTESIAN_POINT ( 'NONE',  ( 5.082755093536325930, 17.15624999795161543, -5.082755093536325930 ) ) ;
#67070=CARTESIAN_POINT ( 'NONE',  ( 5.656854249492380582, 14.99999999590322020, -5.656854249492380582 ) ) ;
#67076=VERTEX_POINT ( 'NONE', #25055 ) ;
#67081=CARTESIAN_POINT ( 'NONE',  ( -5.656854249492381470, 14.43750000000000178, 5.656854249492379694 ) ) ;
#67085=CARTESIAN_POINT ( 'NONE',  ( -3.313708498984762496, 93.96875000409677625, 7.999999999999998224 ) ) ;
#67094=ORIENTED_EDGE ( 'NONE', *, *, #45885, .F. ) ;
#67096=CARTESIAN_POINT ( 'NONE',  ( 2.977408999572650039, 90.68750000204838102, -7.188101187500001821 ) ) ;
#67100=AXIS2_PLACEMENT_3D ( 'NONE', #4759, #45846, #16418 ) ;
#67115=CARTESIAN_POINT ( 'NONE',  ( -4.898587196589412829E-16, 90.31250000409676204, -8.000000000000000000 ) ) ;
#67118=CARTESIAN_POINT ( 'NONE',  ( 5.656854249492380582, 8.999999995903221972, -5.656854249492380582 ) ) ;
#67121=CARTESIAN_POINT ( 'NONE',  ( 5.082755093536324154, 12.65624999795161187, 5.082755093536326818 ) ) ;
#67123=CARTESIAN_POINT ( 'NONE',  ( 0.000000000000000000, 125.0000000000000000, 0.000000000000000000 ) ) ;
#67124=CARTESIAN_POINT ( 'NONE',  ( -2.977408999572652260, 103.8125000020483952, 7.188101187500000044 ) ) ;
#67131=CARTESIAN_POINT ( 'NONE',  ( 3.313708498984762496, 20.71875000000000355, 7.999999999999998224 ) ) ;
#67138=CARTESIAN_POINT ( 'NONE',  ( -5.656854249492381470, 23.24999999590322020, 5.656854249492379694 ) ) ;
#67144=CARTESIAN_POINT ( 'NONE',  ( -7.188101187499999156, 97.25000000204839523, 2.977408999572654924 ) ) ;
#67152=CARTESIAN_POINT ( 'NONE',  ( 2.977408999572654480, 105.5000000020483810, 7.188101187499999156 ) ) ;
#67153=CARTESIAN_POINT ( 'NONE',  ( -3.979266480698733677, 0.4999999999999095723, -6.940132439340585435 ) ) ;
#67164=CYLINDRICAL_SURFACE ( 'NONE', #53814, 8.000000000000000000 ) ;
#67178=CARTESIAN_POINT ( 'NONE',  ( -5.082755093536325042, 7.031249997951611874, -5.082755093536325930 ) ) ;
#67179=CARTESIAN_POINT ( 'NONE',  ( -7.999999999999998224, 110.2812500040967763, 3.313708498984766493 ) ) ;
#67196=ORIENTED_EDGE ( 'NONE', *, *, #31265, .F. ) ;
#67204=CARTESIAN_POINT ( 'NONE',  ( 8.000000000000000000, 107.7500000000000000, -9.797174393178825657E-16 ) ) ;
#67211=CARTESIAN_POINT ( 'NONE',  ( 8.000000000000000000, 23.90624999590322730, -3.313708498984761608 ) ) ;
#67213=CARTESIAN_POINT ( 'NONE',  ( 2.977408999572654480, 120.5000000020483810, 7.188101187499999156 ) ) ;
#67217=CARTESIAN_POINT ( 'NONE',  ( -5.656854249492378806, 114.8750000040967905, 5.656854249492381470 ) ) ;
#67227=CARTESIAN_POINT ( 'NONE',  ( 3.313708498984760276, 102.2187500040967905, -8.000000000000000000 ) ) ;
#67235=CARTESIAN_POINT ( 'NONE',  ( -5.082755093536324154, 119.8437500020483810, 5.082755093536326818 ) ) ;
#67238=EDGE_CURVE ( 'NONE', #56169, #9713, #72590, .T. ) ;
#67241=CARTESIAN_POINT ( 'NONE',  ( -2.977408999572651815, 121.8125000020483810, 7.188101187500000933 ) ) ;
#67243=DIRECTION ( 'NONE',  ( 0.000000000000000000, 0.000000000000000000, 1.000000000000000000 ) ) ;
#67246=CARTESIAN_POINT ( 'NONE',  ( 7.683012701892216079, 0.1830127018922207416, 0.000000000000000000 ) ) ;
#67248=EDGE_CURVE ( 'NONE', #26128, #29891, #32995, .T. ) ;
#67257=CARTESIAN_POINT ( 'NONE',  ( 8.000000000000000000, 22.40624999590322375, -3.313708498984761164 ) ) ;
#67263=ORIENTED_EDGE ( 'NONE', *, *, #60484, .F. ) ;
#67267=CARTESIAN_POINT ( 'NONE',  ( 5.082755093536324154, 22.78124999795161187, 5.082755093536326818 ) ) ;
#67271=CARTESIAN_POINT ( 'NONE',  ( 7.188101187499999156, 15.74999999795161543, 2.977408999572654924 ) ) ;
#67275=LINE ( 'NONE', #9928, #11314 ) ;
#67291=CARTESIAN_POINT ( 'NONE',  ( -2.977408999572650927, 92.75000000204839523, -7.188101187500001821 ) ) ;
#67313=CARTESIAN_POINT ( 'NONE',  ( 5.656854249492381470, 109.2500000040967763, 5.656854249492379694 ) ) ;
#67318=DIRECTION ( 'NONE',  ( -0.000000000000000000, 1.000000000000000000, -0.000000000000000000 ) ) ;
#67323=CARTESIAN_POINT ( 'NONE',  ( 5.082755093536326818, 105.2187500020483952, 5.082755093536325042 ) ) ;
#67333=CARTESIAN_POINT ( 'NONE',  ( -7.999999999999998224, 99.59375000000000000, 3.313708498984766049 ) ) ;
#67338=CARTESIAN_POINT ( 'NONE',  ( 7.594050593750000466, 27.23437499897580949, 0.000000000000000000 ) ) ;
#67342=CARTESIAN_POINT ( 'NONE',  ( 0.000000000000000000, 125.0000000000000000, 0.000000000000000000 ) ) ;
#67347=CARTESIAN_POINT ( 'NONE',  ( -7.188101187500002709, 18.18749999795161187, 2.977408999572649151 ) ) ;
#67355=CARTESIAN_POINT ( 'NONE',  ( -5.082755093536326818, 4.406249997951610986, 5.082755093536325042 ) ) ;
#67359=EDGE_LOOP ( 'NONE', ( #52233, #17883, #54169, #21494 ) ) ;
#67363=AXIS2_PLACEMENT_3D ( 'NONE', #61070, #50124, #33543 ) ;
#67365=CARTESIAN_POINT ( 'NONE',  ( 5.656854249492378806, 26.81250000000000355, 5.656854249492381470 ) ) ;
#67375=CARTESIAN_POINT ( 'NONE',  ( -5.082755093536326818, 11.90624999795161010, 5.082755093536325042 ) ) ;
#67379=CARTESIAN_POINT ( 'NONE',  ( -5.082755093536325930, 110.8437500020483810, -5.082755093536325930 ) ) ;
#67393=CARTESIAN_POINT ( 'NONE',  ( 8.000000000000001776, 91.15624999999998579, 3.313708498984759387 ) ) ;
#67418=CARTESIAN_POINT ( 'NONE',  ( -5.082755093536325042, 22.03124999795161543, -5.082755093536325930 ) ) ;
#67432=EDGE_CURVE ( 'NONE', #4200, #25259, #31348, .T. ) ;
#67437=CYLINDRICAL_SURFACE ( 'NONE', #56969, 8.000000000000000000 ) ;
#67453=( BOUNDED_CURVE ( )  B_SPLINE_CURVE ( 2, ( #37618, #65898, #42518, #55349, #48912, #26653, #71926, #59513, #13464 ),
 .UNSPECIFIED., .F., .F. ) 
 B_SPLINE_CURVE_WITH_KNOTS ( ( 3, 2, 2, 2, 3 ),
 ( 0.6770833333333334814, 0.6822916666666667407, 0.6875000000000001110, 0.6927083333333334814, 0.6979166666666667407 ),
 .UNSPECIFIED. ) 
 CURVE ( )  GEOMETRIC_REPRESENTATION_ITEM ( )  RATIONAL_B_SPLINE_CURVE ( ( 0.9999999999999983347, 0.9238795325112884038, 1.000000000000000000, 0.9238795325112867385, 1.000000000000000000, 0.9238795325112867385, 1.000000000000000000, 0.9238795325112850731, 1.000000000000001554 ) ) 
 REPRESENTATION_ITEM ( '' )  );
#67455=CARTESIAN_POINT ( 'NONE',  ( -5.656854249492381470, 12.93750000000000355, 5.656854249492379694 ) ) ;
#67457=CARTESIAN_POINT ( 'NONE',  ( 8.000000000000000000, 91.43750000409679046, -9.797174393178825657E-16 ) ) ;
#67463=( BOUNDED_CURVE ( )  B_SPLINE_CURVE ( 2, ( #32231, #43527, #66542, #14851, #37891, #60139, #42411, #2808, #60889 ),
 .UNSPECIFIED., .F., .F. ) 
 B_SPLINE_CURVE_WITH_KNOTS ( ( 3, 2, 2, 2, 3 ),
 ( 0.4270833333333332593, 0.4322916666666666297, 0.4374999999999998890, 0.4427083333333332038, 0.4479166666666665741 ),
 .UNSPECIFIED. ) 
 CURVE ( )  GEOMETRIC_REPRESENTATION_ITEM ( )  RATIONAL_B_SPLINE_CURVE ( ( 1.000000000000000888, 0.9238795325112859613, 1.000000000000000000, 0.9238795325112867385, 1.000000000000000000, 0.9238795325112867385, 1.000000000000000000, 0.9238795325112884038, 0.9999999999999983347 ) ) 
 REPRESENTATION_ITEM ( '' )  );
#67470=CARTESIAN_POINT ( 'NONE',  ( 7.188101187500001821, 93.50000000204838102, -2.977408999572651371 ) ) ;
#67487=ADVANCED_FACE ( 'NONE', ( #32106 ), #13973, .T. ) ;
#67489=CARTESIAN_POINT ( 'NONE',  ( 8.000000000000000000, 101.7500000000000000, -9.797174393178825657E-16 ) ) ;
#67492=CARTESIAN_POINT ( 'NONE',  ( -8.000000000000000000, 6.468749995903221084, -3.313708498984762496 ) ) ;
#67495=CARTESIAN_POINT ( 'NONE',  ( -2.977408999572650039, 16.31249999795161543, -7.188101187500001821 ) ) ;
#67497=CARTESIAN_POINT ( 'NONE',  ( 2.977408999572650039, 106.0625000020483668, -7.188101187500000933 ) ) ;
#67514=CARTESIAN_POINT ( 'NONE',  ( -5.082755093536324154, 101.8437500020483810, 5.082755093536326818 ) ) ;
#67519=ADVANCED_FACE ( 'NONE', ( #55124 ), #71328, .T. ) ;
#67521=CARTESIAN_POINT ( 'NONE',  ( 7.188101187500002709, 102.6875000020483810, 2.977408999572649151 ) ) ;
#67539=ORIENTED_EDGE ( 'NONE', *, *, #70228, .F. ) ;
#67547=CARTESIAN_POINT ( 'NONE',  ( 2.977408999572650927, 9.749999997951611874, -7.188101187500001821 ) ) ;
#67548=MANIFOLD_SOLID_BREP ( 'Chamfer2', #930 ) ;
#67549=CARTESIAN_POINT ( 'NONE',  ( 5.656854249492379694, 108.1250000040967763, -5.656854249492380582 ) ) ;
#67558=CARTESIAN_POINT ( 'NONE',  ( 5.656854249492381470, 116.5625000000000000, 5.656854249492379694 ) ) ;
#67576=CARTESIAN_POINT ( 'NONE',  ( 8.000000000000000000, 103.2500000000000000, -9.797174393178825657E-16 ) ) ;
#67578=CIRCLE ( 'NONE', #16960, 8.000000000000000000 ) ;
#67581=CARTESIAN_POINT ( 'NONE',  ( 3.313708498984802020, 19.78125000000000355, -7.999999999999958256 ) ) ;
#67582=( BOUNDED_CURVE ( )  B_SPLINE_CURVE ( 2, ( #29415, #35088, #18459, #58464, #69402, #12419, #69771, #2214, #12781 ),
 .UNSPECIFIED., .F., .F. ) 
 B_SPLINE_CURVE_WITH_KNOTS ( ( 3, 2, 2, 2, 3 ),
 ( 0.06944444444444444753, 0.07638888888888889506, 0.08333333333333331483, 0.09027777777777776236, 0.09722222222222220989 ),
 .UNSPECIFIED. ) 
 CURVE ( )  GEOMETRIC_REPRESENTATION_ITEM ( )  RATIONAL_B_SPLINE_CURVE ( ( 1.000000000000000000, 0.9238795325112867385, 1.000000000000000000, 0.9238795325112867385, 1.000000000000000000, 0.9238795325112867385, 1.000000000000000000, 0.9238795325112868495, 0.9999999999999998890 ) ) 
 REPRESENTATION_ITEM ( '' )  );
#67585=CARTESIAN_POINT ( 'NONE',  ( -5.082755093536325042, 1.406249997951610320, -5.082755093536325930 ) ) ;
#67587=CARTESIAN_POINT ( 'NONE',  ( 5.082755093536326818, 120.5937500020483952, 5.082755093536325042 ) ) ;
#67599=CARTESIAN_POINT ( 'NONE',  ( -4.898587196589412829E-16, 102.3125000040967763, -8.000000000000000000 ) ) ;
#67607=CARTESIAN_POINT ( 'NONE',  ( 2.977408999572654480, 115.6250000020483810, 7.188101187499999156 ) ) ;
#67613=CARTESIAN_POINT ( 'NONE',  ( -7.188101187500001821, 119.9375000020483952, -2.977408999572650483 ) ) ;
#67615=CYLINDRICAL_SURFACE ( 'NONE', #7259, 8.000000000000000000 ) ;
#67623=VECTOR ( 'NONE', #33591, 1000.000000000000000 ) ;
#67639=CARTESIAN_POINT ( 'NONE',  ( -5.656854249492381470, 2.437500000000000444, 5.656854249492379694 ) ) ;
#67641=CARTESIAN_POINT ( 'NONE',  ( 2.977408999572651815, 15.56249999795161365, 7.188101187500000933 ) ) ;
#67654=CARTESIAN_POINT ( 'NONE',  ( 1.469576158976823947E-15, 94.06250000409677625, 8.000000000000000000 ) ) ;
#67656=EDGE_LOOP ( 'NONE', ( #68542, #66723, #23319, #1227 ) ) ;
#67659=VERTEX_POINT ( 'NONE', #22161 ) ;
#67666=CARTESIAN_POINT ( 'NONE',  ( 5.656854249492381470, 124.0625000000000000, 5.656854249492379694 ) ) ;
#67670=CARTESIAN_POINT ( 'NONE',  ( 5.656854249492381470, 94.06250000000000000, 5.656854249492379694 ) ) ;
#67697=CARTESIAN_POINT ( 'NONE',  ( -7.188101187500000044, 104.6562500020483810, 0.000000000000000000 ) ) ;
#67715=CARTESIAN_POINT ( 'NONE',  ( 3.313708498984800688, 117.2187500040967620, -7.999999999999958256 ) ) ;
#67718=CARTESIAN_POINT ( 'NONE',  ( 3.313708498984765161, 106.1562500040967905, 7.999999999999998224 ) ) ;
#67722=CARTESIAN_POINT ( 'NONE',  ( -2.977408999572650039, 16.31249999795161543, -7.188101187500000933 ) ) ;
#67731=CARTESIAN_POINT ( 'NONE',  ( -5.082755093536326818, 10.40624999795161187, 5.082755093536325042 ) ) ;
#67749=CARTESIAN_POINT ( 'NONE',  ( -8.000000000000000000, 21.75000000000000355, -9.797174393178825657E-16 ) ) ;
#67751=EDGE_CURVE ( 'NONE', #54105, #45576, #41563, .T. ) ;
#67752=CARTESIAN_POINT ( 'NONE',  ( -7.188101187500000933, 13.12499999795161187, -2.977408999572651371 ) ) ;
#67756=CARTESIAN_POINT ( 'NONE',  ( 5.082755093536325042, 104.4687500020483952, -5.082755093536325930 ) ) ;
#67770=CARTESIAN_POINT ( 'NONE',  ( -8.000000000000000000, 92.00000000000000000, 0.000000000000000000 ) ) ;
#67772=CARTESIAN_POINT ( 'NONE',  ( 1.469576158976823947E-15, 98.37499999999998579, 8.000000000000000000 ) ) ;
#67776=CARTESIAN_POINT ( 'NONE',  ( 8.000000000000000000, 118.5312500040967905, -3.313708498984762496 ) ) ;
#67784=CARTESIAN_POINT ( 'NONE',  ( -7.188101187500001821, 119.5625000020483810, -2.977408999572650483 ) ) ;
#67792=DIRECTION ( 'NONE',  ( 0.000000000000000000, 0.000000000000000000, 1.000000000000000000 ) ) ;
#67793=CARTESIAN_POINT ( 'NONE',  ( -1.320432766682874540E-15, 22.59374999795161187, 7.188101187500000044 ) ) ;
#67809=DIRECTION ( 'NONE',  ( -0.000000000000000000, 1.000000000000000000, -0.000000000000000000 ) ) ;
#67816=CARTESIAN_POINT ( 'NONE',  ( -8.000000000000001776, 2.156249995903220196, 3.313708498984759387 ) ) ;
#67825=CARTESIAN_POINT ( 'NONE',  ( 3.313708498984762052, 12.28125000000000178, -8.000000000000000000 ) ) ;
#67829=CARTESIAN_POINT ( 'NONE',  ( -8.000000000000000000, 89.09375000409676204, -3.313708498984761608 ) ) ;
#67837=CARTESIAN_POINT ( 'NONE',  ( -7.188101187500000044, 92.65625000204838102, 0.000000000000000000 ) ) ;
#67855=CARTESIAN_POINT ( 'NONE',  ( 0.000000000000000000, 75.00000000000000000, 8.000000000000000000 ) ) ;
#67858=CARTESIAN_POINT ( 'NONE',  ( -8.000000000000000000, 9.562499995903223748, -9.797174393178825657E-16 ) ) ;
#67861=CARTESIAN_POINT ( 'NONE',  ( -1.320432766682874540E-15, 19.96874999795161543, 7.188101187500000044 ) ) ;
#67864=CARTESIAN_POINT ( 'NONE',  ( 5.082755093536325042, 105.9687500020483952, -5.082755093536325930 ) ) ;
#67883=CARTESIAN_POINT ( 'NONE',  ( -4.401442555609581635E-16, 92.28125000204836681, -7.188101187500000044 ) ) ;
#67889=CARTESIAN_POINT ( 'NONE',  ( 7.188101187500002709, 105.6875000020483952, 2.977408999572649151 ) ) ;
#67890=CARTESIAN_POINT ( 'NONE',  ( 4.850062511589654031E-16, 0.4207531754730554074, -7.920753175473053354 ) ) ;
#67917=CARTESIAN_POINT ( 'NONE',  ( -7.188101187500001821, 11.62499999795161187, -2.977408999572651371 ) ) ;
#67918=CARTESIAN_POINT ( 'NONE',  ( -5.656854249492378806, 107.3750000040967763, 5.656854249492381470 ) ) ;
#67926=VECTOR ( 'NONE', #4878, 1000.000000000000000 ) ;
#67928=CARTESIAN_POINT ( 'NONE',  ( 1.469576158976823947E-15, 116.3750000000000000, 8.000000000000000000 ) ) ;
#67929=CARTESIAN_POINT ( 'NONE',  ( -7.188101187500000044, 109.1562500020483810, 0.000000000000000000 ) ) ;
#67930=EDGE_CURVE ( 'NONE', #31825, #43001, #41118, .T. ) ;
#67932=CARTESIAN_POINT ( 'NONE',  ( -7.188101187500000044, 124.1562500020483810, 0.000000000000000000 ) ) ;
#67942=CARTESIAN_POINT ( 'NONE',  ( 1.469576158976823947E-15, 111.8750000000000000, 8.000000000000000000 ) ) ;
#67945=CARTESIAN_POINT ( 'NONE',  ( -8.000000000000000000, 107.0000000000000000, 0.000000000000000000 ) ) ;
#67948=CARTESIAN_POINT ( 'NONE',  ( 1.469576158976823947E-15, 98.37499999999998579, 8.000000000000000000 ) ) ;
#67951=CARTESIAN_POINT ( 'NONE',  ( -5.082755093536326818, 1.781249997951610098, 5.082755093536325042 ) ) ;
#67972=CARTESIAN_POINT ( 'NONE',  ( 3.313708498984761608, 7.593749995903221084, -8.000000000000000000 ) ) ;
#67973=CARTESIAN_POINT ( 'NONE',  ( -5.082755093536325930, 117.9687500020483810, -5.082755093536325930 ) ) ;
#67978=CARTESIAN_POINT ( 'NONE',  ( 7.188101187500001821, 117.8750000020483810, -2.977408999572651371 ) ) ;
#67979=CARTESIAN_POINT ( 'NONE',  ( -3.313708498984727413, 120.4062500040967763, -8.000000000000033751 ) ) ;
#67997=VERTEX_POINT ( 'NONE', #10032 ) ;
#68001=CARTESIAN_POINT ( 'NONE',  ( 5.082755093536325930, 24.65624999795161543, -5.082755093536325930 ) ) ;
#68004=CARTESIAN_POINT ( 'NONE',  ( -1.320432766682874540E-15, 16.96874999795161543, 7.188101187500000044 ) ) ;
#68005=CARTESIAN_POINT ( 'NONE',  ( -8.000000000000000000, 124.5000000000000284, -1.469576158976823947E-15 ) ) ;
#68008=EDGE_CURVE ( 'NONE', #29891, #493, #72393, .T. ) ;
#68033=CARTESIAN_POINT ( 'NONE',  ( 1.469576158976823947E-15, 122.3750000000000000, 8.000000000000000000 ) ) ;
#68043=CARTESIAN_POINT ( 'NONE',  ( 7.999999999999998224, 13.21874999590322375, 3.313708498984766049 ) ) ;
#68065=CARTESIAN_POINT ( 'NONE',  ( -7.188101187500000044, 103.1562500020483810, 0.000000000000000000 ) ) ;
#68081=CARTESIAN_POINT ( 'NONE',  ( 7.999999999999998224, 4.406250000000000000, 3.313708498984766049 ) ) ;
#68083=CARTESIAN_POINT ( 'NONE',  ( -8.000000000000000000, 18.56249999590322020, -9.797174393178825657E-16 ) ) ;
#68092=CARTESIAN_POINT ( 'NONE',  ( 5.082755093536324154, 24.65624999795161543, 5.082755093536326818 ) ) ;
#68100=CARTESIAN_POINT ( 'NONE',  ( 4.401442555609581635E-16, 11.34374999795161010, -7.188101187500000044 ) ) ;
#68103=CARTESIAN_POINT ( 'NONE',  ( -2.977408999572650039, 2.812499997951610542, -7.188101187500001821 ) ) ;
#68117=CARTESIAN_POINT ( 'NONE',  ( -1.320432766682874540E-15, 12.09374999795161187, 7.188101187500000044 ) ) ;
#68121=CARTESIAN_POINT ( 'NONE',  ( 5.082755093536326818, 108.5937500020483810, 5.082755093536325042 ) ) ;
#68136=CARTESIAN_POINT ( 'NONE',  ( 1.469576158976823947E-15, 90.87500000000000000, 8.000000000000000000 ) ) ;
#68149=CARTESIAN_POINT ( 'NONE',  ( -5.082755093536325930, 119.4687500020483810, -5.082755093536325930 ) ) ;
#68153=CARTESIAN_POINT ( 'NONE',  ( -3.313708498984760276, 12.46875000000000178, -8.000000000000000000 ) ) ;
#68157=CARTESIAN_POINT ( 'NONE',  ( -7.188101187500000044, 25.21874999795161543, -8.802885111219163269E-16 ) ) ;
#68176=CARTESIAN_POINT ( 'NONE',  ( 1.469576158976823947E-15, 114.8750000000000000, 8.000000000000000000 ) ) ;
#68181=CARTESIAN_POINT ( 'NONE',  ( -1.320432766682874540E-15, 4.968749997951610986, 7.188101187500000044 ) ) ;
#68188=CARTESIAN_POINT ( 'NONE',  ( -4.898587196589412829E-16, 120.1250000000000000, -8.000000000000000000 ) ) ;
#68196=CARTESIAN_POINT ( 'NONE',  ( -1.469576158976823947E-15, 19.12500000000000355, 8.000000000000000000 ) ) ;
#68198=CARTESIAN_POINT ( 'NONE',  ( 3.313708498984760720, 94.71875000409677625, -8.000000000000000000 ) ) ;
#68199=( NAMED_UNIT ( * ) PLANE_ANGLE_UNIT ( ) SI_UNIT ( $, .RADIAN. ) );
#68222=CARTESIAN_POINT ( 'NONE',  ( -5.656854249492378806, 105.8750000040967763, 5.656854249492381470 ) ) ;
#68227=CARTESIAN_POINT ( 'NONE',  ( -7.999999999999998224, 114.5937500000000000, 3.313708498984766049 ) ) ;
#68230=( BOUNDED_CURVE ( )  B_SPLINE_CURVE ( 2, ( #18424, #35054, #51263, #57315, #63695, #58067, #28626, #46615, #68993 ),
 .UNSPECIFIED., .F., .F. ) 
 B_SPLINE_CURVE_WITH_KNOTS ( ( 3, 2, 2, 2, 3 ),
 ( 0.1145833333333333981, 0.1197916666666667407, 0.1250000000000000833, 0.1302083333333334259, 0.1354166666666667407 ),
 .UNSPECIFIED. ) 
 CURVE ( )  GEOMETRIC_REPRESENTATION_ITEM ( )  RATIONAL_B_SPLINE_CURVE ( ( 0.9999999999999990008, 0.9238795325112877377, 1.000000000000000000, 0.9238795325112867385, 1.000000000000000000, 0.9238795325112867385, 1.000000000000000000, 0.9238795325112855172, 1.000000000000001110 ) ) 
 REPRESENTATION_ITEM ( '' )  );
#68232=CARTESIAN_POINT ( 'NONE',  ( -3.313708498984765161, 11.34374999590322197, 7.999999999999998224 ) ) ;
#68237=CARTESIAN_POINT ( 'NONE',  ( 4.401442555609581635E-16, 16.21874999795161543, -7.188101187500000044 ) ) ;
#68239=CARTESIAN_POINT ( 'NONE',  ( -8.000000000000000000, 105.4062500000000000, -3.313708498984761164 ) ) ;
#68240=CARTESIAN_POINT ( 'NONE',  ( -2.977408999572650927, 104.7500000020483810, -7.188101187500000933 ) ) ;
#68248=ORIENTED_EDGE ( 'NONE', *, *, #32514, .T. ) ;
#68256=CARTESIAN_POINT ( 'NONE',  ( -7.188101187500000933, 95.56250000204838102, -2.977408999572650483 ) ) ;
#68262=CARTESIAN_POINT ( 'NONE',  ( 5.082755093536325042, 99.96875000204838102, -5.082755093536325930 ) ) ;
#68277=CARTESIAN_POINT ( 'NONE',  ( 4.898587196589412829E-16, 21.18749999590322375, -8.000000000000000000 ) ) ;
#68287=CARTESIAN_POINT ( 'NONE',  ( -7.188101187500001821, 16.12499999795161187, -2.977408999572651371 ) ) ;
#68288=CARTESIAN_POINT ( 'NONE',  ( 5.656854249492379694, 112.6250000040967763, -5.656854249492380582 ) ) ;
#68296=CARTESIAN_POINT ( 'NONE',  ( -7.188101187500000044, 104.6562500020483810, 0.000000000000000000 ) ) ;
#68298=CARTESIAN_POINT ( 'NONE',  ( -3.313708498984772710, 123.7812500000000000, 7.999999999999988454 ) ) ;
#68301=EDGE_CURVE ( 'NONE', #17357, #7158, #71060, .T. ) ;
#68306=CARTESIAN_POINT ( 'NONE',  ( -4.898587196589412829E-16, 91.81250000409677625, -8.000000000000000000 ) ) ;
#68315=CARTESIAN_POINT ( 'NONE',  ( 8.000000000000001776, 107.6562500000000000, 3.313708498984759387 ) ) ;
#68320=CARTESIAN_POINT ( 'NONE',  ( 5.082755093536324154, 2.156249997951610542, 5.082755093536326818 ) ) ;
#68322=CARTESIAN_POINT ( 'NONE',  ( -7.188101187500000044, 124.5312500020483810, 0.000000000000000000 ) ) ;
#68345=CARTESIAN_POINT ( 'NONE',  ( -2.977408999572652260, 109.4375000020483810, 7.188101187500000044 ) ) ;
#68351=CARTESIAN_POINT ( 'NONE',  ( 7.188101187500000044, 122.2812500020483810, -8.802885111219163269E-16 ) ) ;
#68352=CARTESIAN_POINT ( 'NONE',  ( -3.313708498984782924, 120.9687500040968189, 7.999999999999979572 ) ) ;
#68357=( BOUNDED_CURVE ( )  B_SPLINE_CURVE ( 2, ( #68789, #62745, #34112, #40121, #57111, #51436, #59702, #71005, #12558 ),
 .UNSPECIFIED., .F., .F. ) 
 B_SPLINE_CURVE_WITH_KNOTS ( ( 3, 2, 2, 2, 3 ),
 ( 0.3194444444444443643, 0.3263888888888888395, 0.3333333333333332593, 0.3402777777777777901, 0.3472222222222222099 ),
 .UNSPECIFIED. ) 
 CURVE ( )  GEOMETRIC_REPRESENTATION_ITEM ( )  RATIONAL_B_SPLINE_CURVE ( ( 1.000000000000000666, 0.9238795325112861834, 1.000000000000000000, 0.9238795325112867385, 1.000000000000000000, 0.9238795325112867385, 1.000000000000000000, 0.9238795325112867385, 1.000000000000000000 ) ) 
 REPRESENTATION_ITEM ( '' )  );
#68374=CARTESIAN_POINT ( 'NONE',  ( -5.082755093536325042, 25.03124999795161543, -5.082755093536325930 ) ) ;
#68375=CARTESIAN_POINT ( 'NONE',  ( 1.469576158976823947E-15, 107.3750000000000000, 8.000000000000000000 ) ) ;
#68377=CARTESIAN_POINT ( 'NONE',  ( 5.082755093536324154, 21.65624999795161543, 5.082755093536326818 ) ) ;
#68400=CARTESIAN_POINT ( 'NONE',  ( 5.082755093536325042, 90.96875000204838102, -5.082755093536325930 ) ) ;
#68407=CARTESIAN_POINT ( 'NONE',  ( 3.313708498984815343, 97.53125000000002842, -7.999999999999944933 ) ) ;
#68427=CARTESIAN_POINT ( 'NONE',  ( 7.188101187500002709, 100.8125000020484094, 2.977408999572649151 ) ) ;
#68438=ORIENTED_EDGE ( 'NONE', *, *, #24956, .F. ) ;
#68455=CARTESIAN_POINT ( 'NONE',  ( 5.082755093536325930, 22.03124999795161543, -5.082755093536325930 ) ) ;
#68459=CARTESIAN_POINT ( 'NONE',  ( 8.000000000000000000, 89.93750000409677625, -9.797174393178825657E-16 ) ) ;
#68463=EDGE_CURVE ( 'NONE', #31186, #42278, #12977, .T. ) ;
#68464=CARTESIAN_POINT ( 'NONE',  ( -5.082755093536325042, 10.03124999795161187, -5.082755093536325930 ) ) ;
#68467=CARTESIAN_POINT ( 'NONE',  ( -1.320432766682874540E-15, 3.468749997951610542, 7.188101187500000044 ) ) ;
#68481=CARTESIAN_POINT ( 'NONE',  ( 7.188101187499999156, 16.87499999795161543, 2.977408999572654924 ) ) ;
#68486=CARTESIAN_POINT ( 'NONE',  ( 1.320432766682874540E-15, 105.4062500020483810, 7.188101187500000044 ) ) ;
#68504=CARTESIAN_POINT ( 'NONE',  ( -3.313708498984762496, 90.78125000000000000, 7.999999999999998224 ) ) ;
#68514=DIRECTION ( 'NONE',  ( -0.000000000000000000, 1.000000000000000000, -0.000000000000000000 ) ) ;
#68518=CARTESIAN_POINT ( 'NONE',  ( 2.977408999572650039, 120.6875000020483952, -7.188101187500001821 ) ) ;
#68527=CARTESIAN_POINT ( 'NONE',  ( -5.082755093536325042, 26.53124999795161543, -5.082755093536325930 ) ) ;
#68542=ORIENTED_EDGE ( 'NONE', *, *, #46747, .F. ) ;
#68550=CARTESIAN_POINT ( 'NONE',  ( -7.188101187500000044, 6.093749997951610986, -8.802885111219163269E-16 ) ) ;
#68562=ORIENTED_EDGE ( 'NONE', *, *, #37312, .F. ) ;
#68568=CARTESIAN_POINT ( 'NONE',  ( 4.898587196589412829E-16, 16.87500000000000000, -8.000000000000000000 ) ) ;
#68569=VERTEX_POINT ( 'NONE', #49167 ) ;
#68570=CARTESIAN_POINT ( 'NONE',  ( -7.188101187499999156, 122.7500000020483952, 2.977408999572654924 ) ) ;
#68579=CARTESIAN_POINT ( 'NONE',  ( -2.977408999572650927, 89.37500000204839523, -7.188101187500001821 ) ) ;
#68584=DIRECTION ( 'NONE',  ( -0.000000000000000000, 1.000000000000000000, -0.000000000000000000 ) ) ;
#68588=CIRCLE ( 'NONE', #3531, 7.499999999999992895 ) ;
#68591=EDGE_CURVE ( 'NONE', #34167, #62240, #51248, .T. ) ;
#68606=CARTESIAN_POINT ( 'NONE',  ( -7.188101187500000044, 15.09374999795161187, -8.802885111219163269E-16 ) ) ;
#68609=CARTESIAN_POINT ( 'NONE',  ( -7.188101187499999156, 103.6250000020483810, 2.977408999572654924 ) ) ;
#68626=CARTESIAN_POINT ( 'NONE',  ( 2.977408999572650039, 93.68750000204838102, -7.188101187500000933 ) ) ;
#68629=CARTESIAN_POINT ( 'NONE',  ( 8.000000000000000000, 110.9375000040967905, -9.797174393178825657E-16 ) ) ;
#68633=CARTESIAN_POINT ( 'NONE',  ( -2.977408999572650927, 98.75000000204838102, -7.188101187500001821 ) ) ;
#68649=ORIENTED_EDGE ( 'NONE', *, *, #34100, .F. ) ;
#68657=CARTESIAN_POINT ( 'NONE',  ( 7.188101187499999156, 13.87499999795161187, 2.977408999572654924 ) ) ;
#68658=CARTESIAN_POINT ( 'NONE',  ( 8.000000000000000000, 107.9375000040967905, -9.797174393178825657E-16 ) ) ;
#68667=CARTESIAN_POINT ( 'NONE',  ( 7.188101187500002709, 103.8125000020483952, 2.977408999572649151 ) ) ;
#68674=ORIENTED_EDGE ( 'NONE', *, *, #15359, .F. ) ;
#68684=CARTESIAN_POINT ( 'NONE',  ( -5.656854249492378806, 104.1874999999999858, 5.656854249492381470 ) ) ;
#68690=CARTESIAN_POINT ( 'NONE',  ( 3.313708498984762052, 27.09374999590322020, -8.000000000000000000 ) ) ;
#68692=CARTESIAN_POINT ( 'NONE',  ( -2.977408999572650927, 119.7500000020483810, -7.188101187500000933 ) ) ;
#68702=CARTESIAN_POINT ( 'NONE',  ( 8.000000000000001776, 124.1562500000000000, 3.313708498984759387 ) ) ;
#68712=CARTESIAN_POINT ( 'NONE',  ( -5.082755093536324154, 110.8437500020483810, 5.082755093536326818 ) ) ;
#68717=CARTESIAN_POINT ( 'NONE',  ( 1.320432766682874540E-15, 123.4062500020483810, 7.188101187500000044 ) ) ;
#68730=EDGE_LOOP ( 'NONE', ( #63448, #46921, #53989, #35886 ) ) ;
#68735=FACE_OUTER_BOUND ( 'NONE', #74526, .T. ) ;
#68742=CARTESIAN_POINT ( 'NONE',  ( 5.656854249492380582, 1.687500000000000222, -5.656854249492380582 ) ) ;
#68743=CARTESIAN_POINT ( 'NONE',  ( -8.000000000000000000, 110.1875000040967905, 0.000000000000000000 ) ) ;
#68745=CARTESIAN_POINT ( 'NONE',  ( 2.977408999572651815, 21.56249999795161898, 7.188101187500000933 ) ) ;
#68746=DIRECTION ( 'NONE',  ( -0.000000000000000000, 1.000000000000000000, -0.000000000000000000 ) ) ;
#68771=CARTESIAN_POINT ( 'NONE',  ( -5.656854249492378806, 123.6875000000000000, 5.656854249492381470 ) ) ;
#68779=CARTESIAN_POINT ( 'NONE',  ( -8.000000000000000000, 23.25000000000000355, -9.797174393178825657E-16 ) ) ;
#68789=CARTESIAN_POINT ( 'NONE',  ( -1.469576158976823947E-15, 9.937499995903220196, 8.000000000000000000 ) ) ;
#68796=FACE_OUTER_BOUND ( 'NONE', #17074, .T. ) ;
#68801=CARTESIAN_POINT ( 'NONE',  ( 7.188101187500002709, 103.8125000020483952, 2.977408999572649151 ) ) ;
#68809=DIRECTION ( 'NONE',  ( 0.000000000000000000, 0.000000000000000000, -1.000000000000000000 ) ) ;
#68812=CARTESIAN_POINT ( 'NONE',  ( -8.000000000000000000, 6.562499995903221084, -9.797174393178825657E-16 ) ) ;
#68814=CARTESIAN_POINT ( 'NONE',  ( 5.656854249492380582, 4.687500000000000888, -5.656854249492380582 ) ) ;
#68816=CARTESIAN_POINT ( 'NONE',  ( 8.000000000000000000, 117.0312500040967763, -3.313708498984762496 ) ) ;
#68817=AXIS2_PLACEMENT_3D ( 'NONE', #22777, #45799, #68809 ) ;
#68825=CARTESIAN_POINT ( 'NONE',  ( -7.188101187500002709, 27.18749999795162609, 2.977408999572649151 ) ) ;
#68835=CARTESIAN_POINT ( 'NONE',  ( 2.977408999572651815, 12.18749999795161187, 7.188101187500000933 ) ) ;
#68838=CARTESIAN_POINT ( 'NONE',  ( -7.188101187500002709, 6.187499997951610986, 2.977408999572649151 ) ) ;
#68856=CARTESIAN_POINT ( 'NONE',  ( -2.977408999572650039, 14.43749999795161365, -7.188101187500000933 ) ) ;
#68860=CARTESIAN_POINT ( 'NONE',  ( 5.082755093536325042, 105.9687500020483952, -5.082755093536325930 ) ) ;
#68877=CARTESIAN_POINT ( 'NONE',  ( -5.656854249492380582, 90.31249999999998579, -5.656854249492380582 ) ) ;
#68880=CARTESIAN_POINT ( 'NONE',  ( -1.469576158976823947E-15, 5.625000000000000888, 8.000000000000000000 ) ) ;
#68884=ORIENTED_EDGE ( 'NONE', *, *, #13491, .T. ) ;
#68892=CARTESIAN_POINT ( 'NONE',  ( -7.188101187499999156, 118.2500000020483952, 2.977408999572654924 ) ) ;
#68901=CARTESIAN_POINT ( 'NONE',  ( 2.977408999572651815, 22.68749999795161543, 7.188101187500000933 ) ) ;
#68922=CARTESIAN_POINT ( 'NONE',  ( 7.188101187500000933, 8.437499997951611874, -2.977408999572650483 ) ) ;
#68938=CARTESIAN_POINT ( 'NONE',  ( 5.656854249492378806, 14.81250000000000355, 5.656854249492381470 ) ) ;
#68941=CARTESIAN_POINT ( 'NONE',  ( 7.188101187500002709, 121.8125000020483810, 2.977408999572649151 ) ) ;
#68948=ORIENTED_EDGE ( 'NONE', *, *, #25390, .T. ) ;
#68950=CARTESIAN_POINT ( 'NONE',  ( -2.977408999572650039, 0.9374999979516102089, -7.188101187500000933 ) ) ;
#68951=CARTESIAN_POINT ( 'NONE',  ( 4.898587196589412829E-16, 25.87500000000000711, -8.000000000000000000 ) ) ;
#68954=CARTESIAN_POINT ( 'NONE',  ( 7.188101187500002709, 123.6875000020484094, 2.977408999572649151 ) ) ;
#68981=CARTESIAN_POINT ( 'NONE',  ( -1.320432766682874540E-15, 21.46874999795161543, 7.188101187500000044 ) ) ;
#68984=CARTESIAN_POINT ( 'NONE',  ( -2.977408999572652260, 97.81250000204840944, 7.188101187500000044 ) ) ;
#68985=DIRECTION ( 'NONE',  ( -0.000000000000000000, 1.000000000000000000, -0.000000000000000000 ) ) ;
#68993=CARTESIAN_POINT ( 'NONE',  ( -4.898587196589412829E-16, 118.8125000040967763, -8.000000000000000000 ) ) ;
#69001=CARTESIAN_POINT ( 'NONE',  ( -7.188101187500000933, 92.56250000204838102, -2.977408999572650483 ) ) ;
#69008=CARTESIAN_POINT ( 'NONE',  ( 2.977408999572654480, 95.00000000204836681, 7.188101187499999156 ) ) ;
#69014=ORIENTED_EDGE ( 'NONE', *, *, #1596, .F. ) ;
#69035=CARTESIAN_POINT ( 'NONE',  ( -5.082755093536326818, 14.90624999795161187, 5.082755093536325042 ) ) ;
#69036=CARTESIAN_POINT ( 'NONE',  ( 8.000000000000001776, 101.8437500040967905, 3.313708498984759387 ) ) ;
#69039=EDGE_CURVE ( 'NONE', #39259, #34934, #56127, .T. ) ;
#69047=CARTESIAN_POINT ( 'NONE',  ( -5.082755093536325930, 105.9687500020483952, -5.082755093536325930 ) ) ;
#69056=CARTESIAN_POINT ( 'NONE',  ( 4.898587196589412829E-16, 3.375000000000000444, -8.000000000000000000 ) ) ;
#69063=CARTESIAN_POINT ( 'NONE',  ( -5.656854249492378806, 99.68750000000000000, 5.656854249492381470 ) ) ;
#69066=CARTESIAN_POINT ( 'NONE',  ( -5.656854249492378806, 98.18750000000000000, 5.656854249492381470 ) ) ;
#69068=CARTESIAN_POINT ( 'NONE',  ( -8.000000000000000000, 25.96874999590322375, -3.313708498984762496 ) ) ;
#69071=CARTESIAN_POINT ( 'NONE',  ( -5.082755093536324154, 115.7187500020483810, 5.082755093536326818 ) ) ;
#69074=CARTESIAN_POINT ( 'NONE',  ( -5.656854249492379694, 3.562500000000000444, -5.656854249492380582 ) ) ;
#69078=CARTESIAN_POINT ( 'NONE',  ( 5.656854249492381470, 100.2500000040967905, 5.656854249492379694 ) ) ;
#69089=CARTESIAN_POINT ( 'NONE',  ( 8.000000000000000000, 7.406249995903221084, -3.313708498984761164 ) ) ;
#69090=CARTESIAN_POINT ( 'NONE',  ( -5.082755093536324154, 113.8437500020483810, 5.082755093536326818 ) ) ;
#69095=CARTESIAN_POINT ( 'NONE',  ( 2.977408999572654480, 113.0000000020483668, 7.188101187499999156 ) ) ;
#69096=CARTESIAN_POINT ( 'NONE',  ( -5.656854249492380582, 120.5000000040967905, -5.656854249492380582 ) ) ;
#69098=AXIS2_PLACEMENT_3D ( 'NONE', #18897, #12850, #69475 ) ;
#69102=CARTESIAN_POINT ( 'NONE',  ( 8.000000000000001776, 107.6562500000000000, 3.313708498984759387 ) ) ;
#69109=ORIENTED_EDGE ( 'NONE', *, *, #39239, .T. ) ;
#69121=VECTOR ( 'NONE', #6073, 1000.000000000000000 ) ;
#69122=CARTESIAN_POINT ( 'NONE',  ( 8.000000000000000000, 1.500000000000000000, 0.000000000000000000 ) ) ;
#69123=CARTESIAN_POINT ( 'NONE',  ( -7.999999999999998224, 110.2812500040967763, 3.313708498984766049 ) ) ;
#69125=CARTESIAN_POINT ( 'NONE',  ( 5.082755093536325930, 25.03124999795161543, -5.082755093536325930 ) ) ;
#69126=CARTESIAN_POINT ( 'NONE',  ( -3.313708498984762052, 120.4062500040967905, -8.000000000000000000 ) ) ;
#69148=CARTESIAN_POINT ( 'NONE',  ( -4.401442555609581635E-16, 89.65625000204838102, -7.188101187500000044 ) ) ;
#69151=VERTEX_POINT ( 'NONE', #25684 ) ;
#69176=EDGE_CURVE ( 'NONE', #30852, #73724, #16330, .T. ) ;
#69179=CARTESIAN_POINT ( 'NONE',  ( -7.188101187500001821, 98.56250000204838102, -2.977408999572650483 ) ) ;
#69185=ORIENTED_EDGE ( 'NONE', *, *, #58132, .T. ) ;
#69203=CARTESIAN_POINT ( 'NONE',  ( 2.977408999572652260, 21.56249999795161543, 7.188101187500000044 ) ) ;
#69210=CARTESIAN_POINT ( 'NONE',  ( 4.401442555609581635E-16, 6.843749997951611874, -7.188101187500000044 ) ) ;
#69214=CARTESIAN_POINT ( 'NONE',  ( 7.188101187500000044, 8.343749997951611874, 0.000000000000000000 ) ) ;
#69228=CARTESIAN_POINT ( 'NONE',  ( 5.082755093536325042, 119.0937500020483810, -5.082755093536325930 ) ) ;
#69232=CARTESIAN_POINT ( 'NONE',  ( 4.401442555609581635E-16, 17.34374999795161187, -7.188101187500000044 ) ) ;
#69238=CARTESIAN_POINT ( 'NONE',  ( 2.977408999572650039, 109.0625000020483810, -7.188101187500001821 ) ) ;
#69267=CARTESIAN_POINT ( 'NONE',  ( 2.977408999572654480, 118.6250000020483810, 7.188101187499999156 ) ) ;
#69275=CYLINDRICAL_SURFACE ( 'NONE', #32777, 8.000000000000000000 ) ;
#69276=CARTESIAN_POINT ( 'NONE',  ( 2.977408999572651815, 27.18749999795161898, 7.188101187500000933 ) ) ;
#69281=CARTESIAN_POINT ( 'NONE',  ( 8.000000000000000000, 25.50000000000000355, 0.000000000000000000 ) ) ;
#69298=CARTESIAN_POINT ( 'NONE',  ( -5.082755093536325042, 4.406249997951610098, -5.082755093536325930 ) ) ;
#69303=CARTESIAN_POINT ( 'NONE',  ( 8.000000000000000000, 99.03125000409677625, -3.313708498984762496 ) ) ;
#69314=VECTOR ( 'NONE', #33360, 1000.000000000000000 ) ;
#69316=CARTESIAN_POINT ( 'NONE',  ( -5.656854249492379694, 20.06250000000000355, -5.656854249492380582 ) ) ;
#69317=ORIENTED_EDGE ( 'NONE', *, *, #70228, .T. ) ;
#69318=CARTESIAN_POINT ( 'NONE',  ( 1.320432766682874540E-15, 123.0312500020483810, 7.188101187500000044 ) ) ;
#69324=CARTESIAN_POINT ( 'NONE',  ( 1.469576158976823947E-15, 113.3750000000000000, 8.000000000000000000 ) ) ;
#69327=CARTESIAN_POINT ( 'NONE',  ( 3.594037731798487290, 89.15552412475317112, -6.225085659181542219 ) ) ;
#69334=ORIENTED_EDGE ( 'NONE', *, *, #27957, .F. ) ;
#69349=VECTOR ( 'NONE', #1400, 1000.000000000000000 ) ;
#69353=CARTESIAN_POINT ( 'NONE',  ( 7.188101187500001821, 23.43749999795161898, -2.977408999572650483 ) ) ;
#69357=CARTESIAN_POINT ( 'NONE',  ( 5.082755093536325042, 96.96875000204838102, -5.082755093536325930 ) ) ;
#69367=DIRECTION ( 'NONE',  ( 0.000000000000000000, -0.000000000000000000, 1.000000000000000000 ) ) ;
#69373=CARTESIAN_POINT ( 'NONE',  ( 7.188101187500000933, 96.50000000204838102, -2.977408999572651371 ) ) ;
#69379=CARTESIAN_POINT ( 'NONE',  ( 2.977408999572650039, 94.06250000204838102, -7.188101187500001821 ) ) ;
#69402=CARTESIAN_POINT ( 'NONE',  ( -8.000000000000000000, 3.562499995903220196, -9.797174393178825657E-16 ) ) ;
#69406=CARTESIAN_POINT ( 'NONE',  ( 5.656854249492379694, 105.1250000040967763, -5.656854249492380582 ) ) ;
#69410=DIRECTION ( 'NONE',  ( -0.000000000000000000, 1.000000000000000000, -0.000000000000000000 ) ) ;
#69415=CARTESIAN_POINT ( 'NONE',  ( -7.188101187499999156, 101.7500000020483810, 2.977408999572654924 ) ) ;
#69431=CARTESIAN_POINT ( 'NONE',  ( -3.313708498984762052, 102.2187500000000000, -8.000000000000000000 ) ) ;
#69437=CARTESIAN_POINT ( 'NONE',  ( -5.082755093536325042, 2.906249997951610542, -5.082755093536325930 ) ) ;
#69440=CARTESIAN_POINT ( 'NONE',  ( -4.401442555609581635E-16, 118.1562500020483810, -7.188101187500000044 ) ) ;
#69449=( BOUNDED_CURVE ( )  B_SPLINE_CURVE ( 2, ( #2554, #24448, #25545, #48558, #70480, #71567, #19890, #37261, #60255 ),
 .UNSPECIFIED., .F., .F. ) 
 B_SPLINE_CURVE_WITH_KNOTS ( ( 3, 2, 2, 2, 3 ),
 ( 0.2916666666666667407, 0.2986111111111111605, 0.3055555555555555802, 0.3125000000000000000, 0.3194444444444443643 ),
 .UNSPECIFIED. ) 
 CURVE ( )  GEOMETRIC_REPRESENTATION_ITEM ( )  RATIONAL_B_SPLINE_CURVE ( ( 0.9999999999999994449, 0.9238795325112872936, 1.000000000000000000, 0.9238795325112867385, 1.000000000000000000, 0.9238795325112867385, 1.000000000000000000, 0.9238795325112872936, 0.9999999999999994449 ) ) 
 REPRESENTATION_ITEM ( '' )  );
#69451=( BOUNDED_CURVE ( )  B_SPLINE_CURVE ( 2, ( #45687, #41154, #73992, #57777, #52109, #68702, #62663, #23797, #63041 ),
 .UNSPECIFIED., .F., .F. ) 
 B_SPLINE_CURVE_WITH_KNOTS ( ( 3, 2, 2, 2, 3 ),
 ( 0.01385927522962447471, 0.01562500000000000347, 0.02083333333333334259, 0.02604166666666668517, 0.03125000000000002082 ),
 .UNSPECIFIED. ) 
 CURVE ( )  GEOMETRIC_REPRESENTATION_ITEM ( )  RATIONAL_B_SPLINE_CURVE ( ( 0.9658850645339600582, 0.9741937033643419674, 1.000000000000000000, 0.9238795325112867385, 1.000000000000000000, 0.9238795325112867385, 1.000000000000000000, 0.9238795325112864054, 1.000000000000000222 ) ) 
 REPRESENTATION_ITEM ( '' )  );
#69462=LINE ( 'NONE', #1557, #4561 ) ;
#69463=CARTESIAN_POINT ( 'NONE',  ( 5.082755093536326818, 112.7187500020483810, 5.082755093536325042 ) ) ;
#69469=CARTESIAN_POINT ( 'NONE',  ( 7.188101187500001821, 114.8750000020483810, -2.977408999572651371 ) ) ;
#69475=DIRECTION ( 'NONE',  ( 0.000000000000000000, 0.000000000000000000, 1.000000000000000000 ) ) ;
#69494=EDGE_LOOP ( 'NONE', ( #22472, #44733, #2223, #49147 ) ) ;
#69495=CARTESIAN_POINT ( 'NONE',  ( 3.313708498984762052, 6.281250000000000888, -8.000000000000000000 ) ) ;
#69498=CARTESIAN_POINT ( 'NONE',  ( 2.977408999572650927, 26.62499999795161543, -7.188101187500001821 ) ) ;
#69499=CARTESIAN_POINT ( 'NONE',  ( -8.000000000000000000, 120.6875000040967763, 0.000000000000000000 ) ) ;
#69520=CARTESIAN_POINT ( 'NONE',  ( -5.656854249492378806, 119.1875000000000000, 5.656854249492381470 ) ) ;
#69527=CARTESIAN_POINT ( 'NONE',  ( 4.898587196589412829E-16, 12.18749999590322197, -8.000000000000000000 ) ) ;
#69542=EDGE_LOOP ( 'NONE', ( #36691, #28293, #41984 ) ) ;
#69547=CARTESIAN_POINT ( 'NONE',  ( 5.656854249492380582, 4.499999995903220196, -5.656854249492380582 ) ) ;
#69551=( BOUNDED_CURVE ( )  B_SPLINE_CURVE ( 2, ( #70162, #41116, #41480, #35462, #17350, #17721, #46760, #23758, #64854 ),
 .UNSPECIFIED., .F., .F. ) 
 B_SPLINE_CURVE_WITH_KNOTS ( ( 3, 2, 2, 2, 3 ),
 ( 0.9027777777777776791, 0.9097222222222220989, 0.9166666666666665186, 0.9236111111111110494, 0.9305555555555554692 ),
 .UNSPECIFIED. ) 
 CURVE ( )  GEOMETRIC_REPRESENTATION_ITEM ( )  RATIONAL_B_SPLINE_CURVE ( ( 1.000000000000001110, 0.9238795325112855172, 1.000000000000000000, 0.9238795325112867385, 1.000000000000000000, 0.9238795325112867385, 1.000000000000000000, 0.9238795325112879597, 0.9999999999999987788 ) ) 
 REPRESENTATION_ITEM ( '' )  );
#69553=CARTESIAN_POINT ( 'NONE',  ( 5.082755093536326818, 94.71875000204838102, 5.082755093536325042 ) ) ;
#69556=CARTESIAN_POINT ( 'NONE',  ( 3.442865974826785802, 0.3519712649008457928, -7.075303620129630211 ) ) ;
#69558=ORIENTED_EDGE ( 'NONE', *, *, #68301, .F. ) ;
#69567=CYLINDRICAL_SURFACE ( 'NONE', #40507, 8.000000000000000000 ) ;
#69578=CARTESIAN_POINT ( 'NONE',  ( 2.977408999572650927, 22.12499999795161543, -7.188101187500000933 ) ) ;
#69586=CARTESIAN_POINT ( 'NONE',  ( 5.082755093536324154, 12.28124999795161187, 5.082755093536326818 ) ) ;
#69589=CARTESIAN_POINT ( 'NONE',  ( 5.082755093536324154, 6.656249997951610986, 5.082755093536326818 ) ) ;
#69596=ORIENTED_EDGE ( 'NONE', *, *, #34723, .T. ) ;
#69601=CARTESIAN_POINT ( 'NONE',  ( -2.977408999572650927, 116.3750000020483810, -7.188101187500001821 ) ) ;
#69605=CARTESIAN_POINT ( 'NONE',  ( -2.977408999572650039, 18.93749999795161543, -7.188101187500000933 ) ) ;
#69608=CARTESIAN_POINT ( 'NONE',  ( 3.313708498984761608, 13.78125000000000178, -8.000000000000000000 ) ) ;
#69610=CARTESIAN_POINT ( 'NONE',  ( -5.082755093536325930, 100.3437500020483810, -5.082755093536325930 ) ) ;
#69614=CARTESIAN_POINT ( 'NONE',  ( -7.999999999999998224, 89.28125000409679046, 3.313708498984766049 ) ) ;
#69620=CARTESIAN_POINT ( 'NONE',  ( -8.000000000000000000, 14.25000000000000178, -9.797174393178825657E-16 ) ) ;
#69626=CARTESIAN_POINT ( 'NONE',  ( 1.469576158976823947E-15, 90.87500000000000000, 8.000000000000000000 ) ) ;
#69640=CARTESIAN_POINT ( 'NONE',  ( 2.977408999572650039, 117.6875000020484094, -7.188101187500001821 ) ) ;
#69653=ORIENTED_EDGE ( 'NONE', *, *, #21816, .T. ) ;
#69670=CARTESIAN_POINT ( 'NONE',  ( -5.082755093536325042, 8.906249997951611874, -5.082755093536325930 ) ) ;
#69671=( BOUNDED_CURVE ( )  B_SPLINE_CURVE ( 2, ( #558, #52226, #35616, #59004, #63908, #1660, #24641, #929, #12587 ),
 .UNSPECIFIED., .F., .F. ) 
 B_SPLINE_CURVE_WITH_KNOTS ( ( 3, 2, 2, 2, 3 ),
 ( 0.5972222222222222099, 0.6041666666666666297, 0.6111111111111111605, 0.6180555555555554692, 0.6249999999999998890 ),
 .UNSPECIFIED. ) 
 CURVE ( )  GEOMETRIC_REPRESENTATION_ITEM ( )  RATIONAL_B_SPLINE_CURVE ( ( 1.000000000000000000, 0.9238795325112867385, 1.000000000000000000, 0.9238795325112867385, 1.000000000000000000, 0.9238795325112867385, 1.000000000000000000, 0.9238795325112879597, 0.9999999999999987788 ) ) 
 REPRESENTATION_ITEM ( '' )  );
#69676=CARTESIAN_POINT ( 'NONE',  ( -4.898587196589412829E-16, 99.31250000409677625, -8.000000000000000000 ) ) ;
#69690=CARTESIAN_POINT ( 'NONE',  ( -8.000000000000001776, 15.84375000000000355, 3.313708498984759387 ) ) ;
#69693=CARTESIAN_POINT ( 'NONE',  ( 5.082755093536326818, 120.2187500020483952, 5.082755093536325042 ) ) ;
#69702=ADVANCED_FACE ( 'NONE', ( #15786 ), #55056, .T. ) ;
#69704=CARTESIAN_POINT ( 'NONE',  ( -7.188101187499999156, 121.6250000020483810, 2.977408999572654924 ) ) ;
#69716=LINE ( 'NONE', #41046, #58957 ) ;
#69728=CARTESIAN_POINT ( 'NONE',  ( -5.082755093536326818, 21.28124999795161543, 5.082755093536325042 ) ) ;
#69730=CARTESIAN_POINT ( 'NONE',  ( -5.082755093536325930, 97.34375000204838102, -5.082755093536325930 ) ) ;
#69747=CARTESIAN_POINT ( 'NONE',  ( -2.977408999572650927, 89.37500000204836681, -7.188101187500000933 ) ) ;
#69751=AXIS2_PLACEMENT_3D ( 'NONE', #32627, #55264, #10712 ) ;
#69753=CARTESIAN_POINT ( 'NONE',  ( -2.977408999572651815, 97.81250000204840944, 7.188101187500000933 ) ) ;
#69758=ORIENTED_EDGE ( 'NONE', *, *, #73889, .F. ) ;
#69771=CARTESIAN_POINT ( 'NONE',  ( -5.656854249492381470, 3.749999995903220640, 5.656854249492379694 ) ) ;
#69772=EDGE_LOOP ( 'NONE', ( #41718, #53897, #55792 ) ) ;
#69774=CARTESIAN_POINT ( 'NONE',  ( 8.000000000000000000, 105.0312500040967763, -3.313708498984762496 ) ) ;
#69782=VECTOR ( 'NONE', #69410, 1000.000000000000000 ) ;
#69786=CARTESIAN_POINT ( 'NONE',  ( -2.977408999572650927, 107.3750000020484094, -7.188101187500001821 ) ) ;
#69803=CARTESIAN_POINT ( 'NONE',  ( -3.313708498984762496, 101.2812499999999858, 7.999999999999998224 ) ) ;
#69806=EDGE_CURVE ( 'NONE', #14878, #52001, #28021, .T. ) ;
#69809=CARTESIAN_POINT ( 'NONE',  ( -7.188101187500002709, 4.687499997951610986, 2.977408999572649151 ) ) ;
#69812=CARTESIAN_POINT ( 'NONE',  ( 7.188101187500000044, 113.2812500020483952, -8.802885111219163269E-16 ) ) ;
#69816=CARTESIAN_POINT ( 'NONE',  ( -7.999999999999998224, 90.59375000000000000, 3.313708498984766049 ) ) ;
#69834=CARTESIAN_POINT ( 'NONE',  ( -5.082755093536325930, 113.4687500020483810, -5.082755093536325930 ) ) ;
#69842=CARTESIAN_POINT ( 'NONE',  ( 2.977408999572650039, 112.0625000020483810, -7.188101187500001821 ) ) ;
#69845=ORIENTED_EDGE ( 'NONE', *, *, #60387, .F. ) ;
#69859=CARTESIAN_POINT ( 'NONE',  ( 8.000000000000000000, 20.81249999590322375, 0.000000000000000000 ) ) ;
#69862=VERTEX_POINT ( 'NONE', #67855 ) ;
#69866=EDGE_LOOP ( 'NONE', ( #48112, #38273, #24648, #65822, #25229 ) ) ;
#69867=CARTESIAN_POINT ( 'NONE',  ( 4.898587196589412829E-16, 6.375000000000000888, -8.000000000000000000 ) ) ;
#69869=CARTESIAN_POINT ( 'NONE',  ( -5.082755093536325042, 22.40624999795161543, -5.082755093536325930 ) ) ;
#69870=CARTESIAN_POINT ( 'NONE',  ( 5.656854249492379694, 120.1250000040967905, -5.656854249492380582 ) ) ;
#69876=LINE ( 'NONE', #40830, #25213 ) ;
#69897=CARTESIAN_POINT ( 'NONE',  ( -4.898587196589412829E-16, 118.6250000000000000, -8.000000000000000000 ) ) ;
#69903=CARTESIAN_POINT ( 'NONE',  ( 4.898587196589412829E-16, 15.18749999590322197, -8.000000000000000000 ) ) ;
#69915=DIRECTION ( 'NONE',  ( 0.000000000000000000, 0.000000000000000000, 1.000000000000000000 ) ) ;
#69918=VERTEX_POINT ( 'NONE', #12370 ) ;
#69923=CARTESIAN_POINT ( 'NONE',  ( 5.656854249492378806, 4.124999995903220196, 5.656854249492381470 ) ) ;
#69928=CARTESIAN_POINT ( 'NONE',  ( -7.188101187500000044, 95.65625000204838102, 0.000000000000000000 ) ) ;
#69933=VERTEX_POINT ( 'NONE', #42140 ) ;
#69948=CARTESIAN_POINT ( 'NONE',  ( -4.898587196589412829E-16, 111.1250000000000000, -8.000000000000000000 ) ) ;
#69961=CARTESIAN_POINT ( 'NONE',  ( 7.188101187499999156, 16.87499999795161543, 2.977408999572654924 ) ) ;
#69964=CARTESIAN_POINT ( 'NONE',  ( -7.188101187500001821, 8.999999997951611874, -2.977408999572651371 ) ) ;
#69974=VECTOR ( 'NONE', #28145, 1000.000000000000000 ) ;
#69977=CARTESIAN_POINT ( 'NONE',  ( -7.188101187499999156, 113.7500000020483668, 2.977408999572654924 ) ) ;
#69983=CARTESIAN_POINT ( 'NONE',  ( 5.082755093536324154, 15.28124999795161187, 5.082755093536326818 ) ) ;
#69987=CARTESIAN_POINT ( 'NONE',  ( 5.082755093536326818, 98.09375000204838102, 5.082755093536325042 ) ) ;
#69989=CARTESIAN_POINT ( 'NONE',  ( -5.656854249492380582, 111.5000000040967763, -5.656854249492380582 ) ) ;
#69993=ORIENTED_EDGE ( 'NONE', *, *, #74202, .F. ) ;
#70001=CARTESIAN_POINT ( 'NONE',  ( -1.469576158976823947E-15, 17.43749999590322375, 8.000000000000000000 ) ) ;
#70006=CARTESIAN_POINT ( 'NONE',  ( -4.898587196589412829E-16, 97.81250000409677625, -8.000000000000000000 ) ) ;
#70019=CARTESIAN_POINT ( 'NONE',  ( 7.188101187500002709, 112.8125000020483952, 2.977408999572649151 ) ) ;
#70027=CARTESIAN_POINT ( 'NONE',  ( 5.656854249492379694, 109.4375000000000000, -5.656854249492380582 ) ) ;
#70040=CARTESIAN_POINT ( 'NONE',  ( 3.594042629939374400, 89.53052393364181683, -6.225082831242716885 ) ) ;
#70048=CARTESIAN_POINT ( 'NONE',  ( 2.977408999572650927, 14.62499999795161187, -7.188101187500000933 ) ) ;
#70067=EDGE_CURVE ( 'NONE', #1872, #34167, #18037, .T. ) ;
#70068=CARTESIAN_POINT ( 'NONE',  ( -8.000000000000001776, 26.34375000000000711, 3.313708498984759387 ) ) ;
#70072=CARTESIAN_POINT ( 'NONE',  ( -5.082755093536324154, 122.8437500020483952, 5.082755093536326818 ) ) ;
#70078=CARTESIAN_POINT ( 'NONE',  ( 5.082755093536324154, 1.781249997951610098, 5.082755093536326818 ) ) ;
#70082=CARTESIAN_POINT ( 'NONE',  ( 2.977408999572654480, 117.5000000020483810, 7.188101187499999156 ) ) ;
#70093=CARTESIAN_POINT ( 'NONE',  ( 8.000000000000000000, 105.0312500040967905, -3.313708498984762496 ) ) ;
#70095=FACE_OUTER_BOUND ( 'NONE', #50827, .T. ) ;
#70108=CARTESIAN_POINT ( 'NONE',  ( -5.082755093536326818, 25.78124999795161543, 5.082755093536325042 ) ) ;
#70110=CARTESIAN_POINT ( 'NONE',  ( 2.977408999572654480, 98.00000000204838102, 7.188101187499999156 ) ) ;
#70126=CARTESIAN_POINT ( 'NONE',  ( -8.000000000000000000, 123.5937500040967763, -3.313708498984761164 ) ) ;
#70129=CARTESIAN_POINT ( 'NONE',  ( -4.898587196589412829E-16, 111.3125000040967905, -8.000000000000000000 ) ) ;
#70132=CARTESIAN_POINT ( 'NONE',  ( 5.082755093536325042, 95.46875000204838102, -5.082755093536325930 ) ) ;
#70143=LINE ( 'NONE', #12775, #70697 ) ;
#70154=CARTESIAN_POINT ( 'NONE',  ( 3.313708498984760720, 106.7187500040967763, -8.000000000000000000 ) ) ;
#70155=AXIS2_PLACEMENT_3D ( 'NONE', #11463, #64257, #57504 ) ;
#70160=CARTESIAN_POINT ( 'NONE',  ( 0.000000000000000000, 125.0000000000000000, 8.000000000000000000 ) ) ;
#70162=CARTESIAN_POINT ( 'NONE',  ( 4.898587196589412829E-16, 24.37500000000000355, -8.000000000000000000 ) ) ;
#70163=CARTESIAN_POINT ( 'NONE',  ( -5.082755093536324154, 95.84375000204838102, 5.082755093536326818 ) ) ;
#70171=ORIENTED_EDGE ( 'NONE', *, *, #55092, .F. ) ;
#70183=AXIS2_PLACEMENT_3D ( 'NONE', #66496, #56313, #44618 ) ;
#70185=CARTESIAN_POINT ( 'NONE',  ( -7.188101187500002709, 7.687499997951611874, 2.977408999572649151 ) ) ;
#70188=CARTESIAN_POINT ( 'NONE',  ( -2.977408999572650927, 115.2500000020483952, -7.188101187500000933 ) ) ;
#70189=CYLINDRICAL_SURFACE ( 'NONE', #74527, 8.000000000000000000 ) ;
#70192=CARTESIAN_POINT ( 'NONE',  ( -8.000000000000000000, 90.40625000000000000, -3.313708498984761164 ) ) ;
#70193=VECTOR ( 'NONE', #59068, 1000.000000000000000 ) ;
#70210=CARTESIAN_POINT ( 'NONE',  ( -7.188101187500000044, 104.6562500020483810, 0.000000000000000000 ) ) ;
#70215=CARTESIAN_POINT ( 'NONE',  ( -7.188101187499999156, 112.6250000020483668, 2.977408999572654924 ) ) ;
#70228=EDGE_CURVE ( 'NONE', #69862, #36620, #16397, .T. ) ;
#70241=CARTESIAN_POINT ( 'NONE',  ( -8.000000000000000000, 5.250000000000000888, -9.797174393178825657E-16 ) ) ;
#70243=CARTESIAN_POINT ( 'NONE',  ( 4.401442555609581635E-16, 0.8437499979516099868, -7.188101187500000044 ) ) ;
#70245=CARTESIAN_POINT ( 'NONE',  ( -5.656854249492378806, 119.3750000040967905, 5.656854249492381470 ) ) ;
#70265=CARTESIAN_POINT ( 'NONE',  ( 3.313708498984760720, 118.5312500000000142, -8.000000000000000000 ) ) ;
#70270=CARTESIAN_POINT ( 'NONE',  ( 5.656854249492378806, 13.12499999590322197, 5.656854249492381470 ) ) ;
#70271=AXIS2_PLACEMENT_3D ( 'NONE', #54164, #19809, #42449 ) ;
#70291=CARTESIAN_POINT ( 'NONE',  ( 7.999999999999998224, 4.218749995903220196, 3.313708498984766049 ) ) ;
#70292=CARTESIAN_POINT ( 'NONE',  ( -5.082755093536324154, 121.3437500020483952, 5.082755093536326818 ) ) ;
#70296=CARTESIAN_POINT ( 'NONE',  ( 7.188101187500002709, 94.81250000204838102, 2.977408999572649151 ) ) ;
#70312=VERTEX_POINT ( 'NONE', #72968 ) ;
#70319=( BOUNDED_CURVE ( )  B_SPLINE_CURVE ( 2, ( #65554, #14226, #54624, #42541, #25919, #19524, #36526, #2562, #25183 ),
 .UNSPECIFIED., .F., .F. ) 
 B_SPLINE_CURVE_WITH_KNOTS ( ( 3, 2, 2, 2, 3 ),
 ( 0.6145833333333333703, 0.6197916666666666297, 0.6250000000000000000, 0.6302083333333334814, 0.6354166666666667407 ),
 .UNSPECIFIED. ) 
 CURVE ( )  GEOMETRIC_REPRESENTATION_ITEM ( )  RATIONAL_B_SPLINE_CURVE ( ( 1.000000000000000000, 0.9238795325112867385, 1.000000000000000000, 0.9238795325112867385, 1.000000000000000000, 0.9238795325112867385, 1.000000000000000000, 0.9238795325112850731, 1.000000000000001554 ) ) 
 REPRESENTATION_ITEM ( '' )  );
#70327=CARTESIAN_POINT ( 'NONE',  ( -2.977408999572650039, 12.93749999795161365, -7.188101187500001821 ) ) ;
#70329=CARTESIAN_POINT ( 'NONE',  ( -3.313708498984816231, 117.9687500040967905, 7.999999999999943157 ) ) ;
#70330=CARTESIAN_POINT ( 'NONE',  ( 5.082755093536325930, 13.03124999795161187, -5.082755093536325930 ) ) ;
#70345=CARTESIAN_POINT ( 'NONE',  ( -5.082755093536324154, 118.3437500020483810, 5.082755093536326818 ) ) ;
#70350=CARTESIAN_POINT ( 'NONE',  ( -7.188101187500000933, 22.12499999795161187, -2.977408999572651371 ) ) ;
#70356=CARTESIAN_POINT ( 'NONE',  ( 5.082755093536326818, 102.5937500020483810, 5.082755093536325042 ) ) ;
#70360=ORIENTED_EDGE ( 'NONE', *, *, #21963, .F. ) ;
#70371=CARTESIAN_POINT ( 'NONE',  ( 1.469576158976823947E-15, 97.06250000409677625, 8.000000000000000000 ) ) ;
#70381=CARTESIAN_POINT ( 'NONE',  ( -4.733156245433696618, 124.6781487883913258, -6.232488682494672361 ) ) ;
#70384=CARTESIAN_POINT ( 'NONE',  ( -5.082755093536325930, 117.9687500020483810, -5.082755093536325930 ) ) ;
#70389=CARTESIAN_POINT ( 'NONE',  ( -5.656854249492381470, 26.43750000000000355, 5.656854249492379694 ) ) ;
#70391=ADVANCED_FACE ( 'NONE', ( #23505 ), #57494, .T. ) ;
#70396=CARTESIAN_POINT ( 'NONE',  ( 5.656854249492380582, 25.68750000000000711, -5.656854249492380582 ) ) ;
#70400=CYLINDRICAL_SURFACE ( 'NONE', #14273, 8.000000000000000000 ) ;
#70407=CARTESIAN_POINT ( 'NONE',  ( 5.656854249492378806, 22.31250000000000355, 5.656854249492381470 ) ) ;
#70411=CARTESIAN_POINT ( 'NONE',  ( 4.401442555609581635E-16, 13.21874999795161187, -7.188101187500000044 ) ) ;
#70420=CARTESIAN_POINT ( 'NONE',  ( 1.469576158976823947E-15, 98.56250000409677625, 8.000000000000000000 ) ) ;
#70428=CARTESIAN_POINT ( 'NONE',  ( 3.313708498984762052, 25.78125000000000355, -8.000000000000000000 ) ) ;
#70438=CARTESIAN_POINT ( 'NONE',  ( 7.188101187499999156, 6.374999997951610986, 2.977408999572654924 ) ) ;
#70442=CARTESIAN_POINT ( 'NONE',  ( -2.977408999572650927, 118.2500000020483952, -7.188101187500001821 ) ) ;
#70448=( BOUNDED_CURVE ( )  B_SPLINE_CURVE ( 2, ( #9245, #32267, #55285, #3589, #26584, #72623, #20927, #4713, #62772 ),
 .UNSPECIFIED., .F., .F. ) 
 B_SPLINE_CURVE_WITH_KNOTS ( ( 3, 2, 2, 2, 3 ),
 ( 0.8645833333333335924, 0.8697916666666668517, 0.8750000000000002220, 0.8802083333333337034, 0.8854166666666669627 ),
 .UNSPECIFIED. ) 
 CURVE ( )  GEOMETRIC_REPRESENTATION_ITEM ( )  RATIONAL_B_SPLINE_CURVE ( ( 0.9999999999999967804, 0.9238795325112899581, 1.000000000000000000, 0.9238795325112867385, 1.000000000000000000, 0.9238795325112867385, 1.000000000000000000, 0.9238795325112818535, 1.000000000000004885 ) ) 
 REPRESENTATION_ITEM ( '' )  );
#70468=CARTESIAN_POINT ( 'NONE',  ( -7.188101187500000044, 24.09374999795161543, -8.802885111219163269E-16 ) ) ;
#70470=CARTESIAN_POINT ( 'NONE',  ( 7.188101187500002709, 96.68750000204838102, 2.977408999572649151 ) ) ;
#70479=ORIENTED_EDGE ( 'NONE', *, *, #20906, .F. ) ;
#70480=CARTESIAN_POINT ( 'NONE',  ( -8.000000000000000000, 9.562499995903223748, -9.797174393178825657E-16 ) ) ;
#70492=CARTESIAN_POINT ( 'NONE',  ( -7.188101187500001821, 89.93750000204840944, -2.977408999572650483 ) ) ;
#70511=CARTESIAN_POINT ( 'NONE',  ( 5.656854249492381470, 106.2500000040967905, 5.656854249492379694 ) ) ;
#70520=CARTESIAN_POINT ( 'NONE',  ( 2.977408999572654480, 99.12500000204838102, 7.188101187499999156 ) ) ;
#70528=CARTESIAN_POINT ( 'NONE',  ( 1.469576158976823947E-15, 105.8750000000000000, 8.000000000000000000 ) ) ;
#70545=CARTESIAN_POINT ( 'NONE',  ( 7.188101187499999156, 8.249999997951611874, 2.977408999572654924 ) ) ;
#70548=CARTESIAN_POINT ( 'NONE',  ( -7.188101187500000044, 118.5312500020483810, 0.000000000000000000 ) ) ;
#70556=CARTESIAN_POINT ( 'NONE',  ( -8.000000000000000000, 9.750000000000001776, -9.797174393178825657E-16 ) ) ;
#70558=CARTESIAN_POINT ( 'NONE',  ( 3.313708498984679895, 112.5312500000000284, -8.000000000000081712 ) ) ;
#70569=CARTESIAN_POINT ( 'NONE',  ( 1.320432766682874540E-15, 103.5312500020483810, 7.188101187500000044 ) ) ;
#70574=CARTESIAN_POINT ( 'NONE',  ( 7.188101187500002709, 114.6875000020484094, 2.977408999572649151 ) ) ;
#70585=CARTESIAN_POINT ( 'NONE',  ( 9.797174393178825657E-16, 125.0000000000000000, -8.000000000000000000 ) ) ;
#70597=CARTESIAN_POINT ( 'NONE',  ( -5.656854249492379694, 5.062500000000000888, -5.656854249492380582 ) ) ;
#70598=DIRECTION ( 'NONE',  ( -0.000000000000000000, 1.000000000000000000, -0.000000000000000000 ) ) ;
#70599=CARTESIAN_POINT ( 'NONE',  ( -7.188101187500002709, 1.312499997951610098, 2.977408999572649151 ) ) ;
#70600=CARTESIAN_POINT ( 'NONE',  ( -5.656854249492378806, 122.3750000040967905, 5.656854249492381470 ) ) ;
#70605=DIRECTION ( 'NONE',  ( -0.000000000000000000, 1.000000000000000000, -0.000000000000000000 ) ) ;
#70617=CARTESIAN_POINT ( 'NONE',  ( 3.313708498984711426, 95.65625000409679046, 8.000000000000053291 ) ) ;
#70620=CARTESIAN_POINT ( 'NONE',  ( -8.000000000000001776, 12.65624999590322197, 3.313708498984759387 ) ) ;
#70624=CARTESIAN_POINT ( 'NONE',  ( -8.000000000000000000, 119.0000000000000000, 0.000000000000000000 ) ) ;
#70627=EDGE_CURVE ( 'NONE', #72853, #65440, #4908, .T. ) ;
#70629=CARTESIAN_POINT ( 'NONE',  ( 8.000000000000000000, 16.31249999590322375, 0.000000000000000000 ) ) ;
#70651=CARTESIAN_POINT ( 'NONE',  ( -7.188101187499999156, 121.2500000020483952, 2.977408999572654924 ) ) ;
#70657=CARTESIAN_POINT ( 'NONE',  ( 2.977408999572650039, 95.18750000204838102, -7.188101187500001821 ) ) ;
#70659=DIRECTION ( 'NONE',  ( -0.000000000000000000, 1.000000000000000000, -0.000000000000000000 ) ) ;
#70660=CARTESIAN_POINT ( 'NONE',  ( 3.887681576892050295, 0.3419578554194728781, -6.829612127959068246 ) ) ;
#70663=EDGE_LOOP ( 'NONE', ( #67041, #16580, #5533, #21007 ) ) ;
#70666=CARTESIAN_POINT ( 'NONE',  ( 0.000000000000000000, 54.99999999999999289, 0.000000000000000000 ) ) ;
#70674=FACE_OUTER_BOUND ( 'NONE', #57663, .T. ) ;
#70684=CARTESIAN_POINT ( 'NONE',  ( 5.082755093536324154, 15.28124999795161187, 5.082755093536326818 ) ) ;
#70687=CARTESIAN_POINT ( 'NONE',  ( 2.977408999572651815, 14.06249999795161365, 7.188101187500000933 ) ) ;
#70697=VECTOR ( 'NONE', #29408, 1000.000000000000000 ) ;
#70699=CARTESIAN_POINT ( 'NONE',  ( 2.977408999572654480, 114.1250000020483952, 7.188101187499999156 ) ) ;
#70703=CARTESIAN_POINT ( 'NONE',  ( -2.977408999572650039, 23.43749999795161187, -7.188101187500000933 ) ) ;
#70710=CARTESIAN_POINT ( 'NONE',  ( -5.082755093536325930, 98.84375000204838102, -5.082755093536325930 ) ) ;
#70728=CARTESIAN_POINT ( 'NONE',  ( 8.000000000000000000, 97.43750000409677625, -9.797174393178825657E-16 ) ) ;
#70738=CARTESIAN_POINT ( 'NONE',  ( -7.683012701892240059, 124.8169872981077901, 0.000000000000000000 ) ) ;
#70742=CARTESIAN_POINT ( 'NONE',  ( 1.320432766682874540E-15, 117.0312500020483810, 7.188101187500000044 ) ) ;
#70747=CARTESIAN_POINT ( 'NONE',  ( -3.313708498984805573, 26.53125000000000000, 7.999999999999956479 ) ) ;
#70750=CARTESIAN_POINT ( 'NONE',  ( -4.898587196589412829E-16, 100.6249999999999858, -8.000000000000000000 ) ) ;
#70754=ORIENTED_EDGE ( 'NONE', *, *, #16478, .T. ) ;
#70767=CARTESIAN_POINT ( 'NONE',  ( 3.313708498984679895, 112.7187500040968047, -8.000000000000081712 ) ) ;
#70772=CARTESIAN_POINT ( 'NONE',  ( -2.977408999572654480, 12.37499999795161187, 7.188101187499999156 ) ) ;
#70777=LINE ( 'NONE', #19090, #39249 ) ;
#70779=DIRECTION ( 'NONE',  ( -0.000000000000000000, 1.000000000000000000, -0.000000000000000000 ) ) ;
#70787=CARTESIAN_POINT ( 'NONE',  ( -8.000000000000000000, 23.15625000000000000, -3.313708498984762496 ) ) ;
#70799=CARTESIAN_POINT ( 'NONE',  ( 5.082755093536324154, 7.781249997951611874, 5.082755093536326818 ) ) ;
#70801=CARTESIAN_POINT ( 'NONE',  ( 7.188101187500000044, 117.7812500020483810, -8.802885111219163269E-16 ) ) ;
#70832=CARTESIAN_POINT ( 'NONE',  ( -5.082755093536324154, 94.71875000204838102, 5.082755093536326818 ) ) ;
#70842=DIRECTION ( 'NONE',  ( 0.000000000000000000, 0.000000000000000000, 1.000000000000000000 ) ) ;
#70856=CARTESIAN_POINT ( 'NONE',  ( 2.977408999572650039, 92.56250000204838102, -7.188101187500001821 ) ) ;
#70864=CARTESIAN_POINT ( 'NONE',  ( -7.999999999999998224, 122.0937500000000000, 3.313708498984766049 ) ) ;
#70871=ORIENTED_EDGE ( 'NONE', *, *, #33912, .T. ) ;
#70873=( BOUNDED_CURVE ( )  B_SPLINE_CURVE ( 2, ( #44516, #62601, #10931, #32840, #10559, #33590, #62982, #33968, #50914 ),
 .UNSPECIFIED., .F., .F. ) 
 B_SPLINE_CURVE_WITH_KNOTS ( ( 3, 2, 2, 2, 3 ),
 ( 0.5972222222222222099, 0.6041666666666666297, 0.6111111111111111605, 0.6180555555555554692, 0.6249999999999998890 ),
 .UNSPECIFIED. ) 
 CURVE ( )  GEOMETRIC_REPRESENTATION_ITEM ( )  RATIONAL_B_SPLINE_CURVE ( ( 1.000000000000000000, 0.9238795325112867385, 1.000000000000000000, 0.9238795325112867385, 1.000000000000000000, 0.9238795325112867385, 1.000000000000000000, 0.9238795325112879597, 0.9999999999999987788 ) ) 
 REPRESENTATION_ITEM ( '' )  );
#70876=CARTESIAN_POINT ( 'NONE',  ( -4.898587196589412829E-16, 97.81250000409677625, -8.000000000000000000 ) ) ;
#70886=CARTESIAN_POINT ( 'NONE',  ( -2.977408999572650927, 96.87500000204836681, -7.188101187500001821 ) ) ;
#70908=CARTESIAN_POINT ( 'NONE',  ( -5.656854249492379694, 4.874999995903221084, -5.656854249492380582 ) ) ;
#70910=CARTESIAN_POINT ( 'NONE',  ( 7.188101187500001821, 8.437499997951611874, -2.977408999572650483 ) ) ;
#70913=CARTESIAN_POINT ( 'NONE',  ( 5.082755093536325042, 108.9687500020483810, -5.082755093536325930 ) ) ;
#70922=CARTESIAN_POINT ( 'NONE',  ( 1.469576158976823947E-15, 111.8750000000000000, 8.000000000000000000 ) ) ;
#70924=ORIENTED_EDGE ( 'NONE', *, *, #9530, .T. ) ;
#70931=DIRECTION ( 'NONE',  ( -0.000000000000000000, 1.000000000000000000, -0.000000000000000000 ) ) ;
#70932=CARTESIAN_POINT ( 'NONE',  ( 7.188101187500002709, 108.3125000020483810, 2.977408999572649151 ) ) ;
#70937=CARTESIAN_POINT ( 'NONE',  ( -7.188101187499999156, 106.6250000020483952, 2.977408999572654924 ) ) ;
#70947=CARTESIAN_POINT ( 'NONE',  ( 5.656854249492378806, 14.81250000000000355, 5.656854249492381470 ) ) ;
#70958=CARTESIAN_POINT ( 'NONE',  ( 8.000000000000000000, 3.000000000000000444, 0.000000000000000000 ) ) ;
#70961=CARTESIAN_POINT ( 'NONE',  ( 2.977408999572651815, 1.687499997951610098, 7.188101187500000933 ) ) ;
#70962=CARTESIAN_POINT ( 'NONE',  ( 8.000000000000001776, 116.8437500040967905, 3.313708498984759387 ) ) ;
#70988=CARTESIAN_POINT ( 'NONE',  ( 1.469576158976823947E-15, 117.8750000000000000, 8.000000000000000000 ) ) ;
#70991=CARTESIAN_POINT ( 'NONE',  ( 3.313708498984762496, 16.03124999590322375, 7.999999999999998224 ) ) ;
#71005=CARTESIAN_POINT ( 'NONE',  ( 3.313708498984761608, 10.59374999590322020, -8.000000000000000000 ) ) ;
#71014=CARTESIAN_POINT ( 'NONE',  ( -2.977408999572650927, 123.8750000020483952, -7.188101187500000933 ) ) ;
#71019=CARTESIAN_POINT ( 'NONE',  ( 7.188101187500002709, 93.31250000204838102, 2.977408999572649151 ) ) ;
#71043=CARTESIAN_POINT ( 'NONE',  ( -1.320432766682874540E-15, 15.09374999795161187, 7.188101187500000044 ) ) ;
#71046=CARTESIAN_POINT ( 'NONE',  ( -2.977408999572654480, 13.87499999795161365, 7.188101187499999156 ) ) ;
#71055=EDGE_CURVE ( 'NONE', #64958, #65034, #69451, .T. ) ;
#71059=CARTESIAN_POINT ( 'NONE',  ( -7.188101187500000044, 107.6562500020483810, 0.000000000000000000 ) ) ;
#71060=LINE ( 'NONE', #64311, #15108 ) ;
#71062=ORIENTED_EDGE ( 'NONE', *, *, #37634, .T. ) ;
#71063=CARTESIAN_POINT ( 'NONE',  ( -7.188101187500000044, 20.71874999795161543, -8.802885111219163269E-16 ) ) ;
#71069=CARTESIAN_POINT ( 'NONE',  ( -5.082755093536325930, 97.34375000204838102, -5.082755093536325930 ) ) ;
#71072=CARTESIAN_POINT ( 'NONE',  ( 9.797174393178825657E-16, 125.0000000000000000, -8.000000000000000000 ) ) ;
#71091=CYLINDRICAL_SURFACE ( 'NONE', #47116, 8.000000000000000000 ) ;
#71100=CARTESIAN_POINT ( 'NONE',  ( 7.188101187500001821, 113.0000000020483668, -2.977408999572651371 ) ) ;
#71106=ORIENTED_EDGE ( 'NONE', *, *, #765, .T. ) ;
#71127=CARTESIAN_POINT ( 'NONE',  ( 2.977408999572652260, 11.06249999795161187, 7.188101187500000044 ) ) ;
#71145=CARTESIAN_POINT ( 'NONE',  ( -8.000000000000000000, 24.65625000000000355, -3.313708498984762496 ) ) ;
#71157=CARTESIAN_POINT ( 'NONE',  ( -7.188101187500000044, 2.718749997951610098, -8.802885111219163269E-16 ) ) ;
#71159=CARTESIAN_POINT ( 'NONE',  ( 5.082755093536326818, 120.5937500020483952, 5.082755093536325042 ) ) ;
#71165=ORIENTED_EDGE ( 'NONE', *, *, #62975, .F. ) ;
#71174=CARTESIAN_POINT ( 'NONE',  ( -4.898587196589412829E-16, 97.62499999999998579, -8.000000000000000000 ) ) ;
#71189=CARTESIAN_POINT ( 'NONE',  ( 7.188101187500000933, 90.87500000204836681, -2.977408999572651371 ) ) ;
#71231=CARTESIAN_POINT ( 'NONE',  ( 8.000000000000000000, 18.09375000000000355, -3.313708498984761164 ) ) ;
#71234=CARTESIAN_POINT ( 'NONE',  ( -7.999999999999998224, 98.28125000409677625, 3.313708498984766493 ) ) ;
#71245=CARTESIAN_POINT ( 'NONE',  ( 7.188101187500001821, 98.00000000204838102, -2.977408999572651371 ) ) ;
#71265=CARTESIAN_POINT ( 'NONE',  ( -1.469576158976823947E-15, 2.437499995903220196, 8.000000000000000000 ) ) ;
#71267=CARTESIAN_POINT ( 'NONE',  ( -1.320432766682874540E-15, 10.96874999795161187, 7.188101187500000044 ) ) ;
#71271=CARTESIAN_POINT ( 'NONE',  ( -7.188101187500000044, 108.0312500020483810, 0.000000000000000000 ) ) ;
#71291=CARTESIAN_POINT ( 'NONE',  ( -7.188101187500000933, 103.0625000020483810, -2.977408999572650483 ) ) ;
#71298=CARTESIAN_POINT ( 'NONE',  ( 7.188101187500002709, 110.1875000020483810, 2.977408999572649151 ) ) ;
#71316=CARTESIAN_POINT ( 'NONE',  ( 7.999999999999998224, 20.71874999590322375, 3.313708498984766049 ) ) ;
#71321=ORIENTED_EDGE ( 'NONE', *, *, #65427, .F. ) ;
#71323=CARTESIAN_POINT ( 'NONE',  ( 3.313708498984762052, 13.78125000000000178, -8.000000000000000000 ) ) ;
#71325=CARTESIAN_POINT ( 'NONE',  ( -2.977408999572650039, 5.437499997951610986, -7.188101187500001821 ) ) ;
#71326=CARTESIAN_POINT ( 'NONE',  ( 1.469576158976823947E-15, 113.5625000040967905, 8.000000000000000000 ) ) ;
#71328=CYLINDRICAL_SURFACE ( 'NONE', #59658, 8.000000000000000000 ) ;
#71338=VECTOR ( 'NONE', #59517, 1000.000000000000000 ) ;
#71342=ORIENTED_EDGE ( 'NONE', *, *, #51817, .T. ) ;
#71350=CARTESIAN_POINT ( 'NONE',  ( 5.656854249492381470, 113.5625000000000000, 5.656854249492379694 ) ) ;
#71354=CARTESIAN_POINT ( 'NONE',  ( 8.000000000000000000, 20.81249999590322375, 0.000000000000000000 ) ) ;
#71365=CARTESIAN_POINT ( 'NONE',  ( 1.469576158976823947E-15, 107.5625000040967905, 8.000000000000000000 ) ) ;
#71381=CARTESIAN_POINT ( 'NONE',  ( 3.594050593751920264, 89.15552362291687416, -6.225078233346985179 ) ) ;
#71387=EDGE_CURVE ( 'NONE', #26713, #5359, #40581, .T. ) ;
#71392=DIRECTION ( 'NONE',  ( -0.000000000000000000, 1.000000000000000000, -0.000000000000000000 ) ) ;
#71396=ORIENTED_EDGE ( 'NONE', *, *, #24659, .F. ) ;
#71412=CARTESIAN_POINT ( 'NONE',  ( -2.977408999572654480, 22.49999999795161543, 7.188101187499999156 ) ) ;
#71415=CARTESIAN_POINT ( 'NONE',  ( 5.082755093536325930, 14.53124999795161187, -5.082755093536325930 ) ) ;
#71424=CARTESIAN_POINT ( 'NONE',  ( -5.082755093536325930, 113.4687500020483810, -5.082755093536325930 ) ) ;
#71428=CARTESIAN_POINT ( 'NONE',  ( -1.320432766682874540E-15, 24.09374999795161543, 7.188101187500000044 ) ) ;
#71434=CARTESIAN_POINT ( 'NONE',  ( 5.082755093536326818, 92.09375000204838102, 5.082755093536325042 ) ) ;
#71452=CARTESIAN_POINT ( 'NONE',  ( 0.000000000000000000, 125.0000000000000000, 0.000000000000000000 ) ) ;
#71457=CIRCLE ( 'NONE', #32951, 8.000000000000000000 ) ;
#71459=EDGE_CURVE ( 'NONE', #11019, #66661, #20292, .T. ) ;
#71467=CARTESIAN_POINT ( 'NONE',  ( 2.977408999572654480, 111.1250000020483810, 7.188101187499999156 ) ) ;
#71473=VERTEX_POINT ( 'NONE', #41395 ) ;
#71474=CARTESIAN_POINT ( 'NONE',  ( 8.000000000000000000, 93.03125000409677625, -3.313708498984762496 ) ) ;
#71495=CARTESIAN_POINT ( 'NONE',  ( 7.188101187499999156, 12.74999999795161187, 2.977408999572654924 ) ) ;
#71513=CARTESIAN_POINT ( 'NONE',  ( 5.656854249492378806, 25.31250000000000355, 5.656854249492381470 ) ) ;
#71523=CARTESIAN_POINT ( 'NONE',  ( -7.188101187500000933, 4.124999997951610986, -2.977408999572651371 ) ) ;
#71526=CARTESIAN_POINT ( 'NONE',  ( -7.188101187500000044, 112.5312500020483952, 0.000000000000000000 ) ) ;
#71541=CARTESIAN_POINT ( 'NONE',  ( 8.000000000000000000, 98.74999999999998579, -9.797174393178825657E-16 ) ) ;
#71558=CARTESIAN_POINT ( 'NONE',  ( -2.977408999572650927, 89.75000000204838102, -7.188101187500000933 ) ) ;
#71566=FACE_OUTER_BOUND ( 'NONE', #69542, .T. ) ;
#71567=CARTESIAN_POINT ( 'NONE',  ( -8.000000000000001776, 9.656249995903223748, 3.313708498984759387 ) ) ;
#71575=CARTESIAN_POINT ( 'NONE',  ( 3.313708498984761608, 24.09374999590322375, -8.000000000000000000 ) ) ;
#71582=CARTESIAN_POINT ( 'NONE',  ( 5.082755093536325042, 90.96875000204838102, -5.082755093536325930 ) ) ;
#71588=ORIENTED_EDGE ( 'NONE', *, *, #44091, .T. ) ;
#71591=CARTESIAN_POINT ( 'NONE',  ( 7.999999999999998224, 14.71874999590322020, 3.313708498984766049 ) ) ;
#71596=DIRECTION ( 'NONE',  ( -0.000000000000000000, 1.000000000000000000, -0.000000000000000000 ) ) ;
#71603=CARTESIAN_POINT ( 'NONE',  ( 5.656854249492381470, 97.25000000409677625, 5.656854249492379694 ) ) ;
#71610=CARTESIAN_POINT ( 'NONE',  ( 4.898587196589412829E-16, 7.875000000000001776, -8.000000000000000000 ) ) ;
#71614=CARTESIAN_POINT ( 'NONE',  ( 7.188101187500002709, 97.81250000204840944, 2.977408999572649151 ) ) ;
#71615=DIRECTION ( 'NONE',  ( 0.000000000000000000, 0.000000000000000000, 1.000000000000000000 ) ) ;
#71633=CARTESIAN_POINT ( 'NONE',  ( -7.999999999999998224, 90.78125000409680467, 3.313708498984766049 ) ) ;
#71636=CARTESIAN_POINT ( 'NONE',  ( 5.656854249492380582, 5.999999995903221084, -5.656854249492380582 ) ) ;
#71639=CARTESIAN_POINT ( 'NONE',  ( -2.977408999572650039, 8.812499997951611874, -7.188101187500001821 ) ) ;
#71643=CARTESIAN_POINT ( 'NONE',  ( 7.188101187500000044, 108.7812500020483810, -8.802885111219163269E-16 ) ) ;
#71660=CARTESIAN_POINT ( 'NONE',  ( 8.000000000000000000, 25.31249999590322375, 0.000000000000000000 ) ) ;
#71661=CARTESIAN_POINT ( 'NONE',  ( -5.082755093536325930, 101.4687500020483810, -5.082755093536325930 ) ) ;
#71668=CARTESIAN_POINT ( 'NONE',  ( -5.082755093536325930, 109.3437500020483810, -5.082755093536325930 ) ) ;
#71678=CARTESIAN_POINT ( 'NONE',  ( -2.977408999572654480, 1.874999997951610320, 7.188101187499999156 ) ) ;
#71684=EDGE_CURVE ( 'NONE', #74424, #44243, #38384, .T. ) ;
#71686=CARTESIAN_POINT ( 'NONE',  ( -5.656854249492380582, 122.0000000040967905, -5.656854249492380582 ) ) ;
#71693=CARTESIAN_POINT ( 'NONE',  ( -7.188101187500001821, 7.124999997951610098, -2.977408999572651371 ) ) ;
#71695=CARTESIAN_POINT ( 'NONE',  ( 1.469576158976823947E-15, 118.0625000040967763, 8.000000000000000000 ) ) ;
#71703=CARTESIAN_POINT ( 'NONE',  ( -1.469576158976823947E-15, 18.93749999590322020, 8.000000000000000000 ) ) ;
#71721=CARTESIAN_POINT ( 'NONE',  ( 1.469576158976823947E-15, 113.3750000000000000, 8.000000000000000000 ) ) ;
#71727=CARTESIAN_POINT ( 'NONE',  ( 3.313708498984762496, 23.53124999590322375, 7.999999999999998224 ) ) ;
#71739=CARTESIAN_POINT ( 'NONE',  ( -8.000000000000000000, 99.68750000409677625, 0.000000000000000000 ) ) ;
#71750=CARTESIAN_POINT ( 'NONE',  ( 1.320432766682874540E-15, 123.0312500020483810, 7.188101187500000044 ) ) ;
#71756=VECTOR ( 'NONE', #66904, 1000.000000000000000 ) ;
#71757=CARTESIAN_POINT ( 'NONE',  ( -5.082755093536325930, 124.3437500020483952, -5.082755093536325930 ) ) ;
#71772=ORIENTED_EDGE ( 'NONE', *, *, #46697, .F. ) ;
#71785=CARTESIAN_POINT ( 'NONE',  ( -5.082755093536326818, 19.40624999795161543, 5.082755093536325042 ) ) ;
#71788=CARTESIAN_POINT ( 'NONE',  ( 4.401442555609581635E-16, 10.21874999795161187, -7.188101187500000044 ) ) ;
#71799=CARTESIAN_POINT ( 'NONE',  ( 5.082755093536325042, 113.0937500020483810, -5.082755093536325930 ) ) ;
#71812=CARTESIAN_POINT ( 'NONE',  ( -7.188101187500001821, 92.93750000204839523, -2.977408999572650483 ) ) ;
#71817=CARTESIAN_POINT ( 'NONE',  ( 3.313708498984761608, 12.28125000000000178, -8.000000000000000000 ) ) ;
#71841=CARTESIAN_POINT ( 'NONE',  ( -7.188101187500000044, 107.6562500020483810, 0.000000000000000000 ) ) ;
#71846=CARTESIAN_POINT ( 'NONE',  ( -1.469576158976823947E-15, 26.62500000000000355, 8.000000000000000000 ) ) ;
#71870=CARTESIAN_POINT ( 'NONE',  ( -5.082755093536325042, 20.90624999795161543, -5.082755093536325930 ) ) ;
#71878=CARTESIAN_POINT ( 'NONE',  ( 5.082755093536325930, 3.656249997951610542, -5.082755093536325930 ) ) ;
#71887=EDGE_CURVE ( 'NONE', #25519, #65440, #5173, .T. ) ;
#71898=CARTESIAN_POINT ( 'NONE',  ( 2.977408999572650927, 5.249999997951610986, -7.188101187500000933 ) ) ;
#71903=CARTESIAN_POINT ( 'NONE',  ( 5.082755093536326818, 111.5937500020483810, 5.082755093536325042 ) ) ;
#71905=CARTESIAN_POINT ( 'NONE',  ( 7.594050593750000466, 0.2343749989758049379, 0.000000000000000000 ) ) ;
#71918=CARTESIAN_POINT ( 'NONE',  ( 5.656854249492381470, 95.56250000000000000, 5.656854249492379694 ) ) ;
#71926=CARTESIAN_POINT ( 'NONE',  ( 5.656854249492381470, 100.0625000000000000, 5.656854249492379694 ) ) ;
#71933=CARTESIAN_POINT ( 'NONE',  ( 7.188101187500002709, 90.68750000204838102, 2.977408999572649151 ) ) ;
#71943=CARTESIAN_POINT ( 'NONE',  ( -3.313708498984789141, 108.4062500040967763, -7.999999999999974243 ) ) ;
#71956=EDGE_CURVE ( 'NONE', #33110, #11312, #30884, .T. ) ;
#71969=DIRECTION ( 'NONE',  ( 0.000000000000000000, 0.000000000000000000, 1.000000000000000000 ) ) ;
#71980=CARTESIAN_POINT ( 'NONE',  ( -5.656854249492378806, 95.37500000409677625, 5.656854249492381470 ) ) ;
#71983=( BOUNDED_CURVE ( )  B_SPLINE_CURVE ( 2, ( #61692, #33045, #56045, #38313, #68459, #62788, #44341, #4354, #73380 ),
 .UNSPECIFIED., .F., .F. ) 
 B_SPLINE_CURVE_WITH_KNOTS ( ( 3, 2, 2, 2, 3 ),
 ( 0.9270833333333335924, 0.9322916666666667407, 0.9375000000000000000, 0.9427083333333333703, 0.9479166666666665186 ),
 .UNSPECIFIED. ) 
 CURVE ( )  GEOMETRIC_REPRESENTATION_ITEM ( )  RATIONAL_B_SPLINE_CURVE ( ( 0.9999999999999967804, 0.9238795325112899581, 1.000000000000000000, 0.9238795325112867385, 1.000000000000000000, 0.9238795325112867385, 1.000000000000000000, 0.9238795325112884038, 0.9999999999999983347 ) ) 
 REPRESENTATION_ITEM ( '' )  );
#71990=CARTESIAN_POINT ( 'NONE',  ( 5.082755093536326818, 93.21875000204838102, 5.082755093536325042 ) ) ;
#72014=CARTESIAN_POINT ( 'NONE',  ( -7.188101187500002709, 13.68749999795161365, 2.977408999572649151 ) ) ;
#72017=CARTESIAN_POINT ( 'NONE',  ( -7.188101187499999156, 109.6250000020483952, 2.977408999572654924 ) ) ;
#72020=LINE ( 'NONE', #32048, #56852 ) ;
#72034=CARTESIAN_POINT ( 'NONE',  ( 2.977408999572654480, 102.1250000020483810, 7.188101187499999156 ) ) ;
#72040=CARTESIAN_POINT ( 'NONE',  ( 5.082755093536325042, 107.4687500020483952, -5.082755093536325930 ) ) ;
#72065=ORIENTED_EDGE ( 'NONE', *, *, #4407, .F. ) ;
#72068=CARTESIAN_POINT ( 'NONE',  ( -7.188101187500001821, 10.12499999795161187, -2.977408999572651371 ) ) ;
#72069=CARTESIAN_POINT ( 'NONE',  ( -8.000000000000000000, 117.5937500040967905, -3.313708498984761608 ) ) ;
#72097=CARTESIAN_POINT ( 'NONE',  ( -3.313708498984815343, 111.2187500000000000, -7.999999999999944933 ) ) ;
#72100=CARTESIAN_POINT ( 'NONE',  ( -8.000000000000000000, 113.0000000000000000, 0.000000000000000000 ) ) ;
#72106=CARTESIAN_POINT ( 'NONE',  ( 5.656854249492380582, 20.99999999590322375, -5.656854249492380582 ) ) ;
#72128=CARTESIAN_POINT ( 'NONE',  ( 7.188101187500000044, 118.9062500020483810, -8.802885111219163269E-16 ) ) ;
#72129=FACE_OUTER_BOUND ( 'NONE', #28117, .T. ) ;
#72134=CARTESIAN_POINT ( 'NONE',  ( 2.977408999572654480, 90.12500000204836681, 7.188101187499999156 ) ) ;
#72160=CARTESIAN_POINT ( 'NONE',  ( -7.188101187500000044, 19.21874999795161543, -8.802885111219163269E-16 ) ) ;
#72163=CARTESIAN_POINT ( 'NONE',  ( -1.320432766682874540E-15, 18.46874999795161187, 7.188101187500000044 ) ) ;
#72175=CARTESIAN_POINT ( 'NONE',  ( 1.320432766682874540E-15, 109.5312500020483810, 7.188101187500000044 ) ) ;
#72188=CARTESIAN_POINT ( 'NONE',  ( -2.977408999572651815, 94.81250000204838102, 7.188101187500000933 ) ) ;
#72194=CARTESIAN_POINT ( 'NONE',  ( 4.898587196589412829E-16, 12.37500000000000178, -8.000000000000000000 ) ) ;
#72202=CYLINDRICAL_SURFACE ( 'NONE', #28372, 8.000000000000000000 ) ;
#72216=CARTESIAN_POINT ( 'NONE',  ( -5.656854249492378806, 116.1875000000000000, 5.656854249492381470 ) ) ;
#72219=CARTESIAN_POINT ( 'NONE',  ( 5.082755093536325042, 110.0937500020483810, -5.082755093536325930 ) ) ;
#72249=CARTESIAN_POINT ( 'NONE',  ( 7.188101187500000933, 20.43749999795161543, -2.977408999572650483 ) ) ;
#72259=CARTESIAN_POINT ( 'NONE',  ( -2.977408999572650039, 2.437499997951610542, -7.188101187500001821 ) ) ;
#72262=CARTESIAN_POINT ( 'NONE',  ( -5.656854249492381470, 17.24999999590322375, 5.656854249492379694 ) ) ;
#72275=CARTESIAN_POINT ( 'NONE',  ( -3.313708498984800688, 21.46875000000000000, -7.999999999999958256 ) ) ;
#72277=CARTESIAN_POINT ( 'NONE',  ( -1.320432766682874540E-15, 13.59374999795161187, 7.188101187500000044 ) ) ;
#72282=CARTESIAN_POINT ( 'NONE',  ( 7.188101187500002709, 113.1875000020483810, 2.977408999572649151 ) ) ;
#72298=CARTESIAN_POINT ( 'NONE',  ( -3.313708498984762052, 96.21875000000000000, -8.000000000000000000 ) ) ;
#72314=CARTESIAN_POINT ( 'NONE',  ( -7.188101187500000933, 91.43750000204838102, -2.977408999572650483 ) ) ;
#72319=CARTESIAN_POINT ( 'NONE',  ( -5.656854249492380582, 96.31250000000000000, -5.656854249492380582 ) ) ;
#72323=CARTESIAN_POINT ( 'NONE',  ( -5.082755093536326818, 17.90624999795161187, 5.082755093536325042 ) ) ;
#72332=CARTESIAN_POINT ( 'NONE',  ( 8.000000000000000000, 23.81249999590322020, 0.000000000000000000 ) ) ;
#72345=EDGE_CURVE ( 'NONE', #36065, #24466, #42980, .T. ) ;
#72358=AXIS2_PLACEMENT_3D ( 'NONE', #61807, #4473, #71615 ) ;
#72364=CARTESIAN_POINT ( 'NONE',  ( -3.313708498984762496, 95.46875000409679046, 7.999999999999998224 ) ) ;
#72373=DIRECTION ( 'NONE',  ( -0.000000000000000000, 1.000000000000000000, -0.000000000000000000 ) ) ;
#72374=CARTESIAN_POINT ( 'NONE',  ( 7.188101187500000044, 93.40625000204838102, -8.802885111219163269E-16 ) ) ;
#72386=CARTESIAN_POINT ( 'NONE',  ( -8.000000000000000000, 105.5937500040967763, -3.313708498984761164 ) ) ;
#72393=( BOUNDED_CURVE ( )  B_SPLINE_CURVE ( 2, ( #16408, #72275, #50385, #44732, #67749, #62079, #45102, #10403, #33429 ),
 .UNSPECIFIED., .F., .F. ) 
 B_SPLINE_CURVE_WITH_KNOTS ( ( 3, 2, 2, 2, 3 ),
 ( 0.7916666666666667407, 0.7986111111111111605, 0.8055555555555555802, 0.8124999999999998890, 0.8194444444444443088 ),
 .UNSPECIFIED. ) 
 CURVE ( )  GEOMETRIC_REPRESENTATION_ITEM ( )  RATIONAL_B_SPLINE_CURVE ( ( 0.9999999999999987788, 0.9238795325112879597, 1.000000000000000000, 0.9238795325112867385, 1.000000000000000000, 0.9238795325112867385, 1.000000000000000000, 0.9238795325112879597, 0.9999999999999987788 ) ) 
 REPRESENTATION_ITEM ( '' )  );
#72396=CARTESIAN_POINT ( 'NONE',  ( 4.898587196589412829E-16, 4.687499995903220196, -8.000000000000000000 ) ) ;
#72397=EDGE_CURVE ( 'NONE', #3980, #66991, #50708, .T. ) ;
#72399=CARTESIAN_POINT ( 'NONE',  ( 7.188101187500000044, 9.843749997951610098, 0.000000000000000000 ) ) ;
#72402=CARTESIAN_POINT ( 'NONE',  ( 1.320432766682874540E-15, 108.4062500020483810, 7.188101187500000044 ) ) ;
#72413=ORIENTED_EDGE ( 'NONE', *, *, #19956, .T. ) ;
#72421=CIRCLE ( 'NONE', #68817, 8.000000000000000000 ) ;
#72423=CARTESIAN_POINT ( 'NONE',  ( 5.082755093536325042, 98.09375000204838102, -5.082755093536325930 ) ) ;
#72430=CARTESIAN_POINT ( 'NONE',  ( 2.977408999572650039, 110.5625000020483810, -7.188101187500001821 ) ) ;
#72442=CARTESIAN_POINT ( 'NONE',  ( 7.188101187499999156, 2.249999997951610098, 2.977408999572654924 ) ) ;
#72455=ORIENTED_EDGE ( 'NONE', *, *, #10268, .F. ) ;
#72459=CARTESIAN_POINT ( 'NONE',  ( 7.188101187499999156, 9.374999997951610098, 2.977408999572654924 ) ) ;
#72460=CARTESIAN_POINT ( 'NONE',  ( -7.999999999999998224, 116.2812500040967620, 3.313708498984766493 ) ) ;
#72478=VERTEX_POINT ( 'NONE', #48665 ) ;
#72487=CARTESIAN_POINT ( 'NONE',  ( -3.313708498984762496, 113.2812500000000000, 7.999999999999998224 ) ) ;
#72491=CARTESIAN_POINT ( 'NONE',  ( 5.656854249492380582, 19.68750000000000355, -5.656854249492380582 ) ) ;
#72492=CARTESIAN_POINT ( 'NONE',  ( -8.000000000000000000, 18.46874999590322020, -3.313708498984762496 ) ) ;
#72516=CARTESIAN_POINT ( 'NONE',  ( 5.082755093536326818, 115.7187500020483810, 5.082755093536325042 ) ) ;
#72522=CARTESIAN_POINT ( 'NONE',  ( -7.188101187500000044, 91.15625000204838102, 0.000000000000000000 ) ) ;
#72550=CARTESIAN_POINT ( 'NONE',  ( -2.977408999572650039, 21.93749999795161543, -7.188101187500001821 ) ) ;
#72553=CARTESIAN_POINT ( 'NONE',  ( 2.977408999572650927, 17.62499999795161543, -7.188101187500001821 ) ) ;
#72577=CARTESIAN_POINT ( 'NONE',  ( -4.401442555609581635E-16, 97.15625000204839523, -7.188101187500000044 ) ) ;
#72590=LINE ( 'NONE', #56361, #53634 ) ;
#72607=CARTESIAN_POINT ( 'NONE',  ( -7.188101187500000044, 112.1562500020483952, 0.000000000000000000 ) ) ;
#72623=CARTESIAN_POINT ( 'NONE',  ( -8.000000000000000000, 93.40625000000000000, -3.313708498984761164 ) ) ;
#72631=CARTESIAN_POINT ( 'NONE',  ( -8.000000000000000000, 109.9062500000000000, -3.313708498984761164 ) ) ;
#72635=CARTESIAN_POINT ( 'NONE',  ( 2.977408999572650927, 19.12499999795161898, -7.188101187500000933 ) ) ;
#72644=CARTESIAN_POINT ( 'NONE',  ( -7.188101187500002709, 1.312499997951610098, 2.977408999572649151 ) ) ;
#72647=CARTESIAN_POINT ( 'NONE',  ( -3.313708498984765161, 17.34374999590322375, 7.999999999999998224 ) ) ;
#72661=CARTESIAN_POINT ( 'NONE',  ( 7.188101187500000044, 13.96874999795161187, 0.000000000000000000 ) ) ;
#72667=CARTESIAN_POINT ( 'NONE',  ( -7.188101187500000044, 111.0312500020483810, 0.000000000000000000 ) ) ;
#72681=CARTESIAN_POINT ( 'NONE',  ( 0.000000000000000000, 125.0000000000000000, 0.000000000000000000 ) ) ;
#72683=CARTESIAN_POINT ( 'NONE',  ( -3.313708498984762496, 95.28125000000000000, 7.999999999999998224 ) ) ;
#72698=VECTOR ( 'NONE', #54589, 1000.000000000000000 ) ;
#72706=CARTESIAN_POINT ( 'NONE',  ( 8.000000000000000000, 92.84375000000000000, -3.313708498984762496 ) ) ;
#72707=CARTESIAN_POINT ( 'NONE',  ( 2.977408999572650927, 21.74999999795162253, -7.188101187500001821 ) ) ;
#72721=CARTESIAN_POINT ( 'NONE',  ( -1.469576158976823947E-15, 21.93749999590322375, 8.000000000000000000 ) ) ;
#72742=( BOUNDED_CURVE ( )  B_SPLINE_CURVE ( 2, ( #43339, #48626, #55057, #71633, #21082, #19955, #44106, #66357, #67115 ),
 .UNSPECIFIED., .F., .F. ) 
 B_SPLINE_CURVE_WITH_KNOTS ( ( 3, 2, 2, 2, 3 ),
 ( 0.9062500000000002220, 0.9114583333333335924, 0.9166666666666668517, 0.9218750000000002220, 0.9270833333333335924 ),
 .UNSPECIFIED. ) 
 CURVE ( )  GEOMETRIC_REPRESENTATION_ITEM ( )  RATIONAL_B_SPLINE_CURVE ( ( 0.9999999999999967804, 0.9238795325112899581, 1.000000000000000000, 0.9238795325112867385, 1.000000000000000000, 0.9238795325112867385, 1.000000000000000000, 0.9238795325112835188, 1.000000000000003331 ) ) 
 REPRESENTATION_ITEM ( '' )  );
#72744=CARTESIAN_POINT ( 'NONE',  ( 4.898587196589412829E-16, 10.87500000000000178, -8.000000000000000000 ) ) ;
#72746=CARTESIAN_POINT ( 'NONE',  ( -5.656854249492380582, 89.00000000409677625, -5.656854249492380582 ) ) ;
#72748=AXIS2_PLACEMENT_3D ( 'NONE', #13332, #35636, #24300 ) ;
#72757=CARTESIAN_POINT ( 'NONE',  ( -5.082755093536324154, 94.34375000204838102, 5.082755093536326818 ) ) ;
#72779=CARTESIAN_POINT ( 'NONE',  ( -1.469576158976823947E-15, 6.937499995903221084, 8.000000000000000000 ) ) ;
#72782=CARTESIAN_POINT ( 'NONE',  ( -5.082755093536326818, 9.281249997951610098, 5.082755093536325042 ) ) ;
#72785=CARTESIAN_POINT ( 'NONE',  ( 5.082755093536326818, 105.5937500020483810, 5.082755093536325042 ) ) ;
#72802=CARTESIAN_POINT ( 'NONE',  ( -7.188101187500000933, 98.56250000204838102, -2.977408999572650483 ) ) ;
#72809=CARTESIAN_POINT ( 'NONE',  ( -5.082755093536324154, 105.2187500020483952, 5.082755093536326818 ) ) ;
#72834=CARTESIAN_POINT ( 'NONE',  ( 5.082755093536324154, 7.781249997951611874, 5.082755093536326818 ) ) ;
#72835=CARTESIAN_POINT ( 'NONE',  ( -3.313708498984762496, 107.4687500040967763, 7.999999999999998224 ) ) ;
#72853=VERTEX_POINT ( 'NONE', #50911 ) ;
#72856=CARTESIAN_POINT ( 'NONE',  ( 3.313708498984922812, 91.71875000409674783, -7.999999999999837463 ) ) ;
#72862=CARTESIAN_POINT ( 'NONE',  ( -7.999999999999998224, 108.5937499999999858, 3.313708498984766493 ) ) ;
#72869=CARTESIAN_POINT ( 'NONE',  ( 5.656854249492378806, 23.62499999590322020, 5.656854249492381470 ) ) ;
#72872=CARTESIAN_POINT ( 'NONE',  ( 3.313708498984731410, 120.9687500000000000, 8.000000000000031974 ) ) ;
#72890=CARTESIAN_POINT ( 'NONE',  ( 5.082755093536325042, 120.5937500020483952, -5.082755093536325930 ) ) ;
#72895=CARTESIAN_POINT ( 'NONE',  ( 5.082755093536326818, 119.0937500020483810, 5.082755093536325042 ) ) ;
#72897=DIRECTION ( 'NONE',  ( -0.000000000000000000, 1.000000000000000000, -0.000000000000000000 ) ) ;
#72916=VERTEX_POINT ( 'NONE', #56962 ) ;
#72920=CARTESIAN_POINT ( 'NONE',  ( 5.082755093536325930, 20.15624999795161543, -5.082755093536325930 ) ) ;
#72923=CARTESIAN_POINT ( 'NONE',  ( 5.082755093536325930, 20.53124999795161543, -5.082755093536325930 ) ) ;
#72937=CARTESIAN_POINT ( 'NONE',  ( 5.656854249492379694, 94.62500000409677625, -5.656854249492380582 ) ) ;
#72939=ORIENTED_EDGE ( 'NONE', *, *, #55092, .T. ) ;
#72940=CARTESIAN_POINT ( 'NONE',  ( -2.977408999572650039, 26.43749999795162253, -7.188101187500000933 ) ) ;
#72947=CARTESIAN_POINT ( 'NONE',  ( 7.188101187500000044, 93.78125000204836681, -8.802885111219163269E-16 ) ) ;
#72968=CARTESIAN_POINT ( 'NONE',  ( -1.469576158976823947E-15, 5.437499995903221084, 8.000000000000000000 ) ) ;
#72970=CARTESIAN_POINT ( 'NONE',  ( -5.656854249492379694, 17.06250000000000000, -5.656854249492380582 ) ) ;
#72979=CARTESIAN_POINT ( 'NONE',  ( -5.082755093536324154, 110.8437500020483810, 5.082755093536326818 ) ) ;
#72985=VERTEX_POINT ( 'NONE', #24467 ) ;
#73005=CARTESIAN_POINT ( 'NONE',  ( 2.977408999572652260, 15.56249999795161365, 7.188101187500000044 ) ) ;
#73014=CARTESIAN_POINT ( 'NONE',  ( 5.082755093536324154, 1.781249997951610098, 5.082755093536326818 ) ) ;
#73031=CARTESIAN_POINT ( 'NONE',  ( -2.977408999572650039, 11.43749999795161187, -7.188101187500000933 ) ) ;
#73035=CARTESIAN_POINT ( 'NONE',  ( -2.977408999572651815, 111.3125000020483810, 7.188101187500000933 ) ) ;
#73050=CARTESIAN_POINT ( 'NONE',  ( -8.000000000000000000, 95.00000000000000000, 0.000000000000000000 ) ) ;
#73059=EDGE_CURVE ( 'NONE', #22422, #31066, #2577, .T. ) ;
#73075=CARTESIAN_POINT ( 'NONE',  ( -7.188101187500002709, 22.31249999795161187, 2.977408999572649151 ) ) ;
#73082=CARTESIAN_POINT ( 'NONE',  ( 4.898587196589412829E-16, 16.68749999590322375, -8.000000000000000000 ) ) ;
#73093=CARTESIAN_POINT ( 'NONE',  ( 0.000000000000000000, 125.0000000000000000, 0.000000000000000000 ) ) ;
#73106=ORIENTED_EDGE ( 'NONE', *, *, #3917, .F. ) ;
#73112=CARTESIAN_POINT ( 'NONE',  ( 7.999999999999998224, 11.90625000000000355, 3.313708498984766493 ) ) ;
#73113=VECTOR ( 'NONE', #65521, 1000.000000000000000 ) ;
#73115=CARTESIAN_POINT ( 'NONE',  ( -4.898587196589412829E-16, 93.31250000409677625, -8.000000000000000000 ) ) ;
#73127=CARTESIAN_POINT ( 'NONE',  ( -7.188101187500000044, 94.15625000204838102, 0.000000000000000000 ) ) ;
#73148=CARTESIAN_POINT ( 'NONE',  ( 4.898587196589412829E-16, 7.687499995903221084, -8.000000000000000000 ) ) ;
#73151=CARTESIAN_POINT ( 'NONE',  ( 4.401442555609581635E-16, 19.21874999795161543, -7.188101187500000044 ) ) ;
#73154=CARTESIAN_POINT ( 'NONE',  ( 1.320432766682874540E-15, 102.4062500020483810, 7.188101187500000044 ) ) ;
#73167=CARTESIAN_POINT ( 'NONE',  ( 1.469576158976823947E-15, 114.8750000000000000, 8.000000000000000000 ) ) ;
#73174=CARTESIAN_POINT ( 'NONE',  ( 5.082755093536325042, 102.5937500020483668, -5.082755093536325930 ) ) ;
#73181=CARTESIAN_POINT ( 'NONE',  ( 2.977408999572654480, 101.0000000020483810, 7.188101187499999156 ) ) ;
#73186=EDGE_LOOP ( 'NONE', ( #2907, #64481, #36453, #73563 ) ) ;
#73193=CARTESIAN_POINT ( 'NONE',  ( 3.313708498984742068, 8.718749999999998224, 8.000000000000019540 ) ) ;
#73206=VERTEX_POINT ( 'NONE', #27818 ) ;
#73209=CARTESIAN_POINT ( 'NONE',  ( -7.188101187500000044, 5.718749997951611874, -8.802885111219163269E-16 ) ) ;
#73210=CARTESIAN_POINT ( 'NONE',  ( -3.313708498984762496, 110.4687500040967905, 7.999999999999998224 ) ) ;
#73232=CARTESIAN_POINT ( 'NONE',  ( -8.000000000000000000, 111.4062499999999858, -3.313708498984761164 ) ) ;
#73234=CARTESIAN_POINT ( 'NONE',  ( -3.313708498984762052, 105.2187500000000000, -8.000000000000000000 ) ) ;
#73241=CARTESIAN_POINT ( 'NONE',  ( -5.656854249492381470, 27.74999999590322020, 5.656854249492379694 ) ) ;
#73243=CARTESIAN_POINT ( 'NONE',  ( 2.977408999572650039, 122.5625000020483668, -7.188101187500000933 ) ) ;
#73244=CARTESIAN_POINT ( 'NONE',  ( 1.469576158976823947E-15, 113.5625000040967905, 8.000000000000000000 ) ) ;
#73264=CARTESIAN_POINT ( 'NONE',  ( 5.082755093536325042, 119.0937500020483810, -5.082755093536325930 ) ) ;
#73270=CARTESIAN_POINT ( 'NONE',  ( 1.320432766682874540E-15, 120.4062500020483810, 7.188101187500000044 ) ) ;
#73296=CARTESIAN_POINT ( 'NONE',  ( -5.656854249492379694, 2.062500000000000444, -5.656854249492380582 ) ) ;
#73299=CARTESIAN_POINT ( 'NONE',  ( 7.188101187500000044, 17.34374999795161543, 0.000000000000000000 ) ) ;
#73304=DIRECTION ( 'NONE',  ( -0.000000000000000000, 1.000000000000000000, -0.000000000000000000 ) ) ;
#73316=CARTESIAN_POINT ( 'NONE',  ( -2.977408999572654480, 26.99999999795161543, 7.188101187499999156 ) ) ;
#73323=CARTESIAN_POINT ( 'NONE',  ( 5.656854249492379694, 124.4375000000000000, -5.656854249492380582 ) ) ;
#73329=CARTESIAN_POINT ( 'NONE',  ( 3.313708498984742068, 11.71875000000000178, 8.000000000000019540 ) ) ;
#73332=CYLINDRICAL_SURFACE ( 'NONE', #41289, 8.000000000000000000 ) ;
#73352=CARTESIAN_POINT ( 'NONE',  ( -5.082755093536325930, 104.4687500020483952, -5.082755093536325930 ) ) ;
#73376=CARTESIAN_POINT ( 'NONE',  ( 5.082755093536325930, 19.03124999795161543, -5.082755093536325930 ) ) ;
#73380=CARTESIAN_POINT ( 'NONE',  ( 1.469576158976823947E-15, 89.56250000409677625, 8.000000000000000000 ) ) ;
#73384=CARTESIAN_POINT ( 'NONE',  ( -7.188101187500000044, 5.718749997951611874, -8.802885111219163269E-16 ) ) ;
#73403=CARTESIAN_POINT ( 'NONE',  ( 5.082755093536324154, 9.281249997951610098, 5.082755093536326818 ) ) ;
#73407=CARTESIAN_POINT ( 'NONE',  ( -5.082755093536324154, 103.7187500020483810, 5.082755093536326818 ) ) ;
#73421=LINE ( 'NONE', #44756, #12632 ) ;
#73422=CARTESIAN_POINT ( 'NONE',  ( -8.000000000000000000, 93.40624999999998579, -3.313708498984761608 ) ) ;
#73434=CARTESIAN_POINT ( 'NONE',  ( 7.188101187500001821, 119.0000000020483810, -2.977408999572651371 ) ) ;
#73439=CARTESIAN_POINT ( 'NONE',  ( -3.313708498984765161, 13.03125000000000355, 7.999999999999998224 ) ) ;
#73444=CARTESIAN_POINT ( 'NONE',  ( 5.082755093536324154, 18.28124999795161187, 5.082755093536326818 ) ) ;
#73477=CARTESIAN_POINT ( 'NONE',  ( 5.656854249492378806, 11.81250000000000178, 5.656854249492381470 ) ) ;
#73479=CARTESIAN_POINT ( 'NONE',  ( 3.313708498984765161, 92.65625000409680467, 7.999999999999998224 ) ) ;
#73491=CARTESIAN_POINT ( 'NONE',  ( 1.320432766682874540E-15, 93.03125000204836681, 7.188101187500000044 ) ) ;
#73500=VERTEX_POINT ( 'NONE', #63631 ) ;
#73513=CARTESIAN_POINT ( 'NONE',  ( -8.000000000000000000, 10.96874999590322020, -3.313708498984762496 ) ) ;
#73516=CARTESIAN_POINT ( 'NONE',  ( 5.082755093536324154, 15.65624999795161365, 5.082755093536326818 ) ) ;
#73519=CARTESIAN_POINT ( 'NONE',  ( -7.188101187500000933, 103.4375000020483810, -2.977408999572650483 ) ) ;
#73526=CARTESIAN_POINT ( 'NONE',  ( 7.999999999999998224, 20.90625000000000355, 3.313708498984766049 ) ) ;
#73537=CARTESIAN_POINT ( 'NONE',  ( 7.188101187500002709, 93.31250000204838102, 2.977408999572649151 ) ) ;
#73546=CARTESIAN_POINT ( 'NONE',  ( -7.188101187500001821, 103.4375000020483668, -2.977408999572650483 ) ) ;
#73558=CARTESIAN_POINT ( 'NONE',  ( 7.999999999999998224, 8.906250000000001776, 3.313708498984766049 ) ) ;
#73563=ORIENTED_EDGE ( 'NONE', *, *, #18816, .F. ) ;
#73572=CARTESIAN_POINT ( 'NONE',  ( -7.188101187500001821, 14.62499999795161010, -2.977408999572651371 ) ) ;
#73573=CARTESIAN_POINT ( 'NONE',  ( 8.000000000000001776, 110.8437500040967763, 3.313708498984759387 ) ) ;
#73577=EDGE_CURVE ( 'NONE', #38745, #56053, #7045, .T. ) ;
#73583=CARTESIAN_POINT ( 'NONE',  ( 9.797174393178825657E-16, 125.0000000000000000, -8.000000000000000000 ) ) ;
#73584=CARTESIAN_POINT ( 'NONE',  ( -5.082755093536324154, 110.8437500020483810, 5.082755093536326818 ) ) ;
#73598=EDGE_CURVE ( 'NONE', #21405, #2977, #30583, .T. ) ;
#73600=CARTESIAN_POINT ( 'NONE',  ( 3.313708498984760720, 103.5312500000000142, -8.000000000000000000 ) ) ;
#73606=CARTESIAN_POINT ( 'NONE',  ( -8.000000000000000000, 27.56249999590322375, -9.797174393178825657E-16 ) ) ;
#73608=CARTESIAN_POINT ( 'NONE',  ( 5.082755093536326818, 122.0937500020483952, 5.082755093536325042 ) ) ;
#73615=( BOUNDED_CURVE ( )  B_SPLINE_CURVE ( 2, ( #43667, #62138, #33491, #27063, #66679, #55379, #9346, #50442, #72721 ),
 .UNSPECIFIED., .F., .F. ) 
 B_SPLINE_CURVE_WITH_KNOTS ( ( 3, 2, 2, 2, 3 ),
 ( 0.7361111111111110494, 0.7430555555555554692, 0.7500000000000000000, 0.7569444444444444198, 0.7638888888888888395 ),
 .UNSPECIFIED. ) 
 CURVE ( )  GEOMETRIC_REPRESENTATION_ITEM ( )  RATIONAL_B_SPLINE_CURVE ( ( 1.000000000000001110, 0.9238795325112855172, 1.000000000000000000, 0.9238795325112867385, 1.000000000000000000, 0.9238795325112867385, 1.000000000000000000, 0.9238795325112867385, 1.000000000000000000 ) ) 
 REPRESENTATION_ITEM ( '' )  );
#73632=CARTESIAN_POINT ( 'NONE',  ( 7.188101187500000044, 115.9062500020483810, -8.802885111219163269E-16 ) ) ;
#73637=CARTESIAN_POINT ( 'NONE',  ( 2.977408999572650039, 118.0625000020483952, -7.188101187500001821 ) ) ;
#73638=CARTESIAN_POINT ( 'NONE',  ( -8.000000000000000000, 14.06249999590322375, -9.797174393178825657E-16 ) ) ;
#73650=ORIENTED_EDGE ( 'NONE', *, *, #62535, .T. ) ;
#73651=CARTESIAN_POINT ( 'NONE',  ( 4.898587196589412829E-16, 27.18749999590322375, -8.000000000000000000 ) ) ;
#73653=CARTESIAN_POINT ( 'NONE',  ( 0.000000000000000000, 0.5000000000000004441, 0.000000000000000000 ) ) ;
#73661=CARTESIAN_POINT ( 'NONE',  ( -2.977408999572654480, 26.99999999795161187, 7.188101187499999156 ) ) ;
#73665=CARTESIAN_POINT ( 'NONE',  ( -7.188101187500002709, 15.18749999795161365, 2.977408999572649151 ) ) ;
#73687=AXIS2_PLACEMENT_3D ( 'NONE', #56820, #40575, #62459 ) ;
#73688=CARTESIAN_POINT ( 'NONE',  ( 5.656854249492379694, 122.9375000000000000, -5.656854249492380582 ) ) ;
#73693=CARTESIAN_POINT ( 'NONE',  ( 8.000000000000001776, 94.15625000000000000, 3.313708498984759387 ) ) ;
#73714=DIRECTION ( 'NONE',  ( -0.000000000000000000, 1.000000000000000000, -0.000000000000000000 ) ) ;
#73718=CARTESIAN_POINT ( 'NONE',  ( -2.977408999572651815, 103.4375000020483668, 7.188101187500000933 ) ) ;
#73724=VERTEX_POINT ( 'NONE', #8145 ) ;
#73737=CARTESIAN_POINT ( 'NONE',  ( -3.313708498984707429, 100.7187500000000000, -8.000000000000055067 ) ) ;
#73740=CARTESIAN_POINT ( 'NONE',  ( 5.656854249492381470, 106.2500000040967905, 5.656854249492379694 ) ) ;
#73744=CARTESIAN_POINT ( 'NONE',  ( 7.188101187499999156, 21.74999999795161898, 2.977408999572654924 ) ) ;
#73752=CARTESIAN_POINT ( 'NONE',  ( -5.082755093536325042, 8.531249997951611874, -5.082755093536325930 ) ) ;
#73755=CARTESIAN_POINT ( 'NONE',  ( 2.977408999572650927, 2.624999997951610986, -7.188101187500001821 ) ) ;
#73769=CARTESIAN_POINT ( 'NONE',  ( -8.000000000000000000, 103.9062499999999716, -3.313708498984761164 ) ) ;
#73771=CARTESIAN_POINT ( 'NONE',  ( 2.977408999572650927, 11.24999999795161187, -7.188101187500000933 ) ) ;
#73775=CARTESIAN_POINT ( 'NONE',  ( -7.188101187499999156, 105.1250000020483668, 2.977408999572654924 ) ) ;
#73797=ORIENTED_EDGE ( 'NONE', *, *, #73577, .F. ) ;
#73805=CARTESIAN_POINT ( 'NONE',  ( 7.188101187500000044, 120.4062500020483810, -8.802885111219163269E-16 ) ) ;
#73814=CARTESIAN_POINT ( 'NONE',  ( -2.977408999572654480, 19.49999999795161898, 7.188101187499999156 ) ) ;
#73832=DIRECTION ( 'NONE',  ( 0.000000000000000000, 0.000000000000000000, 1.000000000000000000 ) ) ;
#73852=CARTESIAN_POINT ( 'NONE',  ( 5.656854249492378806, 8.812500000000000000, 5.656854249492381470 ) ) ;
#73856=CARTESIAN_POINT ( 'NONE',  ( 8.000000000000000000, 94.53125000409677625, -3.313708498984762496 ) ) ;
#73863=EDGE_CURVE ( 'NONE', #66034, #53657, #70777, .T. ) ;
#73864=ORIENTED_EDGE ( 'NONE', *, *, #3515, .T. ) ;
#73867=CARTESIAN_POINT ( 'NONE',  ( -7.188101187500000044, 121.5312500020483810, 0.000000000000000000 ) ) ;
#73889=EDGE_CURVE ( 'NONE', #33995, #4108, #71983, .T. ) ;
#73891=CARTESIAN_POINT ( 'NONE',  ( -5.656854249492381470, 9.749999995903220196, 5.656854249492379694 ) ) ;
#73894=CARTESIAN_POINT ( 'NONE',  ( -1.320432766682874540E-15, 16.96874999795161543, 7.188101187500000044 ) ) ;
#73896=CARTESIAN_POINT ( 'NONE',  ( -4.401442555609581635E-16, 103.1562500020483810, -7.188101187500000044 ) ) ;
#73905=PLANE ( 'NONE',  #50721 ) ;
#73907=CARTESIAN_POINT ( 'NONE',  ( -5.656854249492379694, 19.87499999590322020, -5.656854249492380582 ) ) ;
#73913=CARTESIAN_POINT ( 'NONE',  ( 5.082755093536325042, 95.09375000204838102, -5.082755093536325930 ) ) ;
#73919=CARTESIAN_POINT ( 'NONE',  ( 2.977408999572650039, 100.0625000020483952, -7.188101187500001821 ) ) ;
#73924=ORIENTED_EDGE ( 'NONE', *, *, #68591, .F. ) ;
#73944=EDGE_CURVE ( 'NONE', #1937, #29800, #9871, .T. ) ;
#73946=CARTESIAN_POINT ( 'NONE',  ( -7.188101187500000044, 13.21874999795161187, -8.802885111219163269E-16 ) ) ;
#73947=CARTESIAN_POINT ( 'NONE',  ( 8.000000000000000000, 109.4375000040967905, -9.797174393178825657E-16 ) ) ;
#73956=CARTESIAN_POINT ( 'NONE',  ( -5.082755093536324154, 101.8437500020483810, 5.082755093536326818 ) ) ;
#73973=CARTESIAN_POINT ( 'NONE',  ( -5.656854249492378806, 108.6874999999999858, 5.656854249492381470 ) ) ;
#73979=CARTESIAN_POINT ( 'NONE',  ( 2.977408999572651815, 2.062499997951610098, 7.188101187500000933 ) ) ;
#73982=CARTESIAN_POINT ( 'NONE',  ( 5.082755093536325042, 123.9687500020483952, -5.082755093536325930 ) ) ;
#73992=CARTESIAN_POINT ( 'NONE',  ( 5.656854249492379694, 124.4375000000000000, -5.656854249492380582 ) ) ;
#74001=CARTESIAN_POINT ( 'NONE',  ( 7.188101187500000933, 111.5000000020483810, -2.977408999572651371 ) ) ;
#74007=CARTESIAN_POINT ( 'NONE',  ( -2.977408999572650927, 122.7500000020483952, -7.188101187500001821 ) ) ;
#74017=AXIS2_PLACEMENT_3D ( 'NONE', #25052, #43158, #66173 ) ;
#74029=CARTESIAN_POINT ( 'NONE',  ( 4.401442555609581635E-16, 26.34374999795161543, -7.188101187500000044 ) ) ;
#74032=CARTESIAN_POINT ( 'NONE',  ( -7.188101187500000044, 22.59374999795161187, -8.802885111219163269E-16 ) ) ;
#74037=AXIS2_PLACEMENT_3D ( 'NONE', #18837, #29049, #772 ) ;
#74041=CARTESIAN_POINT ( 'NONE',  ( 4.850062511589654031E-16, 0.4207531754730554074, -7.920753175473053354 ) ) ;
#74051=( BOUNDED_CURVE ( )  B_SPLINE_CURVE ( 1, ( #51097, #5831 ),
 .UNSPECIFIED., .F., .F. ) 
 B_SPLINE_CURVE_WITH_KNOTS ( ( 2, 2 ),
 ( 0.000000000000000000, 1.000000000000000000 ),
 .UNSPECIFIED. ) 
 CURVE ( )  GEOMETRIC_REPRESENTATION_ITEM ( )  RATIONAL_B_SPLINE_CURVE ( ( 0.9660720762559202868, 0.9660720762559202868 ) ) 
 REPRESENTATION_ITEM ( '' )  );
#74061=CARTESIAN_POINT ( 'NONE',  ( -8.000000000000000000, 121.9062500000000000, -3.313708498984761608 ) ) ;
#74069=CARTESIAN_POINT ( 'NONE',  ( 8.000000000000000000, 5.906249995903221084, -3.313708498984761164 ) ) ;
#74092=CARTESIAN_POINT ( 'NONE',  ( -5.082755093536324154, 104.8437500020483810, 5.082755093536326818 ) ) ;
#74105=CARTESIAN_POINT ( 'NONE',  ( -1.469576158976823947E-15, 6.937499995903221084, 8.000000000000000000 ) ) ;
#74110=FACE_OUTER_BOUND ( 'NONE', #52510, .T. ) ;
#74117=CARTESIAN_POINT ( 'NONE',  ( -2.977408999572650039, 26.81249999795161898, -7.188101187500000933 ) ) ;
#74125=CARTESIAN_POINT ( 'NONE',  ( 5.082755093536325930, 8.156249997951611874, -5.082755093536325930 ) ) ;
#74128=CARTESIAN_POINT ( 'NONE',  ( -2.977408999572650039, 7.312499997951610986, -7.188101187500001821 ) ) ;
#74136=EDGE_LOOP ( 'NONE', ( #21386, #216, #5740, #53982 ) ) ;
#74142=CARTESIAN_POINT ( 'NONE',  ( 7.188101187499999156, 18.37499999795161187, 2.977408999572654924 ) ) ;
#74143=DIRECTION ( 'NONE',  ( -0.000000000000000000, 1.000000000000000000, -0.000000000000000000 ) ) ;
#74146=CARTESIAN_POINT ( 'NONE',  ( -7.188101187499999156, 103.6250000020483810, 2.977408999572654924 ) ) ;
#74175=CARTESIAN_POINT ( 'NONE',  ( 7.188101187500002709, 123.3125000020483810, 2.977408999572649151 ) ) ;
#74184=CARTESIAN_POINT ( 'NONE',  ( 2.977408999572651815, 24.18749999795161543, 7.188101187500000933 ) ) ;
#74202=EDGE_CURVE ( 'NONE', #18825, #72985, #17141, .T. ) ;
#74203=CARTESIAN_POINT ( 'NONE',  ( 8.000000000000001776, 115.1562500000000000, 3.313708498984759387 ) ) ;
#74208=CARTESIAN_POINT ( 'NONE',  ( 4.401442555609581635E-16, 4.218749997951610098, -7.188101187500000044 ) ) ;
#74224=CARTESIAN_POINT ( 'NONE',  ( -5.656854249492379694, 17.06250000000000000, -5.656854249492380582 ) ) ;
#74227=CARTESIAN_POINT ( 'NONE',  ( 1.469576158976823947E-15, 91.06250000409676204, 8.000000000000000000 ) ) ;
#74259=CARTESIAN_POINT ( 'NONE',  ( -3.313708498984765161, 8.343749995903221972, 7.999999999999998224 ) ) ;
#74264=CARTESIAN_POINT ( 'NONE',  ( 2.977408999572651815, 17.06249999795161543, 7.188101187500000933 ) ) ;
#74266=CARTESIAN_POINT ( 'NONE',  ( -7.188101187499999156, 105.1250000020483810, 2.977408999572654924 ) ) ;
#74282=CARTESIAN_POINT ( 'NONE',  ( -7.188101187500000933, 91.06250000204838102, -2.977408999572650483 ) ) ;
#74288=CARTESIAN_POINT ( 'NONE',  ( 5.082755093536326818, 104.0937500020483810, 5.082755093536325042 ) ) ;
#74303=CARTESIAN_POINT ( 'NONE',  ( 8.000000000000000000, 9.000000000000001776, 0.000000000000000000 ) ) ;
#74304=ADVANCED_FACE ( 'NONE', ( #34153 ), #939, .T. ) ;
#74315=CARTESIAN_POINT ( 'NONE',  ( 2.977408999572650927, 15.74999999795161543, -7.188101187500001821 ) ) ;
#74317=CARTESIAN_POINT ( 'NONE',  ( 5.656854249492381470, 109.2500000040967763, 5.656854249492379694 ) ) ;
#74326=CARTESIAN_POINT ( 'NONE',  ( 5.082755093536326818, 106.7187500020483952, 5.082755093536325042 ) ) ;
#74341=CARTESIAN_POINT ( 'NONE',  ( -8.000000000000000000, 108.4062500000000000, -3.313708498984761608 ) ) ;
#74346=CARTESIAN_POINT ( 'NONE',  ( -8.000000000000000000, 27.46874999590322730, -3.313708498984762496 ) ) ;
#74348=CARTESIAN_POINT ( 'NONE',  ( 2.977408999572650039, 121.0625000020483810, -7.188101187500000933 ) ) ;
#74369=CARTESIAN_POINT ( 'NONE',  ( -7.188101187500000933, 112.0625000020483810, -2.977408999572650483 ) ) ;
#74375=CARTESIAN_POINT ( 'NONE',  ( 5.082755093536326818, 123.5937500020483952, 5.082755093536325042 ) ) ;
#74403=CARTESIAN_POINT ( 'NONE',  ( -5.082755093536326818, 26.90624999795161543, 5.082755093536325042 ) ) ;
#74406=CARTESIAN_POINT ( 'NONE',  ( -7.188101187500002709, 21.18749999795161187, 2.977408999572649151 ) ) ;
#74424=VERTEX_POINT ( 'NONE', #13686 ) ;
#74432=CARTESIAN_POINT ( 'NONE',  ( 7.188101187500000044, 90.78125000204838102, -8.802885111219163269E-16 ) ) ;
#74434=ORIENTED_EDGE ( 'NONE', *, *, #40791, .T. ) ;
#74439=CARTESIAN_POINT ( 'NONE',  ( 7.999999999999998224, 5.718749995903220196, 3.313708498984766049 ) ) ;
#74454=CARTESIAN_POINT ( 'NONE',  ( 0.000000000000000000, 125.0000000000000000, 0.000000000000000000 ) ) ;
#74460=CARTESIAN_POINT ( 'NONE',  ( 2.977408999572650039, 105.6875000020483952, -7.188101187500001821 ) ) ;
#74487=CARTESIAN_POINT ( 'NONE',  ( 5.082755093536325930, 26.53124999795161543, -5.082755093536325930 ) ) ;
#74494=CARTESIAN_POINT ( 'NONE',  ( -7.188101187500001821, 11.62499999795161187, -2.977408999572651371 ) ) ;
#74497=CARTESIAN_POINT ( 'NONE',  ( 2.977408999572651815, 3.562499997951610542, 7.188101187500000933 ) ) ;
#74500=ADVANCED_FACE ( 'NONE', ( #2766 ), #12783, .T. ) ;
#74515=CARTESIAN_POINT ( 'NONE',  ( -5.082755093536325042, 14.53124999795161187, -5.082755093536325930 ) ) ;
#74521=CARTESIAN_POINT ( 'NONE',  ( -7.188101187500001821, 103.4375000020483668, -2.977408999572650483 ) ) ;
#74526=EDGE_LOOP ( 'NONE', ( #56483, #25596, #7985, #38048, #41833, #708 ) ) ;
#74527=AXIS2_PLACEMENT_3D ( 'NONE', #58502, #25248, #52833 ) ;
#74537=CARTESIAN_POINT ( 'NONE',  ( 3.999982273345623618, 89.99927424231840689, -6.928213464733947724 ) ) ;
#74552=CARTESIAN_POINT ( 'NONE',  ( -2.977408999572650927, 120.8750000020483810, -7.188101187500001821 ) ) ;
#74562=CARTESIAN_POINT ( 'NONE',  ( -7.188101187500002709, 25.31249999795161543, 2.977408999572649151 ) ) ;
#74581=CARTESIAN_POINT ( 'NONE',  ( -5.082755093536326818, 9.281249997951610098, 5.082755093536325042 ) ) ;
#74587=CARTESIAN_POINT ( 'NONE',  ( 8.000000000000001776, 122.8437500040967905, 3.313708498984759387 ) ) ;
#74589=CARTESIAN_POINT ( 'NONE',  ( -3.313708498984796691, 120.7812500000000142, 7.999999999999965361 ) ) ;
#74600=EDGE_CURVE ( 'NONE', #61351, #16528, #10677, .T. ) ;
#74601=CARTESIAN_POINT ( 'NONE',  ( -5.656854249492381470, 20.43750000000000355, 5.656854249492379694 ) ) ;
#74603=CARTESIAN_POINT ( 'NONE',  ( 7.188101187500001821, 123.5000000020483952, -2.977408999572651371 ) ) ;
#74614=CARTESIAN_POINT ( 'NONE',  ( 7.188101187500001821, 123.8750000020483810, -2.977408999572651371 ) ) ;
#74643=CARTESIAN_POINT ( 'NONE',  ( -1.320432766682874540E-15, 15.46874999795161187, 7.188101187500000044 ) ) ;
#74645=FACE_OUTER_BOUND ( 'NONE', #31105, .T. ) ;
#74646=CARTESIAN_POINT ( 'NONE',  ( 1.320432766682874540E-15, 99.40625000204838102, 7.188101187500000044 ) ) ;
#74700=COLOUR_RGB('Black',0.12,0.14,0.17);
#74701=FILL_AREA_STYLE_COLOUR('',#74700);
#74702=FILL_AREA_STYLE('',(#74701));
#74703=SURFACE_STYLE_FILL_AREA(#74702);
#74704=SURFACE_SIDE_STYLE('',(#74703));
#74705=SURFACE_STYLE_USAGE(.BOTH.,#74704);
#74706=PRESENTATION_STYLE_ASSIGNMENT((#74705));
ENDSEC;
END-ISO-10303-21;
